ISO-10303-21;
HEADER;
FILE_DESCRIPTION (('STEP AP214'),
    '1' );
FILE_NAME ('Injection Molded Chain Links 10.step',
    '2026-10-08T22:59:04',
    ( '' ),
    ( '' ),
    'SwSTEP 2.0',
    'SolidWorks 2020',
    '' );
FILE_SCHEMA (( 'AUTOMOTIVE_DESIGN' ));
ENDSEC;

DATA;
#7=EDGE_CURVE ( 'NONE', #162791, #50451, #132568, .T. ) ;
#9=CARTESIAN_POINT ( 'NONE',  ( -18.59999999999999787, 68.22930980752001062, -227.7331931781284879 ) ) ;
#35=ORIENTED_EDGE ( 'NONE', *, *, #78924, .T. ) ;
#37=ORIENTED_EDGE ( 'NONE', *, *, #109345, .T. ) ;
#52=VERTEX_POINT ( 'NONE', #84661 ) ;
#54=CARTESIAN_POINT ( 'NONE',  ( -21.05000000000000071, 56.01362831242966678, -232.7091905853083347 ) ) ;
#62=VERTEX_POINT ( 'NONE', #243781 ) ;
#81=DIRECTION ( 'NONE',  ( 1.000000000000000000, -7.049440681616511973E-16, 1.911869773728122111E-16 ) ) ;
#87=CARTESIAN_POINT ( 'NONE',  ( -18.59999999999999787, 61.54970422893871529, -212.2965875311496688 ) ) ;
#125=VERTEX_POINT ( 'NONE', #228076 ) ;
#168=VERTEX_POINT ( 'NONE', #130234 ) ;
#173=AXIS2_PLACEMENT_3D ( 'NONE', #207427, #126590, #204823 ) ;
#185=DIRECTION ( 'NONE',  ( -1.000000000000000000, 0.000000000000000000, 0.000000000000000000 ) ) ;
#218=EDGE_CURVE ( 'NONE', #140485, #55100, #47742, .T. ) ;
#231=CARTESIAN_POINT ( 'NONE',  ( 22.47007471830798764, 65.21035539001043446, -243.3066537799435878 ) ) ;
#247=VERTEX_POINT ( 'NONE', #134084 ) ;
#326=CARTESIAN_POINT ( 'NONE',  ( 21.05000000000000071, 60.06860817181090795, -221.2964476536733684 ) ) ;
#343=AXIS2_PLACEMENT_3D ( 'NONE', #231284, #38216, #12243 ) ;
#351=AXIS2_PLACEMENT_3D ( 'NONE', #154646, #254933, #132486 ) ;
#373=CARTESIAN_POINT ( 'NONE',  ( 20.94999999999999574, 67.23127455305841238, -235.8551265064783991 ) ) ;
#384=CIRCLE ( 'NONE', #179491, 0.1000000000000124678 ) ;
#405=ORIENTED_EDGE ( 'NONE', *, *, #194450, .F. ) ;
#430=EDGE_LOOP ( 'NONE', ( #122674, #216629, #10019, #127244 ) ) ;
#445=EDGE_LOOP ( 'NONE', ( #60488, #4015, #173917, #89051 ) ) ;
#469=CARTESIAN_POINT ( 'NONE',  ( 18.59999999999999076, 64.75617845954087670, -200.4736850529726269 ) ) ;
#472=EDGE_CURVE ( 'NONE', #99142, #37547, #63531, .T. ) ;
#476=( LENGTH_UNIT ( ) NAMED_UNIT ( * ) SI_UNIT ( .MILLI., .METRE. ) );
#485=ADVANCED_FACE ( 'NONE', ( #188619 ), #68687, .F. ) ;
#489=CARTESIAN_POINT ( 'NONE',  ( -20.94999999999999929, 67.49462292596868451, -195.5612049585272700 ) ) ;
#500=DIRECTION ( 'NONE',  ( 1.000000000000000000, 0.000000000000000000, 0.000000000000000000 ) ) ;
#510=ORIENTED_EDGE ( 'NONE', *, *, #73936, .T. ) ;
#517=CARTESIAN_POINT ( 'NONE',  ( 21.05000000000000071, 78.89331866122350334, -228.7665898296168052 ) ) ;
#544=CARTESIAN_POINT ( 'NONE',  ( -20.64999999999999858, 67.23127455305841238, -235.8551265064783991 ) ) ;
#563=DIRECTION ( 'NONE',  ( 1.000000000000000000, -7.049440681616512959E-16, 1.911869773728117674E-16 ) ) ;
#583=CARTESIAN_POINT ( 'NONE',  ( 22.39999999999999858, 59.68594599439719417, -233.9123800762197902 ) ) ;
#593=DIRECTION ( 'NONE',  ( 1.000000000000000000, 0.000000000000000000, 0.000000000000000000 ) ) ;
#610=EDGE_CURVE ( 'NONE', #44096, #9432, #54358, .T. ) ;
#615=CIRCLE ( 'NONE', #146367, 2.000000000000005773 ) ;
#618=ADVANCED_FACE ( 'NONE', ( #152096 ), #136321, .T. ) ;
#621=ORIENTED_EDGE ( 'NONE', *, *, #77674, .T. ) ;
#646=FACE_OUTER_BOUND ( 'NONE', #203716, .T. ) ;
#677=CARTESIAN_POINT ( 'NONE',  ( -21.05000000000000426, 57.84918772656043018, -226.1321410194968280 ) ) ;
#695=VERTEX_POINT ( 'NONE', #253718 ) ;
#711=EDGE_LOOP ( 'NONE', ( #221584, #172126, #200683, #173138 ) ) ;
#725=EDGE_LOOP ( 'NONE', ( #93746, #200882, #21273 ) ) ;
#772=CARTESIAN_POINT ( 'NONE',  ( 18.59999999999999076, 62.49201502323811752, -208.8221019049098857 ) ) ;
#810=LINE ( 'NONE', #257668, #225073 ) ;
#837=ORIENTED_EDGE ( 'NONE', *, *, #33805, .F. ) ;
#844=AXIS2_PLACEMENT_3D ( 'NONE', #116240, #210200, #54935 ) ;
#881=EDGE_CURVE ( 'NONE', #38302, #220817, #47206, .T. ) ;
#887=ORIENTED_EDGE ( 'NONE', *, *, #95778, .T. ) ;
#896=CARTESIAN_POINT ( 'NONE',  ( 23.24999999999999289, 57.93055674131822741, -245.5071546967800771 ) ) ;
#925=ADVANCED_FACE ( 'NONE', ( #171064 ), #228436, .T. ) ;
#934=ORIENTED_EDGE ( 'NONE', *, *, #121343, .F. ) ;
#938=EDGE_CURVE ( 'NONE', #254106, #142564, #184202, .T. ) ;
#950=CARTESIAN_POINT ( 'NONE',  ( 18.44206774312969443, 86.89455662089525845, -199.6122089586171739 ) ) ;
#952=VERTEX_POINT ( 'NONE', #168495 ) ;
#985=ORIENTED_EDGE ( 'NONE', *, *, #144619, .F. ) ;
#1017=CARTESIAN_POINT ( 'NONE',  ( 21.07016717456946608, 61.13071397353302672, -234.2006012892922797 ) ) ;
#1025=EDGE_CURVE ( 'NONE', #149860, #28751, #199594, .T. ) ;
#1052=CIRCLE ( 'NONE', #79612, 0.09999999999999935330 ) ;
#1066=DIRECTION ( 'NONE',  ( -1.000000000000000000, -0.000000000000000000, -0.000000000000000000 ) ) ;
#1095=VERTEX_POINT ( 'NONE', #78315 ) ;
#1111=EDGE_CURVE ( 'NONE', #101652, #9861, #66472, .T. ) ;
#1113=CARTESIAN_POINT ( 'NONE',  ( -23.25000000000000000, 61.54970422893871529, -212.2965875311496688 ) ) ;
#1124=CARTESIAN_POINT ( 'NONE',  ( 21.05000000000000071, 72.06688615501691686, -225.0895073929160048 ) ) ;
#1133=EDGE_CURVE ( 'NONE', #226006, #125569, #21733, .T. ) ;
#1173=DIRECTION ( 'NONE',  ( 1.000000000000000000, 0.000000000000000000, 0.000000000000000000 ) ) ;
#1211=ORIENTED_EDGE ( 'NONE', *, *, #25154, .T. ) ;
#1225=ORIENTED_EDGE ( 'NONE', *, *, #153604, .F. ) ;
#1228=AXIS2_PLACEMENT_3D ( 'NONE', #234016, #55344, #254814 ) ;
#1261=CIRCLE ( 'NONE', #80352, 0.09999999999999883982 ) ;
#1275=DIRECTION ( 'NONE',  ( 1.000000000000000000, 0.000000000000000000, 0.000000000000000000 ) ) ;
#1305=CARTESIAN_POINT ( 'NONE',  ( -23.25000000000000000, 68.76258920191057200, -222.5680764032308048 ) ) ;
#1316=CARTESIAN_POINT ( 'NONE',  ( 20.95346350065193519, 60.88192102021747587, -225.3139116850534833 ) ) ;
#1337=DIRECTION ( 'NONE',  ( 0.000000000000000000, 0.2617529984165152257, 0.9651348961777124202 ) ) ;
#1391=EDGE_LOOP ( 'NONE', ( #245342, #198224, #7987, #176680 ) ) ;
#1435=AXIS2_PLACEMENT_3D ( 'NONE', #47076, #126633, #27576 ) ;
#1443=DIRECTION ( 'NONE',  ( 1.000000000000000000, 0.000000000000000000, 0.000000000000000000 ) ) ;
#1452=DIRECTION ( 'NONE',  ( 1.000000000000000000, 0.000000000000000000, -0.000000000000000000 ) ) ;
#1481=CARTESIAN_POINT ( 'NONE',  ( -18.59999999999999787, 79.19526988099229925, -196.1889237952725296 ) ) ;
#1510=CARTESIAN_POINT ( 'NONE',  ( 21.53699400383268170, 65.45457063879538850, -242.4061840233472083 ) ) ;
#1534=DIRECTION ( 'NONE',  ( 0.000000000000000000, 0.9651348961777157509, -0.2617529984165031243 ) ) ;
#1536=DIRECTION ( 'NONE',  ( -1.000000000000000000, 3.151514657663852580E-16, -8.547182517843351137E-17 ) ) ;
#1565=CARTESIAN_POINT ( 'NONE',  ( -18.59999999999999787, 70.15623657602074559, -198.0563205710787713 ) ) ;
#1571=ORIENTED_EDGE ( 'NONE', *, *, #45184, .F. ) ;
#1573=VECTOR ( 'NONE', #176745, 1000.000000000000000 ) ;
#1584=EDGE_CURVE ( 'NONE', #45271, #124804, #88508, .T. ) ;
#1586=AXIS2_PLACEMENT_3D ( 'NONE', #32071, #191144, #254875 ) ;
#1589=CARTESIAN_POINT ( 'NONE',  ( -18.50000000000000000, 79.14291928130900544, -196.3819507745080557 ) ) ;
#1609=CARTESIAN_POINT ( 'NONE',  ( -21.44999999999999929, 63.46669608621377279, -222.0380013001639270 ) ) ;
#1659=DIRECTION ( 'NONE',  ( 0.000000000000000000, 0.2617529984165152257, 0.9651348961777124202 ) ) ;
#1670=CIRCLE ( 'NONE', #80777, 0.09999999999999868716 ) ;
#1754=EDGE_CURVE ( 'NONE', #185637, #6907, #16291, .T. ) ;
#1767=DIRECTION ( 'NONE',  ( 0.000000000000000000, 0.2617529984165031243, 0.9651348961777157509 ) ) ;
#1781=DIRECTION ( 'NONE',  ( 0.000000000000000000, 0.9333616406058473647, 0.3589373870824282275 ) ) ;
#1784=CARTESIAN_POINT ( 'NONE',  ( 20.94999999999999574, 68.17695920783671681, -227.9262201573640141 ) ) ;
#1803=EDGE_CURVE ( 'NONE', #177022, #204435, #138747, .T. ) ;
#1839=CARTESIAN_POINT ( 'NONE',  ( 20.94999999999999929, 76.00000000001126921, -203.5231074845248997 ) ) ;
#1848=LINE ( 'NONE', #43576, #118337 ) ;
#1851=STYLED_ITEM ( 'NONE', ( #65603 ), #63721 ) ;
#1865=CARTESIAN_POINT ( 'NONE',  ( -18.40000000000000924, 78.23216008268646249, -231.5864513804630178 ) ) ;
#1897=LINE ( 'NONE', #98400, #254811 ) ;
#1926=VERTEX_POINT ( 'NONE', #147952 ) ;
#1947=ORIENTED_EDGE ( 'NONE', *, *, #71541, .T. ) ;
#1965=ORIENTED_EDGE ( 'NONE', *, *, #65276, .T. ) ;
#1994=EDGE_LOOP ( 'NONE', ( #202796, #207521, #200932, #192769 ) ) ;
#2015=CARTESIAN_POINT ( 'NONE',  ( -23.15000000000000213, 59.16775194334852728, -221.0793150863668473 ) ) ;
#2063=AXIS2_PLACEMENT_3D ( 'NONE', #208848, #48479, #11955 ) ;
#2080=ORIENTED_EDGE ( 'NONE', *, *, #256043, .T. ) ;
#2122=TOROIDAL_SURFACE ( 'NONE', #6414, 0.2000000000000000111, 0.1000000000000000056 ) ;
#2127=ADVANCED_FACE ( 'NONE', ( #137357 ), #72278, .F. ) ;
#2168=CARTESIAN_POINT ( 'NONE',  ( -21.45000000000000284, 65.35370752038342346, -213.3282663891675952 ) ) ;
#2175=EDGE_CURVE ( 'NONE', #61516, #42744, #101312, .T. ) ;
#2198=CARTESIAN_POINT ( 'NONE',  ( -20.85000000000000142, 76.00000000001126921, -203.5231074845248997 ) ) ;
#2217=VECTOR ( 'NONE', #218757, 1000.000000000000000 ) ;
#2290=CIRCLE ( 'NONE', #168784, 0.1000000000000106498 ) ;
#2292=CARTESIAN_POINT ( 'NONE',  ( -22.39999999999999858, 65.09550114356427741, -243.3481044654562879 ) ) ;
#2295=ORIENTED_EDGE ( 'NONE', *, *, #162133, .F. ) ;
#2326=CARTESIAN_POINT ( 'NONE',  ( 23.25000000000000000, 82.67551891922275331, -215.5849511313000164 ) ) ;
#2330=VERTEX_POINT ( 'NONE', #188063 ) ;
#2377=VERTEX_POINT ( 'NONE', #5543 ) ;
#2378=ORIENTED_EDGE ( 'NONE', *, *, #233140, .F. ) ;
#2407=ORIENTED_EDGE ( 'NONE', *, *, #217591, .F. ) ;
#2408=EDGE_CURVE ( 'NONE', #164486, #101793, #222148, .T. ) ;
#2410=CARTESIAN_POINT ( 'NONE',  ( -20.05000000000000426, 63.86602797976523505, -212.9247947273492514 ) ) ;
#2423=CARTESIAN_POINT ( 'NONE',  ( -20.94999999999999929, 74.92681270650359693, -207.4801605588535551 ) ) ;
#2425=AXIS2_PLACEMENT_3D ( 'NONE', #153513, #135160, #16531 ) ;
#2554=CARTESIAN_POINT ( 'NONE',  ( -23.25000000000000000, 67.23127455305841238, -235.8551265064783991 ) ) ;
#2601=ADVANCED_FACE ( 'NONE', ( #107928 ), #145756, .F. ) ;
#2608=EDGE_LOOP ( 'NONE', ( #130509, #146115, #19721, #209502 ) ) ;
#2615=CARTESIAN_POINT ( 'NONE',  ( 21.14999999999999858, 60.94483358488582070, -234.0465764481390636 ) ) ;
#2623=EDGE_CURVE ( 'NONE', #8256, #229929, #114010, .T. ) ;
#2627=CARTESIAN_POINT ( 'NONE',  ( -20.94999999999999929, 72.02722222756958104, -225.1832529173024398 ) ) ;
#2631=DIRECTION ( 'NONE',  ( 0.000000000000000000, 0.2617529984165152257, 0.9651348961777124202 ) ) ;
#2666=CARTESIAN_POINT ( 'NONE',  ( 18.52130828395272033, 78.22078591447844076, -231.5573136408083030 ) ) ;
#2680=ORIENTED_EDGE ( 'NONE', *, *, #249182, .F. ) ;
#2766=VERTEX_POINT ( 'NONE', #37396 ) ;
#2788=CIRCLE ( 'NONE', #27787, 0.6000000000000005329 ) ;
#2808=ORIENTED_EDGE ( 'NONE', *, *, #180461, .F. ) ;
#2820=DIRECTION ( 'NONE',  ( 1.000000000000000000, 0.000000000000000000, 0.000000000000000000 ) ) ;
#2835=ORIENTED_EDGE ( 'NONE', *, *, #26231, .T. ) ;
#2863=CARTESIAN_POINT ( 'NONE',  ( -20.95000000000000284, 62.98323157773609893, -207.0610388790104821 ) ) ;
#2880=ORIENTED_EDGE ( 'NONE', *, *, #167770, .T. ) ;
#2885=CARTESIAN_POINT ( 'NONE',  ( 21.13461538461538680, 60.19324435863628509, -221.2538251110503893 ) ) ;
#2886=CARTESIAN_POINT ( 'NONE',  ( -21.59780538579341069, 60.59700058177565296, -234.1584077978427558 ) ) ;
#2912=CIRCLE ( 'NONE', #161154, 0.1000000000000106498 ) ;
#2916=ADVANCED_FACE ( 'NONE', ( #218557 ), #26941, .F. ) ;
#2917=DIRECTION ( 'NONE',  ( 2.952720810173289112E-16, 0.9651348961777157509, -0.2617529984165031243 ) ) ;
#2918=EDGE_CURVE ( 'NONE', #39036, #129497, #151836, .T. ) ;
#2920=SPHERICAL_SURFACE ( 'NONE', #104217, 0.1000000000000000056 ) ;
#2932=DIRECTION ( 'NONE',  ( 0.000000000000000000, 0.2617529984165030688, 0.9651348961777157509 ) ) ;
#2939=TOROIDAL_SURFACE ( 'NONE', #182013, 0.2000000000000000111, 0.1000000000000000056 ) ;
#2955=CARTESIAN_POINT ( 'NONE',  ( -20.64999999999999858, 70.62751970751253339, -223.3325012285725393 ) ) ;
#2990=AXIS2_PLACEMENT_3D ( 'NONE', #190719, #10773, #149015 ) ;
#3006=CARTESIAN_POINT ( 'NONE',  ( -20.00857864376270001, 61.60676448363446411, -221.6371840927903349 ) ) ;
#3031=DIRECTION ( 'NONE',  ( 0.000000000000000000, 0.2617529984165083423, 0.9651348961777143076 ) ) ;
#3037=EDGE_LOOP ( 'NONE', ( #253687, #57875, #12705 ) ) ;
#3139=CARTESIAN_POINT ( 'NONE',  ( -20.64999999999999858, 70.12557831835937350, -215.6322690948981915 ) ) ;
#3153=CARTESIAN_POINT ( 'NONE',  ( -18.51555513499781469, 78.14120754265996993, -231.3589029833907489 ) ) ;
#3162=CIRCLE ( 'NONE', #44884, 0.1000000000000105804 ) ;
#3163=DIRECTION ( 'NONE',  ( 0.000000000000000000, 0.2617529984165152257, 0.9651348961777124202 ) ) ;
#3166=DIRECTION ( 'NONE',  ( 0.9880948137434723000, -0.1484822917196433334, 0.04026969206407598340 ) ) ;
#3170=DIRECTION ( 'NONE',  ( 0.000000000000000000, 0.2617529984164915779, 0.9651348961777189706 ) ) ;
#3173=LINE ( 'NONE', #98393, #198770 ) ;
#3191=CARTESIAN_POINT ( 'NONE',  ( -23.25000000000000000, 87.34033503009941057, -206.5987052159188124 ) ) ;
#3222=ORIENTED_EDGE ( 'NONE', *, *, #11743, .T. ) ;
#3243=EDGE_CURVE ( 'NONE', #207394, #52103, #218615, .T. ) ;
#3258=DIRECTION ( 'NONE',  ( 0.000000000000000000, 0.7216758089626587047, -0.6922311945860948335 ) ) ;
#3273=ORIENTED_EDGE ( 'NONE', *, *, #6673, .F. ) ;
#3289=ORIENTED_EDGE ( 'NONE', *, *, #81130, .F. ) ;
#3312=AXIS2_PLACEMENT_3D ( 'NONE', #228448, #66790, #146311 ) ;
#3324=DIRECTION ( 'NONE',  ( -4.701977403289178058E-30, 0.2617529984164863599, 0.9651348961777203028 ) ) ;
#3332=CARTESIAN_POINT ( 'NONE',  ( -20.54999999999999716, 78.50726470275243685, -228.6618886302502176 ) ) ;
#3355=DIRECTION ( 'NONE',  ( 0.000000000000000000, 0.7035695228903320331, 0.7106264324241468033 ) ) ;
#3372=EDGE_CURVE ( 'NONE', #231654, #112321, #202363, .T. ) ;
#3386=ORIENTED_EDGE ( 'NONE', *, *, #208781, .T. ) ;
#3433=DIRECTION ( 'NONE',  ( -0.000000000000000000, -0.2617529984165031243, -0.9651348961777157509 ) ) ;
#3462=DIRECTION ( 'NONE',  ( 0.000000000000000000, 0.2617529984164915779, 0.9651348961777187485 ) ) ;
#3465=CARTESIAN_POINT ( 'NONE',  ( -23.25000000000000000, 61.57587952878035509, -212.2000740415318774 ) ) ;
#3483=DIRECTION ( 'NONE',  ( 1.000000000000000000, 0.000000000000000000, 0.000000000000000000 ) ) ;
#3496=DIRECTION ( 'NONE',  ( -1.836970198721029934E-16, -0.9651348961777157509, 0.2617529984165031243 ) ) ;
#3534=ORIENTED_EDGE ( 'NONE', *, *, #99608, .F. ) ;
#3590=AXIS2_PLACEMENT_3D ( 'NONE', #42427, #164940, #20316 ) ;
#3629=CARTESIAN_POINT ( 'NONE',  ( -21.93340585897931660, 65.31415710917114836, -242.9239163822773833 ) ) ;
#3654=CARTESIAN_POINT ( 'NONE',  ( 18.59999999999999432, 68.20313450767837082, -227.8297066677462794 ) ) ;
#3698=DIRECTION ( 'NONE',  ( 0.000000000000000000, -0.2617529984165152257, -0.9651348961777124202 ) ) ;
#3710=LINE ( 'NONE', #63682, #23429 ) ;
#3736=FACE_OUTER_BOUND ( 'NONE', #255407, .T. ) ;
#3751=TOROIDAL_SURFACE ( 'NONE', #103672, 12.97499999999999787, 0.1000000000000000056 ) ;
#3754=EDGE_CURVE ( 'NONE', #152520, #159793, #93340, .T. ) ;
#3755=ORIENTED_EDGE ( 'NONE', *, *, #215318, .F. ) ;
#3780=ADVANCED_FACE ( 'NONE', ( #170576 ), #39783, .T. ) ;
#3788=ADVANCED_FACE ( 'NONE', ( #107980 ), #50540, .T. ) ;
#3806=CARTESIAN_POINT ( 'NONE',  ( -18.59999999999999787, 79.28756800457986742, -196.2274082906208434 ) ) ;
#3856=AXIS2_PLACEMENT_3D ( 'NONE', #158051, #117590, #255772 ) ;
#3873=CARTESIAN_POINT ( 'NONE',  ( -20.94999999999999929, 86.27712145182582049, -209.5223386573213702 ) ) ;
#3890=ORIENTED_EDGE ( 'NONE', *, *, #51001, .T. ) ;
#3903=CARTESIAN_POINT ( 'NONE',  ( 21.05000000000000071, 64.27847795353595473, -247.1247091181747066 ) ) ;
#3904=ADVANCED_FACE ( 'NONE', ( #253891 ), #55660, .T. ) ;
#3927=ORIENTED_EDGE ( 'NONE', *, *, #472, .T. ) ;
#3961=CARTESIAN_POINT ( 'NONE',  ( 18.58685178364170199, 78.17487933103092246, -231.4413402867085665 ) ) ;
#3962=ORIENTED_EDGE ( 'NONE', *, *, #237201, .F. ) ;
#3967=ORIENTED_EDGE ( 'NONE', *, *, #25384, .T. ) ;
#3990=CARTESIAN_POINT ( 'NONE',  ( 21.05095171578076574, 61.94553090543893603, -221.8162262668083429 ) ) ;
#4004=ORIENTED_EDGE ( 'NONE', *, *, #206924, .T. ) ;
#4015=ORIENTED_EDGE ( 'NONE', *, *, #254264, .T. ) ;
#4040=FACE_OUTER_BOUND ( 'NONE', #165999, .T. ) ;
#4063=DIRECTION ( 'NONE',  ( 1.000000000000000000, 0.000000000000000000, 0.000000000000000000 ) ) ;
#4074=DIRECTION ( 'NONE',  ( 1.000000000000000000, 0.000000000000000000, -0.000000000000000000 ) ) ;
#4085=CARTESIAN_POINT ( 'NONE',  ( 21.78635804494511419, 65.29411581985623059, -242.6195740507382084 ) ) ;
#4114=CARTESIAN_POINT ( 'NONE',  ( -2.995603634470891112E-16, 84.13386079949725627, -218.4216076940958260 ) ) ;
#4142=DIRECTION ( 'NONE',  ( 2.952720810173289605E-16, 0.9651348961777155289, -0.2617529984165038459 ) ) ;
#4145=ORIENTED_EDGE ( 'NONE', *, *, #72590, .T. ) ;
#4186=CIRCLE ( 'NONE', #149967, 0.1999999999999945155 ) ;
#4197=CARTESIAN_POINT ( 'NONE',  ( 18.59999999999999787, 79.28756800457986742, -196.2274082906208434 ) ) ;
#4207=DIRECTION ( 'NONE',  ( 1.000000000000000000, 0.000000000000000000, 0.000000000000000000 ) ) ;
#4215=ADVANCED_FACE ( 'NONE', ( #127233 ), #108938, .F. ) ;
#4247=VECTOR ( 'NONE', #78793, 1000.000000000000114 ) ;
#4268=DIRECTION ( 'NONE',  ( 0.000000000000000000, 0.2617529984165033463, 0.9651348961777157509 ) ) ;
#4275=EDGE_LOOP ( 'NONE', ( #20359, #19749, #40015, #160917 ) ) ;
#4286=ORIENTED_EDGE ( 'NONE', *, *, #13491, .F. ) ;
#4288=VERTEX_POINT ( 'NONE', #12440 ) ;
#4319=DIRECTION ( 'NONE',  ( 0.000000000000000000, -0.2558827019434133376, 0.9667078373770113808 ) ) ;
#4412=CARTESIAN_POINT ( 'NONE',  ( -20.85000000000000142, 70.22659352830977753, -197.9852579278363578 ) ) ;
#4422=CARTESIAN_POINT ( 'NONE',  ( 23.14999999999999858, 62.92003201576280702, -207.2439188921395612 ) ) ;
#4452=AXIS2_PLACEMENT_3D ( 'NONE', #124185, #104573, #126735 ) ;
#4458=DIRECTION ( 'NONE',  ( 0.000000000000000000, 0.2617529984165030688, 0.9651348961777157509 ) ) ;
#4469=VERTEX_POINT ( 'NONE', #123082 ) ;
#4475=CARTESIAN_POINT ( 'NONE',  ( 21.05000000000000071, 61.16604239671102761, -234.3115055913011417 ) ) ;
#4478=ORIENTED_EDGE ( 'NONE', *, *, #31768, .T. ) ;
#4486=CARTESIAN_POINT ( 'NONE',  ( -23.25000000000000000, 59.07123845373075710, -221.0531397865252075 ) ) ;
#4492=DIRECTION ( 'NONE',  ( 3.469446951953635015E-14, -0.2617529984165031243, -0.9651348961777157509 ) ) ;
#4513=EDGE_LOOP ( 'NONE', ( #223686, #58460, #163466, #94679 ) ) ;
#4519=CARTESIAN_POINT ( 'NONE',  ( 18.59999999999999076, 76.00000000001126921, -203.5231074845248997 ) ) ;
#4533=CARTESIAN_POINT ( 'NONE',  ( 21.14999999999999503, 79.23417978893664326, -236.1056577391152587 ) ) ;
#4559=VERTEX_POINT ( 'NONE', #183058 ) ;
#4577=DIRECTION ( 'NONE',  ( 0.000000000000000000, 0.2617529984165031243, 0.9651348961777157509 ) ) ;
#4579=ORIENTED_EDGE ( 'NONE', *, *, #106491, .T. ) ;
#4584=VERTEX_POINT ( 'NONE', #31708 ) ;
#4598=FACE_OUTER_BOUND ( 'NONE', #209660, .T. ) ;
#4611=TOROIDAL_SURFACE ( 'NONE', #142186, 1.900000000000002576, 0.1000000000000000056 ) ;
#4612=CARTESIAN_POINT ( 'NONE',  ( -20.94999999999999929, 64.75617845954087670, -200.4736850529726269 ) ) ;
#4616=DIRECTION ( 'NONE',  ( -0.000000000000000000, -0.2617529984165031243, -0.9651348961777157509 ) ) ;
#4622=CIRCLE ( 'NONE', #221106, 0.1000000000000124678 ) ;
#4631=EDGE_CURVE ( 'NONE', #125569, #82116, #135885, .T. ) ;
#4706=CARTESIAN_POINT ( 'NONE',  ( -18.42554971533676778, 78.24001056755894012, -231.5466539090771505 ) ) ;
#4707=ORIENTED_EDGE ( 'NONE', *, *, #186594, .T. ) ;
#4726=VERTEX_POINT ( 'NONE', #62794 ) ;
#4728=CARTESIAN_POINT ( 'NONE',  ( 18.51997666896904349, 78.16595003815976384, -231.4192470149134522 ) ) ;
#4742=CYLINDRICAL_SURFACE ( 'NONE', #50154, 0.1000000000000124678 ) ;
#4796=TOROIDAL_SURFACE ( 'NONE', #205294, 0.2000000000000000111, 0.1000000000000000056 ) ;
#4801=CARTESIAN_POINT ( 'NONE',  ( -20.54999999999999716, 75.47649400317826007, -205.4533772768803317 ) ) ;
#4806=CYLINDRICAL_SURFACE ( 'NONE', #66996, 0.1000000000000048767 ) ;
#4809=CARTESIAN_POINT ( 'NONE',  ( 18.59999999999998366, 70.22659352830977753, -197.9852579278363578 ) ) ;
#4810=CARTESIAN_POINT ( 'NONE',  ( 18.48413544395648955, 87.07667984079645862, -199.6026701993346535 ) ) ;
#4822=CARTESIAN_POINT ( 'NONE',  ( -18.59999999999999787, 61.57587952878036930, -212.2000740415318774 ) ) ;
#4833=VERTEX_POINT ( 'NONE', #9232 ) ;
#4857=EDGE_CURVE ( 'NONE', #66884, #695, #104458, .T. ) ;
#4864=ADVANCED_FACE ( 'NONE', ( #243987 ), #45794, .T. ) ;
#4869=ORIENTED_EDGE ( 'NONE', *, *, #159782, .F. ) ;
#4895=ORIENTED_EDGE ( 'NONE', *, *, #192868, .T. ) ;
#4957=ADVANCED_FACE ( 'NONE', ( #152637 ), #11837, .T. ) ;
#4978=CARTESIAN_POINT ( 'NONE',  ( 18.59999999999999432, 58.44755627554218336, -246.4682640075163818 ) ) ;
#5029=AXIS2_PLACEMENT_3D ( 'NONE', #75671, #16976, #93922 ) ;
#5036=CARTESIAN_POINT ( 'NONE',  ( 20.94999999999999929, 76.00000000001126921, -203.5231074845248997 ) ) ;
#5039=ADVANCED_FACE ( 'NONE', ( #238552 ), #80745, .T. ) ;
#5053=ORIENTED_EDGE ( 'NONE', *, *, #61150, .F. ) ;
#5071=CIRCLE ( 'NONE', #67453, 0.09999999999999975575 ) ;
#5107=CIRCLE ( 'NONE', #188303, 0.09999999999999949207 ) ;
#5109=DIRECTION ( 'NONE',  ( 0.000000000000000000, 0.2617529984165030132, 0.9651348961777158619 ) ) ;
#5117=DIRECTION ( 'NONE',  ( -1.000000000000000000, -0.000000000000000000, 0.000000000000000000 ) ) ;
#5163=VECTOR ( 'NONE', #189839, 1000.000000000000114 ) ;
#5171=DIRECTION ( 'NONE',  ( 0.000000000000000000, -0.4105728183244014562, -0.9118278131605539460 ) ) ;
#5203=ADVANCED_FACE ( 'NONE', ( #27252 ), #55198, .T. ) ;
#5204=ADVANCED_FACE ( 'NONE', ( #241146 ), #246268, .F. ) ;
#5212=DIRECTION ( 'NONE',  ( 1.000000000000000000, 0.000000000000000000, 0.000000000000000000 ) ) ;
#5226=CARTESIAN_POINT ( 'NONE',  ( -18.48179518608914762, 86.98986899361442227, -199.3650623953066372 ) ) ;
#5235=EDGE_CURVE ( 'NONE', #252597, #46377, #121893, .T. ) ;
#5253=ORIENTED_EDGE ( 'NONE', *, *, #117741, .T. ) ;
#5265=EDGE_CURVE ( 'NONE', #191603, #242965, #100975, .T. ) ;
#5282=DIRECTION ( 'NONE',  ( 0.000000000000000000, 0.2466408114429753939, 0.9691069652678959701 ) ) ;
#5300=DIRECTION ( 'NONE',  ( 1.000000000000000000, 0.000000000000000000, 0.000000000000000000 ) ) ;
#5301=DIRECTION ( 'NONE',  ( 1.000000000000000000, 0.000000000000000000, 0.000000000000000000 ) ) ;
#5341=EDGE_CURVE ( 'NONE', #220738, #17623, #13744, .T. ) ;
#5343=CARTESIAN_POINT ( 'NONE',  ( 21.12642695952774119, 65.46697144162916970, -241.9826101524681690 ) ) ;
#5355=CARTESIAN_POINT ( 'NONE',  ( -23.25000000000000000, 86.45856254523214091, -209.4679346046102921 ) ) ;
#5359=EDGE_CURVE ( 'NONE', #164486, #156950, #77501, .T. ) ;
#5372=DIRECTION ( 'NONE',  ( 0.000000000000000000, 0.2617529984165031243, 0.9651348961777157509 ) ) ;
#5382=DIRECTION ( 'NONE',  ( -0.000000000000000000, -0.2617529984165031243, -0.9651348961777157509 ) ) ;
#5398=DIRECTION ( 'NONE',  ( -1.000000000000000000, 0.000000000000000000, 0.000000000000000000 ) ) ;
#5399=DIRECTION ( 'NONE',  ( 1.000000000000000000, 0.000000000000000000, 0.000000000000000000 ) ) ;
#5414=CARTESIAN_POINT ( 'NONE',  ( -18.50000000000000000, 68.50594083727658301, -224.0235912779512830 ) ) ;
#5416=CARTESIAN_POINT ( 'NONE',  ( -20.99749315643147440, 62.82351852664101699, -207.2177435904692118 ) ) ;
#5420=DIRECTION ( 'NONE',  ( -1.000000000000000000, 0.000000000000000000, 0.000000000000000000 ) ) ;
#5421=CARTESIAN_POINT ( 'NONE',  ( -21.05000000000000071, 65.61575147395463148, -242.1939180743342774 ) ) ;
#5475=AXIS2_PLACEMENT_3D ( 'NONE', #11030, #170147, #249650 ) ;
#5502=ORIENTED_EDGE ( 'NONE', *, *, #170963, .F. ) ;
#5526=DIRECTION ( 'NONE',  ( -1.000000000000000000, -0.000000000000000000, -0.000000000000000000 ) ) ;
#5530=VERTEX_POINT ( 'NONE', #220908 ) ;
#5543=CARTESIAN_POINT ( 'NONE',  ( -21.64999999999999858, 65.69978428250288971, -213.4221254243406065 ) ) ;
#5595=TOROIDAL_SURFACE ( 'NONE', #163854, 11.65000000000000036, 0.1000000000000000056 ) ;
#5630=EDGE_CURVE ( 'NONE', #159923, #8256, #202616, .T. ) ;
#5632=DIRECTION ( 'NONE',  ( 0.000000000000000000, -0.9651348961777157509, 0.2617529984165027912 ) ) ;
#5641=EDGE_LOOP ( 'NONE', ( #55625, #28021, #137201, #171340, #191403, #157430, #157861, #4004, #95452, #186498, #98889, #93403, #171168, #205692, #15359, #12002, #3890, #68696 ) ) ;
#5675=VERTEX_POINT ( 'NONE', #209073 ) ;
#5702=CARTESIAN_POINT ( 'NONE',  ( 23.24999999999999645, 76.00000000001126921, -203.5231074845248997 ) ) ;
#5715=EDGE_CURVE ( 'NONE', #72090, #186373, #147827, .T. ) ;
#5733=CARTESIAN_POINT ( 'NONE',  ( -23.25000000000000000, 76.00000000001126921, -203.5231074845248997 ) ) ;
#5750=LINE ( 'NONE', #120613, #173992 ) ;
#5783=CARTESIAN_POINT ( 'NONE',  ( -23.15000000000000213, 59.16775194334852728, -221.0793150863668473 ) ) ;
#5806=VECTOR ( 'NONE', #156639, 1000.000000000000114 ) ;
#5815=CARTESIAN_POINT ( 'NONE',  ( -21.14999999999999858, 56.01362831242966678, -232.7091905853083347 ) ) ;
#5859=DIRECTION ( 'NONE',  ( 4.408576920032447355E-17, -0.1290532225515392817, -0.9916376685811522096 ) ) ;
#5862=DIRECTION ( 'NONE',  ( -1.000000000000000000, 0.000000000000000000, 0.000000000000000000 ) ) ;
#5871=CARTESIAN_POINT ( 'NONE',  ( 20.85000000000000142, 86.55507603484990398, -209.4941099044519319 ) ) ;
#5880=ORIENTED_EDGE ( 'NONE', *, *, #20517, .F. ) ;
#5902=EDGE_CURVE ( 'NONE', #88904, #188870, #44410, .T. ) ;
#5906=ORIENTED_EDGE ( 'NONE', *, *, #51001, .F. ) ;
#5912=ORIENTED_EDGE ( 'NONE', *, *, #141759, .T. ) ;
#6004=DIRECTION ( 'NONE',  ( 1.000000000000000000, 0.000000000000000000, 0.000000000000000000 ) ) ;
#6010=CARTESIAN_POINT ( 'NONE',  ( 21.97500000000000497, 63.38346053167636995, -212.7939182281409956 ) ) ;
#6021=CARTESIAN_POINT ( 'NONE',  ( 18.49351773456764292, 78.22584867798236985, -231.3920583907407718 ) ) ;
#6022=CARTESIAN_POINT ( 'NONE',  ( 20.94999999999997442, 79.28756800457986742, -196.2274082906208434 ) ) ;
#6089=DIRECTION ( 'NONE',  ( 0.000000000000000000, 0.9651348961777428404, -0.2617529984164035373 ) ) ;
#6091=EDGE_LOOP ( 'NONE', ( #38102, #245791, #227864, #8365 ) ) ;
#6099=CARTESIAN_POINT ( 'NONE',  ( 23.14999999999999503, 64.01960172407876826, -222.2915665888316141 ) ) ;
#6105=CARTESIAN_POINT ( 'NONE',  ( 18.47135592147650485, 86.89032914117082385, -199.5516226189558040 ) ) ;
#6123=ORIENTED_EDGE ( 'NONE', *, *, #147088, .T. ) ;
#6170=EDGE_CURVE ( 'NONE', #128905, #147319, #240397, .T. ) ;
#6178=CARTESIAN_POINT ( 'NONE',  ( -20.64999999999999858, 65.79629777212066699, -213.4483007241822747 ) ) ;
#6187=EDGE_CURVE ( 'NONE', #82519, #50332, #66573, .T. ) ;
#6225=ORIENTED_EDGE ( 'NONE', *, *, #8142, .F. ) ;
#6244=DIRECTION ( 'NONE',  ( 0.000000000000000000, 0.9167729611565434977, -0.3994087351226345284 ) ) ;
#6255=DIRECTION ( 'NONE',  ( 0.000000000000000000, 0.2617529984165152257, 0.9651348961777124202 ) ) ;
#6270=FACE_OUTER_BOUND ( 'NONE', #119082, .T. ) ;
#6272=ADVANCED_FACE ( 'NONE', ( #149980 ), #168280, .F. ) ;
#6276=LINE ( 'NONE', #164092, #140075 ) ;
#6279=VERTEX_POINT ( 'NONE', #48280 ) ;
#6291=CARTESIAN_POINT ( 'NONE',  ( 20.95429693346636313, 59.03464676750856910, -225.7981132573195850 ) ) ;
#6292=CARTESIAN_POINT ( 'NONE',  ( -21.05000000000000426, 61.17066907964395739, -234.2475650577967770 ) ) ;
#6337=CARTESIAN_POINT ( 'NONE',  ( 21.13461538461538680, 61.88829803306103372, -221.6099259868126978 ) ) ;
#6414=AXIS2_PLACEMENT_3D ( 'NONE', #95159, #213823, #176007 ) ;
#6471=DIRECTION ( 'NONE',  ( 0.000000000000000000, -0.2617529984164506107, -0.9651348961777299618 ) ) ;
#6511=VECTOR ( 'NONE', #193335, 1000.000000000000000 ) ;
#6532=CARTESIAN_POINT ( 'NONE',  ( -18.49372193242232854, 86.88397309856780737, -199.4657796619476926 ) ) ;
#6571=ORIENTED_EDGE ( 'NONE', *, *, #229001, .F. ) ;
#6591=ADVANCED_FACE ( 'NONE', ( #63678 ), #24587, .F. ) ;
#6602=ORIENTED_EDGE ( 'NONE', *, *, #70734, .T. ) ;
#6605=FACE_OUTER_BOUND ( 'NONE', #125180, .T. ) ;
#6613=CARTESIAN_POINT ( 'NONE',  ( 18.59999999999999076, 63.65372963998873246, -224.5957079722776655 ) ) ;
#6616=DIRECTION ( 'NONE',  ( 1.000000000000000000, 0.000000000000000000, 0.000000000000000000 ) ) ;
#6641=DIRECTION ( 'NONE',  ( -3.265361837132813093E-16, -0.9651348961777146407, 0.2617529984165072321 ) ) ;
#6658=EDGE_LOOP ( 'NONE', ( #138022, #37695, #68643, #254245 ) ) ;
#6660=CARTESIAN_POINT ( 'NONE',  ( -20.00857864376270001, 63.96254146938299101, -212.9509700271909196 ) ) ;
#6673=EDGE_CURVE ( 'NONE', #157057, #20693, #202412, .T. ) ;
#6677=ADVANCED_FACE ( 'NONE', ( #124955 ), #130068, .T. ) ;
#6706=CARTESIAN_POINT ( 'NONE',  ( -20.94999999999999929, 76.00000000001126921, -203.5231074845248997 ) ) ;
#6727=SPHERICAL_SURFACE ( 'NONE', #256450, 0.1000000000000000056 ) ;
#6728=CARTESIAN_POINT ( 'NONE',  ( -20.95000000000000639, 62.88396779178383866, -206.9948552354529738 ) ) ;
#6816=ADVANCED_FACE ( 'NONE', ( #15290 ), #77790, .T. ) ;
#6827=DIRECTION ( 'NONE',  ( 0.000000000000000000, -0.9628525332200033038, 0.2700277750006890298 ) ) ;
#6851=DIRECTION ( 'NONE',  ( -2.978066053179068737E-16, -0.9651348961777163060, 0.2617529984165009038 ) ) ;
#6854=FACE_OUTER_BOUND ( 'NONE', #28428, .T. ) ;
#6898=CARTESIAN_POINT ( 'NONE',  ( 21.05000000000000071, 82.09643798151613225, -215.4278993322501208 ) ) ;
#6902=AXIS2_PLACEMENT_3D ( 'NONE', #179372, #178088, #3258 ) ;
#6907=VERTEX_POINT ( 'NONE', #63040 ) ;
#6935=CARTESIAN_POINT ( 'NONE',  ( 21.05000000000000071, 82.22731448072437388, -214.9453318841612486 ) ) ;
#6939=AXIS2_PLACEMENT_3D ( 'NONE', #103708, #67182, #7187 ) ;
#6969=EDGE_LOOP ( 'NONE', ( #195119, #41893, #28294, #169228 ) ) ;
#6970=CARTESIAN_POINT ( 'NONE',  ( -20.64999999999999858, 63.44052078637213299, -222.1345147897817185 ) ) ;
#6978=AXIS2_PLACEMENT_3D ( 'NONE', #192921, #53404, #33890 ) ;
#7014=VERTEX_POINT ( 'NONE', #208983 ) ;
#7015=CARTESIAN_POINT ( 'NONE',  ( -20.94999999999999929, 67.99035824846625076, -233.0562353075630142 ) ) ;
#7018=DIRECTION ( 'NONE',  ( 0.000000000000000000, 0.2534589355812664757, 0.9673461469267405910 ) ) ;
#7048=VERTEX_POINT ( 'NONE', #150312 ) ;
#7089=AXIS2_PLACEMENT_3D ( 'NONE', #40529, #180014, #164298 ) ;
#7098=EDGE_LOOP ( 'NONE', ( #85149, #3534, #25127, #118805 ) ) ;
#7155=ORIENTED_EDGE ( 'NONE', *, *, #14600, .F. ) ;
#7162=EDGE_LOOP ( 'NONE', ( #253259, #75554, #117177, #254547 ) ) ;
#7187=DIRECTION ( 'NONE',  ( 0.000000000000000000, -0.9651348961777028723, 0.2617529984165503087 ) ) ;
#7290=EDGE_LOOP ( 'NONE', ( #8172, #210937, #256248, #219610 ) ) ;
#7291=EDGE_CURVE ( 'NONE', #155707, #211751, #255774, .T. ) ;
#7319=LINE ( 'NONE', #86836, #187831 ) ;
#7357=CYLINDRICAL_SURFACE ( 'NONE', #240400, 0.09999999999999939493 ) ;
#7365=CIRCLE ( 'NONE', #199096, 0.09999999999999939493 ) ;
#7383=ORIENTED_EDGE ( 'NONE', *, *, #151531, .F. ) ;
#7395=CARTESIAN_POINT ( 'NONE',  ( 18.46163235739475894, 86.89227388589759471, -199.5790731264802105 ) ) ;
#7457=TOROIDAL_SURFACE ( 'NONE', #11581, 1.900000000000002576, 0.1000000000000000056 ) ;
#7469=LINE ( 'NONE', #23217, #88631 ) ;
#7492=CARTESIAN_POINT ( 'NONE',  ( -21.05000000000000071, 62.92003201576280702, -207.2439188921395896 ) ) ;
#7500=DIRECTION ( 'NONE',  ( 0.000000000000000000, 0.2617529984165152257, 0.9651348961777124202 ) ) ;
#7533=VERTEX_POINT ( 'NONE', #107002 ) ;
#7545=LINE ( 'NONE', #87060, #134449 ) ;
#7554=AXIS2_PLACEMENT_3D ( 'NONE', #232486, #17281, #257105 ) ;
#7561=EDGE_LOOP ( 'NONE', ( #157288, #41191, #185856, #75115 ) ) ;
#7599=CARTESIAN_POINT ( 'NONE',  ( 21.05000000000000071, 64.23744694032048130, -224.5446448091673233 ) ) ;
#7602=CARTESIAN_POINT ( 'NONE',  ( 20.85000000000000142, 62.88396779178381735, -206.9948552354529170 ) ) ;
#7604=VECTOR ( 'NONE', #252606, 1000.000000000000000 ) ;
#7606=AXIS2_PLACEMENT_3D ( 'NONE', #199146, #57031, #94896 ) ;
#7617=FACE_OUTER_BOUND ( 'NONE', #74596, .T. ) ;
#7629=AXIS2_PLACEMENT_3D ( 'NONE', #250846, #72240, #96882 ) ;
#7633=EDGE_CURVE ( 'NONE', #232481, #84528, #236355, .T. ) ;
#7634=ORIENTED_EDGE ( 'NONE', *, *, #190682, .T. ) ;
#7647=CARTESIAN_POINT ( 'NONE',  ( -23.25000000000000000, 76.54968129668591814, -201.4963242025517047 ) ) ;
#7662=CARTESIAN_POINT ( 'NONE',  ( -20.85000000000000142, 76.00000000001126921, -203.5231074845248997 ) ) ;
#7676=PRODUCT ( 'Injection Molded Chain Links 10', 'Injection Molded Chain Links 10', '', ( #19534 ) ) ;
#7689=CARTESIAN_POINT ( 'NONE',  ( -21.65000000000000213, 63.02410583447655767, -221.9179669651492759 ) ) ;
#7691=DIRECTION ( 'NONE',  ( -0.000000000000000000, 0.9934243067848629316, -0.1144908148674581572 ) ) ;
#7705=TOROIDAL_SURFACE ( 'NONE', #224342, 11.65000000000000036, 0.1000000000000000056 ) ;
#7740=LINE ( 'NONE', #26020, #115878 ) ;
#7747=CARTESIAN_POINT ( 'NONE',  ( 20.94999999999999929, 67.23127455305841238, -235.8551265064783991 ) ) ;
#7774=ORIENTED_EDGE ( 'NONE', *, *, #85512, .T. ) ;
#7796=ORIENTED_EDGE ( 'NONE', *, *, #113753, .F. ) ;
#7825=ORIENTED_EDGE ( 'NONE', *, *, #175402, .T. ) ;
#7826=VERTEX_POINT ( 'NONE', #184963 ) ;
#7835=FACE_OUTER_BOUND ( 'NONE', #12821, .T. ) ;
#7838=CARTESIAN_POINT ( 'NONE',  ( -18.44232395689846271, 87.01022120691494877, -199.4197499265777367 ) ) ;
#7909=DIRECTION ( 'NONE',  ( 1.000000000000000000, 0.000000000000000000, -0.000000000000000000 ) ) ;
#7942=DIRECTION ( 'NONE',  ( 1.000000000000000000, 0.000000000000000000, 0.000000000000000000 ) ) ;
#7946=EDGE_CURVE ( 'NONE', #49647, #62, #68886, .T. ) ;
#7948=CIRCLE ( 'NONE', #91500, 11.64999999999998614 ) ;
#7951=ORIENTED_EDGE ( 'NONE', *, *, #115334, .F. ) ;
#7957=TOROIDAL_SURFACE ( 'NONE', #32936, 0.9750000000000019762, 0.1000000000000000056 ) ;
#7970=LINE ( 'NONE', #47062, #113125 ) ;
#7987=ORIENTED_EDGE ( 'NONE', *, *, #121216, .F. ) ;
#8018=CARTESIAN_POINT ( 'NONE',  ( 20.94999999999999929, 78.98983215084128062, -228.7927651294584450 ) ) ;
#8036=CARTESIAN_POINT ( 'NONE',  ( -21.09096482362053493, 65.52752482441825066, -241.9864795316534867 ) ) ;
#8050=CARTESIAN_POINT ( 'NONE',  ( 20.94999999999999574, 68.13014604066189861, -227.7202878558733516 ) ) ;
#8065=EDGE_LOOP ( 'NONE', ( #68434, #132216, #204611, #166288 ) ) ;
#8141=EDGE_CURVE ( 'NONE', #255232, #208387, #202929, .T. ) ;
#8142=EDGE_CURVE ( 'NONE', #128048, #79203, #99951, .T. ) ;
#8155=DIRECTION ( 'NONE',  ( 1.000000000000000000, 0.000000000000000000, -0.000000000000000000 ) ) ;
#8159=CARTESIAN_POINT ( 'NONE',  ( -20.54999999999999716, 78.17003882911672008, -228.8770135013149911 ) ) ;
#8172=ORIENTED_EDGE ( 'NONE', *, *, #199277, .T. ) ;
#8176=ADVANCED_FACE ( 'NONE', ( #257710 ), #140377, .T. ) ;
#8183=EDGE_CURVE ( 'NONE', #171727, #182549, #159983, .T. ) ;
#8256=VERTEX_POINT ( 'NONE', #65988 ) ;
#8257=AXIS2_PLACEMENT_3D ( 'NONE', #124428, #203949, #4458 ) ;
#8293=CARTESIAN_POINT ( 'NONE',  ( -23.25000000000000000, 55.98745301258801987, -232.8057040749261262 ) ) ;
#8365=ORIENTED_EDGE ( 'NONE', *, *, #44147, .T. ) ;
#8383=CIRCLE ( 'NONE', #16774, 4.100000000000008527 ) ;
#8455=DIRECTION ( 'NONE',  ( 0.000000000000000000, -0.2617529984165031243, -0.9651348961777157509 ) ) ;
#8464=ORIENTED_EDGE ( 'NONE', *, *, #2918, .F. ) ;
#8466=ADVANCED_FACE ( 'NONE', ( #34586 ), #216540, .T. ) ;
#8491=DIRECTION ( 'NONE',  ( 1.000000000000000000, 0.000000000000000000, 0.000000000000000000 ) ) ;
#8519=ORIENTED_EDGE ( 'NONE', *, *, #202867, .T. ) ;
#8546=CIRCLE ( 'NONE', #37794, 12.87500000000000178 ) ;
#8578=CARTESIAN_POINT ( 'NONE',  ( -21.14999999999999503, 57.70204706108523141, -226.1016183162177526 ) ) ;
#8583=DIRECTION ( 'NONE',  ( 1.000000000000000000, 0.000000000000000000, 0.000000000000000000 ) ) ;
#8595=AXIS2_PLACEMENT_3D ( 'NONE', #62647, #195754, #142169 ) ;
#8598=CIRCLE ( 'NONE', #70980, 0.1000000000000124678 ) ;
#8613=ADVANCED_FACE ( 'NONE', ( #123100 ), #70272, .T. ) ;
#8620=AXIS2_PLACEMENT_3D ( 'NONE', #113694, #152860, #232383 ) ;
#8643=DIRECTION ( 'NONE',  ( 0.000000000000000000, -0.2617529984165031243, -0.9651348961777157509 ) ) ;
#8662=DIRECTION ( 'NONE',  ( 0.000000000000000000, 0.2617529984165036239, 0.9651348961777156399 ) ) ;
#8688=CARTESIAN_POINT ( 'NONE',  ( 20.94999999999999574, 55.13994374908182294, -226.9527081427897315 ) ) ;
#8701=VECTOR ( 'NONE', #100095, 1000.000000000000000 ) ;
#8710=EDGE_CURVE ( 'NONE', #27906, #26421, #182876, .T. ) ;
#8713=CARTESIAN_POINT ( 'NONE',  ( 23.14999999999998437, 67.23127455305841238, -235.8551265064783991 ) ) ;
#8721=VERTEX_POINT ( 'NONE', #206478 ) ;
#8738=DIRECTION ( 'NONE',  ( 0.000000000000000000, -0.2617529984165152257, -0.9651348961777124202 ) ) ;
#8746=VERTEX_POINT ( 'NONE', #25290 ) ;
#8786=DIRECTION ( 'NONE',  ( 0.000000000000000000, -0.2617529984165152257, -0.9651348961777124202 ) ) ;
#8789=ADVANCED_FACE ( 'NONE', ( #54776 ), #134304, .T. ) ;
#8795=EDGE_CURVE ( 'NONE', #22560, #72929, #49582, .T. ) ;
#8809=EDGE_CURVE ( 'NONE', #165270, #200563, #95364, .T. ) ;
#8839=ORIENTED_EDGE ( 'NONE', *, *, #76144, .T. ) ;
#8846=ORIENTED_EDGE ( 'NONE', *, *, #156272, .T. ) ;
#8848=DIRECTION ( 'NONE',  ( 0.000000000000000000, 0.2617529984165027912, 0.9651348961777158619 ) ) ;
#8865=ORIENTED_EDGE ( 'NONE', *, *, #158198, .T. ) ;
#8877=CARTESIAN_POINT ( 'NONE',  ( 19.97071067811864609, 62.37141908057012074, -208.9966201521278037 ) ) ;
#8897=ORIENTED_EDGE ( 'NONE', *, *, #94348, .T. ) ;
#8907=CIRCLE ( 'NONE', #163047, 0.1000000000000124678 ) ;
#8909=CYLINDRICAL_SURFACE ( 'NONE', #254099, 0.09999999999999939493 ) ;
#8924=CARTESIAN_POINT ( 'NONE',  ( 21.13461538461538325, 61.86212273321938682, -221.7064394764304609 ) ) ;
#8937=CARTESIAN_POINT ( 'NONE',  ( 20.94999999999999574, 63.65372963998873246, -224.5957079722776655 ) ) ;
#8948=CARTESIAN_POINT ( 'NONE',  ( -18.59999999999999787, 68.22930980752001062, -227.7331931781284879 ) ) ;
#8987=CIRCLE ( 'NONE', #13103, 0.09999999999999939493 ) ;
#9005=ORIENTED_EDGE ( 'NONE', *, *, #60988, .T. ) ;
#9006=DIRECTION ( 'NONE',  ( 0.000000000000000000, -0.2617529984164955192, -0.9651348961777178603 ) ) ;
#9007=CYLINDRICAL_SURFACE ( 'NONE', #205954, 0.09999999999999543976 ) ;
#9023=CIRCLE ( 'NONE', #83982, 0.09999999999999939493 ) ;
#9114=AXIS2_PLACEMENT_3D ( 'NONE', #146854, #110316, #247248 ) ;
#9116=CARTESIAN_POINT ( 'NONE',  ( -18.50000000000000000, 86.87366311306884370, -199.3414869250131858 ) ) ;
#9172=DIRECTION ( 'NONE',  ( 6.938893903907222067E-15, 0.9651348961777157509, -0.2617529984165031243 ) ) ;
#9188=DIRECTION ( 'NONE',  ( 0.000000000000000000, 0.2617529984164955192, 0.9651348961777178603 ) ) ;
#9229=EDGE_CURVE ( 'NONE', #26209, #193142, #166312, .T. ) ;
#9231=CARTESIAN_POINT ( 'NONE',  ( -20.94999999999999929, 79.14291928130901965, -196.3819507745080557 ) ) ;
#9232=CARTESIAN_POINT ( 'NONE',  ( -23.25000000000000000, 68.69389471299010097, -223.1641309873017462 ) ) ;
#9292=AXIS2_PLACEMENT_3D ( 'NONE', #186308, #87176, #208452 ) ;
#9342=LINE ( 'NONE', #48472, #235524 ) ;
#9352=DIRECTION ( 'NONE',  ( -1.000000000000000000, 0.000000000000000000, 0.000000000000000000 ) ) ;
#9358=VERTEX_POINT ( 'NONE', #105116 ) ;
#9378=AXIS2_PLACEMENT_3D ( 'NONE', #76810, #192922, #255397 ) ;
#9385=CARTESIAN_POINT ( 'NONE',  ( -18.59999999999999787, 68.22930980752001062, -227.7331931781284879 ) ) ;
#9432=VERTEX_POINT ( 'NONE', #166454 ) ;
#9440=CIRCLE ( 'NONE', #196877, 0.1000000000000124678 ) ;
#9463=CYLINDRICAL_SURFACE ( 'NONE', #169628, 0.09999999999999543976 ) ;
#9472=CARTESIAN_POINT ( 'NONE',  ( -20.54999999999999716, 82.09643798151613225, -215.4278993322501208 ) ) ;
#9497=ORIENTED_EDGE ( 'NONE', *, *, #194506, .T. ) ;
#9510=CIRCLE ( 'NONE', #42837, 0.1000000000000124678 ) ;
#9511=ORIENTED_EDGE ( 'NONE', *, *, #209307, .T. ) ;
#9553=CARTESIAN_POINT ( 'NONE',  ( 20.94999999999999929, 86.27712145182582049, -209.5223386573213702 ) ) ;
#9563=CARTESIAN_POINT ( 'NONE',  ( -21.05000000000000071, 65.56055025928534974, -241.8869259205440301 ) ) ;
#9580=FACE_OUTER_BOUND ( 'NONE', #20599, .T. ) ;
#9581=FACE_OUTER_BOUND ( 'NONE', #236060, .T. ) ;
#9584=ORIENTED_EDGE ( 'NONE', *, *, #105583, .F. ) ;
#9616=VECTOR ( 'NONE', #61976, 1000.000000000000000 ) ;
#9652=ADVANCED_FACE ( 'NONE', ( #257444 ), #159701, .F. ) ;
#9656=AXIS2_PLACEMENT_3D ( 'NONE', #94681, #193797, #112978 ) ;
#9667=DIRECTION ( 'NONE',  ( 0.000000000000000000, -0.7092521942343974484, -0.7049548389604062271 ) ) ;
#9680=VERTEX_POINT ( 'NONE', #82683 ) ;
#9690=ADVANCED_FACE ( 'NONE', ( #179284 ), #66510, .F. ) ;
#9701=CIRCLE ( 'NONE', #255355, 0.1000000000000064448 ) ;
#9747=CIRCLE ( 'NONE', #43084, 0.09999999999999738265 ) ;
#9769=LINE ( 'NONE', #149310, #243214 ) ;
#9775=ORIENTED_EDGE ( 'NONE', *, *, #197486, .F. ) ;
#9796=ORIENTED_EDGE ( 'NONE', *, *, #136240, .F. ) ;
#9800=DIRECTION ( 'NONE',  ( 1.000000000000000000, 0.000000000000000000, 0.000000000000000000 ) ) ;
#9809=DIRECTION ( 'NONE',  ( 0.000000000000000000, -0.9916376685811618685, 0.1290532225514649800 ) ) ;
#9822=ORIENTED_EDGE ( 'NONE', *, *, #97299, .F. ) ;
#9843=EDGE_CURVE ( 'NONE', #225728, #130099, #191622, .T. ) ;
#9849=CARTESIAN_POINT ( 'NONE',  ( -22.50000000000000000, 65.09550114356427741, -243.3481044654562879 ) ) ;
#9858=DIRECTION ( 'NONE',  ( -7.304098846218135653E-16, 0.9651348961777157509, -0.2617529984165031243 ) ) ;
#9861=VERTEX_POINT ( 'NONE', #67011 ) ;
#9900=CARTESIAN_POINT ( 'NONE',  ( -18.59999999999999787, 61.51025099401670104, -221.6110087929486951 ) ) ;
#9901=EDGE_CURVE ( 'NONE', #222414, #50332, #241652, .T. ) ;
#9935=EDGE_CURVE ( 'NONE', #114377, #252254, #116752, .T. ) ;
#9939=EDGE_CURVE ( 'NONE', #4726, #211251, #45846, .T. ) ;
#10019=ORIENTED_EDGE ( 'NONE', *, *, #132475, .F. ) ;
#10068=DIRECTION ( 'NONE',  ( 1.000000000000000000, 0.000000000000000000, 0.000000000000000000 ) ) ;
#10077=LINE ( 'NONE', #249975, #117067 ) ;
#10106=DIRECTION ( 'NONE',  ( 1.000000000000000000, -3.151514657663852580E-16, 8.547182517843351137E-17 ) ) ;
#10119=DIRECTION ( 'NONE',  ( -1.000000000000000000, -0.000000000000000000, -0.000000000000000000 ) ) ;
#10120=ORIENTED_EDGE ( 'NONE', *, *, #148917, .F. ) ;
#10173=FACE_OUTER_BOUND ( 'NONE', #76113, .T. ) ;
#10183=AXIS2_PLACEMENT_3D ( 'NONE', #46356, #45092, #125899 ) ;
#10218=DIRECTION ( 'NONE',  ( -1.000000000000000000, 1.772924042024179204E-16, -4.808324575169892332E-17 ) ) ;
#10286=CIRCLE ( 'NONE', #110207, 0.1000000000000124678 ) ;
#10288=LINE ( 'NONE', #188913, #121578 ) ;
#10306=CYLINDRICAL_SURFACE ( 'NONE', #145434, 0.1000000000000124678 ) ;
#10312=ORIENTED_EDGE ( 'NONE', *, *, #76677, .T. ) ;
#10319=FACE_OUTER_BOUND ( 'NONE', #68803, .T. ) ;
#10348=AXIS2_PLACEMENT_3D ( 'NONE', #231308, #55177, #171365 ) ;
#10359=LINE ( 'NONE', #29930, #20961 ) ;
#10366=CARTESIAN_POINT ( 'NONE',  ( -20.94999999999999929, 70.22659352830977753, -197.9852579278363578 ) ) ;
#10370=TOROIDAL_SURFACE ( 'NONE', #39611, 0.4000000000000003553, 0.1000000000000000056 ) ;
#10424=AXIS2_PLACEMENT_3D ( 'NONE', #193460, #14836, #108768 ) ;
#10428=ORIENTED_EDGE ( 'NONE', *, *, #90569, .T. ) ;
#10440=DIRECTION ( 'NONE',  ( 0.000000000000000000, -0.9229812358756199764, 0.3848449534832346086 ) ) ;
#10459=CARTESIAN_POINT ( 'NONE',  ( 23.14999999999999503, 62.92003201576280702, -207.2439188921395612 ) ) ;
#10470=AXIS2_PLACEMENT_3D ( 'NONE', #43935, #47765, #8662 ) ;
#10487=ORIENTED_EDGE ( 'NONE', *, *, #171813, .T. ) ;
#10490=CIRCLE ( 'NONE', #164608, 0.1000000000000124678 ) ;
#10531=AXIS2_PLACEMENT_3D ( 'NONE', #107999, #243653, #225355 ) ;
#10546=FACE_OUTER_BOUND ( 'NONE', #53696, .T. ) ;
#10556=AXIS2_PLACEMENT_3D ( 'NONE', #112687, #51384, #150532 ) ;
#10576=DIRECTION ( 'NONE',  ( -1.000000000000000000, 0.000000000000000000, 0.000000000000000000 ) ) ;
#10596=ORIENTED_EDGE ( 'NONE', *, *, #98462, .F. ) ;
#10616=CARTESIAN_POINT ( 'NONE',  ( -23.15000000000000213, 68.76258920191057200, -222.5680764032308048 ) ) ;
#10625=CIRCLE ( 'NONE', #214605, 0.09999999999999868716 ) ;
#10631=FACE_OUTER_BOUND ( 'NONE', #104856, .T. ) ;
#10636=CARTESIAN_POINT ( 'NONE',  ( -20.94999999999999929, 87.24382154048164750, -206.5725299160771726 ) ) ;
#10643=DIRECTION ( 'NONE',  ( -1.000000000000000000, -0.000000000000000000, 0.000000000000000000 ) ) ;
#10651=AXIS2_PLACEMENT_3D ( 'NONE', #132849, #69031, #11622 ) ;
#10658=DIRECTION ( 'NONE',  ( 0.000000000000000000, 0.2617529984165152257, 0.9651348961777124202 ) ) ;
#10674=CARTESIAN_POINT ( 'NONE',  ( 23.14999999999998437, 63.32247822353865985, -234.7950268628915467 ) ) ;
#10679=FACE_OUTER_BOUND ( 'NONE', #136746, .T. ) ;
#10683=ORIENTED_EDGE ( 'NONE', *, *, #128582, .F. ) ;
#10685=CARTESIAN_POINT ( 'NONE',  ( -21.05000000000001847, 61.10390814609986165, -234.2085808482629261 ) ) ;
#10715=FACE_OUTER_BOUND ( 'NONE', #170032, .T. ) ;
#10747=EDGE_CURVE ( 'NONE', #51386, #142612, #234085, .T. ) ;
#10766=AXIS2_PLACEMENT_3D ( 'NONE', #66050, #88154, #247249 ) ;
#10772=EDGE_CURVE ( 'NONE', #149860, #136295, #5107, .T. ) ;
#10773=DIRECTION ( 'NONE',  ( -2.342056488767301376E-15, -0.1290532225515364506, -0.9916376685811525427 ) ) ;
#10783=ORIENTED_EDGE ( 'NONE', *, *, #134751, .F. ) ;
#10803=AXIS2_PLACEMENT_3D ( 'NONE', #189874, #90751, #230272 ) ;
#10812=ORIENTED_EDGE ( 'NONE', *, *, #185618, .T. ) ;
#10826=COLOUR_RGB ( '', 0.66274510, 0.83137255, 0.94901961) ;
#10829=FACE_OUTER_BOUND ( 'NONE', #233283, .T. ) ;
#10835=VERTEX_POINT ( 'NONE', #253915 ) ;
#10884=APPLICATION_CONTEXT ( 'automotive_design' ) ;
#10891=VECTOR ( 'NONE', #43048, 1000.000000000000000 ) ;
#10938=EDGE_CURVE ( 'NONE', #37547, #185637, #176993, .T. ) ;
#10953=EDGE_LOOP ( 'NONE', ( #30709, #197639, #46562, #126034, #60747 ) ) ;
#10974=ADVANCED_FACE ( 'NONE', ( #243340 ), #204212, .T. ) ;
#11008=VERTEX_POINT ( 'NONE', #167690 ) ;
#11011=FACE_OUTER_BOUND ( 'NONE', #200026, .T. ) ;
#11020=DIRECTION ( 'NONE',  ( -0.000000000000000000, 0.2617529984165031243, 0.9651348961777157509 ) ) ;
#11022=DIRECTION ( 'NONE',  ( 2.557131231893036985E-16, 0.7049548389605068133, -0.7092521942342977503 ) ) ;
#11026=AXIS2_PLACEMENT_3D ( 'NONE', #198977, #136403, #159877 ) ;
#11030=CARTESIAN_POINT ( 'NONE',  ( -21.05000000000000071, 72.02722222756958104, -225.1832529173024398 ) ) ;
#11050=AXIS2_PLACEMENT_3D ( 'NONE', #187387, #90819, #206939 ) ;
#11053=VECTOR ( 'NONE', #5859, 999.9999999999998863 ) ;
#11062=CARTESIAN_POINT ( 'NONE',  ( 20.95512820512820440, 60.90483797576754910, -225.2715357783924333 ) ) ;
#11072=AXIS2_PLACEMENT_3D ( 'NONE', #75032, #196221, #114114 ) ;
#11095=CARTESIAN_POINT ( 'NONE',  ( -20.94999999999999929, 67.23127455305841238, -235.8551265064783991 ) ) ;
#11108=CARTESIAN_POINT ( 'NONE',  ( 23.15000000000000213, 78.98983215084128062, -228.7927651294584450 ) ) ;
#11126=AXIS2_PLACEMENT_3D ( 'NONE', #242528, #161740, #40524 ) ;
#11132=DIRECTION ( 'NONE',  ( 1.000000000000000000, -3.151514657663852580E-16, 8.547182517843351137E-17 ) ) ;
#11147=ORIENTED_EDGE ( 'NONE', *, *, #86433, .T. ) ;
#11153=VERTEX_POINT ( 'NONE', #12458 ) ;
#11155=DIRECTION ( 'NONE',  ( 0.000000000000000000, 0.9651348961777158619, -0.2617529984165031243 ) ) ;
#11177=CARTESIAN_POINT ( 'NONE',  ( 18.59999999999999076, 62.96704557978079464, -212.5773704035085814 ) ) ;
#11184=CARTESIAN_POINT ( 'NONE',  ( 20.84999999999998721, 67.49222854868494892, -195.4187676019683693 ) ) ;
#11217=CYLINDRICAL_SURFACE ( 'NONE', #159993, 0.09999999999999939493 ) ;
#11242=EDGE_LOOP ( 'NONE', ( #150410, #150793, #243849, #188723 ) ) ;
#11374=EDGE_CURVE ( 'NONE', #181858, #184831, #188667, .T. ) ;
#11386=ADVANCED_FACE ( 'NONE', ( #146177 ), #251009, .F. ) ;
#11399=EDGE_CURVE ( 'NONE', #206042, #58070, #86184, .T. ) ;
#11438=DIRECTION ( 'NONE',  ( 1.000000000000000000, 0.000000000000000000, 0.000000000000000000 ) ) ;
#11449=EDGE_LOOP ( 'NONE', ( #19580, #48397, #140121, #34171, #246481 ) ) ;
#11452=DIRECTION ( 'NONE',  ( -0.8660254037843391206, 0.1308764992082676881, 0.4825674480890321805 ) ) ;
#11528=AXIS2_PLACEMENT_3D ( 'NONE', #177590, #100544, #240100 ) ;
#11535=CARTESIAN_POINT ( 'NONE',  ( 21.05000000000000071, 70.65782965956557859, -228.4198064469268559 ) ) ;
#11540=DIRECTION ( 'NONE',  ( 1.000000000000000000, 0.000000000000000000, 0.000000000000000000 ) ) ;
#11564=VECTOR ( 'NONE', #48974, 1000.000000000000000 ) ;
#11577=VERTEX_POINT ( 'NONE', #156500 ) ;
#11581=AXIS2_PLACEMENT_3D ( 'NONE', #249927, #227786, #85674 ) ;
#11601=CARTESIAN_POINT ( 'NONE',  ( 20.99551997958404215, 62.86709121503483999, -207.0570825002670006 ) ) ;
#11607=AXIS2_PLACEMENT_3D ( 'NONE', #182387, #63700, #218915 ) ;
#11622=DIRECTION ( 'NONE',  ( 2.952720810173289112E-16, 0.9651348961777158619, -0.2617529984165024026 ) ) ;
#11631=CARTESIAN_POINT ( 'NONE',  ( 21.14999999999999858, 67.25744985290005218, -235.7586130168606076 ) ) ;
#11667=CARTESIAN_POINT ( 'NONE',  ( 20.52683494730034397, 60.79012627653062850, -225.2957294340843930 ) ) ;
#11672=CIRCLE ( 'NONE', #65811, 0.1000000000000124678 ) ;
#11677=EDGE_LOOP ( 'NONE', ( #209741, #35220, #4895, #39981 ) ) ;
#11691=DIRECTION ( 'NONE',  ( 1.000000000000000000, -3.151514657663852580E-16, 8.547182517843351137E-17 ) ) ;
#11703=CARTESIAN_POINT ( 'NONE',  ( -20.94999999999999929, 76.00000000001126921, -203.5231074845248997 ) ) ;
#11727=DIRECTION ( 'NONE',  ( 1.000000000000000000, 0.000000000000000000, 0.000000000000000000 ) ) ;
#11743=EDGE_CURVE ( 'NONE', #87179, #240058, #185012, .T. ) ;
#11747=VECTOR ( 'NONE', #5382, 1000.000000000000000 ) ;
#11766=CARTESIAN_POINT ( 'NONE',  ( -21.55000000000000426, 65.28755502419014078, -213.4139377145917820 ) ) ;
#11789=DIRECTION ( 'NONE',  ( 1.000000000000000000, 0.000000000000000000, 0.000000000000000000 ) ) ;
#11793=AXIS2_PLACEMENT_3D ( 'NONE', #9553, #192072, #92940 ) ;
#11837=CYLINDRICAL_SURFACE ( 'NONE', #246760, 0.1000000000000124678 ) ;
#11887=CIRCLE ( 'NONE', #166011, 0.09999999999999939493 ) ;
#11920=VECTOR ( 'NONE', #183628, 1000.000000000000000 ) ;
#11955=DIRECTION ( 'NONE',  ( 0.000000000000000000, 0.9916376685811618685, -0.1290532225514649800 ) ) ;
#11980=CARTESIAN_POINT ( 'NONE',  ( -20.94999999999999929, 68.11887992016828264, -227.8068560890360175 ) ) ;
#11988=EDGE_LOOP ( 'NONE', ( #31961, #10312, #232108, #36964 ) ) ;
#12002=ORIENTED_EDGE ( 'NONE', *, *, #44587, .T. ) ;
#12018=EDGE_CURVE ( 'NONE', #231216, #4559, #188860, .T. ) ;
#12050=VERTEX_POINT ( 'NONE', #160026 ) ;
#12058=DIRECTION ( 'NONE',  ( 0.000000000000000000, 0.9651348961777157509, -0.2617529984165031243 ) ) ;
#12061=AXIS2_PLACEMENT_3D ( 'NONE', #107238, #128095, #224610 ) ;
#12079=LINE ( 'NONE', #152886, #16054 ) ;
#12089=ORIENTED_EDGE ( 'NONE', *, *, #95848, .T. ) ;
#12096=ORIENTED_EDGE ( 'NONE', *, *, #119972, .F. ) ;
#12116=VERTEX_POINT ( 'NONE', #141712 ) ;
#12137=CIRCLE ( 'NONE', #257754, 0.09999999999999935330 ) ;
#12151=DIRECTION ( 'NONE',  ( 0.000000000000000000, 0.2617529984165046231, 0.9651348961777154178 ) ) ;
#12170=CARTESIAN_POINT ( 'NONE',  ( -23.25000000000000000, 79.19526988099229925, -196.1889237952725296 ) ) ;
#12176=FACE_OUTER_BOUND ( 'NONE', #167046, .T. ) ;
#12185=FACE_OUTER_BOUND ( 'NONE', #244064, .T. ) ;
#12243=DIRECTION ( 'NONE',  ( 0.000000000000000000, -0.2617529984165030132, -0.9651348961777157509 ) ) ;
#12246=DIRECTION ( 'NONE',  ( 0.000000000000000000, 0.3848449534832868446, 0.9229812358755982160 ) ) ;
#12267=EDGE_CURVE ( 'NONE', #148565, #142261, #39231, .T. ) ;
#12272=DIRECTION ( 'NONE',  ( -0.000000000000000000, 0.2617529984165031243, 0.9651348961777157509 ) ) ;
#12277=EDGE_CURVE ( 'NONE', #17623, #252254, #255631, .T. ) ;
#12309=DIRECTION ( 'NONE',  ( 0.000000000000000000, -0.2617529984165152257, -0.9651348961777124202 ) ) ;
#12328=FACE_OUTER_BOUND ( 'NONE', #114326, .T. ) ;
#12343=ORIENTED_EDGE ( 'NONE', *, *, #149750, .F. ) ;
#12356=ADVANCED_FACE ( 'NONE', ( #210678 ), #12506, .T. ) ;
#12358=DIRECTION ( 'NONE',  ( -2.978066053179066765E-16, -0.9651348961777157509, 0.2617529984165031243 ) ) ;
#12381=EDGE_CURVE ( 'NONE', #178010, #58070, #14092, .T. ) ;
#12386=VERTEX_POINT ( 'NONE', #120589 ) ;
#12420=CARTESIAN_POINT ( 'NONE',  ( 21.05000000000000071, 76.00000000001126921, -203.5231074845248997 ) ) ;
#12421=CARTESIAN_POINT ( 'NONE',  ( -23.15000000000000213, 76.00000000001126921, -203.5231074845248997 ) ) ;
#12440=CARTESIAN_POINT ( 'NONE',  ( -23.15000000000000213, 70.73902226565648732, -215.2805781460175467 ) ) ;
#12455=CARTESIAN_POINT ( 'NONE',  ( 22.49999999999999289, 64.13768741198656187, -247.0874927502468381 ) ) ;
#12458=CARTESIAN_POINT ( 'NONE',  ( -22.39999999999999858, 64.25313205997782973, -247.2214437328673853 ) ) ;
#12479=ORIENTED_EDGE ( 'NONE', *, *, #179070, .F. ) ;
#12506=PLANE ( 'NONE',  #1586 ) ;
#12522=CARTESIAN_POINT ( 'NONE',  ( 18.59999999999999076, 79.15532900748003442, -196.2806010913881778 ) ) ;
#12538=ORIENTED_EDGE ( 'NONE', *, *, #111371, .T. ) ;
#12540=CARTESIAN_POINT ( 'NONE',  ( 22.59999985501178799, 55.87389454177473169, -232.8428744225223284 ) ) ;
#12554=CARTESIAN_POINT ( 'NONE',  ( 20.94999999999999574, 63.67931791018308019, -224.6923787560153301 ) ) ;
#12569=VERTEX_POINT ( 'NONE', #163547 ) ;
#12582=DIRECTION ( 'NONE',  ( -1.000000000000000000, 0.000000000000000000, 0.000000000000000000 ) ) ;
#12585=CARTESIAN_POINT ( 'NONE',  ( -18.39999999999999858, 78.24072131640578220, -231.5548844243369047 ) ) ;
#12599=DIRECTION ( 'NONE',  ( 0.000000000000000000, -0.3848449534832868446, -0.9229812358755983270 ) ) ;
#12635=DIRECTION ( 'NONE',  ( 1.000000000000000000, 0.000000000000000000, 0.000000000000000000 ) ) ;
#12646=CARTESIAN_POINT ( 'NONE',  ( -20.94999999999999929, 80.78317333349157536, -192.9003134612048882 ) ) ;
#12661=AXIS2_PLACEMENT_3D ( 'NONE', #24985, #121521, #43244 ) ;
#12667=DIRECTION ( 'NONE',  ( -1.000000000000000000, 0.000000000000000000, 0.000000000000000000 ) ) ;
#12677=ADVANCED_FACE ( 'NONE', ( #134666 ), #222518, .T. ) ;
#12705=ORIENTED_EDGE ( 'NONE', *, *, #186171, .F. ) ;
#12776=DIRECTION ( 'NONE',  ( -3.787827842127535236E-15, -0.8900778951570268438, -0.4558084472153153266 ) ) ;
#12821=EDGE_LOOP ( 'NONE', ( #182378, #214334, #185204 ) ) ;
#12829=DIRECTION ( 'NONE',  ( 1.000000000000000000, 0.000000000000000000, -0.000000000000000000 ) ) ;
#12847=VECTOR ( 'NONE', #137286, 1000.000000000000000 ) ;
#12848=AXIS2_PLACEMENT_3D ( 'NONE', #194638, #212893, #255815 ) ;
#12874=CARTESIAN_POINT ( 'NONE',  ( 23.24999999999999289, 52.91185528119409298, -244.1460391050142675 ) ) ;
#12923=LINE ( 'NONE', #247650, #28701 ) ;
#12924=VECTOR ( 'NONE', #223058, 1000.000000000000000 ) ;
#12925=DIRECTION ( 'NONE',  ( 0.000000000000000000, -0.9651348961777156399, 0.2617529984165037349 ) ) ;
#12937=DIRECTION ( 'NONE',  ( 0.000000000000000000, -0.2617529984164506107, -0.9651348961777299618 ) ) ;
#12956=CARTESIAN_POINT ( 'NONE',  ( 20.22516295850462598, 59.74753603935580060, -225.6296577699291106 ) ) ;
#12977=AXIS2_PLACEMENT_3D ( 'NONE', #8948, #147166, #227996 ) ;
#12985=FACE_OUTER_BOUND ( 'NONE', #94350, .T. ) ;
#13004=VECTOR ( 'NONE', #256247, 1000.000000000000114 ) ;
#13010=VECTOR ( 'NONE', #145188, 1000.000000000000000 ) ;
#13017=CYLINDRICAL_SURFACE ( 'NONE', #214835, 0.5000000000000014433 ) ;
#13030=ADVANCED_FACE ( 'NONE', ( #48416 ), #56571, .T. ) ;
#13036=CARTESIAN_POINT ( 'NONE',  ( -23.15000000000000213, 59.19392724319018129, -220.9828015967491126 ) ) ;
#13045=DIRECTION ( 'NONE',  ( -1.000000000000000000, 0.000000000000000000, 0.000000000000000000 ) ) ;
#13100=CIRCLE ( 'NONE', #71361, 0.1000000000000124678 ) ;
#13103=AXIS2_PLACEMENT_3D ( 'NONE', #236664, #80129, #181847 ) ;
#13104=DIRECTION ( 'NONE',  ( 0.000000000000000000, -0.2617529984165031243, -0.9651348961777157509 ) ) ;
#13131=FACE_OUTER_BOUND ( 'NONE', #77065, .T. ) ;
#13144=CARTESIAN_POINT ( 'NONE',  ( 21.05000000000000071, 76.00000000001126921, -203.5231074845248997 ) ) ;
#13203=EDGE_LOOP ( 'NONE', ( #198259, #227829, #188806, #145960, #121496 ) ) ;
#13211=AXIS2_PLACEMENT_3D ( 'NONE', #85019, #203720, #2932 ) ;
#13235=ORIENTED_EDGE ( 'NONE', *, *, #45099, .T. ) ;
#13238=ADVANCED_FACE ( 'NONE', ( #38820 ), #98738, .F. ) ;
#13300=ORIENTED_EDGE ( 'NONE', *, *, #221020, .T. ) ;
#13377=B_SPLINE_CURVE_WITH_KNOTS ( 'NONE', 3,
 ( #82567, #46040, #205098, #206406, #81286, #240404, #141298, #123026 ),
 .UNSPECIFIED., .F., .F.,
 ( 4, 2, 2, 4 ),
 ( 0.000000000000000000, 0.0001881495939909292280, 0.0002822243909863938419, 0.0003762991879818584559 ),
 .UNSPECIFIED. ) ;
#13392=CARTESIAN_POINT ( 'NONE',  ( -21.05000000000000071, 86.10439672154322466, -209.4215112426525138 ) ) ;
#13403=DIRECTION ( 'NONE',  ( 0.000000000000000000, 0.2617529984165083423, 0.9651348961777143076 ) ) ;
#13420=ORIENTED_EDGE ( 'NONE', *, *, #26719, .F. ) ;
#13427=ADVANCED_FACE ( 'NONE', ( #34672 ), #29986, .T. ) ;
#13447=CARTESIAN_POINT ( 'NONE',  ( -20.94999999999999929, 74.95298800634525094, -207.3836470692357636 ) ) ;
#13464=DIRECTION ( 'NONE',  ( 0.000000000000000000, -0.2617529984165853363, -0.9651348961776934354 ) ) ;
#13468=DIRECTION ( 'NONE',  ( 0.000000000000000000, 0.5378121776619166905, -0.8430646840892739302 ) ) ;
#13473=EDGE_CURVE ( 'NONE', #38996, #153545, #164089, .T. ) ;
#13485=ORIENTED_EDGE ( 'NONE', *, *, #88917, .T. ) ;
#13488=EDGE_CURVE ( 'NONE', #207394, #77841, #212018, .T. ) ;
#13491=EDGE_CURVE ( 'NONE', #211904, #90469, #111621, .T. ) ;
#13500=ORIENTED_EDGE ( 'NONE', *, *, #145036, .T. ) ;
#13505=CARTESIAN_POINT ( 'NONE',  ( 20.12499999999999645, 60.48513714662838225, -225.3600541895200138 ) ) ;
#13590=DIRECTION ( 'NONE',  ( -2.952720810173289112E-16, -0.9651348961777157509, 0.2617529984165031243 ) ) ;
#13616=CIRCLE ( 'NONE', #126024, 0.09999999999998568367 ) ;
#13632=EDGE_CURVE ( 'NONE', #130829, #135164, #235006, .T. ) ;
#13656=CARTESIAN_POINT ( 'NONE',  ( -18.59999999999999787, 59.16775194334852728, -221.0793150863668473 ) ) ;
#13658=VECTOR ( 'NONE', #193858, 1000.000000000000114 ) ;
#13668=CARTESIAN_POINT ( 'NONE',  ( 20.94999999999999574, 68.51069317435826633, -224.1259271199053842 ) ) ;
#13678=ORIENTED_EDGE ( 'NONE', *, *, #240009, .T. ) ;
#13706=EDGE_CURVE ( 'NONE', #51386, #94361, #116331, .T. ) ;
#13721=ORIENTED_EDGE ( 'NONE', *, *, #252009, .F. ) ;
#13723=TOROIDAL_SURFACE ( 'NONE', #1228, 0.9750000000000019762, 0.1000000000000000056 ) ;
#13737=DIRECTION ( 'NONE',  ( 1.000000000000000000, 0.000000000000000000, 0.000000000000000000 ) ) ;
#13744=LINE ( 'NONE', #253614, #169343 ) ;
#13814=ORIENTED_EDGE ( 'NONE', *, *, #126606, .T. ) ;
#13817=DIRECTION ( 'NONE',  ( 0.000000000000000000, 0.2617529984165034018, 0.9651348961777157509 ) ) ;
#13849=AXIS2_PLACEMENT_3D ( 'NONE', #81369, #159669, #82654 ) ;
#13866=DIRECTION ( 'NONE',  ( 0.000000000000000000, 0.2617529984164915779, 0.9651348961777187485 ) ) ;
#13867=EDGE_LOOP ( 'NONE', ( #33172, #224063, #143466, #200363 ) ) ;
#13898=DIRECTION ( 'NONE',  ( 1.000000000000000000, 0.000000000000000000, 0.000000000000000000 ) ) ;
#13901=ORIENTED_EDGE ( 'NONE', *, *, #175378, .F. ) ;
#13916=EDGE_CURVE ( 'NONE', #16660, #90469, #93331, .T. ) ;
#13946=CARTESIAN_POINT ( 'NONE',  ( -23.25000000000000000, 52.91185528119410009, -244.1460391050142960 ) ) ;
#13952=DIRECTION ( 'NONE',  ( 0.000000000000000000, 0.9651348961777157509, -0.2617529984165031243 ) ) ;
#13965=ORIENTED_EDGE ( 'NONE', *, *, #196357, .T. ) ;
#14012=ORIENTED_EDGE ( 'NONE', *, *, #169781, .F. ) ;
#14092=CIRCLE ( 'NONE', #159829, 0.09999999999999883982 ) ;
#14094=CARTESIAN_POINT ( 'NONE',  ( -20.54999999999999716, 68.28002175382172823, -222.4371999040225774 ) ) ;
#14099=AXIS2_PLACEMENT_3D ( 'NONE', #88988, #166012, #168599 ) ;
#14105=DIRECTION ( 'NONE',  ( -1.000000000000000000, 3.151514657663852580E-16, -8.547182517843351137E-17 ) ) ;
#14137=DIRECTION ( 'NONE',  ( -4.408576920032447355E-17, 0.1290532225515392262, 0.9916376685811520986 ) ) ;
#14156=DIRECTION ( 'NONE',  ( 1.000000000000000000, 0.000000000000000000, 0.000000000000000000 ) ) ;
#14161=ADVANCED_FACE ( 'NONE', ( #251461 ), #9007, .T. ) ;
#14172=VERTEX_POINT ( 'NONE', #51960 ) ;
#14178=FACE_OUTER_BOUND ( 'NONE', #104305, .T. ) ;
#14200=CARTESIAN_POINT ( 'NONE',  ( -20.94999999999999929, 79.03091752131670944, -235.9469187808398942 ) ) ;
#14202=DIRECTION ( 'NONE',  ( 0.000000000000000000, 0.2617529984164938539, 0.9651348961777183044 ) ) ;
#14207=ORIENTED_EDGE ( 'NONE', *, *, #84055, .T. ) ;
#14214=ORIENTED_EDGE ( 'NONE', *, *, #18917, .T. ) ;
#14238=CARTESIAN_POINT ( 'NONE',  ( 20.58091095332318332, 60.73084122572070243, -225.3693818331944669 ) ) ;
#14239=AXIS2_PLACEMENT_3D ( 'NONE', #196980, #95329, #236120 ) ;
#14244=ORIENTED_EDGE ( 'NONE', *, *, #39434, .T. ) ;
#14255=CARTESIAN_POINT ( 'NONE',  ( 21.51976009735019346, 60.56174996242723552, -234.0462932889414560 ) ) ;
#14262=CARTESIAN_POINT ( 'NONE',  ( -18.50000000000000000, 63.79568978998910467, -212.8021059378898485 ) ) ;
#14272=DIRECTION ( 'NONE',  ( 0.000000000000000000, -0.2617529984165031243, -0.9651348961777157509 ) ) ;
#14282=EDGE_CURVE ( 'NONE', #224282, #148469, #178375, .T. ) ;
#14289=AXIS2_PLACEMENT_3D ( 'NONE', #2015, #39910, #136373 ) ;
#14304=CARTESIAN_POINT ( 'NONE',  ( 20.94999999999999929, 62.98048128140160173, -207.0210305352945568 ) ) ;
#14321=ORIENTED_EDGE ( 'NONE', *, *, #213390, .F. ) ;
#14342=ORIENTED_EDGE ( 'NONE', *, *, #87234, .F. ) ;
#14396=VECTOR ( 'NONE', #233357, 1000.000000000000114 ) ;
#14440=VERTEX_POINT ( 'NONE', #103915 ) ;
#14448=CARTESIAN_POINT ( 'NONE',  ( 21.05000000000000071, 67.23127455305841238, -235.8551265064783991 ) ) ;
#14462=CIRCLE ( 'NONE', #176754, 0.09999999999999395484 ) ;
#14528=CARTESIAN_POINT ( 'NONE',  ( 20.95035502843362707, 59.10205934002117090, -225.8004220253184258 ) ) ;
#14543=CARTESIAN_POINT ( 'NONE',  ( -23.15000000000000213, 70.76519756549814133, -215.1840646563997836 ) ) ;
#14567=CARTESIAN_POINT ( 'NONE',  ( -21.05000000000000071, 78.24390740893981899, -231.6169762517609172 ) ) ;
#14600=EDGE_CURVE ( 'NONE', #206482, #222414, #76352, .T. ) ;
#14602=VECTOR ( 'NONE', #88146, 1000.000000000000114 ) ;
#14643=ORIENTED_EDGE ( 'NONE', *, *, #41774, .F. ) ;
#14649=DIRECTION ( 'NONE',  ( -3.265361837132813093E-16, -0.9651348961777146407, 0.2617529984165072321 ) ) ;
#14670=TOROIDAL_SURFACE ( 'NONE', #56315, 0.2000000000000000111, 0.1000000000000000056 ) ;
#14673=DIRECTION ( 'NONE',  ( -1.000000000000000000, -0.000000000000000000, 0.000000000000000000 ) ) ;
#14724=CIRCLE ( 'NONE', #181310, 0.2000000000000076994 ) ;
#14733=ADVANCED_FACE ( 'NONE', ( #65468 ), #85653, .T. ) ;
#14740=EDGE_CURVE ( 'NONE', #198528, #176003, #9342, .T. ) ;
#14741=CIRCLE ( 'NONE', #201983, 0.09999999999999939493 ) ;
#14752=CARTESIAN_POINT ( 'NONE',  ( -21.14999999999999858, 67.23127455305841238, -235.8551265064783991 ) ) ;
#14765=EDGE_CURVE ( 'NONE', #221732, #47300, #194435, .T. ) ;
#14775=TOROIDAL_SURFACE ( 'NONE', #10470, 7.800000000000000711, 0.1000000000000000056 ) ;
#14780=CIRCLE ( 'NONE', #181180, 4.049999999999990941 ) ;
#14813=ADVANCED_FACE ( 'NONE', ( #250522 ), #249257, .T. ) ;
#14816=CARTESIAN_POINT ( 'NONE',  ( 23.24999999999999289, 64.23880400315596262, -222.2474036988971307 ) ) ;
#14836=DIRECTION ( 'NONE',  ( 1.000000000000000000, 0.000000000000000000, 0.000000000000000000 ) ) ;
#14858=CARTESIAN_POINT ( 'NONE',  ( -21.07016717456946608, 61.13071397353302672, -234.2006012892922513 ) ) ;
#14898=AXIS2_PLACEMENT_3D ( 'NONE', #59563, #23070, #120892 ) ;
#14900=EDGE_LOOP ( 'NONE', ( #26759, #70682, #2680, #111596 ) ) ;
#14948=CARTESIAN_POINT ( 'NONE',  ( 21.11701782572533048, 60.08865071491936760, -221.2306002442901729 ) ) ;
#14971=EDGE_CURVE ( 'NONE', #68121, #85685, #156476, .T. ) ;
#14981=ORIENTED_EDGE ( 'NONE', *, *, #193069, .F. ) ;
#14989=CIRCLE ( 'NONE', #223247, 11.65000000000000391 ) ;
#14990=EDGE_CURVE ( 'NONE', #49647, #242990, #185666, .T. ) ;
#15009=EDGE_CURVE ( 'NONE', #147541, #166406, #48099, .T. ) ;
#15030=DIRECTION ( 'NONE',  ( 0.000000000000000000, 0.2617529984165152257, 0.9651348961777124202 ) ) ;
#15042=CARTESIAN_POINT ( 'NONE',  ( -18.50000000000000000, 70.37092869010230345, -198.1237041667535550 ) ) ;
#15050=CARTESIAN_POINT ( 'NONE',  ( -20.94999999999999929, 68.58368164137472434, -224.2353459317783120 ) ) ;
#15051=CARTESIAN_POINT ( 'NONE',  ( 18.59999999999999076, 63.62814136979439184, -224.4990371885399441 ) ) ;
#15055=AXIS2_PLACEMENT_3D ( 'NONE', #112179, #249119, #191727 ) ;
#15064=DIRECTION ( 'NONE',  ( -1.000000000000000000, 0.000000000000000000, 0.000000000000000000 ) ) ;
#15160=EDGE_CURVE ( 'NONE', #188542, #128905, #84690, .T. ) ;
#15176=VERTEX_POINT ( 'NONE', #230677 ) ;
#15193=CARTESIAN_POINT ( 'NONE',  ( 20.85000000000000142, 70.22659352830977753, -197.9852579278363578 ) ) ;
#15225=CARTESIAN_POINT ( 'NONE',  ( 23.14999999999999503, 66.54223038922117439, -213.7542166125332415 ) ) ;
#15241=ORIENTED_EDGE ( 'NONE', *, *, #244045, .F. ) ;
#15266=ORIENTED_EDGE ( 'NONE', *, *, #47286, .T. ) ;
#15269=ADVANCED_FACE ( 'NONE', ( #96266 ), #156296, .F. ) ;
#15280=AXIS2_PLACEMENT_3D ( 'NONE', #169550, #249060, #196629 ) ;
#15282=EDGE_CURVE ( 'NONE', #56738, #164486, #255301, .T. ) ;
#15283=CARTESIAN_POINT ( 'NONE',  ( -21.05000000000000071, 67.23127455305841238, -235.8551265064783991 ) ) ;
#15290=FACE_OUTER_BOUND ( 'NONE', #81324, .T. ) ;
#15293=EDGE_LOOP ( 'NONE', ( #131620, #175146, #4286, #155005 ) ) ;
#15298=DIRECTION ( 'NONE',  ( 1.000000000000000000, 0.000000000000000000, 0.000000000000000000 ) ) ;
#15317=VERTEX_POINT ( 'NONE', #114571 ) ;
#15323=ORIENTED_EDGE ( 'NONE', *, *, #99735, .F. ) ;
#15330=TOROIDAL_SURFACE ( 'NONE', #165148, 0.2000000000000000111, 0.1000000000000000056 ) ;
#15336=ADVANCED_FACE ( 'NONE', ( #60999 ), #164984, .T. ) ;
#15359=ORIENTED_EDGE ( 'NONE', *, *, #192842, .T. ) ;
#15360=CARTESIAN_POINT ( 'NONE',  ( -20.64999999999999858, 81.91411460262999356, -215.0718681741873013 ) ) ;
#15374=DIRECTION ( 'NONE',  ( 1.000000000000000000, -1.772924042024179204E-16, 4.808324575169891715E-17 ) ) ;
#15382=DIRECTION ( 'NONE',  ( 0.000000000000000000, -0.9651348961777157509, 0.2617529984165031243 ) ) ;
#15388=CARTESIAN_POINT ( 'NONE',  ( -21.05000000000000071, 76.00000000001126921, -203.5231074845248997 ) ) ;
#15410=VERTEX_POINT ( 'NONE', #81815 ) ;
#15432=DIRECTION ( 'NONE',  ( -1.000000000000000000, 2.775557561562908012E-13, 0.000000000000000000 ) ) ;
#15438=CARTESIAN_POINT ( 'NONE',  ( -22.57848426163148758, 64.15977721266104083, -247.1966340115571938 ) ) ;
#15457=ADVANCED_FACE ( 'NONE', ( #23191 ), #62290, .F. ) ;
#15477=CARTESIAN_POINT ( 'NONE',  ( 21.05000000000000071, 59.16775194334852017, -221.0793150863668473 ) ) ;
#15494=EDGE_CURVE ( 'NONE', #163406, #41329, #46558, .T. ) ;
#15495=FACE_OUTER_BOUND ( 'NONE', #57722, .T. ) ;
#15515=AXIS2_PLACEMENT_3D ( 'NONE', #159270, #194556, #254465 ) ;
#15525=CARTESIAN_POINT ( 'NONE',  ( 20.96937028524355640, 58.93813165352695904, -225.8439030394954159 ) ) ;
#15526=EDGE_CURVE ( 'NONE', #235080, #254106, #27668, .T. ) ;
#15528=CIRCLE ( 'NONE', #48812, 11.90000000000000213 ) ;
#15536=CARTESIAN_POINT ( 'NONE',  ( -21.05000000000000071, 55.11435547888748232, -226.8560373590520101 ) ) ;
#15544=CARTESIAN_POINT ( 'NONE',  ( 21.14999999999999858, 60.91865828504416669, -234.1430899377568267 ) ) ;
#15550=EDGE_CURVE ( 'NONE', #2377, #256658, #131858, .T. ) ;
#15554=VECTOR ( 'NONE', #30982, 1000.000000000000000 ) ;
#15563=CARTESIAN_POINT ( 'NONE',  ( 18.59999999999999076, 64.18627039993180006, -224.3513032416919089 ) ) ;
#15599=ORIENTED_EDGE ( 'NONE', *, *, #227048, .F. ) ;
#15702=DIRECTION ( 'NONE',  ( 1.000000000000000000, -5.945622153099073960E-16, 5.981866248895712861E-16 ) ) ;
#15719=CIRCLE ( 'NONE', #248740, 0.1000000000000051958 ) ;
#15784=ADVANCED_FACE ( 'NONE', ( #219757 ), #181747, .T. ) ;
#15817=CARTESIAN_POINT ( 'NONE',  ( 21.30000000000002558, 67.23127455305841238, -235.8551265064783991 ) ) ;
#15832=AXIS2_PLACEMENT_3D ( 'NONE', #20017, #81228, #177813 ) ;
#15836=EDGE_LOOP ( 'NONE', ( #42630, #159585, #174437, #214903 ) ) ;
#15871=DIRECTION ( 'NONE',  ( 1.000000000000000000, 0.000000000000000000, 0.000000000000000000 ) ) ;
#15897=ORIENTED_EDGE ( 'NONE', *, *, #61535, .F. ) ;
#15909=EDGE_LOOP ( 'NONE', ( #99667, #105679, #224918, #17767 ) ) ;
#15930=ORIENTED_EDGE ( 'NONE', *, *, #76111, .F. ) ;
#15941=ORIENTED_EDGE ( 'NONE', *, *, #30031, .T. ) ;
#15942=CIRCLE ( 'NONE', #165775, 0.09999999999999939493 ) ;
#15987=ORIENTED_EDGE ( 'NONE', *, *, #202958, .F. ) ;
#16005=ORIENTED_EDGE ( 'NONE', *, *, #101873, .F. ) ;
#16027=ORIENTED_EDGE ( 'NONE', *, *, #134268, .T. ) ;
#16029=CARTESIAN_POINT ( 'NONE',  ( -21.14999999999999858, 64.25313205997782973, -247.2214437328673853 ) ) ;
#16034=DIRECTION ( 'NONE',  ( -0.000000000000000000, 0.9651348961777157509, -0.2617529984165031243 ) ) ;
#16054=VECTOR ( 'NONE', #249393, 1000.000000000000000 ) ;
#16072=VECTOR ( 'NONE', #254560, 1000.000000000000114 ) ;
#16090=AXIS2_PLACEMENT_3D ( 'NONE', #42227, #241703, #106015 ) ;
#16103=AXIS2_PLACEMENT_3D ( 'NONE', #41962, #105733, #100590 ) ;
#16124=FACE_OUTER_BOUND ( 'NONE', #256356, .T. ) ;
#16161=ORIENTED_EDGE ( 'NONE', *, *, #88754, .F. ) ;
#16163=VECTOR ( 'NONE', #186374, 1000.000000000000000 ) ;
#16173=VERTEX_POINT ( 'NONE', #23869 ) ;
#16186=ORIENTED_EDGE ( 'NONE', *, *, #229537, .F. ) ;
#16188=CYLINDRICAL_SURFACE ( 'NONE', #5475, 0.1000000000000124678 ) ;
#16195=ORIENTED_EDGE ( 'NONE', *, *, #169356, .F. ) ;
#16227=CIRCLE ( 'NONE', #220226, 0.1999999999999981515 ) ;
#16230=CARTESIAN_POINT ( 'NONE',  ( 18.59999999999999076, 76.00000000001126921, -203.5231074845248997 ) ) ;
#16233=CYLINDRICAL_SURFACE ( 'NONE', #135895, 0.09999999999999543976 ) ;
#16240=EDGE_CURVE ( 'NONE', #156295, #85685, #65520, .T. ) ;
#16291=B_SPLINE_CURVE_WITH_KNOTS ( 'NONE', 3,
 ( #114265, #54278, #133823, #213349, #36028, #178110, #196361, #17710, #176824, #256266, #173002, #234196, #212099, #135091, #19004, #38582 ),
 .UNSPECIFIED., .F., .F.,
 ( 4, 3, 3, 3, 3, 4 ),
 ( 0.000000000000000000, 2.209833635978134735E-05, 5.595056164119275948E-05, 8.979992002655095445E-05, 0.0001236482757198940658, 0.0001574984039362993960 ),
 .UNSPECIFIED. ) ;
#16297=ORIENTED_EDGE ( 'NONE', *, *, #223502, .T. ) ;
#16298=DIRECTION ( 'NONE',  ( 0.000000000000000000, 0.2617529984165030688, 0.9651348961777158619 ) ) ;
#16303=EDGE_LOOP ( 'NONE', ( #5906, #21744, #142772, #173740 ) ) ;
#16326=DIRECTION ( 'NONE',  ( -1.000000000000000000, 2.849773892568378313E-16, -7.728835255496647986E-17 ) ) ;
#16346=CARTESIAN_POINT ( 'NONE',  ( -18.45037301276627062, 78.22618665882693278, -231.5710384046198271 ) ) ;
#16358=VECTOR ( 'NONE', #34042, 1000.000000000000000 ) ;
#16380=EDGE_CURVE ( 'NONE', #92030, #216037, #198855, .T. ) ;
#16430=DIRECTION ( 'NONE',  ( 1.000000000000000000, 0.000000000000000000, 0.000000000000000000 ) ) ;
#16465=CARTESIAN_POINT ( 'NONE',  ( 23.14999999999998437, 78.57160958314655375, -238.9307242378722833 ) ) ;
#16531=DIRECTION ( 'NONE',  ( 1.000000000000000000, 0.000000000000000000, 0.000000000000000000 ) ) ;
#16539=DIRECTION ( 'NONE',  ( -1.000000000000000000, 0.000000000000000000, 0.000000000000000000 ) ) ;
#16549=VERTEX_POINT ( 'NONE', #45336 ) ;
#16567=ADVANCED_FACE ( 'NONE', ( #124878 ), #171637, .F. ) ;
#16586=VERTEX_POINT ( 'NONE', #84408 ) ;
#16607=ORIENTED_EDGE ( 'NONE', *, *, #163865, .F. ) ;
#16610=DIRECTION ( 'NONE',  ( 0.000000000000000000, 0.2617529984165174461, 0.9651348961777118651 ) ) ;
#16611=CARTESIAN_POINT ( 'NONE',  ( 21.05000000000000071, 82.20113918088273408, -215.0418453737790401 ) ) ;
#16626=DIRECTION ( 'NONE',  ( 1.000000000000000000, 0.000000000000000000, 0.000000000000000000 ) ) ;
#16654=EDGE_CURVE ( 'NONE', #164486, #1095, #207440, .T. ) ;
#16660=VERTEX_POINT ( 'NONE', #171738 ) ;
#16672=DIRECTION ( 'NONE',  ( -1.000000000000000000, 0.000000000000000000, 0.000000000000000000 ) ) ;
#16702=EDGE_LOOP ( 'NONE', ( #106284, #245868, #121127, #6123 ) ) ;
#16710=CARTESIAN_POINT ( 'NONE',  ( -21.05000000000000071, 70.47363787294415260, -228.3418745167492432 ) ) ;
#16717=DIRECTION ( 'NONE',  ( 1.000000000000000000, 0.000000000000000000, 0.000000000000000000 ) ) ;
#16718=DIRECTION ( 'NONE',  ( 0.000000000000000000, -0.9651348961777379554, 0.2617529984164210233 ) ) ;
#16723=FACE_OUTER_BOUND ( 'NONE', #245211, .T. ) ;
#16774=AXIS2_PLACEMENT_3D ( 'NONE', #196186, #234020, #256090 ) ;
#16812=DIRECTION ( 'NONE',  ( 0.000000000000000000, -0.9667078373770112698, -0.2558827019434132821 ) ) ;
#16874=CARTESIAN_POINT ( 'NONE',  ( -21.44999999999999929, 65.77012247227901298, -213.5448142138000378 ) ) ;
#16886=DIRECTION ( 'NONE',  ( 1.000000000000000000, -7.049440681616512959E-16, 1.911869773728117674E-16 ) ) ;
#16908=FACE_OUTER_BOUND ( 'NONE', #36751, .T. ) ;
#16919=FACE_OUTER_BOUND ( 'NONE', #162451, .T. ) ;
#16956=VECTOR ( 'NONE', #56963, 1000.000000000000000 ) ;
#16976=DIRECTION ( 'NONE',  ( 0.000000000000000000, 0.9651348961777156399, -0.2617529984165037349 ) ) ;
#16978=ADVANCED_FACE ( 'NONE', ( #45029 ), #61865, .F. ) ;
#16989=CARTESIAN_POINT ( 'NONE',  ( -18.59999999999999787, 72.06821323333463170, -225.0920403225231610 ) ) ;
#17000=CARTESIAN_POINT ( 'NONE',  ( 22.60000000000000142, 67.23127455305841238, -235.8551265064783991 ) ) ;
#17011=CARTESIAN_POINT ( 'NONE',  ( -20.64999999999999858, 68.28002175382172823, -222.4371999040225774 ) ) ;
#17023=DIRECTION ( 'NONE',  ( -0.000000000000000000, 0.2617529984165031243, 0.9651348961777157509 ) ) ;
#17026=LINE ( 'NONE', #211369, #41520 ) ;
#17032=EDGE_CURVE ( 'NONE', #28751, #68121, #53489, .T. ) ;
#17044=ORIENTED_EDGE ( 'NONE', *, *, #37175, .T. ) ;
#17069=CARTESIAN_POINT ( 'NONE',  ( 21.05000000000000071, 60.85896401437204872, -225.4389122456526025 ) ) ;
#17095=ADVANCED_FACE ( 'NONE', ( #244063 ), #66729, .F. ) ;
#17112=EDGE_CURVE ( 'NONE', #97495, #241107, #128496, .T. ) ;
#17148=CARTESIAN_POINT ( 'NONE',  ( 20.94999999999999574, 67.23127455305841238, -235.8551265064783991 ) ) ;
#17162=ORIENTED_EDGE ( 'NONE', *, *, #138471, .T. ) ;
#17163=ORIENTED_EDGE ( 'NONE', *, *, #156789, .T. ) ;
#17174=EDGE_LOOP ( 'NONE', ( #78536, #233287, #38461, #47343 ) ) ;
#17189=DIRECTION ( 'NONE',  ( 0.000000000000000000, 0.2617529984165152257, 0.9651348961777124202 ) ) ;
#17233=CARTESIAN_POINT ( 'NONE',  ( 20.94999999999999929, 81.86853375790846599, -214.9828603846715964 ) ) ;
#17249=EDGE_LOOP ( 'NONE', ( #223439, #248896, #88222, #251591 ) ) ;
#17267=CARTESIAN_POINT ( 'NONE',  ( 18.52351027002949380, 87.06367156776640570, -199.5660463946405514 ) ) ;
#17277=CARTESIAN_POINT ( 'NONE',  ( 23.24999999999999289, 66.54223038922117439, -213.7542166125332415 ) ) ;
#17281=DIRECTION ( 'NONE',  ( -1.000000000000000000, -0.000000000000000000, 0.000000000000000000 ) ) ;
#17301=LINE ( 'NONE', #138486, #126885 ) ;
#17303=DIRECTION ( 'NONE',  ( 1.000000000000000000, 0.000000000000000000, 0.000000000000000000 ) ) ;
#17314=CIRCLE ( 'NONE', #104734, 12.77500000000000568 ) ;
#17323=AXIS2_PLACEMENT_3D ( 'NONE', #176056, #117341, #196860 ) ;
#17325=CIRCLE ( 'NONE', #179819, 6.258578643762722216 ) ;
#17332=DIRECTION ( 'NONE',  ( 1.000000000000000000, 0.000000000000000000, 0.000000000000000000 ) ) ;
#17398=VECTOR ( 'NONE', #134940, 1000.000000000000000 ) ;
#17400=EDGE_LOOP ( 'NONE', ( #104660, #73171, #232660, #208778 ) ) ;
#17432=DIRECTION ( 'NONE',  ( 0.000000000000000000, 0.2617529984165152257, 0.9651348961777124202 ) ) ;
#17447=ORIENTED_EDGE ( 'NONE', *, *, #84055, .F. ) ;
#17453=ORIENTED_EDGE ( 'NONE', *, *, #250870, .F. ) ;
#17462=CIRCLE ( 'NONE', #163239, 0.09999999999999543976 ) ;
#17523=EDGE_CURVE ( 'NONE', #164185, #149408, #223772, .T. ) ;
#17535=CYLINDRICAL_SURFACE ( 'NONE', #150149, 0.1000000000000124678 ) ;
#17546=ADVANCED_FACE ( 'NONE', ( #183964 ), #200958, .T. ) ;
#17551=CARTESIAN_POINT ( 'NONE',  ( 22.59999999999999432, 64.05844819680035584, -247.1686437718134357 ) ) ;
#17554=DIRECTION ( 'NONE',  ( 0.000000000000000000, -0.9229812358756199764, 0.3848449534832346086 ) ) ;
#17556=VERTEX_POINT ( 'NONE', #118874 ) ;
#17558=EDGE_CURVE ( 'NONE', #53814, #25213, #40649, .T. ) ;
#17570=CARTESIAN_POINT ( 'NONE',  ( -21.05000000000000071, 61.06755371101182561, -205.0964418925513826 ) ) ;
#17587=CARTESIAN_POINT ( 'NONE',  ( -18.49719636458532790, 78.19930753737976659, -231.5026796452758617 ) ) ;
#17598=LINE ( 'NONE', #153317, #155260 ) ;
#17623=VERTEX_POINT ( 'NONE', #129132 ) ;
#17638=ADVANCED_FACE ( 'NONE', ( #6605 ), #65299, .T. ) ;
#17641=CARTESIAN_POINT ( 'NONE',  ( 22.49533356619868130, 55.97040697584030511, -232.8685561480749300 ) ) ;
#17684=SPHERICAL_SURFACE ( 'NONE', #185761, 0.1000000000000000056 ) ;
#17690=CARTESIAN_POINT ( 'NONE',  ( -22.50000000000000000, 67.20509925321675837, -235.9516399960961337 ) ) ;
#17708=VERTEX_POINT ( 'NONE', #76846 ) ;
#17710=CARTESIAN_POINT ( 'NONE',  ( 22.46250603428203618, 64.16148097394537331, -247.0932813659109115 ) ) ;
#17743=EDGE_LOOP ( 'NONE', ( #240706, #218308, #245701, #221088 ) ) ;
#17755=CARTESIAN_POINT ( 'NONE',  ( 20.12500000000000000, 59.94448977088796937, -225.4740812377367263 ) ) ;
#17767=ORIENTED_EDGE ( 'NONE', *, *, #241977, .T. ) ;
#17801=DIRECTION ( 'NONE',  ( 0.000000000000000000, 0.2617529984165033463, 0.9651348961777157509 ) ) ;
#17843=DIRECTION ( 'NONE',  ( 1.000000000000000000, 0.000000000000000000, 0.000000000000000000 ) ) ;
#17844=LINE ( 'NONE', #56951, #187392 ) ;
#17848=ORIENTED_EDGE ( 'NONE', *, *, #5235, .F. ) ;
#17876=EDGE_CURVE ( 'NONE', #90831, #164109, #48996, .T. ) ;
#17881=EDGE_LOOP ( 'NONE', ( #3967, #182900, #93581, #62279 ) ) ;
#17988=CARTESIAN_POINT ( 'NONE',  ( -18.50000000000000000, 71.93512633425886804, -225.1442869522136334 ) ) ;
#18001=ORIENTED_EDGE ( 'NONE', *, *, #226944, .T. ) ;
#18014=ADVANCED_FACE ( 'NONE', ( #25882 ), #186231, .F. ) ;
#18086=DIRECTION ( 'NONE',  ( 0.000000000000000000, 0.001293682058376932620, 0.9999991631930158498 ) ) ;
#18097=VERTEX_POINT ( 'NONE', #93533 ) ;
#18134=DIRECTION ( 'NONE',  ( 0.000000000000000000, 0.2617529984165034573, 0.9651348961777156399 ) ) ;
#18145=ORIENTED_EDGE ( 'NONE', *, *, #90844, .T. ) ;
#18149=CARTESIAN_POINT ( 'NONE',  ( -22.48660254037843842, 55.97436536266720708, -232.8539608197349651 ) ) ;
#18158=VERTEX_POINT ( 'NONE', #90967 ) ;
#18165=CARTESIAN_POINT ( 'NONE',  ( -18.50000000000000000, 68.22930980752001062, -227.7331931781284879 ) ) ;
#18180=CARTESIAN_POINT ( 'NONE',  ( 18.60000000000000142, 78.12133356376091342, -231.3112718935514636 ) ) ;
#18199=CYLINDRICAL_SURFACE ( 'NONE', #220624, 0.09999999999999939493 ) ;
#18214=ORIENTED_EDGE ( 'NONE', *, *, #174641, .F. ) ;
#18216=CARTESIAN_POINT ( 'NONE',  ( 22.57856590037848932, 64.15964591429192865, -247.1965985637075391 ) ) ;
#18224=VECTOR ( 'NONE', #25109, 1000.000000000000000 ) ;
#18226=VECTOR ( 'NONE', #78702, 1000.000000000000000 ) ;
#18245=CYLINDRICAL_SURFACE ( 'NONE', #5029, 0.1000000000000106498 ) ;
#18267=CIRCLE ( 'NONE', #159734, 0.1000000000000124678 ) ;
#18275=CYLINDRICAL_SURFACE ( 'NONE', #51044, 4.049999999999987388 ) ;
#18283=LINE ( 'NONE', #199512, #239235 ) ;
#18284=ORIENTED_EDGE ( 'NONE', *, *, #164388, .F. ) ;
#18291=CARTESIAN_POINT ( 'NONE',  ( 21.05000000000022453, 65.56236711878459289, -242.0759453707015609 ) ) ;
#18325=DIRECTION ( 'NONE',  ( -3.265361837132813093E-16, -0.9651348961777157509, 0.2617529984165031243 ) ) ;
#18328=CARTESIAN_POINT ( 'NONE',  ( 21.05000000000000071, 61.00122447389661318, -225.2976766370351527 ) ) ;
#18330=CARTESIAN_POINT ( 'NONE',  ( 20.95289811251229750, 60.87354190138334076, -225.3219200926538690 ) ) ;
#18337=CARTESIAN_POINT ( 'NONE',  ( 23.25000000000000000, 75.49601185175264106, -250.2710592679604531 ) ) ;
#18339=EDGE_LOOP ( 'NONE', ( #142797, #191647, #23697, #37940 ) ) ;
#18348=CARTESIAN_POINT ( 'NONE',  ( 23.15000000000000213, 84.16003609933891028, -218.3250942044780345 ) ) ;
#18354=DIRECTION ( 'NONE',  ( 0.1538461538461520228, -0.9536447854760599085, 0.2586367802170949082 ) ) ;
#18360=DIRECTION ( 'NONE',  ( -0.000000000000000000, 0.2617529984165031243, 0.9651348961777157509 ) ) ;
#18376=MANIFOLD_SOLID_BREP ( 'Stock-MAS-200-1', #140954 ) ;
#18398=AXIS2_PLACEMENT_3D ( 'NONE', #69978, #184757, #109069 ) ;
#18419=ORIENTED_EDGE ( 'NONE', *, *, #35282, .T. ) ;
#18423=CARTESIAN_POINT ( 'NONE',  ( 21.05995757104869881, 61.95389314678300963, -221.7884135696254475 ) ) ;
#18471=ORIENTED_EDGE ( 'NONE', *, *, #138136, .T. ) ;
#18479=CIRCLE ( 'NONE', #164234, 0.09999999999999939493 ) ;
#18488=CARTESIAN_POINT ( 'NONE',  ( -21.00857864376268935, 57.84918772656043018, -226.1321410194968280 ) ) ;
#18500=CIRCLE ( 'NONE', #205931, 0.1000000000000124678 ) ;
#18505=CARTESIAN_POINT ( 'NONE',  ( 22.39999999999999503, 65.20268881533050376, -243.3349219518556765 ) ) ;
#18517=CARTESIAN_POINT ( 'NONE',  ( 23.24999999999999289, 59.16775194334852017, -221.0793150863668473 ) ) ;
#18519=ADVANCED_FACE ( 'NONE', ( #98319 ), #136851, .F. ) ;
#18550=AXIS2_PLACEMENT_3D ( 'NONE', #105017, #185878, #42516 ) ;
#18552=LINE ( 'NONE', #238881, #102860 ) ;
#18574=AXIS2_PLACEMENT_3D ( 'NONE', #167917, #248707, #47920 ) ;
#18608=CARTESIAN_POINT ( 'NONE',  ( 20.00000000000000355, 62.34315093393704643, -208.9889535843037436 ) ) ;
#18616=AXIS2_PLACEMENT_3D ( 'NONE', #152408, #173279, #214912 ) ;
#18625=EDGE_LOOP ( 'NONE', ( #169334, #164077, #142258, #253728 ) ) ;
#18641=EDGE_CURVE ( 'NONE', #206043, #140485, #132778, .T. ) ;
#18702=CIRCLE ( 'NONE', #143600, 0.09999999999999939493 ) ;
#18716=CARTESIAN_POINT ( 'NONE',  ( -20.64999999999999858, 63.56320957583155717, -222.0641766000055668 ) ) ;
#18723=VECTOR ( 'NONE', #221678, 1000.000000000000114 ) ;
#18725=DIRECTION ( 'NONE',  ( 0.000000000000000000, -0.9651348961777157509, 0.2617529984165031243 ) ) ;
#18741=ORIENTED_EDGE ( 'NONE', *, *, #102791, .T. ) ;
#18754=DIRECTION ( 'NONE',  ( 0.000000000000000000, -0.2617529984164856383, -0.9651348961777204138 ) ) ;
#18799=AXIS2_PLACEMENT_3D ( 'NONE', #254413, #140922, #75810 ) ;
#18811=ORIENTED_EDGE ( 'NONE', *, *, #109709, .F. ) ;
#18825=CARTESIAN_POINT ( 'NONE',  ( 21.13614978966382196, 65.53011441033059725, -242.1276392481308619 ) ) ;
#18829=DIRECTION ( 'NONE',  ( 1.000000000000000000, 0.000000000000000000, 0.000000000000000000 ) ) ;
#18834=CARTESIAN_POINT ( 'NONE',  ( 20.94999999999999929, 65.69992488703364586, -222.9708107233114163 ) ) ;
#18839=DIRECTION ( 'NONE',  ( 1.224646799147353207E-16, -0.9651348961777157509, 0.2617529984165031243 ) ) ;
#18911=DIRECTION ( 'NONE',  ( 0.000000000000000000, 0.9651348961777157509, -0.2617529984165031243 ) ) ;
#18917=EDGE_CURVE ( 'NONE', #142612, #250542, #70442, .T. ) ;
#18938=DIRECTION ( 'NONE',  ( 0.000000000000000000, 0.9651348961777157509, -0.2617529984165031243 ) ) ;
#18946=DIRECTION ( 'NONE',  ( 0.000000000000000000, -0.9651348961777161950, 0.2617529984165014589 ) ) ;
#18979=LINE ( 'NONE', #17690, #122042 ) ;
#19004=CARTESIAN_POINT ( 'NONE',  ( 22.49999999999999645, 64.09620057108240587, -247.0754729532595206 ) ) ;
#19006=DIRECTION ( 'NONE',  ( 0.000000000000000000, -0.1071148137998806232, -0.9942466578594150173 ) ) ;
#19020=DIRECTION ( 'NONE',  ( -1.000000000000000000, 2.849773892568378313E-16, -7.728835255496647986E-17 ) ) ;
#19053=AXIS2_PLACEMENT_3D ( 'NONE', #122596, #203406, #6471 ) ;
#19084=DIRECTION ( 'NONE',  ( 0.000000000000000000, 0.7106264324241517993, -0.7035695228903270371 ) ) ;
#19088=DIRECTION ( 'NONE',  ( -0.000000000000000000, -0.2617529984165031243, -0.9651348961777157509 ) ) ;
#19099=ORIENTED_EDGE ( 'NONE', *, *, #96921, .F. ) ;
#19130=ADVANCED_FACE ( 'NONE', ( #54450 ), #120493, .T. ) ;
#19131=ORIENTED_EDGE ( 'NONE', *, *, #5630, .F. ) ;
#19139=CARTESIAN_POINT ( 'NONE',  ( 20.94999999999999929, 70.60134440767089359, -223.4290147181903023 ) ) ;
#19140=DIRECTION ( 'NONE',  ( 0.000000000000000000, 0.2617529984165152257, 0.9651348961777124202 ) ) ;
#19142=ORIENTED_EDGE ( 'NONE', *, *, #47631, .T. ) ;
#19150=VERTEX_POINT ( 'NONE', #136540 ) ;
#19156=ORIENTED_EDGE ( 'NONE', *, *, #82656, .F. ) ;
#19171=B_SPLINE_CURVE_WITH_KNOTS ( 'NONE', 3,
 ( #257435, #158431, #93938, #226038, #244342, #86532, #65715, #246912 ),
 .UNSPECIFIED., .F., .F.,
 ( 4, 2, 2, 4 ),
 ( 0.000000000000000000, 0.0001094981963948357250, 0.0002189963927896714500, 0.0004379927855794142947 ),
 .UNSPECIFIED. ) ;
#19172=AXIS2_PLACEMENT_3D ( 'NONE', #11703, #108223, #91233 ) ;
#19179=DIRECTION ( 'NONE',  ( 1.000000000000000000, 0.000000000000000000, 0.000000000000000000 ) ) ;
#19188=CARTESIAN_POINT ( 'NONE',  ( 20.85000000000000142, 76.30149234032609229, -203.6488173052385946 ) ) ;
#19189=ORIENTED_EDGE ( 'NONE', *, *, #108037, .F. ) ;
#19191=EDGE_CURVE ( 'NONE', #138432, #231688, #212060, .T. ) ;
#19270=CARTESIAN_POINT ( 'NONE',  ( 18.31325810956447953, 87.00173612015743174, -199.3903144367706943 ) ) ;
#19283=CARTESIAN_POINT ( 'NONE',  ( 23.14999999999999503, 62.92003201576280702, -207.2439188921395612 ) ) ;
#19289=CARTESIAN_POINT ( 'NONE',  ( 18.59999999999999432, 70.47363787294415260, -228.3418745167492432 ) ) ;
#19309=CARTESIAN_POINT ( 'NONE',  ( -21.05000000000000071, 72.05339752741123505, -225.0867394276846483 ) ) ;
#19345=ADVANCED_FACE ( 'NONE', ( #49006 ), #89410, .T. ) ;
#19358=CARTESIAN_POINT ( 'NONE',  ( 20.94999999999999929, 86.45856254523212669, -209.4679346046102921 ) ) ;
#19369=FACE_OUTER_BOUND ( 'NONE', #30442, .T. ) ;
#19388=AXIS2_PLACEMENT_3D ( 'NONE', #71087, #129755, #29413 ) ;
#19463=ORIENTED_EDGE ( 'NONE', *, *, #67790, .F. ) ;
#19483=CARTESIAN_POINT ( 'NONE',  ( 19.88284271247462343, 62.42586252704481353, -208.9077732303340440 ) ) ;
#19534=PRODUCT_CONTEXT ( 'NONE', #20799, 'mechanical' ) ;
#19558=CIRCLE ( 'NONE', #36311, 0.1000000000000124678 ) ;
#19580=ORIENTED_EDGE ( 'NONE', *, *, #231334, .T. ) ;
#19584=AXIS2_PLACEMENT_3D ( 'NONE', #2627, #204676, #1337 ) ;
#19590=CARTESIAN_POINT ( 'NONE',  ( 21.05000000000000426, 65.51923798433686841, -242.1677427744925808 ) ) ;
#19612=ORIENTED_EDGE ( 'NONE', *, *, #138131, .T. ) ;
#19623=CYLINDRICAL_SURFACE ( 'NONE', #71936, 0.09999999999999939493 ) ;
#19631=PLANE ( 'NONE',  #250327 ) ;
#19649=DIRECTION ( 'NONE',  ( -0.9880948137434723000, -0.1484822917196432779, 0.04026969206407596952 ) ) ;
#19660=VECTOR ( 'NONE', #187002, 1000.000000000000000 ) ;
#19686=EDGE_LOOP ( 'NONE', ( #91709, #195489, #141138, #129426, #131841 ) ) ;
#19696=ADVANCED_FACE ( 'NONE', ( #164807 ), #185651, .F. ) ;
#19721=ORIENTED_EDGE ( 'NONE', *, *, #72032, .F. ) ;
#19722=VERTEX_POINT ( 'NONE', #205192 ) ;
#19724=CARTESIAN_POINT ( 'NONE',  ( 21.07199075132372101, 61.95919758692989632, -221.7705522472584221 ) ) ;
#19749=ORIENTED_EDGE ( 'NONE', *, *, #73936, .F. ) ;
#19752=ORIENTED_EDGE ( 'NONE', *, *, #131149, .F. ) ;
#19777=AXIS2_PLACEMENT_3D ( 'NONE', #93730, #155017, #33804 ) ;
#19855=LINE ( 'NONE', #57659, #81875 ) ;
#19866=DIRECTION ( 'NONE',  ( -1.000000000000000000, -5.945622153099073960E-16, 5.981866248895712861E-16 ) ) ;
#19878=DIRECTION ( 'NONE',  ( 1.000000000000000000, 0.000000000000000000, 0.000000000000000000 ) ) ;
#19890=CARTESIAN_POINT ( 'NONE',  ( -22.59999999999999787, 67.23127455305841238, -235.8551265064783991 ) ) ;
#19905=CARTESIAN_POINT ( 'NONE',  ( 19.87657994471983258, 62.37345882273933739, -208.8772024246652848 ) ) ;
#19907=EDGE_LOOP ( 'NONE', ( #177883, #232608, #248019, #151934 ) ) ;
#19917=DIRECTION ( 'NONE',  ( 1.000000000000000000, 0.000000000000000000, 0.000000000000000000 ) ) ;
#19924=AXIS2_PLACEMENT_3D ( 'NONE', #87817, #108695, #7018 ) ;
#19933=VERTEX_POINT ( 'NONE', #16029 ) ;
#19939=DIRECTION ( 'NONE',  ( 1.000000000000000000, 0.000000000000000000, 0.000000000000000000 ) ) ;
#19956=VERTEX_POINT ( 'NONE', #95532 ) ;
#19995=DIRECTION ( 'NONE',  ( 1.000000000000000000, 0.000000000000000000, 0.000000000000000000 ) ) ;
#20004=ORIENTED_EDGE ( 'NONE', *, *, #164578, .F. ) ;
#20008=ORIENTED_EDGE ( 'NONE', *, *, #7633, .F. ) ;
#20017=CARTESIAN_POINT ( 'NONE',  ( 21.05000000000000071, 67.23127455305841238, -235.8551265064783991 ) ) ;
#20033=AXIS2_PLACEMENT_3D ( 'NONE', #85948, #66422, #187673 ) ;
#20078=ORIENTED_EDGE ( 'NONE', *, *, #57496, .F. ) ;
#20086=AXIS2_PLACEMENT_3D ( 'NONE', #79810, #197211, #141103 ) ;
#20101=CIRCLE ( 'NONE', #157500, 0.1000000000000124678 ) ;
#20122=DIRECTION ( 'NONE',  ( 1.000000000000000000, 0.000000000000000000, 0.000000000000000000 ) ) ;
#20124=DIRECTION ( 'NONE',  ( -1.000000000000000000, 1.772924042024179204E-16, -4.808324575169892332E-17 ) ) ;
#20145=CARTESIAN_POINT ( 'NONE',  ( 23.14999999999999858, 78.02678328198446422, -204.0727887811995629 ) ) ;
#20146=AXIS2_PLACEMENT_3D ( 'NONE', #246096, #88261, #28358 ) ;
#20190=ORIENTED_EDGE ( 'NONE', *, *, #132845, .T. ) ;
#20281=CARTESIAN_POINT ( 'NONE',  ( 20.94999999999999929, 70.37092869010230345, -198.1237041667535550 ) ) ;
#20287=CARTESIAN_POINT ( 'NONE',  ( -23.25000000000000000, 70.60814576644823148, -215.7631455941064189 ) ) ;
#20293=ORIENTED_EDGE ( 'NONE', *, *, #225350, .F. ) ;
#20302=ORIENTED_EDGE ( 'NONE', *, *, #197449, .T. ) ;
#20316=DIRECTION ( 'NONE',  ( 0.000000000000000000, 0.2617529984164915779, 0.9651348961777189706 ) ) ;
#20359=ORIENTED_EDGE ( 'NONE', *, *, #47897, .F. ) ;
#20382=CARTESIAN_POINT ( 'NONE',  ( 21.87500000000000355, 63.35728523183471594, -212.8904317177587870 ) ) ;
#20396=CARTESIAN_POINT ( 'NONE',  ( -21.14999999999999858, 78.57160958314655375, -238.9307242378722833 ) ) ;
#20463=FACE_OUTER_BOUND ( 'NONE', #189315, .T. ) ;
#20466=DIRECTION ( 'NONE',  ( 4.408576920032446739E-17, 0.3896596508880098009, 0.9209589331071360574 ) ) ;
#20517=EDGE_CURVE ( 'NONE', #154671, #175678, #161630, .T. ) ;
#20527=CYLINDRICAL_SURFACE ( 'NONE', #7606, 0.1000000000000124678 ) ;
#20555=AXIS2_PLACEMENT_3D ( 'NONE', #17148, #15871, #131933 ) ;
#20573=CYLINDRICAL_SURFACE ( 'NONE', #251066, 0.09999999999999939493 ) ;
#20575=CARTESIAN_POINT ( 'NONE',  ( 18.39999999999999858, 87.08727414655709254, -199.6327537731849873 ) ) ;
#20590=CYLINDRICAL_SURFACE ( 'NONE', #181195, 0.1000000000000124678 ) ;
#20599=EDGE_LOOP ( 'NONE', ( #193845, #18145, #137465 ) ) ;
#20611=LINE ( 'NONE', #156287, #8701 ) ;
#20616=AXIS2_PLACEMENT_3D ( 'NONE', #95917, #157223, #257512 ) ;
#20618=VERTEX_POINT ( 'NONE', #68077 ) ;
#20619=CARTESIAN_POINT ( 'NONE',  ( -20.85000000000000142, 79.19526988099229925, -196.1889237952725296 ) ) ;
#20628=ORIENTED_EDGE ( 'NONE', *, *, #251635, .T. ) ;
#20630=CYLINDRICAL_SURFACE ( 'NONE', #78006, 0.09999999999999939493 ) ;
#20639=CARTESIAN_POINT ( 'NONE',  ( 22.00356870141986576, 60.22995210369071373, -233.9563068168734787 ) ) ;
#20645=CARTESIAN_POINT ( 'NONE',  ( 21.98333005346336577, 65.30108822512866595, -242.9721039335941555 ) ) ;
#20691=ORIENTED_EDGE ( 'NONE', *, *, #153245, .F. ) ;
#20693=VERTEX_POINT ( 'NONE', #145033 ) ;
#20701=EDGE_LOOP ( 'NONE', ( #100535, #184863, #15323, #202214 ) ) ;
#20735=LINE ( 'NONE', #140655, #156335 ) ;
#20772=CIRCLE ( 'NONE', #154072, 3.899999999999987477 ) ;
#20778=VERTEX_POINT ( 'NONE', #134136 ) ;
#20792=CIRCLE ( 'NONE', #128922, 2.099999999999995204 ) ;
#20799=APPLICATION_CONTEXT ( 'automotive_design' ) ;
#20821=DIRECTION ( 'NONE',  ( 1.000000000000000000, 0.000000000000000000, 0.000000000000000000 ) ) ;
#20830=CARTESIAN_POINT ( 'NONE',  ( 23.14999999999999503, 59.16775194334852017, -221.0793150863668473 ) ) ;
#20855=EDGE_CURVE ( 'NONE', #139316, #232566, #79288, .T. ) ;
#20860=DIRECTION ( 'NONE',  ( 0.000000000000000000, 0.2617529984164856383, 0.9651348961777204138 ) ) ;
#20868=ADVANCED_FACE ( 'NONE', ( #238376 ), #83699, .F. ) ;
#20869=ORIENTED_EDGE ( 'NONE', *, *, #128913, .T. ) ;
#20959=EDGE_CURVE ( 'NONE', #154671, #256377, #211694, .T. ) ;
#20961=VECTOR ( 'NONE', #112025, 1000.000000000000000 ) ;
#20997=EDGE_CURVE ( 'NONE', #168, #96108, #28152, .T. ) ;
#21004=DIRECTION ( 'NONE',  ( 0.000000000000000000, -0.2617529984165152257, -0.9651348961777124202 ) ) ;
#21020=CARTESIAN_POINT ( 'NONE',  ( 21.06600267594171783, 61.95655793666846023, -221.7794405828697393 ) ) ;
#21024=CIRCLE ( 'NONE', #137674, 0.5000000000000051070 ) ;
#21029=ORIENTED_EDGE ( 'NONE', *, *, #201611, .F. ) ;
#21034=VECTOR ( 'NONE', #191175, 1000.000000000000114 ) ;
#21069=ORIENTED_EDGE ( 'NONE', *, *, #54203, .T. ) ;
#21072=EDGE_CURVE ( 'NONE', #101793, #176003, #162784, .T. ) ;
#21079=DIRECTION ( 'NONE',  ( 0.000000000000000000, 0.2617529984165024026, 0.9651348961777158619 ) ) ;
#21105=DIRECTION ( 'NONE',  ( 6.938893903907223644E-15, 0.9651348961777157509, -0.2617529984165028467 ) ) ;
#21116=CARTESIAN_POINT ( 'NONE',  ( 22.00411653889229058, 65.23707900164814077, -242.8297538143178258 ) ) ;
#21118=ORIENTED_EDGE ( 'NONE', *, *, #175402, .F. ) ;
#21153=VECTOR ( 'NONE', #244706, 1000.000000000000000 ) ;
#21176=ORIENTED_EDGE ( 'NONE', *, *, #43733, .F. ) ;
#21235=FACE_OUTER_BOUND ( 'NONE', #71693, .T. ) ;
#21273=ORIENTED_EDGE ( 'NONE', *, *, #201565, .F. ) ;
#21280=CIRCLE ( 'NONE', #233649, 0.1000000000000124678 ) ;
#21287=ORIENTED_EDGE ( 'NONE', *, *, #124774, .T. ) ;
#21294=EDGE_CURVE ( 'NONE', #253128, #45881, #128662, .T. ) ;
#21328=ORIENTED_EDGE ( 'NONE', *, *, #113538, .F. ) ;
#21332=ORIENTED_EDGE ( 'NONE', *, *, #197969, .F. ) ;
#21368=CARTESIAN_POINT ( 'NONE',  ( -22.47886152344871036, 64.14566162948754879, -247.0891211027675070 ) ) ;
#21415=EDGE_CURVE ( 'NONE', #242736, #101417, #35746, .T. ) ;
#21449=CARTESIAN_POINT ( 'NONE',  ( 20.94999999999999929, 76.00000000001126921, -203.5231074845248997 ) ) ;
#21465=ADVANCED_FACE ( 'NONE', ( #237770 ), #77393, .T. ) ;
#21487=DIRECTION ( 'NONE',  ( -0.1538461538461520228, -0.9536447854760599085, 0.2586367802170949082 ) ) ;
#21574=ORIENTED_EDGE ( 'NONE', *, *, #86400, .T. ) ;
#21578=CIRCLE ( 'NONE', #92294, 0.1000000000000124678 ) ;
#21589=VECTOR ( 'NONE', #113480, 1000.000000000000000 ) ;
#21592=AXIS2_PLACEMENT_3D ( 'NONE', #120928, #143003, #200437 ) ;
#21603=CARTESIAN_POINT ( 'NONE',  ( 18.59999999999999076, 68.59681812508419796, -224.1344059333694361 ) ) ;
#21620=FACE_OUTER_BOUND ( 'NONE', #40657, .T. ) ;
#21631=CYLINDRICAL_SURFACE ( 'NONE', #143074, 0.1000000000000124678 ) ;
#21633=EDGE_CURVE ( 'NONE', #129900, #146108, #3162, .T. ) ;
#21657=EDGE_LOOP ( 'NONE', ( #245248, #49385, #41429, #96026 ) ) ;
#21696=EDGE_CURVE ( 'NONE', #203694, #175678, #57326, .T. ) ;
#21711=DIRECTION ( 'NONE',  ( -4.239556034732055511E-17, -0.3848449534832868446, -0.9229812358755982160 ) ) ;
#21715=CARTESIAN_POINT ( 'NONE',  ( -21.10257677756357708, 61.04944212076151189, -234.2044117394509044 ) ) ;
#21733=CIRCLE ( 'NONE', #150889, 0.1000000000000124678 ) ;
#21744=ORIENTED_EDGE ( 'NONE', *, *, #252508, .T. ) ;
#21751=VECTOR ( 'NONE', #161548, 1000.000000000000000 ) ;
#21753=AXIS2_PLACEMENT_3D ( 'NONE', #6660, #69235, #27560 ) ;
#21761=VECTOR ( 'NONE', #24342, 1000.000000000000000 ) ;
#21765=CARTESIAN_POINT ( 'NONE',  ( 18.49713797159830264, 78.19937966003901408, -231.5028605801859385 ) ) ;
#21770=DIRECTION ( 'NONE',  ( 1.000000000000000000, 0.000000000000000000, 0.000000000000000000 ) ) ;
#21777=LINE ( 'NONE', #92620, #189915 ) ;
#21831=CARTESIAN_POINT ( 'NONE',  ( -18.59999999999999787, 79.14291928130900544, -196.3819507745080557 ) ) ;
#21868=PLANE ( 'NONE',  #206432 ) ;
#21899=CIRCLE ( 'NONE', #209318, 0.1000000000000124678 ) ;
#21947=CARTESIAN_POINT ( 'NONE',  ( -20.54999999999999716, 70.60814576644823148, -215.7631455941064189 ) ) ;
#22002=AXIS2_PLACEMENT_3D ( 'NONE', #104809, #86536, #180542 ) ;
#22013=EDGE_CURVE ( 'NONE', #44096, #112321, #91798, .T. ) ;
#22014=LINE ( 'NONE', #1124, #156527 ) ;
#22046=AXIS2_PLACEMENT_3D ( 'NONE', #202535, #4319, #83825 ) ;
#22050=EDGE_CURVE ( 'NONE', #29748, #251252, #28470, .T. ) ;
#22088=DIRECTION ( 'NONE',  ( 0.000000000000000000, -0.9651348961777157509, 0.2617529984165031243 ) ) ;
#22110=SPHERICAL_SURFACE ( 'NONE', #187755, 0.1000000000000000056 ) ;
#22118=EDGE_CURVE ( 'NONE', #165864, #123166, #156823, .T. ) ;
#22135=ORIENTED_EDGE ( 'NONE', *, *, #202051, .F. ) ;
#22162=CARTESIAN_POINT ( 'NONE',  ( 22.60000000000000142, 55.86495732666938352, -232.8769840133977880 ) ) ;
#22179=CARTESIAN_POINT ( 'NONE',  ( -21.05000000000000071, 77.04701199367727327, -199.6625678998140359 ) ) ;
#22183=CARTESIAN_POINT ( 'NONE',  ( -22.39999999999999858, 55.89093952297024970, -232.7795287750844579 ) ) ;
#22194=VECTOR ( 'NONE', #74444, 1000.000000000000114 ) ;
#22229=DIRECTION ( 'NONE',  ( 1.000000000000000000, 0.000000000000000000, 0.000000000000000000 ) ) ;
#22273=ORIENTED_EDGE ( 'NONE', *, *, #128198, .T. ) ;
#22278=CARTESIAN_POINT ( 'NONE',  ( -18.50000000000000000, 63.86602797976523505, -212.9247947273492514 ) ) ;
#22295=EDGE_CURVE ( 'NONE', #46773, #20778, #16227, .T. ) ;
#22341=DIRECTION ( 'NONE',  ( 1.000000000000000000, 0.000000000000000000, 0.000000000000000000 ) ) ;
#22350=DIRECTION ( 'NONE',  ( -1.000000000000000000, -0.000000000000000000, -0.000000000000000000 ) ) ;
#22378=DIRECTION ( 'NONE',  ( -1.000000000000000000, -5.945622153099073960E-16, 5.981866248895714834E-16 ) ) ;
#22419=FACE_OUTER_BOUND ( 'NONE', #94465, .T. ) ;
#22422=CIRCLE ( 'NONE', #89021, 2.099999999999995204 ) ;
#22423=DIRECTION ( 'NONE',  ( 1.000000000000000000, 0.000000000000000000, 0.000000000000000000 ) ) ;
#22424=FACE_OUTER_BOUND ( 'NONE', #117743, .T. ) ;
#22481=CARTESIAN_POINT ( 'NONE',  ( 19.80993210785520375, 62.37380685587606166, -208.8759191578901664 ) ) ;
#22491=CARTESIAN_POINT ( 'NONE',  ( -21.05000000000000071, 67.23127455305841238, -235.8551265064783991 ) ) ;
#22492=CARTESIAN_POINT ( 'NONE',  ( 21.08804281139606474, 60.21242112883888353, -221.1554135929782490 ) ) ;
#22513=EDGE_CURVE ( 'NONE', #112321, #230038, #153629, .T. ) ;
#22559=CARTESIAN_POINT ( 'NONE',  ( 18.59999999999997655, 78.06784868750165174, -195.8985418047209350 ) ) ;
#22560=VERTEX_POINT ( 'NONE', #16989 ) ;
#22569=ORIENTED_EDGE ( 'NONE', *, *, #205139, .T. ) ;
#22574=VECTOR ( 'NONE', #35608, 1000.000000000000114 ) ;
#22640=AXIS2_PLACEMENT_3D ( 'NONE', #94632, #55472, #253702 ) ;
#22647=ORIENTED_EDGE ( 'NONE', *, *, #121668, .F. ) ;
#22652=CARTESIAN_POINT ( 'NONE',  ( -22.49072729836729678, 64.12733727798033101, -247.0841716932466738 ) ) ;
#22655=( NAMED_UNIT ( * ) PLANE_ANGLE_UNIT ( ) SI_UNIT ( $, .RADIAN. ) );
#22657=CARTESIAN_POINT ( 'NONE',  ( 21.14999999999999858, 56.01362831242965967, -232.7091905853083347 ) ) ;
#22669=AXIS2_PLACEMENT_3D ( 'NONE', #17570, #253611, #155836 ) ;
#22677=AXIS2_PLACEMENT_3D ( 'NONE', #214691, #135140, #37366 ) ;
#22684=DIRECTION ( 'NONE',  ( 0.000000000000000000, 0.2617529984164915779, 0.9651348961777187485 ) ) ;
#22691=VERTEX_POINT ( 'NONE', #182483 ) ;
#22711=CIRCLE ( 'NONE', #14898, 0.1000000000000124678 ) ;
#22739=CARTESIAN_POINT ( 'NONE',  ( 23.25000000000000000, 61.47936603916258491, -212.1738987416902376 ) ) ;
#22758=CARTESIAN_POINT ( 'NONE',  ( 23.15000000000000213, 86.43238724539048690, -209.5644480942280836 ) ) ;
#22761=CARTESIAN_POINT ( 'NONE',  ( 20.89878130938411616, 67.49249915771264341, -195.4369143829851510 ) ) ;
#22772=CARTESIAN_POINT ( 'NONE',  ( 21.95218792049437440, 60.25492730956543852, -234.0656861121678673 ) ) ;
#22805=VERTEX_POINT ( 'NONE', #132783 ) ;
#22862=ORIENTED_EDGE ( 'NONE', *, *, #121865, .T. ) ;
#22898=ORIENTED_EDGE ( 'NONE', *, *, #5265, .F. ) ;
#22906=ORIENTED_EDGE ( 'NONE', *, *, #65866, .T. ) ;
#22929=ORIENTED_EDGE ( 'NONE', *, *, #219576, .F. ) ;
#22973=ORIENTED_EDGE ( 'NONE', *, *, #214730, .T. ) ;
#22975=CARTESIAN_POINT ( 'NONE',  ( -20.85000000000000142, 70.15623657602074559, -198.0563205710787713 ) ) ;
#23014=ORIENTED_EDGE ( 'NONE', *, *, #71245, .F. ) ;
#23047=ORIENTED_EDGE ( 'NONE', *, *, #24882, .T. ) ;
#23070=DIRECTION ( 'NONE',  ( -0.000000000000000000, 0.9651348961777157509, -0.2617529984165031243 ) ) ;
#23087=DIRECTION ( 'NONE',  ( 0.000000000000000000, 0.2617529984165152257, 0.9651348961777124202 ) ) ;
#23096=CARTESIAN_POINT ( 'NONE',  ( -20.54999999999999716, 82.48249193998721296, -215.5326005316167084 ) ) ;
#23098=CARTESIAN_POINT ( 'NONE',  ( -21.65000000000000213, 65.35370752038342346, -213.3282663891675952 ) ) ;
#23144=CARTESIAN_POINT ( 'NONE',  ( 22.50000000000000000, 65.09550114356429162, -243.3481044654562879 ) ) ;
#23159=EDGE_CURVE ( 'NONE', #208387, #123814, #245530, .T. ) ;
#23166=DIRECTION ( 'NONE',  ( -1.000000000000000000, -0.000000000000000000, -0.000000000000000000 ) ) ;
#23189=TOROIDAL_SURFACE ( 'NONE', #168956, 0.2000000000000000111, 0.1000000000000000056 ) ;
#23191=FACE_OUTER_BOUND ( 'NONE', #34389, .T. ) ;
#23196=DIRECTION ( 'NONE',  ( 0.000000000000000000, 0.2617529984164856383, 0.9651348961777204138 ) ) ;
#23204=CARTESIAN_POINT ( 'NONE',  ( 21.97500000000000497, 61.05385884576949707, -221.3836188041226762 ) ) ;
#23217=CARTESIAN_POINT ( 'NONE',  ( -18.50000000000000000, 63.83985267992358104, -213.0213082169670145 ) ) ;
#23234=CARTESIAN_POINT ( 'NONE',  ( -21.07094088545368749, 65.48150606888252412, -241.9290547188616074 ) ) ;
#23248=EDGE_LOOP ( 'NONE', ( #108853, #165569, #123906, #167153 ) ) ;
#23250=LINE ( 'NONE', #42784, #158016 ) ;
#23287=DIRECTION ( 'NONE',  ( 0.000000000000000000, 0.9209589331071758034, -0.3896596508879157650 ) ) ;
#23312=ORIENTED_EDGE ( 'NONE', *, *, #138350, .F. ) ;
#23316=FACE_OUTER_BOUND ( 'NONE', #203653, .T. ) ;
#23321=DIRECTION ( 'NONE',  ( 4.239556034732056127E-17, 0.3848449534832867891, 0.9229812358755983270 ) ) ;
#23336=CARTESIAN_POINT ( 'NONE',  ( 21.04999999999999716, 58.97995181213600091, -225.7513643067558746 ) ) ;
#23370=DIRECTION ( 'NONE',  ( 1.000000000000000000, 0.000000000000000000, 0.000000000000000000 ) ) ;
#23373=EDGE_CURVE ( 'NONE', #7826, #65719, #112444, .T. ) ;
#23378=DIRECTION ( 'NONE',  ( 1.000000000000000000, 0.000000000000000000, 0.000000000000000000 ) ) ;
#23382=VERTEX_POINT ( 'NONE', #75076 ) ;
#23391=DIRECTION ( 'NONE',  ( -1.000000000000000000, -0.000000000000000000, 0.000000000000000000 ) ) ;
#23401=DIRECTION ( 'NONE',  ( 0.000000000000000000, -0.2617529984164506107, -0.9651348961777299618 ) ) ;
#23424=DIRECTION ( 'NONE',  ( -0.7071067811865389130, -0.1850873201762232578, -0.6824534298470456006 ) ) ;
#23428=ORIENTED_EDGE ( 'NONE', *, *, #80674, .F. ) ;
#23429=VECTOR ( 'NONE', #205762, 1000.000000000000000 ) ;
#23441=ORIENTED_EDGE ( 'NONE', *, *, #30319, .T. ) ;
#23479=DIRECTION ( 'NONE',  ( 0.000000000000000000, 0.2617529984165031243, 0.9651348961777157509 ) ) ;
#23499=FACE_OUTER_BOUND ( 'NONE', #80613, .T. ) ;
#23503=CARTESIAN_POINT ( 'NONE',  ( 23.24999999999999645, 58.75092140306929167, -245.7296447454341148 ) ) ;
#23535=ORIENTED_EDGE ( 'NONE', *, *, #199981, .T. ) ;
#23540=LINE ( 'NONE', #142157, #18723 ) ;
#23547=AXIS2_PLACEMENT_3D ( 'NONE', #101262, #201701, #123455 ) ;
#23570=AXIS2_PLACEMENT_3D ( 'NONE', #29613, #93394, #8738 ) ;
#23573=EDGE_LOOP ( 'NONE', ( #87331, #234560, #23441, #202511 ) ) ;
#23582=CARTESIAN_POINT ( 'NONE',  ( -18.33981767444424804, 87.02086759565104046, -199.4465615830173135 ) ) ;
#23613=ORIENTED_EDGE ( 'NONE', *, *, #63703, .T. ) ;
#23634=CARTESIAN_POINT ( 'NONE',  ( -18.50000000000000000, 72.02722222756958104, -225.1832529173024398 ) ) ;
#23663=DIRECTION ( 'NONE',  ( 1.000000000000000000, 0.000000000000000000, 0.000000000000000000 ) ) ;
#23679=FACE_OUTER_BOUND ( 'NONE', #144545, .T. ) ;
#23688=VECTOR ( 'NONE', #86199, 1000.000000000000000 ) ;
#23697=ORIENTED_EDGE ( 'NONE', *, *, #228776, .F. ) ;
#23704=AXIS2_PLACEMENT_3D ( 'NONE', #37275, #153396, #116790 ) ;
#23719=DIRECTION ( 'NONE',  ( 0.000000000000000000, 0.2617529984164955192, 0.9651348961777177493 ) ) ;
#23746=DIRECTION ( 'NONE',  ( 0.000000000000000000, 0.2617529984164915779, 0.9651348961777189706 ) ) ;
#23782=ORIENTED_EDGE ( 'NONE', *, *, #219485, .F. ) ;
#23827=CARTESIAN_POINT ( 'NONE',  ( -23.15000000000000213, 68.66552716081216090, -214.3300732090495444 ) ) ;
#23855=CARTESIAN_POINT ( 'NONE',  ( -21.15000000000000213, 60.91865828504416669, -234.1430899377568551 ) ) ;
#23865=CARTESIAN_POINT ( 'NONE',  ( -20.64999999999999858, 70.60814576644823148, -215.7631455941064189 ) ) ;
#23869=CARTESIAN_POINT ( 'NONE',  ( 20.04142135623730070, 62.34315093393704643, -208.9889535843037720 ) ) ;
#23873=ADVANCED_FACE ( 'NONE', ( #51236 ), #210353, .T. ) ;
#23879=DIRECTION ( 'NONE',  ( 0.000000000000000000, -0.9651348961777157509, 0.2617529984165031243 ) ) ;
#23903=VERTEX_POINT ( 'NONE', #102000 ) ;
#23904=ADVANCED_FACE ( 'NONE', ( #236712 ), #2920, .F. ) ;
#23905=FACE_OUTER_BOUND ( 'NONE', #218932, .T. ) ;
#23910=ADVANCED_FACE ( 'NONE', ( #202419 ), #66770, .F. ) ;
#23919=VECTOR ( 'NONE', #180349, 1000.000000000000000 ) ;
#23927=CIRCLE ( 'NONE', #40693, 0.09999999999999961697 ) ;
#23947=CARTESIAN_POINT ( 'NONE',  ( 21.05000000000000071, 67.70174932746996888, -211.7710791003628401 ) ) ;
#23977=ADVANCED_FACE ( 'NONE', ( #217139 ), #38536, .T. ) ;
#23987=FACE_OUTER_BOUND ( 'NONE', #200468, .T. ) ;
#24001=EDGE_CURVE ( 'NONE', #166612, #146108, #245889, .T. ) ;
#24112=ORIENTED_EDGE ( 'NONE', *, *, #86433, .F. ) ;
#24141=AXIS2_PLACEMENT_3D ( 'NONE', #204210, #62150, #43868 ) ;
#24167=CARTESIAN_POINT ( 'NONE',  ( -20.54999999999999716, 75.50266930301991408, -205.3568637872625686 ) ) ;
#24176=CARTESIAN_POINT ( 'NONE',  ( -20.85000000000000142, 87.24382154048164750, -206.5725299160771726 ) ) ;
#24180=FACE_OUTER_BOUND ( 'NONE', #175439, .T. ) ;
#24186=CARTESIAN_POINT ( 'NONE',  ( 21.05000000000000071, 65.69992488703364586, -222.9708107233114163 ) ) ;
#24223=CARTESIAN_POINT ( 'NONE',  ( -21.05000000000000071, 68.17695920783671681, -227.9262201573640141 ) ) ;
#24254=VERTEX_POINT ( 'NONE', #54 ) ;
#24265=DIRECTION ( 'NONE',  ( 1.000000000000000000, 0.000000000000000000, 0.000000000000000000 ) ) ;
#24293=( NAMED_UNIT ( * ) PLANE_ANGLE_UNIT ( ) SI_UNIT ( $, .RADIAN. ) );
#24299=CARTESIAN_POINT ( 'NONE',  ( 20.85000000000000142, 80.78317333349157536, -192.9003134612048882 ) ) ;
#24324=CARTESIAN_POINT ( 'NONE',  ( -22.50000000000000000, 64.18196446391819165, -247.0985338183330668 ) ) ;
#24328=EDGE_CURVE ( 'NONE', #244346, #84318, #77024, .T. ) ;
#24339=CARTESIAN_POINT ( 'NONE',  ( 18.45036689428365051, 78.22617660076507207, -231.5710132021329173 ) ) ;
#24342=DIRECTION ( 'NONE',  ( 1.000000000000000000, 0.000000000000000000, -0.000000000000000000 ) ) ;
#24386=FACE_OUTER_BOUND ( 'NONE', #220934, .T. ) ;
#24432=CARTESIAN_POINT ( 'NONE',  ( 18.43466021071410310, 86.89521045040650904, -199.6218833434545843 ) ) ;
#24435=CARTESIAN_POINT ( 'NONE',  ( 23.15000000000000213, 78.08573236070779444, -228.9307947190811774 ) ) ;
#24455=FACE_OUTER_BOUND ( 'NONE', #70495, .T. ) ;
#24457=EDGE_CURVE ( 'NONE', #137090, #236044, #142195, .T. ) ;
#24552=VECTOR ( 'NONE', #192896, 1000.000000000000000 ) ;
#24587=PLANE ( 'NONE',  #98312 ) ;
#24589=DIRECTION ( 'NONE',  ( -1.000000000000000000, 0.000000000000000000, 0.000000000000000000 ) ) ;
#24595=DIRECTION ( 'NONE',  ( 1.000000000000000000, 0.000000000000000000, 0.000000000000000000 ) ) ;
#24618=AXIS2_PLACEMENT_3D ( 'NONE', #57863, #197385, #137410 ) ;
#24652=VECTOR ( 'NONE', #168159, 1000.000000000000000 ) ;
#24658=EDGE_LOOP ( 'NONE', ( #167349, #35286, #183783, #195604 ) ) ;
#24663=FACE_OUTER_BOUND ( 'NONE', #49884, .T. ) ;
#24692=LINE ( 'NONE', #228969, #33025 ) ;
#24699=CARTESIAN_POINT ( 'NONE',  ( 21.14999999999999503, 79.33069327855442054, -236.1318330389568985 ) ) ;
#24726=CIRCLE ( 'NONE', #91343, 0.09999999999999868716 ) ;
#24771=AXIS2_PLACEMENT_3D ( 'NONE', #72424, #211928, #112816 ) ;
#24857=FACE_OUTER_BOUND ( 'NONE', #181639, .T. ) ;
#24858=LINE ( 'NONE', #249028, #219976 ) ;
#24882=EDGE_CURVE ( 'NONE', #22560, #38351, #47052, .T. ) ;
#24897=CARTESIAN_POINT ( 'NONE',  ( 20.85000000000000142, 79.28756800457986742, -196.2274082906208434 ) ) ;
#24970=CIRCLE ( 'NONE', #225008, 0.5000000000000014433 ) ;
#24972=DIRECTION ( 'NONE',  ( 0.000000000000000000, -0.2617529984165152257, -0.9651348961777124202 ) ) ;
#24985=CARTESIAN_POINT ( 'NONE',  ( -22.39999999999999858, 55.86476422312859569, -232.8760422647022494 ) ) ;
#24993=EDGE_CURVE ( 'NONE', #5675, #72740, #167908, .T. ) ;
#25004=AXIS2_PLACEMENT_3D ( 'NONE', #256944, #220453, #142181 ) ;
#25017=DIRECTION ( 'NONE',  ( 1.000000000000000000, 0.000000000000000000, 0.000000000000000000 ) ) ;
#25044=CARTESIAN_POINT ( 'NONE',  ( 20.94999999999999574, 79.33069327855442054, -236.1318330389568985 ) ) ;
#25073=CIRCLE ( 'NONE', #29177, 0.1000000000000040579 ) ;
#25090=AXIS2_PLACEMENT_3D ( 'NONE', #234049, #252318, #110252 ) ;
#25103=ORIENTED_EDGE ( 'NONE', *, *, #129431, .T. ) ;
#25109=DIRECTION ( 'NONE',  ( 3.265361837132813093E-16, 0.9651348961777157509, -0.2617529984165031243 ) ) ;
#25114=ORIENTED_EDGE ( 'NONE', *, *, #233140, .T. ) ;
#25126=B_SPLINE_CURVE_WITH_KNOTS ( 'NONE', 3,
 ( #212727, #35402, #174931, #131893 ),
 .UNSPECIFIED., .F., .F.,
 ( 4, 4 ),
 ( 0.000000000000000000, 0.001767853679387140298 ),
 .UNSPECIFIED. ) ;
#25127=ORIENTED_EDGE ( 'NONE', *, *, #16654, .F. ) ;
#25140=ORIENTED_EDGE ( 'NONE', *, *, #71541, .F. ) ;
#25141=DIRECTION ( 'NONE',  ( 1.000000000000000000, 0.000000000000000000, 0.000000000000000000 ) ) ;
#25154=EDGE_CURVE ( 'NONE', #9680, #211904, #138978, .T. ) ;
#25168=DIRECTION ( 'NONE',  ( 0.000000000000000000, -0.9651348961777157509, 0.2617529984165031243 ) ) ;
#25172=ORIENTED_EDGE ( 'NONE', *, *, #214869, .T. ) ;
#25185=AXIS2_PLACEMENT_3D ( 'NONE', #7492, #183575, #105275 ) ;
#25213=VERTEX_POINT ( 'NONE', #230046 ) ;
#25251=CARTESIAN_POINT ( 'NONE',  ( -18.50000000000000000, 55.32469252163839712, -244.8004216010555183 ) ) ;
#25264=ORIENTED_EDGE ( 'NONE', *, *, #165682, .T. ) ;
#25270=CARTESIAN_POINT ( 'NONE',  ( -20.64999999999999858, 68.56901367119438362, -214.3038979092079046 ) ) ;
#25281=ORIENTED_EDGE ( 'NONE', *, *, #143257, .F. ) ;
#25290=CARTESIAN_POINT ( 'NONE',  ( -18.59999999999999787, 63.76951449014745066, -212.8986194275075832 ) ) ;
#25300=DIRECTION ( 'NONE',  ( 1.000000000000000000, 0.000000000000000000, 0.000000000000000000 ) ) ;
#25321=CARTESIAN_POINT ( 'NONE',  ( -20.94999999999999929, 68.22930980752001062, -227.7331931781284879 ) ) ;
#25361=CARTESIAN_POINT ( 'NONE',  ( 21.05000000000000071, 61.18232994059686547, -234.2475056001613325 ) ) ;
#25384=EDGE_CURVE ( 'NONE', #37547, #128905, #176633, .T. ) ;
#25432=CYLINDRICAL_SURFACE ( 'NONE', #144125, 0.1000000000000124678 ) ;
#25441=EDGE_CURVE ( 'NONE', #130340, #159456, #151718, .T. ) ;
#25446=DIRECTION ( 'NONE',  ( -1.000000000000000000, -0.000000000000000000, 0.000000000000000000 ) ) ;
#25485=CIRCLE ( 'NONE', #79444, 0.1000000000000124678 ) ;
#25506=ORIENTED_EDGE ( 'NONE', *, *, #60511, .T. ) ;
#25512=ORIENTED_EDGE ( 'NONE', *, *, #70279, .T. ) ;
#25530=CARTESIAN_POINT ( 'NONE',  ( -18.50000000000000000, 63.74333919030581086, -212.9951329171253747 ) ) ;
#25582=DIRECTION ( 'NONE',  ( 1.000000000000000000, 0.000000000000000000, 0.000000000000000000 ) ) ;
#25587=CARTESIAN_POINT ( 'NONE',  ( -18.59999999999999787, 64.18627039993180006, -224.3513032416919089 ) ) ;
#25596=DIRECTION ( 'NONE',  ( -0.7071067811865475727, 0.6824534298470373850, -0.1850873201762210096 ) ) ;
#25615=VECTOR ( 'NONE', #40091, 1000.000000000000000 ) ;
#25617=DIRECTION ( 'NONE',  ( 0.000000000000000000, -0.2617529984165034018, -0.9651348961777157509 ) ) ;
#25624=ORIENTED_EDGE ( 'NONE', *, *, #46370, .T. ) ;
#25646=DIRECTION ( 'NONE',  ( -1.000000000000000000, 1.772924042024179204E-16, -4.808324575169892332E-17 ) ) ;
#25650=FACE_OUTER_BOUND ( 'NONE', #82181, .T. ) ;
#25659=AXIS2_PLACEMENT_3D ( 'NONE', #52000, #213663, #112013 ) ;
#25663=CIRCLE ( 'NONE', #233782, 0.1000000000000124678 ) ;
#25664=LINE ( 'NONE', #107755, #156227 ) ;
#25692=CARTESIAN_POINT ( 'NONE',  ( 18.33996824403804737, 87.02090424921982503, -199.4466712054037885 ) ) ;
#25708=LINE ( 'NONE', #199221, #35468 ) ;
#25718=SPHERICAL_SURFACE ( 'NONE', #113488, 0.1000000000000000056 ) ;
#25744=ORIENTED_EDGE ( 'NONE', *, *, #21072, .T. ) ;
#25779=DIRECTION ( 'NONE',  ( 0.000000000000000000, 0.2617529984165027912, 0.9651348961777157509 ) ) ;
#25796=VERTEX_POINT ( 'NONE', #186942 ) ;
#25820=ORIENTED_EDGE ( 'NONE', *, *, #52596, .F. ) ;
#25844=CARTESIAN_POINT ( 'NONE',  ( 21.05000000000000071, 62.82351852614503684, -207.2177435922979214 ) ) ;
#25849=DIRECTION ( 'NONE',  ( 1.000000000000000000, -2.849773892568378313E-16, 7.728835255496647986E-17 ) ) ;
#25850=ADVANCED_FACE ( 'NONE', ( #150369 ), #55076, .T. ) ;
#25862=VERTEX_POINT ( 'NONE', #17277 ) ;
#25882=FACE_OUTER_BOUND ( 'NONE', #198597, .T. ) ;
#25933=CIRCLE ( 'NONE', #217611, 0.1000000000000022676 ) ;
#25936=EDGE_CURVE ( 'NONE', #34168, #72701, #201171, .T. ) ;
#25940=DIRECTION ( 'NONE',  ( -0.000000000000000000, 0.9651348961777158619, -0.2617529984165030132 ) ) ;
#25969=CARTESIAN_POINT ( 'NONE',  ( -20.64999999999999858, 82.22731448072437388, -214.9453318841612486 ) ) ;
#25996=DIRECTION ( 'NONE',  ( 0.000000000000000000, 0.2617529984164980728, 0.9651348961777171942 ) ) ;
#26002=CARTESIAN_POINT ( 'NONE',  ( 20.04142135623730070, 62.43966442355481661, -209.0151288841454118 ) ) ;
#26009=CIRCLE ( 'NONE', #184203, 7.791421356237304252 ) ;
#26020=CARTESIAN_POINT ( 'NONE',  ( -18.50000000000000000, 97.49741144064424248, -225.2667035127916790 ) ) ;
#26034=ORIENTED_EDGE ( 'NONE', *, *, #610, .T. ) ;
#26082=LINE ( 'NONE', #164310, #251355 ) ;
#26088=AXIS2_PLACEMENT_3D ( 'NONE', #90082, #168407, #191799 ) ;
#26089=DIRECTION ( 'NONE',  ( 1.000000000000000000, 0.000000000000000000, 0.000000000000000000 ) ) ;
#26096=EDGE_CURVE ( 'NONE', #248002, #55604, #151502, .T. ) ;
#26126=DIRECTION ( 'NONE',  ( 0.000000000000000000, 0.2617529984165031243, 0.9651348961777157509 ) ) ;
#26128=EDGE_LOOP ( 'NONE', ( #236561, #128336, #103187 ) ) ;
#26137=EDGE_CURVE ( 'NONE', #49363, #200563, #131446, .T. ) ;
#26141=CARTESIAN_POINT ( 'NONE',  ( -22.50000000000094147, 64.08545097430051385, -247.0723585184914555 ) ) ;
#26158=ORIENTED_EDGE ( 'NONE', *, *, #155311, .F. ) ;
#26179=ADVANCED_FACE ( 'NONE', ( #225701 ), #171900, .F. ) ;
#26191=CARTESIAN_POINT ( 'NONE',  ( -20.54999999999999716, 63.74333919030581086, -212.9951329171253747 ) ) ;
#26206=AXIS2_PLACEMENT_3D ( 'NONE', #111671, #12599, #152110 ) ;
#26209=VERTEX_POINT ( 'NONE', #57014 ) ;
#26231=EDGE_CURVE ( 'NONE', #43859, #19722, #158633, .T. ) ;
#26275=CARTESIAN_POINT ( 'NONE',  ( -20.64999999999999858, 68.56901367119438362, -214.3038979092079046 ) ) ;
#26296=CARTESIAN_POINT ( 'NONE',  ( 21.05000000000000071, 61.94127660284455317, -221.8315191551248517 ) ) ;
#26297=AXIS2_PLACEMENT_3D ( 'NONE', #240499, #200094, #117983 ) ;
#26302=AXIS2_PLACEMENT_3D ( 'NONE', #180926, #63526, #179655 ) ;
#26329=CARTESIAN_POINT ( 'NONE',  ( 21.05000012384897801, 60.16074777168594068, -221.3196362128388159 ) ) ;
#26330=VECTOR ( 'NONE', #210901, 1000.000000000000000 ) ;
#26355=CIRCLE ( 'NONE', #122020, 0.1000000000000106498 ) ;
#26373=CARTESIAN_POINT ( 'NONE',  ( 20.94999999999999929, 70.22659352830977753, -197.9852579278363578 ) ) ;
#26383=VECTOR ( 'NONE', #203743, 1000.000000000000000 ) ;
#26398=AXIS2_PLACEMENT_3D ( 'NONE', #133782, #34713, #195073 ) ;
#26420=ORIENTED_EDGE ( 'NONE', *, *, #114369, .T. ) ;
#26421=VERTEX_POINT ( 'NONE', #182137 ) ;
#26444=EDGE_CURVE ( 'NONE', #258034, #241107, #114045, .T. ) ;
#26514=AXIS2_PLACEMENT_3D ( 'NONE', #220326, #80775, #178654 ) ;
#26517=CIRCLE ( 'NONE', #209863, 12.87499999999999822 ) ;
#26523=DIRECTION ( 'NONE',  ( -1.000000000000000000, 0.000000000000000000, 0.000000000000000000 ) ) ;
#26527=DIRECTION ( 'NONE',  ( 0.000000000000000000, 0.2617529984165027912, 0.9651348961777157509 ) ) ;
#26577=( BOUNDED_SURFACE ( )  B_SPLINE_SURFACE ( 3, 2, ( 
 ( #197242, #160719, #81126 ),
 ( #121592, #22481, #79834 ),
 ( #237658, #19905, #58982 ),
 ( #77282, #43313, #159416 ),
 ( #141131, #179005, #122854 ),
 ( #101959, #18608, #99401 ) ),
 .UNSPECIFIED., .F., .F., .F. ) 
 B_SPLINE_SURFACE_WITH_KNOTS ( ( 4, 2, 4 ),
 ( 3, 3 ),
 ( 4.712388980384689674, 5.497787143782137953, 6.283185307179586232 ),
 ( 0.000000000000000000, 1.000000000000000000 ),
 .UNSPECIFIED. ) 
 GEOMETRIC_REPRESENTATION_ITEM ( )  RATIONAL_B_SPLINE_SURFACE ( (
 ( 1.000000000000000000, 0.7071067811865819897, 1.000000000000000000),
 ( 1.000000000000000000, 0.7727932973487859902, 1.000000000000000000),
 ( 1.000000000000000000, 0.8282379607655473430, 1.000000000000000000),
 ( 1.000000000000000000, 0.9038128468033935770, 1.000000000000000000),
 ( 1.000000000000000000, 0.9240297172247979862, 1.000000000000000000),
 ( 1.000000000000000000, 0.9238795325112969525, 1.000000000000000000) ) ) 
 REPRESENTATION_ITEM ( '' )  SURFACE ( )  );
#26606=DIRECTION ( 'NONE',  ( 0.000000000000000000, -0.4558084472153119959, 0.8900778951570285091 ) ) ;
#26616=VECTOR ( 'NONE', #176199, 1000.000000000000114 ) ;
#26654=CYLINDRICAL_SURFACE ( 'NONE', #146636, 0.09999999999999961697 ) ;
#26664=ADVANCED_FACE ( 'NONE', ( #239225 ), #214516, .F. ) ;
#26668=DIRECTION ( 'NONE',  ( -1.000000000000000000, -0.000000000000000000, -0.000000000000000000 ) ) ;
#26719=EDGE_CURVE ( 'NONE', #211733, #19150, #155412, .T. ) ;
#26759=ORIENTED_EDGE ( 'NONE', *, *, #8710, .T. ) ;
#26774=EDGE_CURVE ( 'NONE', #38351, #153545, #164149, .T. ) ;
#26781=AXIS2_PLACEMENT_3D ( 'NONE', #28753, #109504, #230769 ) ;
#26820=ORIENTED_EDGE ( 'NONE', *, *, #82869, .F. ) ;
#26847=VECTOR ( 'NONE', #187547, 1000.000000000000114 ) ;
#26904=AXIS2_PLACEMENT_3D ( 'NONE', #228981, #232845, #54175 ) ;
#26917=CARTESIAN_POINT ( 'NONE',  ( -21.05000000000000071, 72.93748991853819064, -214.8151857698041738 ) ) ;
#26930=ORIENTED_EDGE ( 'NONE', *, *, #251875, .F. ) ;
#26941=CONICAL_SURFACE ( 'NONE', #64327, 4.299999999999945643, 0.7853981633974466137 ) ;
#26946=CIRCLE ( 'NONE', #18550, 0.09999999999999939493 ) ;
#26948=EDGE_CURVE ( 'NONE', #242965, #39036, #43521, .T. ) ;
#26959=DIRECTION ( 'NONE',  ( -1.000000000000000000, 0.000000000000000000, 0.000000000000000000 ) ) ;
#26963=CARTESIAN_POINT ( 'NONE',  ( -23.25000000000000000, 82.25348978056602789, -214.8488183945435139 ) ) ;
#26986=ORIENTED_EDGE ( 'NONE', *, *, #225238, .F. ) ;
#27001=CARTESIAN_POINT ( 'NONE',  ( 18.44208962363008197, 87.01025646670076696, -199.4198412699713003 ) ) ;
#27017=DIRECTION ( 'NONE',  ( 1.000000000000000000, 0.000000000000000000, 0.000000000000000000 ) ) ;
#27047=DIRECTION ( 'NONE',  ( 0.000000000000000000, -0.2617529984165031243, -0.9651348961777157509 ) ) ;
#27068=TOROIDAL_SURFACE ( 'NONE', #238858, 0.2000000000000000111, 0.1000000000000000056 ) ;
#27091=ORIENTED_EDGE ( 'NONE', *, *, #37158, .F. ) ;
#27092=CARTESIAN_POINT ( 'NONE',  ( -22.39999999999999503, 65.19201463318204048, -243.3742797652979277 ) ) ;
#27098=EDGE_CURVE ( 'NONE', #84395, #73566, #201722, .T. ) ;
#27102=CARTESIAN_POINT ( 'NONE',  ( -20.64999999999999858, 70.71284696581484752, -215.3770916356353382 ) ) ;
#27104=TOROIDAL_SURFACE ( 'NONE', #210256, 0.2000000000000000111, 0.1000000000000000056 ) ;
#27116=ORIENTED_EDGE ( 'NONE', *, *, #147406, .F. ) ;
#27129=ORIENTED_EDGE ( 'NONE', *, *, #254845, .T. ) ;
#27148=DIRECTION ( 'NONE',  ( 0.000000000000000000, 0.9651348961777157509, -0.2617529984165031243 ) ) ;
#27173=ORIENTED_EDGE ( 'NONE', *, *, #194171, .T. ) ;
#27181=AXIS2_PLACEMENT_3D ( 'NONE', #192302, #54059, #34525 ) ;
#27191=DIRECTION ( 'NONE',  ( 0.000000000000000000, -0.9651348961777379554, 0.2617529984164210233 ) ) ;
#27211=DIRECTION ( 'NONE',  ( 1.000000000000000000, 0.000000000000000000, 0.000000000000000000 ) ) ;
#27235=CARTESIAN_POINT ( 'NONE',  ( 21.11345278033240191, 61.86426160980555977, -221.7111410851087498 ) ) ;
#27252=FACE_OUTER_BOUND ( 'NONE', #207353, .T. ) ;
#27264=ORIENTED_EDGE ( 'NONE', *, *, #123570, .F. ) ;
#27296=ORIENTED_EDGE ( 'NONE', *, *, #131669, .T. ) ;
#27302=CARTESIAN_POINT ( 'NONE',  ( -20.94999999999999929, 70.53171716061257257, -228.4612385850772682 ) ) ;
#27324=CIRCLE ( 'NONE', #56487, 0.1000000000000124678 ) ;
#27337=ADVANCED_FACE ( 'NONE', ( #148824 ), #246615, .F. ) ;
#27395=VECTOR ( 'NONE', #49982, 999.9999999999998863 ) ;
#27416=ORIENTED_EDGE ( 'NONE', *, *, #117741, .F. ) ;
#27431=CARTESIAN_POINT ( 'NONE',  ( -18.41809261886929150, 87.08727407717567814, -199.6327535754520852 ) ) ;
#27467=CARTESIAN_POINT ( 'NONE',  ( -18.59999999999999787, 70.22659352830977753, -197.9852579278363578 ) ) ;
#27485=ORIENTED_EDGE ( 'NONE', *, *, #30338, .T. ) ;
#27533=CARTESIAN_POINT ( 'NONE',  ( -18.59999999999999787, 63.24832102809784118, -245.4188802514362635 ) ) ;
#27544=VECTOR ( 'NONE', #254183, 1000.000000000000114 ) ;
#27547=EDGE_CURVE ( 'NONE', #218378, #11577, #248546, .T. ) ;
#27560=DIRECTION ( 'NONE',  ( 1.000000000000000000, 0.000000000000000000, 0.000000000000000000 ) ) ;
#27576=DIRECTION ( 'NONE',  ( 1.000000000000000000, 7.049440681616512959E-16, -1.911869773728117674E-16 ) ) ;
#27619=AXIS2_PLACEMENT_3D ( 'NONE', #220367, #121297, #177408 ) ;
#27622=ADVANCED_FACE ( 'NONE', ( #35940 ), #256182, .F. ) ;
#27639=ORIENTED_EDGE ( 'NONE', *, *, #196171, .T. ) ;
#27668=CIRCLE ( 'NONE', #11050, 11.80000000000000782 ) ;
#27695=EDGE_LOOP ( 'NONE', ( #208267, #173950, #25281, #252559 ) ) ;
#27705=ORIENTED_EDGE ( 'NONE', *, *, #86441, .F. ) ;
#27717=CARTESIAN_POINT ( 'NONE',  ( -21.04999999999965610, 61.13727535989644224, -234.2557234744361381 ) ) ;
#27748=DIRECTION ( 'NONE',  ( -0.000000000000000000, 0.6922311945860613047, 0.7216758089626910122 ) ) ;
#27783=LINE ( 'NONE', #44754, #232378 ) ;
#27787=AXIS2_PLACEMENT_3D ( 'NONE', #107373, #232491, #49970 ) ;
#27822=LINE ( 'NONE', #201280, #94952 ) ;
#27846=EDGE_CURVE ( 'NONE', #160646, #166855, #152239, .T. ) ;
#27873=ORIENTED_EDGE ( 'NONE', *, *, #90242, .T. ) ;
#27892=AXIS2_PLACEMENT_3D ( 'NONE', #37126, #4074, #81026 ) ;
#27903=DIRECTION ( 'NONE',  ( 0.000000000000000000, -0.2617529984165152257, -0.9651348961777124202 ) ) ;
#27906=VERTEX_POINT ( 'NONE', #130865 ) ;
#27909=CARTESIAN_POINT ( 'NONE',  ( -21.05000000000000071, 76.00000000001126921, -203.5231074845248997 ) ) ;
#27912=AXIS2_PLACEMENT_3D ( 'NONE', #137806, #245599, #146472 ) ;
#27928=B_SPLINE_CURVE_WITH_KNOTS ( 'NONE', 3,
 ( #15544, #113332, #14255, #252831, #254109, #148625, #109464 ),
 .UNSPECIFIED., .F., .F.,
 ( 4, 3, 4 ),
 ( 0.000000000000000000, 0.0007844235214594263332, 0.001767853679404340298 ),
 .UNSPECIFIED. ) ;
#27933=ORIENTED_EDGE ( 'NONE', *, *, #99306, .T. ) ;
#27947=AXIS2_PLACEMENT_3D ( 'NONE', #199766, #238868, #137193 ) ;
#28021=ORIENTED_EDGE ( 'NONE', *, *, #175034, .T. ) ;
#28050=ORIENTED_EDGE ( 'NONE', *, *, #13632, .F. ) ;
#28052=CARTESIAN_POINT ( 'NONE',  ( -20.94999999999999929, 72.02722222756958104, -225.1832529173024398 ) ) ;
#28053=ORIENTED_EDGE ( 'NONE', *, *, #147768, .F. ) ;
#28054=ORIENTED_EDGE ( 'NONE', *, *, #114725, .F. ) ;
#28075=DIRECTION ( 'NONE',  ( 1.301042606982683418E-14, 0.7049548389604990417, -0.7092521942343054109 ) ) ;
#28087=DIRECTION ( 'NONE',  ( -1.000000000000000000, 0.000000000000000000, 0.000000000000000000 ) ) ;
#28102=VERTEX_POINT ( 'NONE', #215536 ) ;
#28139=EDGE_CURVE ( 'NONE', #25796, #249301, #252324, .T. ) ;
#28152=CIRCLE ( 'NONE', #224319, 0.09999999999999939493 ) ;
#28173=ADVANCED_FACE ( 'NONE', ( #122872 ), #110697, .T. ) ;
#28242=CARTESIAN_POINT ( 'NONE',  ( 20.94999999999999929, 60.85896401437205583, -225.4389122456526025 ) ) ;
#28246=CARTESIAN_POINT ( 'NONE',  ( -23.15000000000000213, 61.64632609160243248, -246.5149037406836214 ) ) ;
#28281=CARTESIAN_POINT ( 'NONE',  ( 20.94999999999999574, 70.47363787294415260, -228.3418745167492432 ) ) ;
#28282=DIRECTION ( 'NONE',  ( 0.000000000000000000, 0.2617529984165152257, 0.9651348961777124202 ) ) ;
#28294=ORIENTED_EDGE ( 'NONE', *, *, #163309, .F. ) ;
#28322=AXIS2_PLACEMENT_3D ( 'NONE', #9472, #185548, #125568 ) ;
#28358=DIRECTION ( 'NONE',  ( 0.000000000000000000, 0.2741185865636956431, 0.9616958981405304696 ) ) ;
#28385=FACE_OUTER_BOUND ( 'NONE', #235835, .T. ) ;
#28420=ADVANCED_FACE ( 'NONE', ( #155295 ), #215236, .T. ) ;
#28428=EDGE_LOOP ( 'NONE', ( #149983, #237374, #201953, #16005 ) ) ;
#28453=CARTESIAN_POINT ( 'NONE',  ( -20.85000000000000142, 70.22659352830977753, -197.9852579278363578 ) ) ;
#28470=( BOUNDED_CURVE ( )  B_SPLINE_CURVE ( 3, ( #69688, #194775, #149224, #153099 ),
 .UNSPECIFIED., .F., .T. ) 
 B_SPLINE_CURVE_WITH_KNOTS ( ( 4, 4 ),
 ( 3.141592653589791784, 4.712388980384688786 ),
 .UNSPECIFIED. ) 
 CURVE ( )  GEOMETRIC_REPRESENTATION_ITEM ( )  RATIONAL_B_SPLINE_CURVE ( ( 1.000000000000000000, 0.8047378541243649375, 0.8047378541243649375, 1.000000000000000000 ) ) 
 REPRESENTATION_ITEM ( '' )  );
#28484=CARTESIAN_POINT ( 'NONE',  ( -23.15000000000000213, 67.23127455305841238, -235.8551265064783991 ) ) ;
#28514=ORIENTED_EDGE ( 'NONE', *, *, #139148, .F. ) ;
#28576=EDGE_CURVE ( 'NONE', #210786, #252597, #165041, .T. ) ;
#28597=LINE ( 'NONE', #205884, #218527 ) ;
#28636=CARTESIAN_POINT ( 'NONE',  ( 23.14999999999999503, 66.34920340998563404, -213.7018660128499334 ) ) ;
#28687=VECTOR ( 'NONE', #235693, 1000.000000000000000 ) ;
#28689=ORIENTED_EDGE ( 'NONE', *, *, #138201, .T. ) ;
#28701=VECTOR ( 'NONE', #67731, 1000.000000000000000 ) ;
#28747=ORIENTED_EDGE ( 'NONE', *, *, #2408, .T. ) ;
#28751=VERTEX_POINT ( 'NONE', #99757 ) ;
#28753=CARTESIAN_POINT ( 'NONE',  ( -21.05000000000000071, 76.00000000001126921, -203.5231074845248997 ) ) ;
#28784=AXIS2_PLACEMENT_3D ( 'NONE', #216423, #217684, #58621 ) ;
#28800=FACE_OUTER_BOUND ( 'NONE', #60067, .T. ) ;
#28822=ORIENTED_EDGE ( 'NONE', *, *, #123894, .T. ) ;
#28837=DIRECTION ( 'NONE',  ( 1.000000000000000000, -3.151514657663852580E-16, 8.547182517843351137E-17 ) ) ;
#28841=ADVANCED_FACE ( 'NONE', ( #67083 ), #224856, .F. ) ;
#28865=DIRECTION ( 'NONE',  ( 0.000000000000000000, 0.7092521942343286145, 0.7049548389604757270 ) ) ;
#28881=CARTESIAN_POINT ( 'NONE',  ( -23.25000000000000000, 67.23127455305841238, -235.8551265064783991 ) ) ;
#28900=PLANE ( 'NONE',  #33151 ) ;
#28903=ORIENTED_EDGE ( 'NONE', *, *, #158198, .F. ) ;
#28929=DIRECTION ( 'NONE',  ( -1.000000000000000000, -5.551115123125816024E-13, 2.775557561562908012E-13 ) ) ;
#28988=FACE_OUTER_BOUND ( 'NONE', #212380, .T. ) ;
#29002=ORIENTED_EDGE ( 'NONE', *, *, #117134, .F. ) ;
#29013=CARTESIAN_POINT ( 'NONE',  ( 21.14999999999999858, 65.49889199258218753, -241.8691648588935266 ) ) ;
#29042=CIRCLE ( 'NONE', #49838, 11.74999999999999822 ) ;
#29044=VERTEX_POINT ( 'NONE', #227432 ) ;
#29053=CARTESIAN_POINT ( 'NONE',  ( 23.15000000000000213, 82.09643798151613225, -215.4278993322501208 ) ) ;
#29081=CIRCLE ( 'NONE', #158260, 0.1000000000000106498 ) ;
#29169=VERTEX_POINT ( 'NONE', #35693 ) ;
#29177=AXIS2_PLACEMENT_3D ( 'NONE', #151740, #147869, #52597 ) ;
#29186=ADVANCED_FACE ( 'NONE', ( #16124 ), #157051, .F. ) ;
#29192=ORIENTED_EDGE ( 'NONE', *, *, #47897, .T. ) ;
#29197=CARTESIAN_POINT ( 'NONE',  ( 21.05000000000000071, 70.62751970751253339, -223.3325012285725109 ) ) ;
#29200=CARTESIAN_POINT ( 'NONE',  ( -23.15000000000000213, 82.09643798151613225, -215.4278993322501208 ) ) ;
#29205=DIRECTION ( 'NONE',  ( -3.265361837132813093E-16, -0.9651348961777157509, 0.2617529984165031243 ) ) ;
#29209=DIRECTION ( 'NONE',  ( 0.000000000000000000, 0.2617529984165031243, 0.9651348961777157509 ) ) ;
#29229=ORIENTED_EDGE ( 'NONE', *, *, #202946, .F. ) ;
#29235=CARTESIAN_POINT ( 'NONE',  ( 21.05000000000000071, 61.15208969432440966, -234.1845329146948131 ) ) ;
#29241=CARTESIAN_POINT ( 'NONE',  ( -20.64999999999999858, 70.76939748184450707, -215.3970883796142743 ) ) ;
#29284=CARTESIAN_POINT ( 'NONE',  ( 18.59999999999999432, 70.47363787294415260, -228.3418745167492432 ) ) ;
#29331=CARTESIAN_POINT ( 'NONE',  ( -23.15000000000000213, 68.70534379447684614, -223.0647885566232560 ) ) ;
#29334=CARTESIAN_POINT ( 'NONE',  ( -21.70464131381649509, 60.38329692807814553, -233.9978952701749506 ) ) ;
#29340=CIRCLE ( 'NONE', #58495, 4.049999999999990941 ) ;
#29371=CARTESIAN_POINT ( 'NONE',  ( -21.44999999999999929, 65.67360898266123570, -213.5186389139583980 ) ) ;
#29392=DIRECTION ( 'NONE',  ( -1.000000000000000000, 0.000000000000000000, 0.000000000000000000 ) ) ;
#29413=DIRECTION ( 'NONE',  ( 0.000000000000000000, 0.2617529984165022361, 0.9651348961777159730 ) ) ;
#29429=VERTEX_POINT ( 'NONE', #129319 ) ;
#29459=EDGE_CURVE ( 'NONE', #69945, #75171, #256918, .T. ) ;
#29473=FACE_OUTER_BOUND ( 'NONE', #189984, .T. ) ;
#29498=CARTESIAN_POINT ( 'NONE',  ( -20.85000000000000142, 70.20041822846812352, -198.0817714174541493 ) ) ;
#29522=CARTESIAN_POINT ( 'NONE',  ( -21.55000000000000071, 63.37018259659601682, -222.0118260003222872 ) ) ;
#29535=ADVANCED_FACE ( 'NONE', ( #113607 ), #226577, .T. ) ;
#29539=AXIS2_PLACEMENT_3D ( 'NONE', #14752, #108685, #207816 ) ;
#29563=DIRECTION ( 'NONE',  ( -0.000000000000000000, -0.2617529984165028467, -0.9651348961777159730 ) ) ;
#29569=DIRECTION ( 'NONE',  ( 0.000000000000000000, 0.4031292884907143326, 0.9151430362303863975 ) ) ;
#29587=CARTESIAN_POINT ( 'NONE',  ( -18.59999999999999787, 67.49222854868494892, -195.4187676019683693 ) ) ;
#29606=AXIS2_PLACEMENT_3D ( 'NONE', #241851, #163613, #166212 ) ;
#29613=CARTESIAN_POINT ( 'NONE',  ( -21.64999999999999858, 65.67360898266123570, -213.5186389139583980 ) ) ;
#29623=AXIS2_PLACEMENT_3D ( 'NONE', #104932, #86662, #222319 ) ;
#29627=ADVANCED_FACE ( 'NONE', ( #173640 ), #116196, .T. ) ;
#29663=ADVANCED_FACE ( 'NONE', ( #99154 ), #100432, .T. ) ;
#29665=FACE_OUTER_BOUND ( 'NONE', #149932, .T. ) ;
#29708=CARTESIAN_POINT ( 'NONE',  ( -1.820710678118657944, 83.29276488265931278, -214.5670590782273166 ) ) ;
#29738=DIRECTION ( 'NONE',  ( -0.000000000000000000, 0.2617529984165031243, 0.9651348961777157509 ) ) ;
#29739=CARTESIAN_POINT ( 'NONE',  ( 20.97224591636399538, 60.18302304980271344, -221.2511297749800008 ) ) ;
#29748=VERTEX_POINT ( 'NONE', #63905 ) ;
#29758=FACE_OUTER_BOUND ( 'NONE', #57657, .T. ) ;
#29760=CARTESIAN_POINT ( 'NONE',  ( -21.05000000000000071, 61.16604239671104892, -234.3115055913011417 ) ) ;
#29765=EDGE_CURVE ( 'NONE', #228509, #51680, #222278, .T. ) ;
#29819=FACE_OUTER_BOUND ( 'NONE', #118142, .T. ) ;
#29823=ORIENTED_EDGE ( 'NONE', *, *, #162173, .F. ) ;
#29900=AXIS2_PLACEMENT_3D ( 'NONE', #128260, #207822, #227345 ) ;
#29917=DIRECTION ( 'NONE',  ( 0.000000000000000000, 0.7106264324241465813, -0.7035695228903323661 ) ) ;
#29921=CARTESIAN_POINT ( 'NONE',  ( 21.14999999999999858, 60.91865828504416669, -234.1430899377568267 ) ) ;
#29930=CARTESIAN_POINT ( 'NONE',  ( 22.50000000000000000, 64.05916333204672242, -247.1692862367248722 ) ) ;
#29941=EDGE_CURVE ( 'NONE', #198941, #211904, #18500, .T. ) ;
#29952=AXIS2_PLACEMENT_3D ( 'NONE', #123431, #179571, #223797 ) ;
#29968=EDGE_LOOP ( 'NONE', ( #53964, #13965, #101412 ) ) ;
#29973=AXIS2_PLACEMENT_3D ( 'NONE', #26373, #47185, #126747 ) ;
#29984=AXIS2_PLACEMENT_3D ( 'NONE', #229284, #88447, #149761 ) ;
#29986=( BOUNDED_SURFACE ( )  B_SPLINE_SURFACE ( 3, 2, ( 
 ( #191178, #114181, #252390 ),
 ( #12540, #116750, #193729 ),
 ( #196286, #52918, #17641 ),
 ( #75091, #234123, #97143 ) ),
 .UNSPECIFIED., .F., .F., .T. ) 
 B_SPLINE_SURFACE_WITH_KNOTS ( ( 4, 4 ),
 ( 3, 3 ),
 ( 0.0006461284895274140927, 0.0007503702773985949665 ),
 ( 0.000000000000000000, 1.000000000000000000 ),
 .UNSPECIFIED. ) 
 GEOMETRIC_REPRESENTATION_ITEM ( )  RATIONAL_B_SPLINE_SURFACE ( (
 ( 1.000000000000000000, 0.7071067811865475727, 1.000000000000000000),
 ( 1.000000000000000000, 0.7076476444649274500, 1.000000000000000000),
 ( 1.000000000000000000, 0.7075727925191175327, 1.000000000000000000),
 ( 1.000000000000000000, 0.7071067811865558994, 1.000000000000000000) ) ) 
 REPRESENTATION_ITEM ( '' )  SURFACE ( )  );
#29993=CARTESIAN_POINT ( 'NONE',  ( 18.50000000000049383, 63.63806804479052914, -209.2187978148434979 ) ) ;
#30028=VECTOR ( 'NONE', #172230, 1000.000000000000000 ) ;
#30031=EDGE_CURVE ( 'NONE', #249034, #206711, #243344, .T. ) ;
#30047=CARTESIAN_POINT ( 'NONE',  ( -23.15000000000000213, 82.09643798151613225, -215.4278993322501208 ) ) ;
#30048=AXIS2_PLACEMENT_3D ( 'NONE', #177328, #118621, #256770 ) ;
#30057=DIRECTION ( 'NONE',  ( 1.000000000000000000, 0.000000000000000000, 0.000000000000000000 ) ) ;
#30065=VERTEX_POINT ( 'NONE', #41482 ) ;
#30067=CARTESIAN_POINT ( 'NONE',  ( -20.94999999999999929, 72.02722222756959525, -225.1832529173024398 ) ) ;
#30158=ORIENTED_EDGE ( 'NONE', *, *, #256647, .T. ) ;
#30183=CARTESIAN_POINT ( 'NONE',  ( 21.05000000000000071, 78.98983215084128062, -228.7927651294584450 ) ) ;
#30253=CIRCLE ( 'NONE', #130172, 0.1000000000000048767 ) ;
#30275=AXIS2_PLACEMENT_3D ( 'NONE', #238111, #116897, #140283 ) ;
#30303=ORIENTED_EDGE ( 'NONE', *, *, #42357, .T. ) ;
#30308=AXIS2_PLACEMENT_3D ( 'NONE', #202603, #63080, #60500 ) ;
#30319=EDGE_CURVE ( 'NONE', #245391, #255725, #254990, .T. ) ;
#30320=LINE ( 'NONE', #229784, #88701 ) ;
#30323=DIRECTION ( 'NONE',  ( 1.000000000000000000, 7.049440681616513945E-16, -1.911869773728117674E-16 ) ) ;
#30336=VECTOR ( 'NONE', #199195, 1000.000000000000114 ) ;
#30338=EDGE_CURVE ( 'NONE', #218378, #258034, #159905, .T. ) ;
#30391=ORIENTED_EDGE ( 'NONE', *, *, #153492, .T. ) ;
#30418=AXIS2_PLACEMENT_3D ( 'NONE', #136368, #19020, #215920 ) ;
#30439=DIRECTION ( 'NONE',  ( -0.000000000000000000, 0.2617529984165031243, 0.9651348961777157509 ) ) ;
#30442=EDGE_LOOP ( 'NONE', ( #17162, #252191, #79292, #109650 ) ) ;
#30471=DIRECTION ( 'NONE',  ( 1.000000000000000000, 0.000000000000000000, -0.000000000000000000 ) ) ;
#30552=DIRECTION ( 'NONE',  ( 1.000000000000000000, 0.000000000000000000, 0.000000000000000000 ) ) ;
#30553=AXIS2_PLACEMENT_3D ( 'NONE', #69621, #228699, #55141 ) ;
#30608=CYLINDRICAL_SURFACE ( 'NONE', #126254, 0.09999999999999149847 ) ;
#30658=CYLINDRICAL_SURFACE ( 'NONE', #65310, 0.09999999999999939493 ) ;
#30684=ORIENTED_EDGE ( 'NONE', *, *, #33724, .F. ) ;
#30694=DIRECTION ( 'NONE',  ( 0.000000000000000000, -0.9651348961777157509, 0.2617529984165031243 ) ) ;
#30706=DIRECTION ( 'NONE',  ( 0.000000000000000000, 0.2617529984165030132, 0.9651348961777157509 ) ) ;
#30709=ORIENTED_EDGE ( 'NONE', *, *, #56372, .T. ) ;
#30737=ORIENTED_EDGE ( 'NONE', *, *, #48807, .T. ) ;
#30741=ORIENTED_EDGE ( 'NONE', *, *, #237990, .F. ) ;
#30763=EDGE_CURVE ( 'NONE', #180736, #44180, #38325, .T. ) ;
#30766=CYLINDRICAL_SURFACE ( 'NONE', #67283, 0.1000000000000106498 ) ;
#30769=ORIENTED_EDGE ( 'NONE', *, *, #65055, .T. ) ;
#30775=DIRECTION ( 'NONE',  ( 0.000000000000000000, -0.2617529984165152257, -0.9651348961777124202 ) ) ;
#30782=CIRCLE ( 'NONE', #201430, 0.4999999999999892308 ) ;
#30784=DIRECTION ( 'NONE',  ( 1.000000000000000000, -3.151514657663852580E-16, 8.547182517843351137E-17 ) ) ;
#30815=EDGE_CURVE ( 'NONE', #255081, #138609, #227139, .T. ) ;
#30831=ORIENTED_EDGE ( 'NONE', *, *, #53744, .F. ) ;
#30892=CARTESIAN_POINT ( 'NONE',  ( 18.49999999999999645, 80.78317333349157536, -192.9003134612048882 ) ) ;
#30893=ORIENTED_EDGE ( 'NONE', *, *, #209808, .T. ) ;
#30982=DIRECTION ( 'NONE',  ( -1.000000000000000000, -0.000000000000000000, -0.000000000000000000 ) ) ;
#30986=VERTEX_POINT ( 'NONE', #141738 ) ;
#30999=ORIENTED_EDGE ( 'NONE', *, *, #84218, .F. ) ;
#31019=CARTESIAN_POINT ( 'NONE',  ( -20.64999999999999858, 68.56901367119438362, -214.3038979092079046 ) ) ;
#31029=CARTESIAN_POINT ( 'NONE',  ( -2.995603634470891112E-16, 81.77808381374873647, -227.1078217596952697 ) ) ;
#31032=ORIENTED_EDGE ( 'NONE', *, *, #123051, .T. ) ;
#31035=B_SPLINE_CURVE_WITH_KNOTS ( 'NONE', 3,
 ( #72862, #194080, #169404, #15438, #191522, #49415 ),
 .UNSPECIFIED., .F., .F.,
 ( 4, 2, 4 ),
 ( 0.000000000000000000, 0.0001568709654583518899, 0.0003137419309167037798 ),
 .UNSPECIFIED. ) ;
#31058=CIRCLE ( 'NONE', #10183, 0.1000000000000124678 ) ;
#31071=CARTESIAN_POINT ( 'NONE',  ( 20.94999999999999929, 68.48451787451661232, -224.2224406095231757 ) ) ;
#31082=EDGE_CURVE ( 'NONE', #110369, #148934, #221262, .T. ) ;
#31124=EDGE_CURVE ( 'NONE', #40380, #87179, #245338, .T. ) ;
#31166=CARTESIAN_POINT ( 'NONE',  ( 20.94999999999999929, 65.26666169030359299, -222.4689051838086300 ) ) ;
#31193=CARTESIAN_POINT ( 'NONE',  ( 21.04386569057588119, 62.86478208612204810, -207.0655967136942479 ) ) ;
#31228=ORIENTED_EDGE ( 'NONE', *, *, #239374, .T. ) ;
#31288=LINE ( 'NONE', #96328, #24552 ) ;
#31303=ORIENTED_EDGE ( 'NONE', *, *, #237990, .T. ) ;
#31317=CARTESIAN_POINT ( 'NONE',  ( -20.94999999999999929, 72.02722222756959525, -225.1832529173024398 ) ) ;
#31329=CARTESIAN_POINT ( 'NONE',  ( 23.25000000000000000, 64.14229051353817113, -222.2212283990554624 ) ) ;
#31395=VECTOR ( 'NONE', #2917, 1000.000000000000000 ) ;
#31415=CARTESIAN_POINT ( 'NONE',  ( 21.05000000000000071, 76.00000000001126921, -203.5231074845248997 ) ) ;
#31420=DIRECTION ( 'NONE',  ( 0.000000000000000000, 0.2617529984165152257, 0.9651348961777124202 ) ) ;
#31436=DIRECTION ( 'NONE',  ( -1.000000000000000000, -0.000000000000000000, -0.000000000000000000 ) ) ;
#31500=AXIS2_PLACEMENT_3D ( 'NONE', #86935, #88218, #109085 ) ;
#31513=CARTESIAN_POINT ( 'NONE',  ( 21.05000000000000071, 67.32778804267617545, -235.8813018063200388 ) ) ;
#31530=DIRECTION ( 'NONE',  ( 0.000000000000000000, 0.2617529984165152257, 0.9651348961777124202 ) ) ;
#31581=EDGE_CURVE ( 'NONE', #144320, #234918, #160342, .T. ) ;
#31583=CARTESIAN_POINT ( 'NONE',  ( 23.15000000000000213, 86.45856254523212669, -209.4679346046102921 ) ) ;
#31625=DIRECTION ( 'NONE',  ( 1.000000000000000000, 0.000000000000000000, 0.000000000000000000 ) ) ;
#31663=CARTESIAN_POINT ( 'NONE',  ( -18.46902351632712680, 78.23792127434718680, -231.6013883309054222 ) ) ;
#31708=CARTESIAN_POINT ( 'NONE',  ( 21.30000000000002558, 68.29137419664525055, -231.9463301769586394 ) ) ;
#31710=DIRECTION ( 'NONE',  ( -0.000000000000000000, -0.9651348961777157509, 0.2617529984165031243 ) ) ;
#31732=FACE_OUTER_BOUND ( 'NONE', #167635, .T. ) ;
#31752=DIRECTION ( 'NONE',  ( 0.000000000000000000, 0.9651348961777157509, -0.2617529984165031243 ) ) ;
#31768=EDGE_CURVE ( 'NONE', #167923, #69945, #60341, .T. ) ;
#31777=EDGE_LOOP ( 'NONE', ( #18284, #163471, #36846 ) ) ;
#31798=AXIS2_PLACEMENT_3D ( 'NONE', #15225, #230406, #235528 ) ;
#31807=DIRECTION ( 'NONE',  ( 0.000000000000000000, 0.2617529984165152257, 0.9651348961777124202 ) ) ;
#31813=EDGE_CURVE ( 'NONE', #51771, #14172, #151961, .T. ) ;
#31831=ORIENTED_EDGE ( 'NONE', *, *, #210993, .F. ) ;
#31949=CARTESIAN_POINT ( 'NONE',  ( -18.59999999999999787, 57.82359945636609666, -226.0354702357591350 ) ) ;
#31950=CARTESIAN_POINT ( 'NONE',  ( -20.15000000000000568, 61.47027379766506527, -221.6001666287551188 ) ) ;
#31954=CARTESIAN_POINT ( 'NONE',  ( 21.05000000000000071, 60.06466898236885044, -221.3109722682306995 ) ) ;
#31961=ORIENTED_EDGE ( 'NONE', *, *, #173934, .F. ) ;
#31965=FACE_OUTER_BOUND ( 'NONE', #123556, .T. ) ;
#31973=CIRCLE ( 'NONE', #240258, 0.1000000000000124678 ) ;
#31992=ORIENTED_EDGE ( 'NONE', *, *, #135606, .F. ) ;
#32071=CARTESIAN_POINT ( 'NONE',  ( -2.995603634470891112E-16, 85.04999629395501870, -215.0436355574738343 ) ) ;
#32085=CARTESIAN_POINT ( 'NONE',  ( 18.50000000000000000, 86.89640087696871262, -199.6396878666313341 ) ) ;
#32104=CARTESIAN_POINT ( 'NONE',  ( -20.94999999999999929, 77.04701199367727327, -199.6625678998140359 ) ) ;
#32109=DIRECTION ( 'NONE',  ( 0.000000000000000000, 0.2617529984165152257, 0.9651348961777124202 ) ) ;
#32123=CARTESIAN_POINT ( 'NONE',  ( 20.85000000000000142, 79.37986612816742138, -196.2658927859692142 ) ) ;
#32124=UNCERTAINTY_MEASURE_WITH_UNIT (LENGTH_MEASURE( 1.000000000000000082E-05 ), #107297, 'distance_accuracy_value', 'NONE');
#32129=SPHERICAL_SURFACE ( 'NONE', #41882, 0.1000000000000000056 ) ;
#32189=FACE_OUTER_BOUND ( 'NONE', #174409, .T. ) ;
#32238=DIRECTION ( 'NONE',  ( 0.000000000000000000, 0.2617529984165033463, 0.9651348961777157509 ) ) ;
#32307=DIRECTION ( 'NONE',  ( -1.000000000000000000, -7.049440681616512959E-16, 1.911869773728122357E-16 ) ) ;
#32310=VERTEX_POINT ( 'NONE', #131839 ) ;
#32336=CARTESIAN_POINT ( 'NONE',  ( 22.60000000000000142, 55.86495732666938352, -232.8769840133977880 ) ) ;
#32340=CARTESIAN_POINT ( 'NONE',  ( 23.24999999999999289, 66.49806749928671934, -213.5350143334560471 ) ) ;
#32352=DIRECTION ( 'NONE',  ( 2.952720810173289112E-16, 0.9651348961777191926, -0.2617529984164898571 ) ) ;
#32361=ADVANCED_FACE ( 'NONE', ( #57420 ), #135674, .F. ) ;
#32370=CARTESIAN_POINT ( 'NONE',  ( 20.94999999999999929, 63.53162788017662166, -224.4728618886983043 ) ) ;
#32441=AXIS2_PLACEMENT_3D ( 'NONE', #33793, #135398, #35074 ) ;
#32460=ORIENTED_EDGE ( 'NONE', *, *, #40818, .T. ) ;
#32469=DIRECTION ( 'NONE',  ( -1.000000000000000000, -0.000000000000000000, 0.000000000000000000 ) ) ;
#32503=CIRCLE ( 'NONE', #169882, 7.900000000000010125 ) ;
#32526=CARTESIAN_POINT ( 'NONE',  ( -23.15000000000000213, 62.92003201576280702, -207.2439188921395896 ) ) ;
#32561=DIRECTION ( 'NONE',  ( -3.265361837132813093E-16, -0.9651348961777155289, 0.2617529984165037904 ) ) ;
#32609=AXIS2_PLACEMENT_3D ( 'NONE', #238835, #118904, #40677 ) ;
#32626=ADVANCED_FACE ( 'NONE', ( #69014 ), #208522, .T. ) ;
#32643=DIRECTION ( 'NONE',  ( 1.000000000000000000, 0.000000000000000000, -0.000000000000000000 ) ) ;
#32662=ORIENTED_EDGE ( 'NONE', *, *, #134953, .T. ) ;
#32683=EDGE_CURVE ( 'NONE', #74935, #85530, #110603, .T. ) ;
#32729=CARTESIAN_POINT ( 'NONE',  ( 18.49999999999999289, 63.61019970229975229, -209.1253633388161006 ) ) ;
#32755=CARTESIAN_POINT ( 'NONE',  ( -21.08078803292166725, 65.49716426111221779, -241.9466111468314296 ) ) ;
#32761=FACE_OUTER_BOUND ( 'NONE', #151018, .T. ) ;
#32771=ORIENTED_EDGE ( 'NONE', *, *, #25936, .F. ) ;
#32789=AXIS2_PLACEMENT_3D ( 'NONE', #27533, #129166, #148735 ) ;
#32826=ORIENTED_EDGE ( 'NONE', *, *, #163044, .T. ) ;
#32844=ORIENTED_EDGE ( 'NONE', *, *, #168846, .F. ) ;
#32845=DIRECTION ( 'NONE',  ( 0.000000000000000000, -0.2617529984165031243, -0.9651348961777157509 ) ) ;
#32898=ORIENTED_EDGE ( 'NONE', *, *, #4857, .F. ) ;
#32904=ADVANCED_FACE ( 'NONE', ( #221309 ), #160103, .T. ) ;
#32936=AXIS2_PLACEMENT_3D ( 'NONE', #58367, #76669, #80490 ) ;
#32962=CARTESIAN_POINT ( 'NONE',  ( -18.58671080940899856, 78.17500251348390350, -231.4416493083392083 ) ) ;
#32969=EDGE_CURVE ( 'NONE', #211107, #158004, #178386, .T. ) ;
#32998=EDGE_CURVE ( 'NONE', #164109, #120691, #139978, .T. ) ;
#33025=VECTOR ( 'NONE', #203302, 1000.000000000000114 ) ;
#33028=DIRECTION ( 'NONE',  ( 1.000000000000000000, 0.000000000000000000, 0.000000000000000000 ) ) ;
#33037=DIRECTION ( 'NONE',  ( 0.000000000000000000, 0.2617529984165031243, 0.9651348961777157509 ) ) ;
#33051=CARTESIAN_POINT ( 'NONE',  ( -20.64999999999999858, 76.00000000001126921, -203.5231074845248997 ) ) ;
#33066=CIRCLE ( 'NONE', #20555, 11.79999999999999361 ) ;
#33105=CIRCLE ( 'NONE', #128734, 0.1000000000000027117 ) ;
#33121=ADVANCED_FACE ( 'NONE', ( #234161 ), #253717, .T. ) ;
#33151=AXIS2_PLACEMENT_3D ( 'NONE', #147511, #227040, #207505 ) ;
#33154=CARTESIAN_POINT ( 'NONE',  ( -22.47007471830798409, 59.77974727959313839, -233.8342073434303643 ) ) ;
#33172=ORIENTED_EDGE ( 'NONE', *, *, #17032, .T. ) ;
#33173=EDGE_CURVE ( 'NONE', #162955, #210786, #115245, .T. ) ;
#33175=ORIENTED_EDGE ( 'NONE', *, *, #92358, .F. ) ;
#33194=PLANE ( 'NONE',  #36207 ) ;
#33250=DIRECTION ( 'NONE',  ( 0.000000000000000000, 0.9229812358756199764, -0.3848449534832346086 ) ) ;
#33313=DIRECTION ( 'NONE',  ( -0.000000000000000000, -0.7049548389605067023, 0.7092521942342977503 ) ) ;
#33320=CARTESIAN_POINT ( 'NONE',  ( -18.44362607810620602, 78.23832416459919159, -231.5274147598107959 ) ) ;
#33323=CARTESIAN_POINT ( 'NONE',  ( 22.45380639572771742, 64.15556337341597271, -247.1958792975366066 ) ) ;
#33342=CARTESIAN_POINT ( 'NONE',  ( 23.14999999999999503, 61.47936603916258491, -212.1738987416902376 ) ) ;
#33356=DIRECTION ( 'NONE',  ( 0.000000000000000000, -0.9651348961777157509, 0.2617529984165031243 ) ) ;
#33402=CARTESIAN_POINT ( 'NONE',  ( -21.05000000000000071, 72.06821323333463170, -225.0920403225231610 ) ) ;
#33411=ORIENTED_EDGE ( 'NONE', *, *, #27846, .F. ) ;
#33421=DIRECTION ( 'NONE',  ( 1.000000000000000000, 0.000000000000000000, 0.000000000000000000 ) ) ;
#33441=ORIENTED_EDGE ( 'NONE', *, *, #22013, .F. ) ;
#33448=CARTESIAN_POINT ( 'NONE',  ( -18.50000972452446035, 67.49459761544872549, -195.5598716110968667 ) ) ;
#33454=ORIENTED_EDGE ( 'NONE', *, *, #40961, .T. ) ;
#33456=FACE_OUTER_BOUND ( 'NONE', #70280, .T. ) ;
#33478=CARTESIAN_POINT ( 'NONE',  ( 22.48970261584622676, 55.97295988302632708, -232.8591431001882484 ) ) ;
#33496=CARTESIAN_POINT ( 'NONE',  ( -20.94999999999999929, 62.98048128140160173, -207.0210305352945852 ) ) ;
#33499=CIRCLE ( 'NONE', #183491, 0.1000000000000106498 ) ;
#33504=EDGE_CURVE ( 'NONE', #251232, #128048, #48788, .T. ) ;
#33505=DIRECTION ( 'NONE',  ( 0.000000000000000000, 0.2617529984164955192, 0.9651348961777178603 ) ) ;
#33513=CARTESIAN_POINT ( 'NONE',  ( 18.52928932188133970, 63.76258513157054608, -209.3739165141045078 ) ) ;
#33533=VECTOR ( 'NONE', #193342, 1000.000000000000000 ) ;
#33549=ORIENTED_EDGE ( 'NONE', *, *, #193954, .T. ) ;
#33569=DIRECTION ( 'NONE',  ( -1.000000000000000000, -0.000000000000000000, -0.000000000000000000 ) ) ;
#33586=AXIS2_PLACEMENT_3D ( 'NONE', #204398, #103998, #25779 ) ;
#33640=ORIENTED_EDGE ( 'NONE', *, *, #170808, .F. ) ;
#33651=ADVANCED_FACE ( 'NONE', ( #120055 ), #136248, .F. ) ;
#33656=AXIS2_PLACEMENT_3D ( 'NONE', #178582, #79428, #41631 ) ;
#33660=CARTESIAN_POINT ( 'NONE',  ( -20.64999999999999858, 68.56901367119438362, -214.3038979092079046 ) ) ;
#33669=CARTESIAN_POINT ( 'NONE',  ( 18.39999999999999858, 86.99291436658650412, -199.6658631664729739 ) ) ;
#33699=EDGE_LOOP ( 'NONE', ( #140606, #161783, #93399, #190021 ) ) ;
#33724=EDGE_CURVE ( 'NONE', #171424, #179646, #219467, .T. ) ;
#33733=DIRECTION ( 'NONE',  ( 0.000000000000000000, -0.9209589331071864615, 0.3896596508878908960 ) ) ;
#33736=VECTOR ( 'NONE', #193953, 1000.000000000000114 ) ;
#33738=ORIENTED_EDGE ( 'NONE', *, *, #197806, .T. ) ;
#33746=CARTESIAN_POINT ( 'NONE',  ( 18.59999999999999787, 72.06821323333463170, -225.0920403225231610 ) ) ;
#33754=DIRECTION ( 'NONE',  ( 0.000000000000000000, -0.9651348961777379554, 0.2617529984164210233 ) ) ;
#33793=CARTESIAN_POINT ( 'NONE',  ( -20.94999999999999929, 78.93126476241668854, -235.8702625865613243 ) ) ;
#33796=CIRCLE ( 'NONE', #108755, 0.1000000000000106498 ) ;
#33804=DIRECTION ( 'NONE',  ( 0.000000000000000000, 0.2617529984165083423, 0.9651348961777143076 ) ) ;
#33805=EDGE_CURVE ( 'NONE', #204719, #194645, #52017, .T. ) ;
#33810=VECTOR ( 'NONE', #117788, 1000.000000000000000 ) ;
#33815=SPHERICAL_SURFACE ( 'NONE', #81240, 0.1000000000000000056 ) ;
#33820=EDGE_CURVE ( 'NONE', #5530, #143771, #247673, .T. ) ;
#33826=CARTESIAN_POINT ( 'NONE',  ( 20.22894356738840571, 60.44058279725945937, -225.4462117791892979 ) ) ;
#33857=ORIENTED_EDGE ( 'NONE', *, *, #153492, .F. ) ;
#33873=DIRECTION ( 'NONE',  ( -1.000000000000000000, -0.000000000000000000, 0.000000000000000000 ) ) ;
#33875=ORIENTED_EDGE ( 'NONE', *, *, #25936, .T. ) ;
#33879=DIRECTION ( 'NONE',  ( -1.000000000000000000, -0.000000000000000000, -0.000000000000000000 ) ) ;
#33890=DIRECTION ( 'NONE',  ( 0.000000000000000000, 0.2617529984165034018, 0.9651348961777157509 ) ) ;
#33893=CIRCLE ( 'NONE', #130074, 0.3999999999999926392 ) ;
#33952=CARTESIAN_POINT ( 'NONE',  ( 19.97071067811866385, 62.38675221621814870, -208.9400838588616693 ) ) ;
#33957=ADVANCED_FACE ( 'NONE', ( #231982 ), #182263, .T. ) ;
#33969=EDGE_CURVE ( 'NONE', #217985, #68121, #132874, .T. ) ;
#33984=DIRECTION ( 'NONE',  ( 0.000000000000000000, -0.2617529984165152257, -0.9651348961777124202 ) ) ;
#34004=AXIS2_PLACEMENT_3D ( 'NONE', #49747, #90136, #129292 ) ;
#34031=ADVANCED_FACE ( 'NONE', ( #100117 ), #20630, .T. ) ;
#34033=DIRECTION ( 'NONE',  ( 0.000000000000000000, 0.2617529984165024026, 0.9651348961777158619 ) ) ;
#34037=CARTESIAN_POINT ( 'NONE',  ( -21.08376601933334271, 65.50969838531518974, -241.9592675656176937 ) ) ;
#34042=DIRECTION ( 'NONE',  ( 0.000000000000000000, 0.9651348961777157509, -0.2617529984165031243 ) ) ;
#34084=AXIS2_PLACEMENT_3D ( 'NONE', #37608, #117132, #233253 ) ;
#34101=CIRCLE ( 'NONE', #100661, 12.77500000000000391 ) ;
#34103=DIRECTION ( 'NONE',  ( 1.000000000000000000, 0.000000000000000000, -0.000000000000000000 ) ) ;
#34105=CARTESIAN_POINT ( 'NONE',  ( 20.95566103547454517, 58.98089026282059422, -225.7100130536167342 ) ) ;
#34116=AXIS2_PLACEMENT_3D ( 'NONE', #203540, #5300, #21079 ) ;
#34168=VERTEX_POINT ( 'NONE', #110405 ) ;
#34171=ORIENTED_EDGE ( 'NONE', *, *, #103792, .F. ) ;
#34189=ADVANCED_FACE ( 'NONE', ( #246087 ), #7457, .F. ) ;
#34279=DIRECTION ( 'NONE',  ( 0.000000000000000000, 0.9651348961777197477, -0.2617529984164879142 ) ) ;
#34282=CARTESIAN_POINT ( 'NONE',  ( 21.13461538461538325, 61.88829803306103372, -221.6099259868126694 ) ) ;
#34284=DIRECTION ( 'NONE',  ( -1.000000000000000000, -0.000000000000000000, -0.000000000000000000 ) ) ;
#34302=DIRECTION ( 'NONE',  ( 0.000000000000000000, 0.7049548389604869403, -0.7092521942343174013 ) ) ;
#34331=ORIENTED_EDGE ( 'NONE', *, *, #88099, .F. ) ;
#34389=EDGE_LOOP ( 'NONE', ( #41930, #36038, #136353, #36093 ) ) ;
#34411=B_SPLINE_CURVE_WITH_KNOTS ( 'NONE', 3,
 ( #102490, #219905, #184626, #162524, #21715, #41302, #36492, #182072 ),
 .UNSPECIFIED., .F., .F.,
 ( 4, 2, 2, 4 ),
 ( 0.000000000000000000, 6.534141206311692811E-05, 0.0001306828241262338562, 0.0002613656482524238022 ),
 .UNSPECIFIED. ) ;
#34452=EDGE_LOOP ( 'NONE', ( #122387, #156066, #197439, #168174 ) ) ;
#34460=EDGE_CURVE ( 'NONE', #18158, #205787, #170018, .T. ) ;
#34525=DIRECTION ( 'NONE',  ( -1.000000000000000000, 0.000000000000000000, 0.000000000000000000 ) ) ;
#34542=DIRECTION ( 'NONE',  ( 0.000000000000000000, 0.2617529984164915779, 0.9651348961777189706 ) ) ;
#34586=FACE_OUTER_BOUND ( 'NONE', #180677, .T. ) ;
#34590=ORIENTED_EDGE ( 'NONE', *, *, #185387, .F. ) ;
#34630=ORIENTED_EDGE ( 'NONE', *, *, #252508, .F. ) ;
#34645=EDGE_CURVE ( 'NONE', #37547, #147319, #70229, .T. ) ;
#34672=FACE_OUTER_BOUND ( 'NONE', #101608, .T. ) ;
#34688=UNCERTAINTY_MEASURE_WITH_UNIT (LENGTH_MEASURE( 1.000000000000000082E-05 ), #476, 'distance_accuracy_value', 'NONE');
#34692=CIRCLE ( 'NONE', #180424, 0.1000000000000063199 ) ;
#34713=DIRECTION ( 'NONE',  ( -1.000000000000000000, 5.945622153099073960E-16, -5.981866248895712861E-16 ) ) ;
#34714=PLANE ( 'NONE',  #136205 ) ;
#34726=CARTESIAN_POINT ( 'NONE',  ( 20.94999999999999574, 79.26035508877829727, -236.0091442494974956 ) ) ;
#34736=ORIENTED_EDGE ( 'NONE', *, *, #209710, .F. ) ;
#34766=ORIENTED_EDGE ( 'NONE', *, *, #20855, .F. ) ;
#34795=ORIENTED_EDGE ( 'NONE', *, *, #185543, .F. ) ;
#34885=CARTESIAN_POINT ( 'NONE',  ( -20.94999999999999929, 68.59681812508419796, -224.1344059333694361 ) ) ;
#34908=EDGE_LOOP ( 'NONE', ( #88123, #77536, #62699, #126128 ) ) ;
#34936=DIRECTION ( 'NONE',  ( -0.000000000000000000, 0.1290532225515392817, 0.9916376685811522096 ) ) ;
#34971=TOROIDAL_SURFACE ( 'NONE', #214005, 0.2000000000000000111, 0.1000000000000000056 ) ;
#34991=ORIENTED_EDGE ( 'NONE', *, *, #249136, .T. ) ;
#35024=CARTESIAN_POINT ( 'NONE',  ( -21.05000000000000071, 68.22930980752001062, -227.7331931781284879 ) ) ;
#35051=DIRECTION ( 'NONE',  ( 1.000000000000000000, 0.000000000000000000, 0.000000000000000000 ) ) ;
#35070=DIRECTION ( 'NONE',  ( -0.000000000000000000, 0.2617529984165031243, 0.9651348961777157509 ) ) ;
#35071=DIRECTION ( 'NONE',  ( 1.000000000000000000, 0.000000000000000000, 0.000000000000000000 ) ) ;
#35074=DIRECTION ( 'NONE',  ( 0.000000000000000000, -0.9999991631930157387, 0.001293682058423061953 ) ) ;
#35076=EDGE_CURVE ( 'NONE', #159793, #69974, #228611, .T. ) ;
#35104=DIRECTION ( 'NONE',  ( -1.000000000000000000, 3.151514657663852580E-16, -8.547182517843351137E-17 ) ) ;
#35111=DIRECTION ( 'NONE',  ( -1.000000000000000000, 1.772924042024179204E-16, -4.808324575169891715E-17 ) ) ;
#35122=EDGE_CURVE ( 'NONE', #233526, #19722, #124546, .T. ) ;
#35125=CARTESIAN_POINT ( 'NONE',  ( -23.25000000000000000, 67.55989888862310977, -211.9120700681549465 ) ) ;
#35156=ORIENTED_EDGE ( 'NONE', *, *, #163309, .T. ) ;
#35162=TOROIDAL_SURFACE ( 'NONE', #80894, 0.4000000000000003553, 0.1000000000000000056 ) ;
#35183=DIRECTION ( 'NONE',  ( 0.000000000000000000, -0.9229812358756199764, 0.3848449534832346086 ) ) ;
#35199=VERTEX_POINT ( 'NONE', #146387 ) ;
#35220=ORIENTED_EDGE ( 'NONE', *, *, #211005, .T. ) ;
#35258=ORIENTED_EDGE ( 'NONE', *, *, #121036, .F. ) ;
#35263=DIRECTION ( 'NONE',  ( 0.000000000000000000, -0.2617529984187939029, -0.9651348961770944701 ) ) ;
#35269=AXIS2_PLACEMENT_3D ( 'NONE', #127013, #206550, #170041 ) ;
#35282=EDGE_CURVE ( 'NONE', #77452, #113079, #232704, .T. ) ;
#35286=ORIENTED_EDGE ( 'NONE', *, *, #4857, .T. ) ;
#35323=ORIENTED_EDGE ( 'NONE', *, *, #254490, .T. ) ;
#35325=CARTESIAN_POINT ( 'NONE',  ( -21.05000000000000071, 55.11435547888748232, -226.8560373590520101 ) ) ;
#35371=CARTESIAN_POINT ( 'NONE',  ( 21.05000000000000071, 60.98263066423243117, -225.3662366191166200 ) ) ;
#35382=ADVANCED_FACE ( 'NONE', ( #96672 ), #114987, .T. ) ;
#35390=ORIENTED_EDGE ( 'NONE', *, *, #213108, .T. ) ;
#35402=CARTESIAN_POINT ( 'NONE',  ( -21.56666275994540172, 65.41016251146584182, -242.5699255415354685 ) ) ;
#35433=DIRECTION ( 'NONE',  ( -1.000000000000000000, 0.000000000000000000, 0.000000000000000000 ) ) ;
#35438=VERTEX_POINT ( 'NONE', #195838 ) ;
#35445=ORIENTED_EDGE ( 'NONE', *, *, #54578, .F. ) ;
#35459=ORIENTED_EDGE ( 'NONE', *, *, #77674, .F. ) ;
#35468=VECTOR ( 'NONE', #203049, 1000.000000000000000 ) ;
#35475=ORIENTED_EDGE ( 'NONE', *, *, #78991, .T. ) ;
#35498=CIRCLE ( 'NONE', #118687, 0.1000000000000124678 ) ;
#35518=ORIENTED_EDGE ( 'NONE', *, *, #18917, .F. ) ;
#35520=LINE ( 'NONE', #152897, #55028 ) ;
#35526=EDGE_CURVE ( 'NONE', #234655, #110369, #216292, .T. ) ;
#35546=DIRECTION ( 'NONE',  ( 0.000000000000000000, 0.2617529984165152257, 0.9651348961777124202 ) ) ;
#35594=AXIS2_PLACEMENT_3D ( 'NONE', #48668, #146473, #243014 ) ;
#35608=DIRECTION ( 'NONE',  ( -0.000000000000000000, 0.9651348961777157509, -0.2617529984165028467 ) ) ;
#35661=CARTESIAN_POINT ( 'NONE',  ( -23.15000000000000213, 70.57516910782923958, -223.5255282078080654 ) ) ;
#35665=ORIENTED_EDGE ( 'NONE', *, *, #179237, .F. ) ;
#35672=AXIS2_PLACEMENT_3D ( 'NONE', #158544, #136350, #218467 ) ;
#35681=( BOUNDED_CURVE ( )  B_SPLINE_CURVE ( 3, ( #14304, #233351, #129094, #152540 ),
 .UNSPECIFIED., .F., .F. ) 
 B_SPLINE_CURVE_WITH_KNOTS ( ( 4, 4 ),
 ( 4.712388980384689674, 6.283185307179586232 ),
 .UNSPECIFIED. ) 
 CURVE ( )  GEOMETRIC_REPRESENTATION_ITEM ( )  RATIONAL_B_SPLINE_CURVE ( ( 1.000000000000000000, 0.8047378541243649375, 0.8047378541243649375, 1.000000000000000000 ) ) 
 REPRESENTATION_ITEM ( '' )  );
#35693=CARTESIAN_POINT ( 'NONE',  ( -20.54999999999999716, 82.20113918088273408, -215.0418453737790401 ) ) ;
#35695=VECTOR ( 'NONE', #23378, 1000.000000000000000 ) ;
#35712=ADVANCED_FACE ( 'NONE', ( #233047 ), #68830, .T. ) ;
#35746=LINE ( 'NONE', #76122, #207397 ) ;
#35749=DIRECTION ( 'NONE',  ( 1.000000000000000000, 0.000000000000000000, 0.000000000000000000 ) ) ;
#35805=CARTESIAN_POINT ( 'NONE',  ( -20.54999999999999716, 70.62751970751253339, -223.3325012285725393 ) ) ;
#35849=DIRECTION ( 'NONE',  ( 1.000000000000000000, 0.000000000000000000, 0.000000000000000000 ) ) ;
#35861=VECTOR ( 'NONE', #70858, 1000.000000000000000 ) ;
#35866=ORIENTED_EDGE ( 'NONE', *, *, #170997, .F. ) ;
#35902=CARTESIAN_POINT ( 'NONE',  ( 22.47071067811865319, 59.75442326890421896, -233.9300113800879046 ) ) ;
#35909=CARTESIAN_POINT ( 'NONE',  ( -18.46093223321787846, 78.23581486479142200, -231.4991767757356058 ) ) ;
#35915=DIRECTION ( 'NONE',  ( 1.000000000000000000, 0.000000000000000000, 0.000000000000000000 ) ) ;
#35920=DIRECTION ( 'NONE',  ( 0.7071067811865474617, -0.6824534298470372740, 0.1850873201762209819 ) ) ;
#35940=FACE_OUTER_BOUND ( 'NONE', #171123, .T. ) ;
#35949=EDGE_LOOP ( 'NONE', ( #62616, #197133, #159284, #147548 ) ) ;
#35977=CARTESIAN_POINT ( 'NONE',  ( -20.94999999999999929, 62.98048128140160173, -207.0210305352945852 ) ) ;
#36028=CARTESIAN_POINT ( 'NONE',  ( 22.43288208788031568, 64.17721423152049454, -247.0973294774646831 ) ) ;
#36038=ORIENTED_EDGE ( 'NONE', *, *, #75773, .F. ) ;
#36089=ORIENTED_EDGE ( 'NONE', *, *, #209169, .F. ) ;
#36093=ORIENTED_EDGE ( 'NONE', *, *, #190682, .F. ) ;
#36102=CARTESIAN_POINT ( 'NONE',  ( -18.59999999999999787, 76.00000000001126921, -203.5231074845248997 ) ) ;
#36174=CIRCLE ( 'NONE', #115260, 0.09999999999999939493 ) ;
#36179=EDGE_CURVE ( 'NONE', #254106, #136295, #97011, .T. ) ;
#36196=EDGE_CURVE ( 'NONE', #62193, #91550, #177890, .T. ) ;
#36207=AXIS2_PLACEMENT_3D ( 'NONE', #132248, #171416, #8455 ) ;
#36220=ORIENTED_EDGE ( 'NONE', *, *, #472, .F. ) ;
#36227=CIRCLE ( 'NONE', #90355, 0.1000000000000124678 ) ;
#36233=LINE ( 'NONE', #14094, #96567 ) ;
#36242=ADVANCED_FACE ( 'NONE', ( #106013 ), #149486, .T. ) ;
#36311=AXIS2_PLACEMENT_3D ( 'NONE', #85111, #207684, #245522 ) ;
#36313=LINE ( 'NONE', #255280, #180273 ) ;
#36342=EDGE_CURVE ( 'NONE', #211751, #52, #212415, .T. ) ;
#36381=ORIENTED_EDGE ( 'NONE', *, *, #2623, .F. ) ;
#36449=EDGE_CURVE ( 'NONE', #25213, #100977, #212020, .T. ) ;
#36454=CARTESIAN_POINT ( 'NONE',  ( 23.14999999999999858, 76.00000000001126921, -203.5231074845248997 ) ) ;
#36470=ORIENTED_EDGE ( 'NONE', *, *, #2623, .T. ) ;
#36488=PLANE ( 'NONE',  #93261 ) ;
#36492=CARTESIAN_POINT ( 'NONE',  ( -21.13614978966382196, 60.95876181140594952, -234.1539663637506123 ) ) ;
#36582=VERTEX_POINT ( 'NONE', #253246 ) ;
#36587=CYLINDRICAL_SURFACE ( 'NONE', #105920, 0.1000000000000106498 ) ;
#36615=DIRECTION ( 'NONE',  ( 1.000000000000000000, 0.000000000000000000, 0.000000000000000000 ) ) ;
#36618=LINE ( 'NONE', #152714, #123443 ) ;
#36634=TOROIDAL_SURFACE ( 'NONE', #236497, 12.97499999999999609, 0.1000000000000000056 ) ;
#36644=CARTESIAN_POINT ( 'NONE',  ( 21.05000000000000071, 67.92720994251783395, -214.1870976236629929 ) ) ;
#36677=AXIS2_PLACEMENT_3D ( 'NONE', #51826, #251321, #88384 ) ;
#36683=DIRECTION ( 'NONE',  ( 0.000000000000000000, 0.9651348961777158619, -0.2617529984165031243 ) ) ;
#36684=EDGE_CURVE ( 'NONE', #42158, #129497, #178900, .T. ) ;
#36686=CARTESIAN_POINT ( 'NONE',  ( -20.85000000000000142, 79.15532900748003442, -196.2806010913881778 ) ) ;
#36704=ORIENTED_EDGE ( 'NONE', *, *, #11374, .T. ) ;
#36707=EDGE_LOOP ( 'NONE', ( #183125, #221018, #50564, #54388 ) ) ;
#36751=EDGE_LOOP ( 'NONE', ( #230220, #108539, #187295, #63285 ) ) ;
#36757=AXIS2_PLACEMENT_3D ( 'NONE', #61554, #25017, #204893 ) ;
#36765=DIRECTION ( 'NONE',  ( -1.000000000000000000, 0.000000000000000000, 0.000000000000000000 ) ) ;
#36780=VECTOR ( 'NONE', #3433, 1000.000000000000000 ) ;
#36814=CARTESIAN_POINT ( 'NONE',  ( 18.59999999999999076, 62.96704557978079464, -212.5773704035085814 ) ) ;
#36846=ORIENTED_EDGE ( 'NONE', *, *, #204520, .F. ) ;
#36851=CARTESIAN_POINT ( 'NONE',  ( 18.59999999999999432, 86.96699927712941758, -199.3055931863049182 ) ) ;
#36863=TOROIDAL_SURFACE ( 'NONE', #144960, 3.899999999999999467, 0.1000000000000000056 ) ;
#36872=DIRECTION ( 'NONE',  ( 0.000000000000000000, -0.2617529984165031243, -0.9651348961777157509 ) ) ;
#36942=EDGE_LOOP ( 'NONE', ( #91248, #150473, #213588, #98109, #171404 ) ) ;
#36943=AXIS2_PLACEMENT_3D ( 'NONE', #117912, #240445, #158378 ) ;
#36962=CIRCLE ( 'NONE', #53669, 0.09999999999999789613 ) ;
#36964=ORIENTED_EDGE ( 'NONE', *, *, #162028, .T. ) ;
#36975=VECTOR ( 'NONE', #209769, 1000.000000000000000 ) ;
#36993=DIRECTION ( 'NONE',  ( 0.000000000000000000, 0.2741185865636956431, 0.9616958981405304696 ) ) ;
#37026=CARTESIAN_POINT ( 'NONE',  ( -20.94999999999999929, 79.13126459505528487, -235.8705213229730191 ) ) ;
#37066=CARTESIAN_POINT ( 'NONE',  ( 23.25000000000000000, 86.27712145182582049, -209.5223386573213702 ) ) ;
#37099=ORIENTED_EDGE ( 'NONE', *, *, #170997, .T. ) ;
#37126=CARTESIAN_POINT ( 'NONE',  ( 21.05000000000000071, 67.23127455305841238, -235.8551265064783991 ) ) ;
#37140=CARTESIAN_POINT ( 'NONE',  ( -21.07928932188134041, 65.47931918658504458, -241.9371126717015841 ) ) ;
#37150=DIRECTION ( 'NONE',  ( 0.000000000000000000, 0.2617529984165031243, 0.9651348961777158619 ) ) ;
#37158=EDGE_CURVE ( 'NONE', #111271, #162073, #108332, .T. ) ;
#37175=EDGE_CURVE ( 'NONE', #221590, #158004, #183343, .T. ) ;
#37178=EDGE_CURVE ( 'NONE', #103686, #7048, #246236, .T. ) ;
#37210=EDGE_LOOP ( 'NONE', ( #39735, #247515, #190953, #80035 ) ) ;
#37241=CARTESIAN_POINT ( 'NONE',  ( -22.39999999999999858, 55.91711482281189660, -232.6830152854666949 ) ) ;
#37275=CARTESIAN_POINT ( 'NONE',  ( 20.94999999999999929, 65.65271564877468791, -222.5736063831752176 ) ) ;
#37278=CARTESIAN_POINT ( 'NONE',  ( -18.50000000000000000, 67.49462292596869872, -195.5612049585272700 ) ) ;
#37287=DIRECTION ( 'NONE',  ( 1.000000000000000000, -3.151514657663852580E-16, 8.547182517843351137E-17 ) ) ;
#37317=ADVANCED_FACE ( 'NONE', ( #71470 ), #87459, .T. ) ;
#37351=FACE_OUTER_BOUND ( 'NONE', #88452, .T. ) ;
#37364=DIRECTION ( 'NONE',  ( 0.000000000000000000, -0.9651348961777157509, 0.2617529984165031243 ) ) ;
#37366=DIRECTION ( 'NONE',  ( 0.000000000000000000, -0.2617529984165152257, -0.9651348961777124202 ) ) ;
#37378=EDGE_CURVE ( 'NONE', #118480, #20778, #39725, .T. ) ;
#37380=ORIENTED_EDGE ( 'NONE', *, *, #82285, .F. ) ;
#37396=CARTESIAN_POINT ( 'NONE',  ( 23.24999999999999289, 63.22596473392088967, -234.7688515630498785 ) ) ;
#37402=ORIENTED_EDGE ( 'NONE', *, *, #141759, .F. ) ;
#37450=EDGE_LOOP ( 'NONE', ( #156674, #109395, #97056, #161312, #139798 ) ) ;
#37481=LINE ( 'NONE', #156158, #46424 ) ;
#37484=DIRECTION ( 'NONE',  ( 1.000000000000000000, 0.000000000000000000, 0.000000000000000000 ) ) ;
#37491=DIRECTION ( 'NONE',  ( 1.000000000000000000, -1.809991526360996944E-16, 4.908854824437060108E-17 ) ) ;
#37545=AXIS2_PLACEMENT_3D ( 'NONE', #190266, #192830, #194127 ) ;
#37547=VERTEX_POINT ( 'NONE', #126937 ) ;
#37570=DIRECTION ( 'NONE',  ( 0.000000000000000000, 0.2617529984165031243, 0.9651348961777157509 ) ) ;
#37575=ORIENTED_EDGE ( 'NONE', *, *, #123570, .T. ) ;
#37582=DIRECTION ( 'NONE',  ( 1.000000000000000000, -2.849773892568378313E-16, 7.728835255496647986E-17 ) ) ;
#37608=CARTESIAN_POINT ( 'NONE',  ( 21.00000000000000000, 63.35728523183471594, -212.8904317177587870 ) ) ;
#37632=EDGE_CURVE ( 'NONE', #17556, #110910, #112610, .T. ) ;
#37636=EDGE_CURVE ( 'NONE', #54157, #191015, #58400, .T. ) ;
#37695=ORIENTED_EDGE ( 'NONE', *, *, #134953, .F. ) ;
#37698=EDGE_CURVE ( 'NONE', #173665, #65394, #96759, .T. ) ;
#37706=ORIENTED_EDGE ( 'NONE', *, *, #149888, .T. ) ;
#37714=DIRECTION ( 'NONE',  ( 0.000000000000000000, 0.2617529984165031243, 0.9651348961777157509 ) ) ;
#37744=AXIS2_PLACEMENT_3D ( 'NONE', #101903, #203599, #139748 ) ;
#37766=CYLINDRICAL_SURFACE ( 'NONE', #176677, 0.09999999999999939493 ) ;
#37794=AXIS2_PLACEMENT_3D ( 'NONE', #67929, #129199, #108353 ) ;
#37813=AXIS2_PLACEMENT_3D ( 'NONE', #96412, #196804, #231147 ) ;
#37819=ORIENTED_EDGE ( 'NONE', *, *, #94872, .F. ) ;
#37821=CARTESIAN_POINT ( 'NONE',  ( 23.15000000000000213, 86.43238724539048690, -209.5644480942280836 ) ) ;
#37844=DIRECTION ( 'NONE',  ( 1.000000000000000000, 0.000000000000000000, -0.000000000000000000 ) ) ;
#37853=CARTESIAN_POINT ( 'NONE',  ( 21.05000000000000071, 68.22930980752001062, -227.7331931781284879 ) ) ;
#37874=EDGE_CURVE ( 'NONE', #117062, #102375, #204343, .T. ) ;
#37890=CYLINDRICAL_SURFACE ( 'NONE', #235672, 0.1000000000000124678 ) ;
#37891=ORIENTED_EDGE ( 'NONE', *, *, #86453, .T. ) ;
#37911=CARTESIAN_POINT ( 'NONE',  ( -23.15000000000000213, 68.76204065042992397, -214.3562485088912126 ) ) ;
#37921=CARTESIAN_POINT ( 'NONE',  ( 20.95483826173900255, 60.90159005582668073, -225.2834546194827965 ) ) ;
#37940=ORIENTED_EDGE ( 'NONE', *, *, #75312, .F. ) ;
#37944=DIRECTION ( 'NONE',  ( 0.000000000000000000, -0.2617529984165152257, -0.9651348961777124202 ) ) ;
#38006=CARTESIAN_POINT ( 'NONE',  ( 20.94999999999999929, 86.32947205150912851, -209.3293116780858156 ) ) ;
#38020=CARTESIAN_POINT ( 'NONE',  ( 18.49999999999999289, 64.75617845954087670, -200.4736850529726269 ) ) ;
#38102=ORIENTED_EDGE ( 'NONE', *, *, #7291, .T. ) ;
#38146=CYLINDRICAL_SURFACE ( 'NONE', #155531, 0.09999999999999543976 ) ;
#38154=DIRECTION ( 'NONE',  ( 0.000000000000000000, -0.2617529984165152257, -0.9651348961777124202 ) ) ;
#38184=CARTESIAN_POINT ( 'NONE',  ( 20.94999999999999929, 79.11538813396778380, -196.3722783875038544 ) ) ;
#38210=CARTESIAN_POINT ( 'NONE',  ( 23.14999999999999858, 76.00000000001126921, -203.5231074845248997 ) ) ;
#38212=EDGE_CURVE ( 'NONE', #66847, #239682, #10077, .T. ) ;
#38216=DIRECTION ( 'NONE',  ( 0.000000000000000000, -0.9651348961777157509, 0.2617529984165030132 ) ) ;
#38255=ORIENTED_EDGE ( 'NONE', *, *, #58933, .F. ) ;
#38263=LINE ( 'NONE', #156943, #33810 ) ;
#38289=CARTESIAN_POINT ( 'NONE',  ( 23.14999999999999858, 62.92003201576280702, -207.2439188921395612 ) ) ;
#38302=VERTEX_POINT ( 'NONE', #99849 ) ;
#38315=EDGE_CURVE ( 'NONE', #133447, #113811, #238096, .T. ) ;
#38318=ORIENTED_EDGE ( 'NONE', *, *, #100871, .T. ) ;
#38325=B_SPLINE_CURVE_WITH_KNOTS ( 'NONE', 3,
 ( #180044, #101746, #3961, #83468, #2666, #181340, #182620, #82184 ),
 .UNSPECIFIED., .F., .F.,
 ( 4, 2, 2, 4 ),
 ( 0.000000000000000000, 0.0002114466876441958789, 0.0003171700314663007301, 0.0004228933752884056355 ),
 .UNSPECIFIED. ) ;
#38347=DIRECTION ( 'NONE',  ( 0.000000000000000000, -0.9651348961777157509, 0.2617529984165031243 ) ) ;
#38351=VERTEX_POINT ( 'NONE', #136406 ) ;
#38358=DIRECTION ( 'NONE',  ( 0.000000000000000000, -0.7092521942343286145, -0.7049548389604757270 ) ) ;
#38360=DIRECTION ( 'NONE',  ( 0.000000000000000000, -0.2617529984165030132, -0.9651348961777157509 ) ) ;
#38404=CARTESIAN_POINT ( 'NONE',  ( 23.14999999999998437, 55.89093952297024970, -232.7795287750844579 ) ) ;
#38459=DIRECTION ( 'NONE',  ( -1.000000000000000000, -0.000000000000000000, -0.000000000000000000 ) ) ;
#38461=ORIENTED_EDGE ( 'NONE', *, *, #187650, .T. ) ;
#38483=CARTESIAN_POINT ( 'NONE',  ( -21.65000000000000213, 62.99793053463489656, -222.0144804547670390 ) ) ;
#38497=DIRECTION ( 'NONE',  ( 1.000000000000000000, 0.000000000000000000, 0.000000000000000000 ) ) ;
#38498=AXIS2_PLACEMENT_3D ( 'NONE', #42388, #141483, #224861 ) ;
#38520=CARTESIAN_POINT ( 'NONE',  ( 21.05000000000000071, 68.03191114188443578, -213.8010436651919122 ) ) ;
#38533=ORIENTED_EDGE ( 'NONE', *, *, #122678, .F. ) ;
#38536=CYLINDRICAL_SURFACE ( 'NONE', #179277, 0.1000000000000124678 ) ;
#38549=VERTEX_POINT ( 'NONE', #211948 ) ;
#38582=CARTESIAN_POINT ( 'NONE',  ( 22.50000000000000000, 64.08545097430041437, -247.0723585184913986 ) ) ;
#38583=CARTESIAN_POINT ( 'NONE',  ( 18.57399277249656322, 67.49230083716666684, -195.4236814984208479 ) ) ;
#38601=DIRECTION ( 'NONE',  ( 0.000000000000000000, -0.4099100576505548821, -0.9121259477928028714 ) ) ;
#38638=ORIENTED_EDGE ( 'NONE', *, *, #157185, .T. ) ;
#38673=DIRECTION ( 'NONE',  ( 0.000000000000000000, -0.3848449534832867891, -0.9229812358755983270 ) ) ;
#38698=EDGE_CURVE ( 'NONE', #23382, #237933, #55496, .T. ) ;
#38725=DIRECTION ( 'NONE',  ( 1.000000000000000000, 0.000000000000000000, -0.000000000000000000 ) ) ;
#38727=LINE ( 'NONE', #178259, #33736 ) ;
#38736=ORIENTED_EDGE ( 'NONE', *, *, #104029, .F. ) ;
#38792=DIRECTION ( 'NONE',  ( -0.000000000000000000, -0.2617529984165031243, -0.9651348961777157509 ) ) ;
#38800=AXIS2_PLACEMENT_3D ( 'NONE', #58085, #137627, #133792 ) ;
#38820=FACE_OUTER_BOUND ( 'NONE', #236458, .T. ) ;
#38867=DIRECTION ( 'NONE',  ( 0.000000000000000000, 0.9209589331071864615, -0.3896596508878908960 ) ) ;
#38868=AXIS2_PLACEMENT_3D ( 'NONE', #170803, #11691, #32561 ) ;
#38879=AXIS2_PLACEMENT_3D ( 'NONE', #224469, #5399, #79809 ) ;
#38918=ORIENTED_EDGE ( 'NONE', *, *, #182863, .F. ) ;
#38996=VERTEX_POINT ( 'NONE', #192086 ) ;
#39036=VERTEX_POINT ( 'NONE', #212917 ) ;
#39094=CARTESIAN_POINT ( 'NONE',  ( -20.54999999999999716, 78.08573236070779444, -228.9307947190811774 ) ) ;
#39132=ADVANCED_FACE ( 'NONE', ( #216756 ), #38146, .T. ) ;
#39169=AXIS2_PLACEMENT_3D ( 'NONE', #79542, #23479, #139526 ) ;
#39175=CIRCLE ( 'NONE', #235153, 0.09999999999999939493 ) ;
#39198=DIRECTION ( 'NONE',  ( -1.000000000000000000, 0.000000000000000000, 0.000000000000000000 ) ) ;
#39202=DIRECTION ( 'NONE',  ( -1.000000000000000000, 0.000000000000000000, 0.000000000000000000 ) ) ;
#39211=FACE_OUTER_BOUND ( 'NONE', #241639, .T. ) ;
#39231=CIRCLE ( 'NONE', #247280, 4.049999999999990941 ) ;
#39241=VECTOR ( 'NONE', #47872, 1000.000000000000000 ) ;
#39286=EDGE_LOOP ( 'NONE', ( #93215, #254461, #72465 ) ) ;
#39304=CARTESIAN_POINT ( 'NONE',  ( -23.15000000000000213, 81.86853375790846599, -214.9828603846715964 ) ) ;
#39321=CARTESIAN_POINT ( 'NONE',  ( 21.30000000000002558, 68.29137419664525055, -231.9463301769586394 ) ) ;
#39356=CIRCLE ( 'NONE', #101641, 7.900000000000010125 ) ;
#39407=CIRCLE ( 'NONE', #51821, 0.1000000000000124678 ) ;
#39419=EDGE_CURVE ( 'NONE', #49647, #205311, #205542, .T. ) ;
#39425=DIRECTION ( 'NONE',  ( 0.000000000000000000, 0.2617529984165031243, 0.9651348961777157509 ) ) ;
#39434=EDGE_CURVE ( 'NONE', #194529, #146536, #188820, .T. ) ;
#39475=VECTOR ( 'NONE', #93500, 1000.000000000000000 ) ;
#39500=DIRECTION ( 'NONE',  ( 1.000000000000000000, -3.151514657663852580E-16, 8.547182517843351137E-17 ) ) ;
#39547=CIRCLE ( 'NONE', #251878, 2.000000000000009326 ) ;
#39556=ORIENTED_EDGE ( 'NONE', *, *, #222009, .T. ) ;
#39566=ORIENTED_EDGE ( 'NONE', *, *, #148262, .T. ) ;
#39611=AXIS2_PLACEMENT_3D ( 'NONE', #163457, #82590, #22684 ) ;
#39629=ORIENTED_EDGE ( 'NONE', *, *, #229735, .T. ) ;
#39638=DIRECTION ( 'NONE',  ( 0.000000000000000000, 0.9651348961777157509, -0.2617529984165031243 ) ) ;
#39654=CARTESIAN_POINT ( 'NONE',  ( -22.41119224318417125, 64.18196446391819165, -247.0985338183330668 ) ) ;
#39710=FACE_OUTER_BOUND ( 'NONE', #136016, .T. ) ;
#39725=LINE ( 'NONE', #256104, #4247 ) ;
#39730=DIRECTION ( 'NONE',  ( -1.000000000000000000, -0.000000000000000000, 0.000000000000000000 ) ) ;
#39733=CARTESIAN_POINT ( 'NONE',  ( -20.54999999999999716, 71.09390016509016164, -212.4439151503019900 ) ) ;
#39735=ORIENTED_EDGE ( 'NONE', *, *, #80674, .T. ) ;
#39741=CARTESIAN_POINT ( 'NONE',  ( 21.05000000000000071, 65.71172719659838890, -223.0701118083454446 ) ) ;
#39762=AXIS2_PLACEMENT_3D ( 'NONE', #2615, #225499, #46871 ) ;
#39772=ORIENTED_EDGE ( 'NONE', *, *, #216275, .F. ) ;
#39783=TOROIDAL_SURFACE ( 'NONE', #97987, 4.149999999999999467, 0.1000000000000000056 ) ;
#39811=AXIS2_PLACEMENT_3D ( 'NONE', #133730, #178022, #38497 ) ;
#39829=CARTESIAN_POINT ( 'NONE',  ( -20.94999999999999929, 67.70174932746996888, -211.7710791003628401 ) ) ;
#39856=FACE_OUTER_BOUND ( 'NONE', #250590, .T. ) ;
#39873=DIRECTION ( 'NONE',  ( 0.000000000000000000, -0.2617529984165152257, -0.9651348961777124202 ) ) ;
#39910=DIRECTION ( 'NONE',  ( 0.000000000000000000, 0.2617529984164947421, 0.9651348961777179714 ) ) ;
#39912=ORIENTED_EDGE ( 'NONE', *, *, #221345, .F. ) ;
#39956=AXIS2_PLACEMENT_3D ( 'NONE', #168970, #148081, #188481 ) ;
#39958=VECTOR ( 'NONE', #48682, 1000.000000000000000 ) ;
#39967=ORIENTED_EDGE ( 'NONE', *, *, #201895, .F. ) ;
#39975=CARTESIAN_POINT ( 'NONE',  ( -21.05000000000000071, 67.23127455305841238, -235.8551265064783991 ) ) ;
#39981=ORIENTED_EDGE ( 'NONE', *, *, #142924, .T. ) ;
#40015=ORIENTED_EDGE ( 'NONE', *, *, #222490, .F. ) ;
#40021=DIRECTION ( 'NONE',  ( -3.469446951953772592E-14, 0.9651348961777379554, -0.2617529984164210233 ) ) ;
#40026=CARTESIAN_POINT ( 'NONE',  ( -21.05000000000000071, 68.48451787451661232, -224.2224406095231757 ) ) ;
#40030=ORIENTED_EDGE ( 'NONE', *, *, #130920, .T. ) ;
#40044=CARTESIAN_POINT ( 'NONE',  ( -18.59999999999999787, 57.82359945636609666, -226.0354702357591350 ) ) ;
#40069=DIRECTION ( 'NONE',  ( 0.000000000000000000, -0.9229812358756199764, 0.3848449534832346086 ) ) ;
#40081=DIRECTION ( 'NONE',  ( 1.000000000000000000, 0.000000000000000000, 0.000000000000000000 ) ) ;
#40084=CARTESIAN_POINT ( 'NONE',  ( 21.05000000000000426, 58.98862984610919824, -225.8934610823798437 ) ) ;
#40091=DIRECTION ( 'NONE',  ( 1.000000000000000000, 0.000000000000000000, 0.000000000000000000 ) ) ;
#40126=DIRECTION ( 'NONE',  ( 0.000000000000000000, 0.2617529984165024026, 0.9651348961777158619 ) ) ;
#40154=CARTESIAN_POINT ( 'NONE',  ( -20.07928932188135107, 63.89429612639829514, -212.9324612951732831 ) ) ;
#40163=DIRECTION ( 'NONE',  ( 0.000000000000000000, 0.2617529984165031243, 0.9651348961777157509 ) ) ;
#40169=FACE_BOUND ( 'NONE', #88632, .T. ) ;
#40171=AXIS2_PLACEMENT_3D ( 'NONE', #12420, #208049, #248445 ) ;
#40217=ORIENTED_EDGE ( 'NONE', *, *, #209307, .F. ) ;
#40237=DIRECTION ( 'NONE',  ( -0.000000000000000000, 0.2617529984165031243, 0.9651348961777157509 ) ) ;
#40245=CARTESIAN_POINT ( 'NONE',  ( 21.05000000000000071, 62.99095723518624368, -207.1734234082435080 ) ) ;
#40273=EDGE_CURVE ( 'NONE', #175607, #247253, #11887, .T. ) ;
#40282=CARTESIAN_POINT ( 'NONE',  ( 21.05000000000000071, 70.42128727326085880, -228.5349014959848262 ) ) ;
#40311=EDGE_CURVE ( 'NONE', #175607, #130829, #126696, .T. ) ;
#40333=VERTEX_POINT ( 'NONE', #247914 ) ;
#40334=VERTEX_POINT ( 'NONE', #203664 ) ;
#40380=VERTEX_POINT ( 'NONE', #30183 ) ;
#40418=EDGE_CURVE ( 'NONE', #84512, #242965, #156562, .T. ) ;
#40451=CIRCLE ( 'NONE', #227837, 0.5000000000000051070 ) ;
#40462=AXIS2_PLACEMENT_3D ( 'NONE', #96686, #61453, #158033 ) ;
#40510=DIRECTION ( 'NONE',  ( -1.000000000000000000, -0.000000000000000000, -0.000000000000000000 ) ) ;
#40524=DIRECTION ( 'NONE',  ( 0.000000000000000000, 0.9209589331071864615, -0.3896596508878908960 ) ) ;
#40529=CARTESIAN_POINT ( 'NONE',  ( -21.05000000000000071, 76.00000000001126921, -203.5231074845248997 ) ) ;
#40547=EDGE_CURVE ( 'NONE', #7533, #62695, #45172, .T. ) ;
#40556=VECTOR ( 'NONE', #209998, 1000.000000000000000 ) ;
#40572=DIRECTION ( 'NONE',  ( 1.000000000000000000, 0.000000000000000000, -0.000000000000000000 ) ) ;
#40573=DIRECTION ( 'NONE',  ( 1.000000000000000000, 0.000000000000000000, 0.000000000000000000 ) ) ;
#40597=CARTESIAN_POINT ( 'NONE',  ( 21.07964655665547227, 61.96144568752238513, -221.7624746465921817 ) ) ;
#40599=EDGE_LOOP ( 'NONE', ( #114250, #186347, #156606, #182065, #257317, #621, #34991 ) ) ;
#40608=ORIENTED_EDGE ( 'NONE', *, *, #214154, .T. ) ;
#40609=ORIENTED_EDGE ( 'NONE', *, *, #88099, .T. ) ;
#40614=CIRCLE ( 'NONE', #236391, 0.09999999999999543976 ) ;
#40649=LINE ( 'NONE', #198392, #257057 ) ;
#40655=ADVANCED_FACE ( 'NONE', ( #106807 ), #49457, .T. ) ;
#40657=EDGE_LOOP ( 'NONE', ( #246281, #68885, #107629, #200299 ) ) ;
#40665=AXIS2_PLACEMENT_3D ( 'NONE', #218313, #100909, #239186 ) ;
#40677=DIRECTION ( 'NONE',  ( 0.000000000000000000, 0.2617529984164915779, 0.9651348961777189706 ) ) ;
#40681=CARTESIAN_POINT ( 'NONE',  ( -18.59999999999999787, 61.43991280424057777, -221.4883200034892923 ) ) ;
#40693=AXIS2_PLACEMENT_3D ( 'NONE', #209316, #71123, #51504 ) ;
#40699=AXIS2_PLACEMENT_3D ( 'NONE', #63646, #203159, #66226 ) ;
#40705=EDGE_LOOP ( 'NONE', ( #197155, #92790, #160202, #188458, #30999 ) ) ;
#40707=DIRECTION ( 'NONE',  ( 2.694716079187273439E-16, 0.9651348961777159730, -0.2617529984165023471 ) ) ;
#40709=ORIENTED_EDGE ( 'NONE', *, *, #143062, .T. ) ;
#40716=DIRECTION ( 'NONE',  ( 1.000000000000000000, 0.000000000000000000, 0.000000000000000000 ) ) ;
#40718=AXIS2_PLACEMENT_3D ( 'NONE', #257167, #83678, #57724 ) ;
#40729=CARTESIAN_POINT ( 'NONE',  ( 18.59999999999999076, 68.11887992016826843, -227.8068560890359890 ) ) ;
#40755=AXIS2_PLACEMENT_3D ( 'NONE', #246070, #45295, #186090 ) ;
#40771=AXIS2_PLACEMENT_3D ( 'NONE', #252920, #32643, #89992 ) ;
#40780=DIRECTION ( 'NONE',  ( 1.000000000000000000, -2.849773892568378313E-16, 7.728835255496647986E-17 ) ) ;
#40793=ORIENTED_EDGE ( 'NONE', *, *, #137161, .T. ) ;
#40804=EDGE_CURVE ( 'NONE', #19956, #8721, #63847, .T. ) ;
#40818=EDGE_CURVE ( 'NONE', #193798, #90505, #191135, .T. ) ;
#40831=AXIS2_PLACEMENT_3D ( 'NONE', #215754, #196206, #17554 ) ;
#40842=MECHANICAL_DESIGN_GEOMETRIC_PRESENTATION_REPRESENTATION('',(#240721),#244996);
#40848=VERTEX_POINT ( 'NONE', #91108 ) ;
#40849=ORIENTED_EDGE ( 'NONE', *, *, #67596, .T. ) ;
#40889=CARTESIAN_POINT ( 'NONE',  ( 20.94999999999999929, 65.65271564877468791, -222.5736063831752176 ) ) ;
#40895=ORIENTED_EDGE ( 'NONE', *, *, #119972, .T. ) ;
#40929=ADVANCED_FACE ( 'NONE', ( #16723 ), #7957, .F. ) ;
#40946=AXIS2_PLACEMENT_3D ( 'NONE', #213562, #255206, #76621 ) ;
#40961=EDGE_CURVE ( 'NONE', #41172, #24254, #178675, .T. ) ;
#40965=DIRECTION ( 'NONE',  ( 0.000000000000000000, -0.2617529984165031243, -0.9651348961777157509 ) ) ;
#40967=DIRECTION ( 'NONE',  ( -1.000000000000000000, 0.000000000000000000, 0.000000000000000000 ) ) ;
#40976=DIRECTION ( 'NONE',  ( -1.000000000000000000, -0.000000000000000000, 0.000000000000000000 ) ) ;
#40995=DIRECTION ( 'NONE',  ( 0.000000000000000000, -0.9651348961777157509, 0.2617529984165031243 ) ) ;
#41035=AXIS2_PLACEMENT_3D ( 'NONE', #469, #241671, #103418 ) ;
#41042=AXIS2_PLACEMENT_3D ( 'NONE', #4412, #39730, #83910 ) ;
#41056=CYLINDRICAL_SURFACE ( 'NONE', #132940, 0.1000000000000124678 ) ;
#41064=DIRECTION ( 'NONE',  ( -1.000000000000000000, -0.000000000000000000, -0.000000000000000000 ) ) ;
#41069=VERTEX_POINT ( 'NONE', #24435 ) ;
#41071=CYLINDRICAL_SURFACE ( 'NONE', #98708, 0.5000000000000014433 ) ;
#41072=ORIENTED_EDGE ( 'NONE', *, *, #26096, .F. ) ;
#41083=ORIENTED_EDGE ( 'NONE', *, *, #154585, .F. ) ;
#41088=AXIS2_PLACEMENT_3D ( 'NONE', #193361, #33037, #172552 ) ;
#41108=CARTESIAN_POINT ( 'NONE',  ( -21.05000000000000071, 67.23127455305841238, -235.8551265064783991 ) ) ;
#41147=CIRCLE ( 'NONE', #78531, 0.1000000000000086514 ) ;
#41153=EDGE_CURVE ( 'NONE', #89267, #9358, #110355, .T. ) ;
#41168=AXIS2_PLACEMENT_3D ( 'NONE', #26191, #225630, #48307 ) ;
#41172=VERTEX_POINT ( 'NONE', #154655 ) ;
#41177=CARTESIAN_POINT ( 'NONE',  ( 18.56579813702274961, 67.49234744263520724, -195.4268335588911327 ) ) ;
#41182=EDGE_CURVE ( 'NONE', #73870, #90836, #52946, .T. ) ;
#41191=ORIENTED_EDGE ( 'NONE', *, *, #70809, .F. ) ;
#41234=ORIENTED_EDGE ( 'NONE', *, *, #93560, .F. ) ;
#41253=CARTESIAN_POINT ( 'NONE',  ( -20.85000000000000142, 70.08587962373171365, -198.1273832143211848 ) ) ;
#41272=CIRCLE ( 'NONE', #120384, 6.258578643762687577 ) ;
#41287=ADVANCED_FACE ( 'NONE', ( #198884 ), #78838, .T. ) ;
#41302=CARTESIAN_POINT ( 'NONE',  ( -21.12230431290521082, 60.99748793727087559, -234.1698672821734988 ) ) ;
#41306=DIRECTION ( 'NONE',  ( 1.000000000000000000, 0.000000000000000000, 0.000000000000000000 ) ) ;
#41329=VERTEX_POINT ( 'NONE', #35977 ) ;
#41343=DIRECTION ( 'NONE',  ( 0.000000000000000000, -0.2617529984165031243, -0.9651348961777157509 ) ) ;
#41373=DIRECTION ( 'NONE',  ( 0.000000000000000000, -0.2617529984165031243, -0.9651348961777157509 ) ) ;
#41429=ORIENTED_EDGE ( 'NONE', *, *, #99597, .F. ) ;
#41445=CARTESIAN_POINT ( 'NONE',  ( 23.25000000000000000, 75.49601185175264106, -250.2710592679604531 ) ) ;
#41449=ORIENTED_EDGE ( 'NONE', *, *, #14971, .F. ) ;
#41469=EDGE_LOOP ( 'NONE', ( #220691, #178036, #5502 ) ) ;
#41474=EDGE_LOOP ( 'NONE', ( #17044, #131109, #240740, #25140 ) ) ;
#41482=CARTESIAN_POINT ( 'NONE',  ( -18.50000000000000000, 64.75617845954087670, -200.4736850529726269 ) ) ;
#41497=ORIENTED_EDGE ( 'NONE', *, *, #86453, .F. ) ;
#41502=ORIENTED_EDGE ( 'NONE', *, *, #33969, .F. ) ;
#41520=VECTOR ( 'NONE', #93966, 1000.000000000000114 ) ;
#41531=CARTESIAN_POINT ( 'NONE',  ( 20.94999999999999929, 67.49463558145296815, -195.5618716440587548 ) ) ;
#41603=ORIENTED_EDGE ( 'NONE', *, *, #48546, .F. ) ;
#41610=CARTESIAN_POINT ( 'NONE',  ( 21.05000000000000071, 59.10678033798690478, -225.7992625810339575 ) ) ;
#41616=ORIENTED_EDGE ( 'NONE', *, *, #190877, .F. ) ;
#41631=DIRECTION ( 'NONE',  ( 2.952720810173289112E-16, 0.9651348961777159730, -0.2617529984165024026 ) ) ;
#41634=CARTESIAN_POINT ( 'NONE',  ( -20.64999999999999858, 82.48249193998721296, -215.5326005316167084 ) ) ;
#41672=ORIENTED_EDGE ( 'NONE', *, *, #251909, .T. ) ;
#41701=DIRECTION ( 'NONE',  ( 0.000000000000000000, -0.2768012769485524438, -0.9609271840673728748 ) ) ;
#41721=VECTOR ( 'NONE', #175336, 1000.000000000000000 ) ;
#41727=DIRECTION ( 'NONE',  ( 0.000000000000000000, 0.2617529984164506107, 0.9651348961777299618 ) ) ;
#41732=EDGE_CURVE ( 'NONE', #137094, #170116, #217797, .T. ) ;
#41747=CARTESIAN_POINT ( 'NONE',  ( -23.25000000000000000, 68.31754949648690456, -231.8498166873408763 ) ) ;
#41759=ORIENTED_EDGE ( 'NONE', *, *, #189167, .T. ) ;
#41774=EDGE_CURVE ( 'NONE', #147541, #19150, #196012, .T. ) ;
#41830=ORIENTED_EDGE ( 'NONE', *, *, #33805, .T. ) ;
#41861=ADVANCED_FACE ( 'NONE', ( #71610 ), #113282, .T. ) ;
#41865=CARTESIAN_POINT ( 'NONE',  ( 21.08832698747859169, 61.96276761393131238, -221.7557866019214998 ) ) ;
#41882=AXIS2_PLACEMENT_3D ( 'NONE', #67379, #110349, #146888 ) ;
#41883=EDGE_CURVE ( 'NONE', #1926, #250042, #93716, .T. ) ;
#41893=ORIENTED_EDGE ( 'NONE', *, *, #138471, .F. ) ;
#41930=ORIENTED_EDGE ( 'NONE', *, *, #35122, .T. ) ;
#41942=DIRECTION ( 'NONE',  ( 0.000000000000000000, 0.2617529984165152257, 0.9651348961777124202 ) ) ;
#41945=DIRECTION ( 'NONE',  ( 0.000000000000000000, -0.2617529984165031243, -0.9651348961777158619 ) ) ;
#41954=CIRCLE ( 'NONE', #200153, 0.1000000000000124678 ) ;
#41962=CARTESIAN_POINT ( 'NONE',  ( -18.59999999999999787, 78.52025535392039046, -230.5241873323956554 ) ) ;
#42014=DIRECTION ( 'NONE',  ( -1.000000000000000000, 2.849773892568378313E-16, -7.728835255496647986E-17 ) ) ;
#42029=CIRCLE ( 'NONE', #104341, 0.09999999999999543976 ) ;
#42035=AXIS2_PLACEMENT_3D ( 'NONE', #64720, #84226, #166426 ) ;
#42037=CARTESIAN_POINT ( 'NONE',  ( 20.94999999999999929, 76.00000000001126921, -203.5231074845248997 ) ) ;
#42039=CIRCLE ( 'NONE', #204507, 7.899999999999987921 ) ;
#42051=CARTESIAN_POINT ( 'NONE',  ( 21.06280952165509746, 60.16910602115198969, -221.2948844812638924 ) ) ;
#42058=ORIENTED_EDGE ( 'NONE', *, *, #211006, .T. ) ;
#42066=TOROIDAL_SURFACE ( 'NONE', #125251, 11.65000000000000036, 0.1000000000000000056 ) ;
#42068=CIRCLE ( 'NONE', #175344, 11.79999999999999361 ) ;
#42144=CARTESIAN_POINT ( 'NONE',  ( -18.59999999999999787, 61.41373750439892376, -221.5848334931070553 ) ) ;
#42155=DIRECTION ( 'NONE',  ( 0.000000000000000000, 0.2617529984165033463, 0.9651348961777157509 ) ) ;
#42158=VERTEX_POINT ( 'NONE', #69797 ) ;
#42201=EDGE_LOOP ( 'NONE', ( #137794, #115569, #219154, #19189 ) ) ;
#42214=CARTESIAN_POINT ( 'NONE',  ( -20.92356734117541706, 67.49293571122092317, -195.4648732548341741 ) ) ;
#42227=CARTESIAN_POINT ( 'NONE',  ( -21.05000000000000071, 67.23127455305841238, -235.8551265064783991 ) ) ;
#42229=FACE_OUTER_BOUND ( 'NONE', #129654, .T. ) ;
#42253=FACE_OUTER_BOUND ( 'NONE', #58767, .T. ) ;
#42286=LINE ( 'NONE', #22739, #84050 ) ;
#42298=DIRECTION ( 'NONE',  ( 1.000000000000000000, 0.000000000000000000, 0.000000000000000000 ) ) ;
#42300=CARTESIAN_POINT ( 'NONE',  ( 20.93975676684922504, 67.49344847133114911, -195.4961807846321733 ) ) ;
#42306=CARTESIAN_POINT ( 'NONE',  ( -23.15000000000000213, 68.18350826420393673, -222.4110246041809091 ) ) ;
#42312=AXIS2_PLACEMENT_3D ( 'NONE', #114801, #227820, #159086 ) ;
#42341=ORIENTED_EDGE ( 'NONE', *, *, #165761, .T. ) ;
#42357=EDGE_CURVE ( 'NONE', #74489, #231873, #171482, .T. ) ;
#42364=EDGE_CURVE ( 'NONE', #174276, #173665, #257851, .T. ) ;
#42365=VERTEX_POINT ( 'NONE', #111474 ) ;
#42388=CARTESIAN_POINT ( 'NONE',  ( 23.25000000000000000, 82.09643798151613225, -215.4278993322501208 ) ) ;
#42427=CARTESIAN_POINT ( 'NONE',  ( -20.64999999999999858, 70.60814576644823148, -215.7631455941064189 ) ) ;
#42453=DIRECTION ( 'NONE',  ( 1.000000000000000000, 0.000000000000000000, -0.000000000000000000 ) ) ;
#42484=CIRCLE ( 'NONE', #250786, 0.3999999999999926392 ) ;
#42487=B_SPLINE_CURVE_WITH_KNOTS ( 'NONE', 3,
 ( #74879, #53991, #248341, #29334, #50129, #90538, #69722 ),
 .UNSPECIFIED., .F., .F.,
 ( 4, 3, 4 ),
 ( 0.000000000000000000, 0.0009834301579440000909, 0.001767853679402678867 ),
 .UNSPECIFIED. ) ;
#42507=CARTESIAN_POINT ( 'NONE',  ( -23.15000000000000213, 67.23127455305841238, -235.8551265064783991 ) ) ;
#42516=DIRECTION ( 'NONE',  ( 1.000000000000000000, 0.000000000000000000, 0.000000000000000000 ) ) ;
#42555=CARTESIAN_POINT ( 'NONE',  ( 21.14999999999999858, 81.77808381374873647, -227.1078217596952697 ) ) ;
#42590=AXIS2_PLACEMENT_3D ( 'NONE', #52858, #230222, #50282 ) ;
#42593=ORIENTED_EDGE ( 'NONE', *, *, #196269, .F. ) ;
#42601=LINE ( 'NONE', #161283, #100640 ) ;
#42604=CARTESIAN_POINT ( 'NONE',  ( 21.13461538461538325, 61.88829803306103372, -221.6099259868126694 ) ) ;
#42624=ADVANCED_FACE ( 'NONE', ( #28800 ), #150006, .T. ) ;
#42627=ORIENTED_EDGE ( 'NONE', *, *, #67596, .F. ) ;
#42630=ORIENTED_EDGE ( 'NONE', *, *, #160764, .T. ) ;
#42744=VERTEX_POINT ( 'NONE', #57272 ) ;
#42772=AXIS2_PLACEMENT_3D ( 'NONE', #236150, #233595, #215300 ) ;
#42777=PLANE ( 'NONE',  #117962 ) ;
#42784=CARTESIAN_POINT ( 'NONE',  ( 20.94999999999999929, 68.22899648672319017, -213.7884437866858889 ) ) ;
#42823=ORIENTED_EDGE ( 'NONE', *, *, #238324, .F. ) ;
#42837=AXIS2_PLACEMENT_3D ( 'NONE', #118986, #238926, #139799 ) ;
#42838=DIRECTION ( 'NONE',  ( -1.000000000000000000, -7.049440681616513945E-16, 1.911869773728117920E-16 ) ) ;
#42855=AXIS2_PLACEMENT_3D ( 'NONE', #49017, #86841, #25617 ) ;
#42863=AXIS2_PLACEMENT_3D ( 'NONE', #13392, #214150, #154224 ) ;
#42907=DIRECTION ( 'NONE',  ( -1.000000000000000000, -0.000000000000000000, -0.000000000000000000 ) ) ;
#42994=DIRECTION ( 'NONE',  ( 1.000000000000000000, 0.000000000000000000, 0.000000000000000000 ) ) ;
#43007=ORIENTED_EDGE ( 'NONE', *, *, #45841, .T. ) ;
#43048=DIRECTION ( 'NONE',  ( -1.000000000000000000, -0.000000000000000000, -0.000000000000000000 ) ) ;
#43051=DIRECTION ( 'NONE',  ( -1.000000000000000000, -0.000000000000000000, 0.000000000000000000 ) ) ;
#43084=AXIS2_PLACEMENT_3D ( 'NONE', #240490, #63119, #179258 ) ;
#43152=AXIS2_PLACEMENT_3D ( 'NONE', #134764, #133506, #137339 ) ;
#43167=DIRECTION ( 'NONE',  ( 0.000000000000000000, -0.2617529984164856383, -0.9651348961777204138 ) ) ;
#43188=DIRECTION ( 'NONE',  ( 0.000000000000000000, -0.9651348961777157509, 0.2617529984165030132 ) ) ;
#43197=DIRECTION ( 'NONE',  ( 0.000000000000000000, -0.8430646840892555005, -0.5378121776619452232 ) ) ;
#43220=ADVANCED_FACE ( 'NONE', ( #141657 ), #245803, .F. ) ;
#43244=DIRECTION ( 'NONE',  ( 1.000000000000000000, 0.000000000000000000, 0.000000000000000000 ) ) ;
#43266=FACE_OUTER_BOUND ( 'NONE', #29968, .T. ) ;
#43282=CARTESIAN_POINT ( 'NONE',  ( 20.94999999999999929, 67.92720994251783395, -214.1870976236629929 ) ) ;
#43306=CARTESIAN_POINT ( 'NONE',  ( -21.15000000000000213, 65.51923798433685420, -242.1677427744926092 ) ) ;
#43313=CARTESIAN_POINT ( 'NONE',  ( 19.96984138294339317, 62.36267039717171201, -208.9169814761061730 ) ) ;
#43314=EDGE_CURVE ( 'NONE', #149860, #146093, #129104, .T. ) ;
#43329=AXIS2_PLACEMENT_3D ( 'NONE', #233440, #136880, #134295 ) ;
#43342=AXIS2_PLACEMENT_3D ( 'NONE', #197520, #35915, #236648 ) ;
#43384=CIRCLE ( 'NONE', #59933, 0.09999999999999939493 ) ;
#43386=ORIENTED_EDGE ( 'NONE', *, *, #4631, .F. ) ;
#43411=ADVANCED_FACE ( 'NONE', ( #253583 ), #17535, .F. ) ;
#43413=DIRECTION ( 'NONE',  ( 1.000000000000000000, 0.000000000000000000, 0.000000000000000000 ) ) ;
#43425=CIRCLE ( 'NONE', #168560, 0.1000000000000124678 ) ;
#43428=EDGE_LOOP ( 'NONE', ( #228091, #230722, #29002, #206940, #25820 ) ) ;
#43432=VERTEX_POINT ( 'NONE', #177927 ) ;
#43440=DIRECTION ( 'NONE',  ( 0.000000000000000000, -0.9651348961777379554, 0.2617529984164210233 ) ) ;
#43466=FACE_OUTER_BOUND ( 'NONE', #174926, .T. ) ;
#43470=EDGE_CURVE ( 'NONE', #256377, #84395, #151915, .T. ) ;
#43491=DIRECTION ( 'NONE',  ( 1.000000000000000000, 0.000000000000000000, 0.000000000000000000 ) ) ;
#43521=CIRCLE ( 'NONE', #247527, 4.000000000000000000 ) ;
#43539=CYLINDRICAL_SURFACE ( 'NONE', #30308, 0.09999999999999543976 ) ;
#43562=ORIENTED_EDGE ( 'NONE', *, *, #178859, .T. ) ;
#43576=CARTESIAN_POINT ( 'NONE',  ( -23.25000000000000000, 79.15532900748003442, -196.2806010913881778 ) ) ;
#43584=DIRECTION ( 'NONE',  ( 2.710505431213777355E-16, 0.9651348961777157509, -0.2617529984165031243 ) ) ;
#43594=CARTESIAN_POINT ( 'NONE',  ( -18.50000000000000355, 78.21362219944487038, -231.2727646510690533 ) ) ;
#43606=AXIS2_PLACEMENT_3D ( 'NONE', #253992, #153684, #75401 ) ;
#43607=VECTOR ( 'NONE', #127663, 1000.000000000000000 ) ;
#43677=AXIS2_PLACEMENT_3D ( 'NONE', #110685, #190232, #171988 ) ;
#43694=CARTESIAN_POINT ( 'NONE',  ( 23.14999999999999858, 67.23127455305841238, -235.8551265064783991 ) ) ;
#43704=CARTESIAN_POINT ( 'NONE',  ( 23.15000000000000213, 78.50726470275242264, -228.6618886302502176 ) ) ;
#43706=VERTEX_POINT ( 'NONE', #206462 ) ;
#43733=EDGE_CURVE ( 'NONE', #54640, #138432, #87748, .T. ) ;
#43759=CARTESIAN_POINT ( 'NONE',  ( 23.14999999999999858, 75.49601185175264106, -250.2710592679604531 ) ) ;
#43766=DIRECTION ( 'NONE',  ( 0.000000000000000000, -0.2617529984165031243, -0.9651348961777157509 ) ) ;
#43825=EDGE_CURVE ( 'NONE', #188424, #12569, #46239, .T. ) ;
#43859=VERTEX_POINT ( 'NONE', #142318 ) ;
#43868=DIRECTION ( 'NONE',  ( 0.000000000000000000, 0.2617529984165152257, 0.9651348961777124202 ) ) ;
#43870=DIRECTION ( 'NONE',  ( 2.952720810173289112E-16, 0.9651348961777174162, -0.2617529984164969070 ) ) ;
#43884=CARTESIAN_POINT ( 'NONE',  ( 18.54147908293605695, 78.20968212019604948, -231.5289770586088309 ) ) ;
#43885=LINE ( 'NONE', #6022, #246078 ) ;
#43934=ORIENTED_EDGE ( 'NONE', *, *, #235378, .T. ) ;
#43935=CARTESIAN_POINT ( 'NONE',  ( 20.85000000000000142, 76.00000000001126921, -203.5231074845248997 ) ) ;
#43959=CIRCLE ( 'NONE', #85612, 0.5000000000000051070 ) ;
#43966=CARTESIAN_POINT ( 'NONE',  ( 18.33683296300310772, 86.98713236139516880, -199.3477403010566888 ) ) ;
#43968=ORIENTED_EDGE ( 'NONE', *, *, #161303, .F. ) ;
#43980=CARTESIAN_POINT ( 'NONE',  ( 21.14999999999999503, 65.59531831295525706, -241.8872196075891168 ) ) ;
#43993=CARTESIAN_POINT ( 'NONE',  ( 20.85000000000000142, 80.78317333349157536, -192.9003134612048882 ) ) ;
#44021=( BOUNDED_SURFACE ( )  B_SPLINE_SURFACE ( 3, 2, ( 
 ( #243445, #63516, #20575 ),
 ( #197896, #199197, #222578 ),
 ( #179645, #43966, #123508 ),
 ( #24432, #19270, #103910 ),
 ( #950, #80487, #4810 ),
 ( #7395, #25692, #227730 ),
 ( #6105, #45250, #208193 ),
 ( #69973, #27001, #188604 ),
 ( #127358, #88195, #126053 ),
 ( #247288, #165199, #68673 ) ),
 .UNSPECIFIED., .F., .F., .F. ) 
 B_SPLINE_SURFACE_WITH_KNOTS ( ( 4, 2, 2, 2, 4 ),
 ( 3, 3 ),
 ( 0.0001701955120502368938, 0.0002247052511886077396, 0.0002792149903269785854, 0.0003882344686037202228, 0.0006062734251572035517 ),
 ( 0.000000000000000000, 1.000000000000000000 ),
 .UNSPECIFIED. ) 
 GEOMETRIC_REPRESENTATION_ITEM ( )  RATIONAL_B_SPLINE_SURFACE ( (
 ( 1.000000000000000000, 0.2966190024559618443, 1.000000000000000000),
 ( 1.000000000000000000, 0.2964522492724643299, 1.000000000000000000),
 ( 1.000000000000000000, 0.3059923531867425051, 1.000000000000000000),
 ( 1.000000000000000000, 0.3355751146960955222, 1.000000000000000000),
 ( 1.000000000000000000, 0.3550672384944031923, 1.000000000000000000),
 ( 1.000000000000000000, 0.4157034672218395399, 1.000000000000000000),
 ( 1.000000000000000000, 0.4588031877619547227, 1.000000000000000000),
 ( 1.000000000000000000, 0.5771441759730387977, 1.000000000000000000),
 ( 1.000000000000000000, 0.6469377121719541712, 1.000000000000000000),
 ( 1.000000000000000000, 0.7071067811865933139, 1.000000000000000000) ) ) 
 REPRESENTATION_ITEM ( '' )  SURFACE ( )  );
#44073=EDGE_CURVE ( 'NONE', #65920, #176003, #212862, .T. ) ;
#44080=ORIENTED_EDGE ( 'NONE', *, *, #5715, .F. ) ;
#44096=VERTEX_POINT ( 'NONE', #185312 ) ;
#44097=ORIENTED_EDGE ( 'NONE', *, *, #89221, .T. ) ;
#44120=VECTOR ( 'NONE', #197190, 1000.000000000000000 ) ;
#44126=EDGE_CURVE ( 'NONE', #171580, #206042, #75330, .T. ) ;
#44140=DIRECTION ( 'NONE',  ( 0.000000000000000000, -0.9651348961777157509, 0.2617529984165028467 ) ) ;
#44146=FACE_OUTER_BOUND ( 'NONE', #7098, .T. ) ;
#44147=EDGE_CURVE ( 'NONE', #62695, #155707, #37481, .T. ) ;
#44162=CARTESIAN_POINT ( 'NONE',  ( 21.05000000000000071, 58.98867006934395363, -225.8934842717049492 ) ) ;
#44178=AXIS2_PLACEMENT_3D ( 'NONE', #65888, #3324, #47592 ) ;
#44180=VERTEX_POINT ( 'NONE', #197812 ) ;
#44204=ORIENTED_EDGE ( 'NONE', *, *, #222285, .T. ) ;
#44215=DIRECTION ( 'NONE',  ( 0.000000000000000000, 0.2617529984165035128, 0.9651348961777155289 ) ) ;
#44243=CARTESIAN_POINT ( 'NONE',  ( -23.25000000000000000, 76.00000000001126921, -203.5231074845248997 ) ) ;
#44250=DIRECTION ( 'NONE',  ( 1.000000000000000000, 0.000000000000000000, 0.000000000000000000 ) ) ;
#44277=ADVANCED_FACE ( 'NONE', ( #82970 ), #240807, .T. ) ;
#44354=AXIS2_PLACEMENT_3D ( 'NONE', #208005, #226225, #45059 ) ;
#44376=CIRCLE ( 'NONE', #131844, 0.1000000000000124678 ) ;
#44381=DIRECTION ( 'NONE',  ( -1.000000000000000000, 0.000000000000000000, 0.000000000000000000 ) ) ;
#44400=CARTESIAN_POINT ( 'NONE',  ( -18.31572283045056437, 87.00870235977620837, -199.4106618404662754 ) ) ;
#44409=ORIENTED_EDGE ( 'NONE', *, *, #55888, .T. ) ;
#44410=CIRCLE ( 'NONE', #6978, 11.64999999999998970 ) ;
#44412=ORIENTED_EDGE ( 'NONE', *, *, #1584, .T. ) ;
#44427=ADVANCED_FACE ( 'NONE', ( #51548 ), #30766, .T. ) ;
#44442=AXIS2_PLACEMENT_3D ( 'NONE', #31029, #231772, #90960 ) ;
#44447=ORIENTED_EDGE ( 'NONE', *, *, #106016, .F. ) ;
#44451=DIRECTION ( 'NONE',  ( 0.000000000000000000, 0.2617529984165083423, 0.9651348961777143076 ) ) ;
#44486=FACE_OUTER_BOUND ( 'NONE', #89155, .T. ) ;
#44514=DIRECTION ( 'NONE',  ( -1.000000000000000000, 0.000000000000000000, 0.000000000000000000 ) ) ;
#44567=DIRECTION ( 'NONE',  ( 1.000000000000000000, 0.000000000000000000, 0.000000000000000000 ) ) ;
#44587=EDGE_CURVE ( 'NONE', #163063, #24254, #75034, .T. ) ;
#44614=DIRECTION ( 'NONE',  ( 1.000000000000000000, 0.000000000000000000, 0.000000000000000000 ) ) ;
#44622=TOROIDAL_SURFACE ( 'NONE', #240263, 0.2000000000000000111, 0.1000000000000000056 ) ;
#44679=EDGE_CURVE ( 'NONE', #165270, #133438, #171552, .T. ) ;
#44683=SPHERICAL_SURFACE ( 'NONE', #52867, 0.1000000000000000056 ) ;
#44708=FACE_OUTER_BOUND ( 'NONE', #17400, .T. ) ;
#44712=VECTOR ( 'NONE', #137969, 1000.000000000000000 ) ;
#44754=CARTESIAN_POINT ( 'NONE',  ( -23.25000000000000000, 66.17117490947157421, -239.7639228359981303 ) ) ;
#44757=DIRECTION ( 'NONE',  ( 0.000000000000000000, -0.8900778951570211817, -0.4558084472153261513 ) ) ;
#44763=DIRECTION ( 'NONE',  ( 1.000000000000000000, 0.000000000000000000, 0.000000000000000000 ) ) ;
#44785=ADVANCED_FACE ( 'NONE', ( #69581 ), #249499, .F. ) ;
#44807=EDGE_CURVE ( 'NONE', #230992, #10835, #75680, .T. ) ;
#44837=( BOUNDED_CURVE ( )  B_SPLINE_CURVE ( 3, ( #183370, #8578, #146768, #144212 ),
 .UNSPECIFIED., .F., .F. ) 
 B_SPLINE_CURVE_WITH_KNOTS ( ( 4, 4 ),
 ( 1.570796326794895448, 3.141592653589791784 ),
 .UNSPECIFIED. ) 
 CURVE ( )  GEOMETRIC_REPRESENTATION_ITEM ( )  RATIONAL_B_SPLINE_CURVE ( ( 1.000000000000000000, 0.8047378541243650485, 0.8047378541243650485, 1.000000000000000000 ) ) 
 REPRESENTATION_ITEM ( '' )  );
#44874=ADVANCED_FACE ( 'NONE', ( #12185 ), #106091, .F. ) ;
#44884=AXIS2_PLACEMENT_3D ( 'NONE', #45984, #27748, #105936 ) ;
#44886=ADVANCED_FACE ( 'NONE', ( #9580 ), #108690, .T. ) ;
#44906=CARTESIAN_POINT ( 'NONE',  ( 21.05000000000080718, 61.13731265359255929, -234.2555725237206445 ) ) ;
#44914=EDGE_LOOP ( 'NONE', ( #162155, #192806 ) ) ;
#44941=CARTESIAN_POINT ( 'NONE',  ( -20.54999999999999716, 78.89331866122350334, -228.7665898296168052 ) ) ;
#44969=DIRECTION ( 'NONE',  ( 2.952720810173289112E-16, 0.9651348961777157509, -0.2617529984165031243 ) ) ;
#44974=AXIS2_PLACEMENT_3D ( 'NONE', #33660, #71475, #16626 ) ;
#44977=CARTESIAN_POINT ( 'NONE',  ( -18.41418431465368855, 86.89640087696879789, -199.6396878666320447 ) ) ;
#44997=ADVANCED_FACE ( 'NONE', ( #56400 ), #238914, .F. ) ;
#45029=FACE_OUTER_BOUND ( 'NONE', #11242, .T. ) ;
#45048=CARTESIAN_POINT ( 'NONE',  ( -21.05000000000000071, 65.49889199258218753, -241.8691648588935266 ) ) ;
#45050=VECTOR ( 'NONE', #33879, 1000.000000000000000 ) ;
#45056=EDGE_LOOP ( 'NONE', ( #68100, #103137, #196764, #26420, #256378, #50145, #245394, #150291, #83760, #242914, #140395, #155187 ) ) ;
#45059=DIRECTION ( 'NONE',  ( 0.000000000000000000, 0.7216758089626587047, -0.6922311945860948335 ) ) ;
#45092=DIRECTION ( 'NONE',  ( -0.000000000000000000, -0.9651348961777161950, 0.2617529984165015700 ) ) ;
#45099=EDGE_CURVE ( 'NONE', #110678, #15317, #225833, .T. ) ;
#45135=ORIENTED_EDGE ( 'NONE', *, *, #76413, .T. ) ;
#45172=CIRCLE ( 'NONE', #70149, 0.1000000000000124678 ) ;
#45183=CARTESIAN_POINT ( 'NONE',  ( -23.15000000000000213, 78.50726470275243685, -228.6618886302502176 ) ) ;
#45184=EDGE_CURVE ( 'NONE', #229783, #70381, #121829, .T. ) ;
#45201=DIRECTION ( 'NONE',  ( 0.000000000000000000, -0.2617529984165031243, -0.9651348961777157509 ) ) ;
#45206=CARTESIAN_POINT ( 'NONE',  ( -18.59999999999999787, 70.20041822846812352, -198.0817714174541493 ) ) ;
#45229=AXIS2_PLACEMENT_3D ( 'NONE', #176107, #17023, #118694 ) ;
#45250=CARTESIAN_POINT ( 'NONE',  ( 18.37172112093625032, 87.02156976317876058, -199.4492670956951770 ) ) ;
#45257=ORIENTED_EDGE ( 'NONE', *, *, #214757, .F. ) ;
#45268=VECTOR ( 'NONE', #59719, 1000.000000000000000 ) ;
#45271=VERTEX_POINT ( 'NONE', #161508 ) ;
#45288=DIRECTION ( 'NONE',  ( 1.000000000000000000, 0.000000000000000000, 0.000000000000000000 ) ) ;
#45290=AXIS2_PLACEMENT_3D ( 'NONE', #170292, #16326, #193664 ) ;
#45295=DIRECTION ( 'NONE',  ( 4.026293107431335996E-15, 0.7106264324241517993, -0.7035695228903270371 ) ) ;
#45336=CARTESIAN_POINT ( 'NONE',  ( 18.59999999999999076, 80.80934863333322937, -192.8037999715871535 ) ) ;
#45346=DIRECTION ( 'NONE',  ( 1.000000000000000000, 0.000000000000000000, 0.000000000000000000 ) ) ;
#45347=CIRCLE ( 'NONE', #12061, 0.1000000000000124678 ) ;
#45379=ORIENTED_EDGE ( 'NONE', *, *, #43314, .F. ) ;
#45444=LINE ( 'NONE', #7599, #26847 ) ;
#45493=CARTESIAN_POINT ( 'NONE',  ( -18.59999999999999787, 68.58368164137472434, -224.2353459317783120 ) ) ;
#45516=DIRECTION ( 'NONE',  ( 0.000000000000000000, 0.2617529984165035684, 0.9651348961777156399 ) ) ;
#45535=EDGE_CURVE ( 'NONE', #104826, #255232, #7545, .T. ) ;
#45589=DIRECTION ( 'NONE',  ( 1.000000000000000000, 0.000000000000000000, 0.000000000000000000 ) ) ;
#45590=VECTOR ( 'NONE', #121566, 1000.000000000000114 ) ;
#45599=DIRECTION ( 'NONE',  ( -0.000000000000000000, 0.2617529984165031243, 0.9651348961777157509 ) ) ;
#45611=ORIENTED_EDGE ( 'NONE', *, *, #195879, .F. ) ;
#45640=ORIENTED_EDGE ( 'NONE', *, *, #178611, .T. ) ;
#45643=CARTESIAN_POINT ( 'NONE',  ( -21.05000000000000071, 67.23127455305841238, -235.8551265064783991 ) ) ;
#45648=DIRECTION ( 'NONE',  ( 0.000000000000000000, -0.2617529984165031243, -0.9651348961777157509 ) ) ;
#45662=ORIENTED_EDGE ( 'NONE', *, *, #65280, .T. ) ;
#45670=CARTESIAN_POINT ( 'NONE',  ( -18.36527282682019191, 86.98067533972476895, -199.3289536043583325 ) ) ;
#45759=DIRECTION ( 'NONE',  ( 0.000000000000000000, -0.1290532225515364506, -0.9916376685811525427 ) ) ;
#45764=FACE_OUTER_BOUND ( 'NONE', #21657, .T. ) ;
#45782=DIRECTION ( 'NONE',  ( 1.000000000000000000, 7.049440681616511973E-16, -1.911869773728122111E-16 ) ) ;
#45794=CYLINDRICAL_SURFACE ( 'NONE', #21753, 0.09999999999999939493 ) ;
#45841=EDGE_CURVE ( 'NONE', #169290, #231688, #9747, .T. ) ;
#45846=CIRCLE ( 'NONE', #224881, 2.099999999999995204 ) ;
#45849=EDGE_CURVE ( 'NONE', #187774, #164049, #251151, .T. ) ;
#45867=AXIS2_PLACEMENT_3D ( 'NONE', #41253, #19084, #3355 ) ;
#45878=DIRECTION ( 'NONE',  ( 0.000000000000000000, 0.2617529984165026247, 0.9651348961777158619 ) ) ;
#45881=VERTEX_POINT ( 'NONE', #3139 ) ;
#45889=AXIS2_PLACEMENT_3D ( 'NONE', #135853, #202274, #104423 ) ;
#45897=ORIENTED_EDGE ( 'NONE', *, *, #225357, .T. ) ;
#45899=CARTESIAN_POINT ( 'NONE',  ( 21.14999999999999858, 59.16775194334852728, -221.0793150863668473 ) ) ;
#45913=ORIENTED_EDGE ( 'NONE', *, *, #112848, .F. ) ;
#45956=DIRECTION ( 'NONE',  ( -1.000000000000000000, -0.000000000000000000, -0.000000000000000000 ) ) ;
#45984=CARTESIAN_POINT ( 'NONE',  ( 18.59999999999998721, 70.37092869010230345, -198.1237041667535550 ) ) ;
#46001=ORIENTED_EDGE ( 'NONE', *, *, #52662, .F. ) ;
#46014=EDGE_CURVE ( 'NONE', #952, #252597, #242973, .T. ) ;
#46016=CIRCLE ( 'NONE', #121071, 0.09999999999999939493 ) ;
#46021=PLANE ( 'NONE',  #22046 ) ;
#46030=ORIENTED_EDGE ( 'NONE', *, *, #172178, .T. ) ;
#46040=CARTESIAN_POINT ( 'NONE',  ( 21.05000000000000071, 65.63240173135991995, -242.1325252935470189 ) ) ;
#46065=LINE ( 'NONE', #150328, #217281 ) ;
#46085=CARTESIAN_POINT ( 'NONE',  ( 23.14999999999999147, 67.23127455305841238, -235.8551265064783991 ) ) ;
#46155=ORIENTED_EDGE ( 'NONE', *, *, #187128, .T. ) ;
#46176=CARTESIAN_POINT ( 'NONE',  ( 18.49999999999999289, 62.49201502323811752, -208.8221019049098857 ) ) ;
#46185=DIRECTION ( 'NONE',  ( 0.000000000000000000, 0.7035695228903320331, 0.7106264324241468033 ) ) ;
#46195=CARTESIAN_POINT ( 'NONE',  ( -20.85000000000000142, 76.00000000001126921, -203.5231074845248997 ) ) ;
#46218=LINE ( 'NONE', #31513, #208653 ) ;
#46222=DIRECTION ( 'NONE',  ( 0.000000000000000000, -0.3896596508880098009, -0.9209589331071360574 ) ) ;
#46239=CIRCLE ( 'NONE', #196106, 0.09999999999999939493 ) ;
#46244=CARTESIAN_POINT ( 'NONE',  ( -18.49513951962168079, 86.88285858378623061, -199.4517059375024814 ) ) ;
#46325=DIRECTION ( 'NONE',  ( 0.000000000000000000, 0.2617529984165045120, 0.9651348961777153068 ) ) ;
#46356=CARTESIAN_POINT ( 'NONE',  ( 20.94999999999999574, 79.07891399537199106, -236.0635483022085452 ) ) ;
#46364=AXIS2_PLACEMENT_3D ( 'NONE', #54093, #93218, #232755 ) ;
#46370=EDGE_CURVE ( 'NONE', #62193, #125, #97183, .T. ) ;
#46377=VERTEX_POINT ( 'NONE', #191475 ) ;
#46417=CARTESIAN_POINT ( 'NONE',  ( 18.57071067811864040, 62.99531372641386895, -212.5850369713326131 ) ) ;
#46424=VECTOR ( 'NONE', #34936, 999.9999999999998863 ) ;
#46433=EDGE_LOOP ( 'NONE', ( #234346, #164650, #109868, #63906 ) ) ;
#46435=CARTESIAN_POINT ( 'NONE',  ( 18.40000000000000568, 78.23216008268646249, -231.5864513804630178 ) ) ;
#46446=CARTESIAN_POINT ( 'NONE',  ( -23.15000000000000213, 70.60134440767090780, -223.4290147181903023 ) ) ;
#46455=CARTESIAN_POINT ( 'NONE',  ( 21.00000000000000000, 63.35728523183471594, -212.8904317177587870 ) ) ;
#46479=EDGE_CURVE ( 'NONE', #1926, #85926, #110066, .T. ) ;
#46539=CARTESIAN_POINT ( 'NONE',  ( 23.25000000000000000, 86.43238724539048690, -209.5644480942280836 ) ) ;
#46558=LINE ( 'NONE', #225189, #219340 ) ;
#46559=ORIENTED_EDGE ( 'NONE', *, *, #201895, .T. ) ;
#46562=ORIENTED_EDGE ( 'NONE', *, *, #13916, .F. ) ;
#46649=ADVANCED_FACE ( 'NONE', ( #227677 ), #11217, .T. ) ;
#46658=VERTEX_POINT ( 'NONE', #29522 ) ;
#46681=DIRECTION ( 'NONE',  ( 0.000000000000000000, -0.9651348961777157509, 0.2617529984165031243 ) ) ;
#46703=DIRECTION ( 'NONE',  ( 0.000000000000000000, 0.2617529984165030132, 0.9651348961777156399 ) ) ;
#46735=ADVANCED_FACE ( 'NONE', ( #252365 ), #51581, .T. ) ;
#46748=CARTESIAN_POINT ( 'NONE',  ( 21.12400222705985797, 61.96530060562854203, -221.7344222149888822 ) ) ;
#46773=VERTEX_POINT ( 'NONE', #38483 ) ;
#46833=DIRECTION ( 'NONE',  ( 0.000000000000000000, -0.7106264324241464703, 0.7035695228903323661 ) ) ;
#46871=DIRECTION ( 'NONE',  ( 0.000000000000000000, 0.2617529984164506107, 0.9651348961777299618 ) ) ;
#46886=DIRECTION ( 'NONE',  ( -0.000000000000000000, -0.9651348961777157509, 0.2617529984165031243 ) ) ;
#46917=ORIENTED_EDGE ( 'NONE', *, *, #215303, .F. ) ;
#46922=CIRCLE ( 'NONE', #105350, 0.1000000000000124678 ) ;
#46923=ORIENTED_EDGE ( 'NONE', *, *, #206068, .T. ) ;
#46928=CARTESIAN_POINT ( 'NONE',  ( -18.46919391072062311, 87.08044166374625661, -199.6133279112425214 ) ) ;
#46934=ORIENTED_EDGE ( 'NONE', *, *, #16240, .T. ) ;
#46977=EDGE_LOOP ( 'NONE', ( #120103, #178935, #103550, #126756 ) ) ;
#47008=AXIS2_PLACEMENT_3D ( 'NONE', #238426, #18086, #59756 ) ;
#47025=TOROIDAL_SURFACE ( 'NONE', #84397, 0.2000000000000000111, 0.1000000000000000056 ) ;
#47034=AXIS2_PLACEMENT_3D ( 'NONE', #24176, #4577, #5862 ) ;
#47047=DIRECTION ( 'NONE',  ( -0.7071067811865474617, 0.6824534298470372740, -0.1850873201762209819 ) ) ;
#47050=VERTEX_POINT ( 'NONE', #147868 ) ;
#47052=CIRCLE ( 'NONE', #88744, 0.1000000000000090677 ) ;
#47062=CARTESIAN_POINT ( 'NONE',  ( 21.05000000000000071, 71.93512633425886804, -225.1442869522136334 ) ) ;
#47073=ORIENTED_EDGE ( 'NONE', *, *, #34460, .F. ) ;
#47076=CARTESIAN_POINT ( 'NONE',  ( -18.50000000000000000, 52.81534179157634412, -244.1198638051726277 ) ) ;
#47079=ORIENTED_EDGE ( 'NONE', *, *, #17112, .F. ) ;
#47081=DIRECTION ( 'NONE',  ( 0.000000000000000000, 0.2617529984165152257, 0.9651348961777124202 ) ) ;
#47113=AXIS2_PLACEMENT_3D ( 'NONE', #72546, #210752, #149521 ) ;
#47132=CARTESIAN_POINT ( 'NONE',  ( 20.85000000000000142, 76.00000000001126921, -203.5231074845248997 ) ) ;
#47183=ORIENTED_EDGE ( 'NONE', *, *, #52260, .F. ) ;
#47185=DIRECTION ( 'NONE',  ( 1.000000000000000000, 0.000000000000000000, 0.000000000000000000 ) ) ;
#47192=AXIS2_PLACEMENT_3D ( 'NONE', #86715, #146687, #129721 ) ;
#47206=CIRCLE ( 'NONE', #88721, 0.09999999999999939493 ) ;
#47233=DIRECTION ( 'NONE',  ( -0.000000000000000000, -0.9651348961777157509, 0.2617529984165031243 ) ) ;
#47271=CIRCLE ( 'NONE', #80586, 0.1000000000000048767 ) ;
#47283=CARTESIAN_POINT ( 'NONE',  ( 21.00000000000000000, 63.38346053167636995, -212.7939182281409956 ) ) ;
#47286=EDGE_CURVE ( 'NONE', #204366, #41069, #198532, .T. ) ;
#47287=VECTOR ( 'NONE', #125737, 1000.000000000000114 ) ;
#47300=VERTEX_POINT ( 'NONE', #1609 ) ;
#47327=DIRECTION ( 'NONE',  ( -0.7070776581708965169, 0.6824815363281260261, -0.1850949428989399070 ) ) ;
#47343=ORIENTED_EDGE ( 'NONE', *, *, #5359, .F. ) ;
#47361=ADVANCED_FACE ( 'NONE', ( #65439 ), #207126, .F. ) ;
#47387=ORIENTED_EDGE ( 'NONE', *, *, #9229, .T. ) ;
#47414=CARTESIAN_POINT ( 'NONE',  ( 18.49999999999999289, 52.81534179157633702, -244.1198638051726277 ) ) ;
#47434=CARTESIAN_POINT ( 'NONE',  ( -20.64999999999999858, 82.09643798151613225, -215.4278993322501208 ) ) ;
#47561=AXIS2_PLACEMENT_3D ( 'NONE', #138939, #218488, #162412 ) ;
#47586=EDGE_CURVE ( 'NONE', #79203, #160294, #105751, .T. ) ;
#47592=DIRECTION ( 'NONE',  ( 0.000000000000000000, -0.9651348961777379554, 0.2617529984164210233 ) ) ;
#47614=CIRCLE ( 'NONE', #18616, 0.1000000000000124678 ) ;
#47631=EDGE_CURVE ( 'NONE', #67070, #174276, #155699, .T. ) ;
#47641=CIRCLE ( 'NONE', #168345, 0.1000000000000124678 ) ;
#47678=CARTESIAN_POINT ( 'NONE',  ( -20.94999999999999929, 72.02722222756958104, -225.1832529173024398 ) ) ;
#47688=DIRECTION ( 'NONE',  ( 0.000000000000000000, -0.2558827019434435912, 0.9667078373770033872 ) ) ;
#47742=CIRCLE ( 'NONE', #43677, 0.09999999999999123479 ) ;
#47754=VERTEX_POINT ( 'NONE', #41747 ) ;
#47765=DIRECTION ( 'NONE',  ( 1.000000000000000000, 0.000000000000000000, 0.000000000000000000 ) ) ;
#47824=CARTESIAN_POINT ( 'NONE',  ( -21.52071067811865746, 62.95586049149184760, -221.8994582331316394 ) ) ;
#47854=AXIS2_PLACEMENT_3D ( 'NONE', #29241, #189568, #231272 ) ;
#47872=DIRECTION ( 'NONE',  ( -1.000000000000000000, -0.000000000000000000, 0.000000000000000000 ) ) ;
#47897=EDGE_CURVE ( 'NONE', #193798, #107947, #43425, .T. ) ;
#47904=CIRCLE ( 'NONE', #193681, 0.3999999999999890310 ) ;
#47920=DIRECTION ( 'NONE',  ( 2.715809747126116015E-16, 0.9651348961777156399, -0.2617529984165029577 ) ) ;
#47925=AXIS2_PLACEMENT_3D ( 'NONE', #241706, #26527, #5632 ) ;
#47962=ORIENTED_EDGE ( 'NONE', *, *, #244745, .T. ) ;
#47972=DIRECTION ( 'NONE',  ( 1.000000000000000000, -1.772924042024179204E-16, 4.808324575169891715E-17 ) ) ;
#47985=DIRECTION ( 'NONE',  ( 0.000000000000000000, -0.9651348961777157509, 0.2617529984165031243 ) ) ;
#48003=EDGE_CURVE ( 'NONE', #50777, #185233, #93474, .T. ) ;
#48022=CARTESIAN_POINT ( 'NONE',  ( -23.15000000000000213, 60.15036700252697699, -246.1091865931380482 ) ) ;
#48030=AXIS2_PLACEMENT_3D ( 'NONE', #210332, #34284, #190791 ) ;
#48038=DIRECTION ( 'NONE',  ( 0.000000000000000000, 0.2617529984165030132, 0.9651348961777157509 ) ) ;
#48041=VERTEX_POINT ( 'NONE', #44941 ) ;
#48078=CARTESIAN_POINT ( 'NONE',  ( -20.64999999999999858, 78.37638820354418101, -229.1444560783390898 ) ) ;
#48099=CIRCLE ( 'NONE', #39762, 0.1000000000000106498 ) ;
#48114=CARTESIAN_POINT ( 'NONE',  ( 20.04142135623730070, 61.57587952878035509, -212.2000740415318774 ) ) ;
#48152=CARTESIAN_POINT ( 'NONE',  ( -23.25000000000000000, 59.16775194334852728, -221.0793150863668473 ) ) ;
#48165=CARTESIAN_POINT ( 'NONE',  ( 21.07928932188134397, 61.09751618602743406, -234.2940654522722639 ) ) ;
#48193=DIRECTION ( 'NONE',  ( -0.000000000000000000, -0.2617529984165031243, -0.9651348961777157509 ) ) ;
#48200=ORIENTED_EDGE ( 'NONE', *, *, #50731, .T. ) ;
#48236=CARTESIAN_POINT ( 'NONE',  ( 18.53691006697085797, 63.75418316127379370, -209.3175534518712766 ) ) ;
#48256=AXIS2_PLACEMENT_3D ( 'NONE', #78527, #60248, #156828 ) ;
#48280=CARTESIAN_POINT ( 'NONE',  ( -21.05000000000000071, 78.93126476241668854, -235.8702625865613243 ) ) ;
#48307=DIRECTION ( 'NONE',  ( 0.000000000000000000, 0.2617529984165152257, 0.9651348961777124202 ) ) ;
#48336=LINE ( 'NONE', #191737, #191758 ) ;
#48397=ORIENTED_EDGE ( 'NONE', *, *, #244532, .F. ) ;
#48416=FACE_OUTER_BOUND ( 'NONE', #96041, .T. ) ;
#48422=CIRCLE ( 'NONE', #194202, 0.1000000000000124678 ) ;
#48424=CARTESIAN_POINT ( 'NONE',  ( 21.13461538461538325, 60.21941965847794620, -221.1573116214326831 ) ) ;
#48430=CARTESIAN_POINT ( 'NONE',  ( 18.52928932188133970, 63.78876043141220009, -209.2774030244867163 ) ) ;
#48469=DIRECTION ( 'NONE',  ( 0.000000000000000000, 0.7049548389605067023, -0.7092521942342977503 ) ) ;
#48472=CARTESIAN_POINT ( 'NONE',  ( 18.39999999999999858, 86.97871406799755789, -199.3361829075352603 ) ) ;
#48479=DIRECTION ( 'NONE',  ( 0.000000000000000000, -0.1290532225515364506, -0.9916376685811525427 ) ) ;
#48481=CARTESIAN_POINT ( 'NONE',  ( 20.95265033839679347, 59.06589578572285859, -225.8015307137926015 ) ) ;
#48499=EDGE_CURVE ( 'NONE', #217985, #211107, #135348, .T. ) ;
#48515=ORIENTED_EDGE ( 'NONE', *, *, #178611, .F. ) ;
#48532=CARTESIAN_POINT ( 'NONE',  ( -20.64999999999999858, 76.00000000001126921, -203.5231074845248997 ) ) ;
#48546=EDGE_CURVE ( 'NONE', #74710, #151096, #102022, .T. ) ;
#48555=ORIENTED_EDGE ( 'NONE', *, *, #134458, .F. ) ;
#48636=ORIENTED_EDGE ( 'NONE', *, *, #214730, .F. ) ;
#48668=CARTESIAN_POINT ( 'NONE',  ( -21.05000000000000071, 87.22043517378990884, -209.5709486447514678 ) ) ;
#48682=DIRECTION ( 'NONE',  ( -0.000000000000000000, 0.2617529984165031243, 0.9651348961777157509 ) ) ;
#48702=CARTESIAN_POINT ( 'NONE',  ( 20.94999999999999929, 75.24091630460340241, -206.3219986834402846 ) ) ;
#48740=FACE_OUTER_BOUND ( 'NONE', #104366, .T. ) ;
#48741=ORIENTED_EDGE ( 'NONE', *, *, #181141, .T. ) ;
#48763=CARTESIAN_POINT ( 'NONE',  ( 18.49999999999999289, 63.83083047455526327, -209.3924252461221158 ) ) ;
#48766=CIRCLE ( 'NONE', #61805, 3.999999999999996447 ) ;
#48774=EDGE_CURVE ( 'NONE', #220166, #1095, #58730, .T. ) ;
#48788=CIRCLE ( 'NONE', #102936, 0.1000000000000124678 ) ;
#48798=ADVANCED_FACE ( 'NONE', ( #217809, #176165 ), #255624, .T. ) ;
#48807=EDGE_CURVE ( 'NONE', #148962, #77283, #181816, .T. ) ;
#48812=AXIS2_PLACEMENT_3D ( 'NONE', #244207, #245525, #65590 ) ;
#48847=EDGE_CURVE ( 'NONE', #9680, #159529, #152627, .T. ) ;
#48849=AXIS2_PLACEMENT_3D ( 'NONE', #102577, #3496, #25646 ) ;
#48859=AXIS2_PLACEMENT_3D ( 'NONE', #91732, #212964, #253368 ) ;
#48873=ORIENTED_EDGE ( 'NONE', *, *, #136914, .F. ) ;
#48904=DIRECTION ( 'NONE',  ( -1.000000000000000000, 0.000000000000000000, 0.000000000000000000 ) ) ;
#48925=PLANE ( 'NONE',  #170660 ) ;
#48948=ORIENTED_EDGE ( 'NONE', *, *, #52662, .T. ) ;
#48959=( LENGTH_UNIT ( ) NAMED_UNIT ( * ) SI_UNIT ( .MILLI., .METRE. ) );
#48974=DIRECTION ( 'NONE',  ( 0.000000000000000000, 0.2617529984165031243, 0.9651348961777157509 ) ) ;
#48977=CARTESIAN_POINT ( 'NONE',  ( -21.44999999999999929, 65.69978428250288971, -213.4221254243406065 ) ) ;
#48996=CIRCLE ( 'NONE', #11607, 0.09999999999999875655 ) ;
#49006=FACE_OUTER_BOUND ( 'NONE', #232360, .T. ) ;
#49009=DIRECTION ( 'NONE',  ( 1.000000000000000000, 0.000000000000000000, 0.000000000000000000 ) ) ;
#49017=CARTESIAN_POINT ( 'NONE',  ( -20.94999999999999929, 76.00000000001126921, -203.5231074845248997 ) ) ;
#49048=DIRECTION ( 'NONE',  ( 0.000000000000000000, -0.2617529984165031243, -0.9651348961777157509 ) ) ;
#49056=CARTESIAN_POINT ( 'NONE',  ( 18.50000000000000000, 84.35952707724818822, -212.2592855339655671 ) ) ;
#49070=CARTESIAN_POINT ( 'NONE',  ( 20.46382478191414478, 60.87711246931931441, -225.2773833193266171 ) ) ;
#49113=ADVANCED_FACE ( 'NONE', ( #63431 ), #187314, .T. ) ;
#49129=FACE_OUTER_BOUND ( 'NONE', #244644, .T. ) ;
#49147=CARTESIAN_POINT ( 'NONE',  ( -20.54999999999999716, 78.50726470275243685, -228.6618886302502176 ) ) ;
#49216=CIRCLE ( 'NONE', #215797, 0.1000000000000106498 ) ;
#49279=CARTESIAN_POINT ( 'NONE',  ( -21.05000000000000071, 61.06354069362765813, -234.0936775124800704 ) ) ;
#49363=VERTEX_POINT ( 'NONE', #132087 ) ;
#49385=ORIENTED_EDGE ( 'NONE', *, *, #201857, .F. ) ;
#49411=CARTESIAN_POINT ( 'NONE',  ( -21.05000000000000071, 61.17710000698043871, -234.1095691268366465 ) ) ;
#49412=CARTESIAN_POINT ( 'NONE',  ( -23.15000000000000213, 74.97916330618690495, -207.2871335796180006 ) ) ;
#49415=CARTESIAN_POINT ( 'NONE',  ( -22.59999999999999787, 64.05844819680034163, -247.1686437718134073 ) ) ;
#49418=CARTESIAN_POINT ( 'NONE',  ( -18.59999999999999787, 68.48451787451661232, -224.2224406095231757 ) ) ;
#49425=CYLINDRICAL_SURFACE ( 'NONE', #151195, 0.09999999999999939493 ) ;
#49427=DIRECTION ( 'NONE',  ( 0.000000000000000000, -0.2617529984164955192, -0.9651348961777178603 ) ) ;
#49441=DIRECTION ( 'NONE',  ( 0.000000000000000000, 0.2617529984164856383, 0.9651348961777204138 ) ) ;
#49452=ORIENTED_EDGE ( 'NONE', *, *, #98376, .T. ) ;
#49457=TOROIDAL_SURFACE ( 'NONE', #141045, 0.2000000000000000111, 0.1000000000000000056 ) ;
#49470=FACE_OUTER_BOUND ( 'NONE', #217586, .T. ) ;
#49529=CARTESIAN_POINT ( 'NONE',  ( 18.49999999999962697, 63.80058314495188654, -209.3457071354949619 ) ) ;
#49551=CARTESIAN_POINT ( 'NONE',  ( 20.94999999999999929, 82.09643798151613225, -215.4278993322501208 ) ) ;
#49557=AXIS2_PLACEMENT_3D ( 'NONE', #161275, #122138, #19179 ) ;
#49577=CARTESIAN_POINT ( 'NONE',  ( 23.25000000000000000, 78.47509609352879068, -238.9045489380306435 ) ) ;
#49582=CIRCLE ( 'NONE', #120351, 0.09999999999999022171 ) ;
#49594=CARTESIAN_POINT ( 'NONE',  ( -2.995603634470891112E-16, 66.34920340998563404, -213.7018660128499334 ) ) ;
#49604=CARTESIAN_POINT ( 'NONE',  ( -18.59999999999999787, 64.21185867012613357, -224.4479740254296303 ) ) ;
#49623=AXIS2_PLACEMENT_3D ( 'NONE', #211523, #12058, #17189 ) ;
#49647=VERTEX_POINT ( 'NONE', #67953 ) ;
#49671=DIRECTION ( 'NONE',  ( 0.000000000000000000, 0.9651348961777157509, -0.2617529984165031243 ) ) ;
#49677=CIRCLE ( 'NONE', #207917, 11.70000000000000817 ) ;
#49707=DIRECTION ( 'NONE',  ( -0.7071067811865546782, -0.6824534298470523730, 0.1850873201761376874 ) ) ;
#49733=ORIENTED_EDGE ( 'NONE', *, *, #67164, .T. ) ;
#49747=CARTESIAN_POINT ( 'NONE',  ( 21.05000000000000071, 65.65271564877468791, -222.5736063831752176 ) ) ;
#49828=ORIENTED_EDGE ( 'NONE', *, *, #40418, .F. ) ;
#49838=AXIS2_PLACEMENT_3D ( 'NONE', #169397, #130206, #132809 ) ;
#49862=CYLINDRICAL_SURFACE ( 'NONE', #187715, 0.1000000000000124678 ) ;
#49871=EDGE_CURVE ( 'NONE', #16586, #162715, #128624, .T. ) ;
#49884=EDGE_LOOP ( 'NONE', ( #251231, #139758, #7825, #232240, #49828 ) ) ;
#49885=ORIENTED_EDGE ( 'NONE', *, *, #13706, .T. ) ;
#49904=ORIENTED_EDGE ( 'NONE', *, *, #232856, .T. ) ;
#49969=ORIENTED_EDGE ( 'NONE', *, *, #179024, .F. ) ;
#49970=DIRECTION ( 'NONE',  ( 0.000000000000000000, 0.9651348961777163060, -0.2617529984165013479 ) ) ;
#49982=DIRECTION ( 'NONE',  ( 0.000000000000000000, -0.1290532225515392262, -0.9916376685811522096 ) ) ;
#49990=AXIS2_PLACEMENT_3D ( 'NONE', #174482, #173196, #57011 ) ;
#49991=DIRECTION ( 'NONE',  ( -1.000000000000000000, 2.849773892568378313E-16, -7.728835255496647986E-17 ) ) ;
#49996=DIRECTION ( 'NONE',  ( 0.000000000000000000, 0.2617529984165174461, 0.9651348961777118651 ) ) ;
#50049=ORIENTED_EDGE ( 'NONE', *, *, #40804, .F. ) ;
#50087=DIRECTION ( 'NONE',  ( -1.000000000000000000, 2.849773892568378313E-16, -7.728835255496647986E-17 ) ) ;
#50097=CARTESIAN_POINT ( 'NONE',  ( -21.53699400377577433, 60.68021703623777796, -234.0784225921609050 ) ) ;
#50129=CARTESIAN_POINT ( 'NONE',  ( -21.51976009735018636, 60.56174996242723552, -234.0462932889414560 ) ) ;
#50132=LINE ( 'NONE', #51392, #130241 ) ;
#50145=ORIENTED_EDGE ( 'NONE', *, *, #235077, .T. ) ;
#50154=AXIS2_PLACEMENT_3D ( 'NONE', #239537, #40081, #222508 ) ;
#50177=DIRECTION ( 'NONE',  ( 0.000000000000000000, -0.9651348961777379554, 0.2617529984164210233 ) ) ;
#50204=CYLINDRICAL_SURFACE ( 'NONE', #215700, 0.1000000000000018374 ) ;
#50220=DIRECTION ( 'NONE',  ( 1.000000000000000000, 0.000000000000000000, 0.000000000000000000 ) ) ;
#50221=AXIS2_PLACEMENT_3D ( 'NONE', #109926, #52517, #248169 ) ;
#50240=ORIENTED_EDGE ( 'NONE', *, *, #56634, .F. ) ;
#50243=CARTESIAN_POINT ( 'NONE',  ( -20.64999999999999858, 68.59518897103603763, -214.2073844195901131 ) ) ;
#50248=EDGE_CURVE ( 'NONE', #229678, #250282, #257780, .T. ) ;
#50251=DIRECTION ( 'NONE',  ( -1.000000000000000000, -0.000000000000000000, 0.000000000000000000 ) ) ;
#50279=EDGE_CURVE ( 'NONE', #228033, #78723, #163881, .T. ) ;
#50282=DIRECTION ( 'NONE',  ( 0.000000000000000000, -0.2617529984164856383, -0.9651348961777204138 ) ) ;
#50292=AXIS2_PLACEMENT_3D ( 'NONE', #104107, #143248, #178568 ) ;
#50332=VERTEX_POINT ( 'NONE', #167749 ) ;
#50333=ORIENTED_EDGE ( 'NONE', *, *, #133464, .T. ) ;
#50366=ORIENTED_EDGE ( 'NONE', *, *, #53445, .T. ) ;
#50379=CIRCLE ( 'NONE', #83689, 0.09999999999999939493 ) ;
#50412=ORIENTED_EDGE ( 'NONE', *, *, #72617, .T. ) ;
#50451=VERTEX_POINT ( 'NONE', #12522 ) ;
#50493=EDGE_CURVE ( 'NONE', #252057, #198528, #56722, .T. ) ;
#50502=CARTESIAN_POINT ( 'NONE',  ( 20.94999999999999929, 78.89331866122350334, -228.7665898296168052 ) ) ;
#50512=ORIENTED_EDGE ( 'NONE', *, *, #15550, .T. ) ;
#50532=DIRECTION ( 'NONE',  ( 0.5000000000001141309, 0.2266847461454224444, 0.8358313381686951482 ) ) ;
#50540=CYLINDRICAL_SURFACE ( 'NONE', #131321, 0.1000000000000124678 ) ;
#50545=ORIENTED_EDGE ( 'NONE', *, *, #104602, .T. ) ;
#50549=CARTESIAN_POINT ( 'NONE',  ( -23.25000000000000000, 52.81534179157633702, -244.1198638051726277 ) ) ;
#50556=TOROIDAL_SURFACE ( 'NONE', #75546, 3.899999999999999467, 0.1000000000000000056 ) ;
#50564=ORIENTED_EDGE ( 'NONE', *, *, #31813, .F. ) ;
#50574=FACE_OUTER_BOUND ( 'NONE', #155093, .T. ) ;
#50591=CARTESIAN_POINT ( 'NONE',  ( -23.15000000000000213, 68.31754949648690456, -231.8498166873408763 ) ) ;
#50626=CARTESIAN_POINT ( 'NONE',  ( 23.14999999999999858, 76.00000000001126921, -203.5231074845248997 ) ) ;
#50639=VERTEX_POINT ( 'NONE', #48424 ) ;
#50669=DIRECTION ( 'NONE',  ( 0.000000000000000000, -0.2617529984165152257, -0.9651348961777124202 ) ) ;
#50678=CARTESIAN_POINT ( 'NONE',  ( 21.05315837483509966, 62.86884413562100349, -207.0506191170989041 ) ) ;
#50706=DIRECTION ( 'NONE',  ( 0.000000000000000000, 0.2617529984165028467, 0.9651348961777159730 ) ) ;
#50707=CARTESIAN_POINT ( 'NONE',  ( -23.25000000000000000, 68.56901367119438362, -214.3038979092079046 ) ) ;
#50724=CARTESIAN_POINT ( 'NONE',  ( 21.05000000000000071, 87.19425987394825484, -209.6674621343692024 ) ) ;
#50728=DIRECTION ( 'NONE',  ( -1.000000000000000000, -0.000000000000000000, 0.000000000000000000 ) ) ;
#50731=EDGE_CURVE ( 'NONE', #163993, #185233, #17026, .T. ) ;
#50741=CARTESIAN_POINT ( 'NONE',  ( -21.55000000000000426, 65.35370752038342346, -213.3282663891675952 ) ) ;
#50745=CARTESIAN_POINT ( 'NONE',  ( 20.74897398619089017, 59.01508426811044927, -225.6701006227075368 ) ) ;
#50762=AXIS2_PLACEMENT_3D ( 'NONE', #1839, #65687, #81367 ) ;
#50776=CARTESIAN_POINT ( 'NONE',  ( -18.39999999999999858, 86.89640087696872683, -199.6396878666313341 ) ) ;
#50777=VERTEX_POINT ( 'NONE', #74454 ) ;
#50822=CARTESIAN_POINT ( 'NONE',  ( 21.14999999999999503, 64.27847795353595473, -247.1247091181747066 ) ) ;
#50849=CARTESIAN_POINT ( 'NONE',  ( 23.14999999999999858, 67.34812900481119868, -214.0300458246130972 ) ) ;
#50855=DIRECTION ( 'NONE',  ( 0.000000000000000000, -0.9651348961777157509, 0.2617529984165031243 ) ) ;
#50873=EDGE_CURVE ( 'NONE', #46377, #191700, #204162, .T. ) ;
#50897=CARTESIAN_POINT ( 'NONE',  ( -21.59142135623730852, 62.88761514850714462, -221.8809495011140314 ) ) ;
#50926=CIRCLE ( 'NONE', #150914, 7.899999999999996803 ) ;
#50927=FACE_OUTER_BOUND ( 'NONE', #94779, .T. ) ;
#51001=EDGE_CURVE ( 'NONE', #24254, #159793, #144643, .T. ) ;
#51044=AXIS2_PLACEMENT_3D ( 'NONE', #118681, #198193, #34033 ) ;
#51063=AXIS2_PLACEMENT_3D ( 'NONE', #190892, #172634, #12246 ) ;
#51114=DIRECTION ( 'NONE',  ( -1.000000000000000000, -0.000000000000000000, -0.000000000000000000 ) ) ;
#51135=DIRECTION ( 'NONE',  ( 1.000000000000000000, 0.000000000000000000, 0.000000000000000000 ) ) ;
#51141=ORIENTED_EDGE ( 'NONE', *, *, #74453, .F. ) ;
#51167=ORIENTED_EDGE ( 'NONE', *, *, #45099, .F. ) ;
#51181=AXIS2_PLACEMENT_3D ( 'NONE', #103545, #243068, #64445 ) ;
#51194=CIRCLE ( 'NONE', #26302, 0.8750000000000007772 ) ;
#51236=FACE_OUTER_BOUND ( 'NONE', #17174, .T. ) ;
#51266=CARTESIAN_POINT ( 'NONE',  ( -23.15000000000000213, 59.16775194334852728, -221.0793150863668473 ) ) ;
#51291=ORIENTED_EDGE ( 'NONE', *, *, #204960, .T. ) ;
#51298=CARTESIAN_POINT ( 'NONE',  ( -21.05000000000000071, 72.06821323333463170, -225.0920403225231610 ) ) ;
#51302=TOROIDAL_SURFACE ( 'NONE', #38868, 11.90000000000000391, 0.1000000000000000056 ) ;
#51307=CARTESIAN_POINT ( 'NONE',  ( -21.05000000000000071, 68.13014604066189861, -227.7202878558733516 ) ) ;
#51313=CARTESIAN_POINT ( 'NONE',  ( -23.15000000000000213, 77.04701199367727327, -199.6625678998140359 ) ) ;
#51380=ADVANCED_FACE ( 'NONE', ( #124791 ), #4806, .F. ) ;
#51384=DIRECTION ( 'NONE',  ( -1.000000000000000000, 3.151514657663852580E-16, -8.547182517843351137E-17 ) ) ;
#51386=VERTEX_POINT ( 'NONE', #184742 ) ;
#51392=CARTESIAN_POINT ( 'NONE',  ( 18.49999999999999289, 57.93055674131822741, -245.5071546967800771 ) ) ;
#51447=FACE_OUTER_BOUND ( 'NONE', #97920, .T. ) ;
#51459=CARTESIAN_POINT ( 'NONE',  ( 21.14261333020286671, 60.09565987114967811, -221.2273593472489779 ) ) ;
#51490=ADVANCED_FACE ( 'NONE', ( #252411 ), #231596, .T. ) ;
#51504=DIRECTION ( 'NONE',  ( 0.000000000000000000, 0.7035695228903320331, 0.7106264324241468033 ) ) ;
#51510=ORIENTED_EDGE ( 'NONE', *, *, #119112, .F. ) ;
#51520=CARTESIAN_POINT ( 'NONE',  ( -18.47653818581421703, 78.23178856761811062, -231.4551785763766816 ) ) ;
#51548=FACE_OUTER_BOUND ( 'NONE', #46433, .T. ) ;
#51570=CIRCLE ( 'NONE', #118256, 0.09999999999999939493 ) ;
#51581=CYLINDRICAL_SURFACE ( 'NONE', #26904, 0.8750000000000007772 ) ;
#51593=FACE_OUTER_BOUND ( 'NONE', #220017, .T. ) ;
#51596=DIRECTION ( 'NONE',  ( 0.000000000000000000, -0.9651348961777157509, 0.2617529984165028467 ) ) ;
#51600=CARTESIAN_POINT ( 'NONE',  ( 20.85000000000000142, 70.22889768795992893, -198.1282601183952750 ) ) ;
#51633=CIRCLE ( 'NONE', #130781, 0.1000000000000124678 ) ;
#51654=CARTESIAN_POINT ( 'NONE',  ( -18.57399277249657032, 67.49230083716666684, -195.4236814984208479 ) ) ;
#51670=FACE_OUTER_BOUND ( 'NONE', #182009, .T. ) ;
#51680=VERTEX_POINT ( 'NONE', #98443 ) ;
#51686=CARTESIAN_POINT ( 'NONE',  ( -23.15000000000000213, 61.57587952878035509, -212.2000740415318774 ) ) ;
#51693=DIRECTION ( 'NONE',  ( 1.000000000000000000, 0.000000000000000000, -0.000000000000000000 ) ) ;
#51695=CARTESIAN_POINT ( 'NONE',  ( 18.52643265882457868, 67.49293571122092317, -195.4648732548341741 ) ) ;
#51701=CARTESIAN_POINT ( 'NONE',  ( 18.44444291854881612, 86.89436330702220346, -199.6093833839856870 ) ) ;
#51708=ADVANCED_FACE ( 'NONE', ( #106177 ), #4611, .F. ) ;
#51729=AXIS2_PLACEMENT_3D ( 'NONE', #185263, #6616, #9188 ) ;
#51760=EDGE_CURVE ( 'NONE', #82125, #175678, #229506, .T. ) ;
#51771=VERTEX_POINT ( 'NONE', #222261 ) ;
#51792=CARTESIAN_POINT ( 'NONE',  ( 18.39999999999999858, 78.33723480602354527, -231.5810597241785729 ) ) ;
#51802=LINE ( 'NONE', #72703, #26330 ) ;
#51821=AXIS2_PLACEMENT_3D ( 'NONE', #31019, #110512, #233059 ) ;
#51826=CARTESIAN_POINT ( 'NONE',  ( -21.14999999999999858, 64.27847795353595473, -247.1247091181747066 ) ) ;
#51853=DIRECTION ( 'NONE',  ( 0.000000000000000000, 0.4558084472153119959, -0.8900778951570285091 ) ) ;
#51858=CIRCLE ( 'NONE', #226235, 0.1000000000000106498 ) ;
#51861=CARTESIAN_POINT ( 'NONE',  ( -20.97625342178426067, 57.84918772564461875, -226.1321410197392368 ) ) ;
#51927=CARTESIAN_POINT ( 'NONE',  ( 20.12500000000000000, 63.35728523183471594, -212.8904317177587870 ) ) ;
#51958=ORIENTED_EDGE ( 'NONE', *, *, #104808, .T. ) ;
#51960=CARTESIAN_POINT ( 'NONE',  ( -20.64999999999999858, 70.80971041069356886, -215.3055740759912453 ) ) ;
#51967=DIRECTION ( 'NONE',  ( 0.000000000000000000, -0.2617529984165031243, -0.9651348961777157509 ) ) ;
#52000=CARTESIAN_POINT ( 'NONE',  ( -23.15000000000000213, 82.67551891922275331, -215.5849511313000164 ) ) ;
#52017=LINE ( 'NONE', #50724, #115423 ) ;
#52031=EDGE_CURVE ( 'NONE', #10835, #207046, #17314, .T. ) ;
#52040=DIRECTION ( 'NONE',  ( -0.000000000000000000, 0.9651348961777157509, -0.2617529984165031243 ) ) ;
#52048=FACE_OUTER_BOUND ( 'NONE', #104492, .T. ) ;
#52077=VERTEX_POINT ( 'NONE', #23827 ) ;
#52080=ADVANCED_FACE ( 'NONE', ( #227117 ), #229684, .F. ) ;
#52103=VERTEX_POINT ( 'NONE', #204976 ) ;
#52135=CIRCLE ( 'NONE', #73040, 0.1000000000000035028 ) ;
#52154=FACE_OUTER_BOUND ( 'NONE', #236201, .T. ) ;
#52168=VECTOR ( 'NONE', #106437, 1000.000000000000000 ) ;
#52191=EDGE_CURVE ( 'NONE', #57461, #103650, #217174, .T. ) ;
#52193=DIRECTION ( 'NONE',  ( -0.7071067811865475727, 0.6824534298470373850, -0.1850873201762210096 ) ) ;
#52213=VECTOR ( 'NONE', #88586, 1000.000000000000114 ) ;
#52221=EDGE_CURVE ( 'NONE', #72258, #41069, #179809, .T. ) ;
#52250=EDGE_CURVE ( 'NONE', #77989, #123153, #21578, .T. ) ;
#52260=EDGE_CURVE ( 'NONE', #242736, #64537, #146446, .T. ) ;
#52284=DIRECTION ( 'NONE',  ( 0.000000000000000000, -0.2617529984165031243, -0.9651348961777157509 ) ) ;
#52288=DIRECTION ( 'NONE',  ( -6.938893903907222856E-15, -0.9651348961777157509, 0.2617529984165031243 ) ) ;
#52342=CIRCLE ( 'NONE', #198111, 0.1000000000000106498 ) ;
#52361=AXIS2_PLACEMENT_3D ( 'NONE', #83711, #186724, #144991 ) ;
#52383=CARTESIAN_POINT ( 'NONE',  ( -18.59999999999999787, 70.47363787294415260, -228.3418745167492432 ) ) ;
#52472=AXIS2_PLACEMENT_3D ( 'NONE', #22278, #241323, #26126 ) ;
#52489=EDGE_CURVE ( 'NONE', #148648, #115416, #150746, .T. ) ;
#52499=EDGE_CURVE ( 'NONE', #205311, #242990, #184067, .T. ) ;
#52509=CARTESIAN_POINT ( 'NONE',  ( -18.50000000000000000, 79.19526988099229925, -196.1889237952725296 ) ) ;
#52517=DIRECTION ( 'NONE',  ( 1.000000000000000000, 0.000000000000000000, 0.000000000000000000 ) ) ;
#52530=ORIENTED_EDGE ( 'NONE', *, *, #233998, .T. ) ;
#52548=DIRECTION ( 'NONE',  ( -1.000000000000000000, 0.000000000000000000, 0.000000000000000000 ) ) ;
#52567=ORIENTED_EDGE ( 'NONE', *, *, #147099, .F. ) ;
#52571=DIRECTION ( 'NONE',  ( 1.000000000000000000, -2.849773892568378313E-16, 7.728835255496647986E-17 ) ) ;
#52580=AXIS2_PLACEMENT_3D ( 'NONE', #134326, #212612, #150082 ) ;
#52596=EDGE_CURVE ( 'NONE', #121380, #23903, #17462, .T. ) ;
#52597=DIRECTION ( 'NONE',  ( 0.000000000000000000, -0.8430646840892555005, -0.5378121776619452232 ) ) ;
#52607=CARTESIAN_POINT ( 'NONE',  ( -21.44999999999999929, 65.86663596189677605, -213.5709895136416776 ) ) ;
#52619=ORIENTED_EDGE ( 'NONE', *, *, #124539, .T. ) ;
#52662=EDGE_CURVE ( 'NONE', #121787, #103650, #75927, .T. ) ;
#52665=EDGE_CURVE ( 'NONE', #188424, #205311, #42286, .T. ) ;
#52699=EDGE_LOOP ( 'NONE', ( #121674, #250689, #41449, #41502 ) ) ;
#52701=FACE_OUTER_BOUND ( 'NONE', #231149, .T. ) ;
#52705=CIRCLE ( 'NONE', #240173, 0.1000000000000124678 ) ;
#52750=PLANE ( 'NONE',  #194342 ) ;
#52782=DIRECTION ( 'NONE',  ( 1.000000000000000000, 0.000000000000000000, 0.000000000000000000 ) ) ;
#52807=ADVANCED_FACE ( 'NONE', ( #175613 ), #156068, .F. ) ;
#52824=CARTESIAN_POINT ( 'NONE',  ( -18.50000000000000000, 78.21362219944489880, -231.2727646510690533 ) ) ;
#52830=EDGE_CURVE ( 'NONE', #93031, #142612, #33893, .T. ) ;
#52836=CIRCLE ( 'NONE', #27947, 12.97499999999998366 ) ;
#52858=CARTESIAN_POINT ( 'NONE',  ( -20.94999999999999929, 79.19526988099229925, -196.1889237952725296 ) ) ;
#52862=DIRECTION ( 'NONE',  ( 1.000000000000000000, 0.000000000000000000, 0.000000000000000000 ) ) ;
#52867=AXIS2_PLACEMENT_3D ( 'NONE', #9385, #206319, #165928 ) ;
#52870=ADVANCED_FACE ( 'NONE', ( #222388 ), #234312, .F. ) ;
#52899=LINE ( 'NONE', #72489, #168758 ) ;
#52910=DIRECTION ( 'NONE',  ( -0.000000000000000000, 0.3848449534832868446, 0.9229812358755982160 ) ) ;
#52918=CARTESIAN_POINT ( 'NONE',  ( 22.49544290803662960, 55.87396915977497969, -232.8425975917333233 ) ) ;
#52920=EDGE_CURVE ( 'NONE', #56738, #122095, #1052, .T. ) ;
#52946=LINE ( 'NONE', #128656, #57991 ) ;
#52977=CARTESIAN_POINT ( 'NONE',  ( -20.64999999999999858, 70.60814576644823148, -215.7631455941064189 ) ) ;
#52986=CARTESIAN_POINT ( 'NONE',  ( -20.85000000000000142, 70.37092869010230345, -198.1237041667535550 ) ) ;
#52999=CARTESIAN_POINT ( 'NONE',  ( 20.94999999999999929, 76.00000000001126921, -203.5231074845248997 ) ) ;
#53019=CIRCLE ( 'NONE', #202860, 0.9750000000000036415 ) ;
#53038=AXIS2_PLACEMENT_3D ( 'NONE', #70166, #229223, #209648 ) ;
#53041=CARTESIAN_POINT ( 'NONE',  ( -21.05000000000000071, 79.26035508877831148, -236.0091442494974956 ) ) ;
#53077=CARTESIAN_POINT ( 'NONE',  ( -22.50000000000000000, 67.23127455305841238, -235.8551265064783991 ) ) ;
#53100=VERTEX_POINT ( 'NONE', #155761 ) ;
#53107=CARTESIAN_POINT ( 'NONE',  ( 21.05000000000000071, 67.44464249442897597, -214.0562211244547655 ) ) ;
#53119=LINE ( 'NONE', #149680, #231697 ) ;
#53126=DIRECTION ( 'NONE',  ( -0.000000000000000000, -0.1290532225515392817, -0.9916376685811522096 ) ) ;
#53144=DIRECTION ( 'NONE',  ( -1.000000000000000000, -0.000000000000000000, -0.000000000000000000 ) ) ;
#53152=ORIENTED_EDGE ( 'NONE', *, *, #168861, .F. ) ;
#53183=CIRCLE ( 'NONE', #240615, 0.09999999999999939493 ) ;
#53189=EDGE_LOOP ( 'NONE', ( #175382, #157677, #149949, #146594, #162208, #99093, #246149, #175649, #72579, #148920, #40030, #94846, #212078, #211122, #157633, #199965, #219444, #247792, #18001, #192927, #74244, #114612, #137626, #120738, #120676 ) ) ;
#53198=ORIENTED_EDGE ( 'NONE', *, *, #210910, .F. ) ;
#53232=ADVANCED_FACE ( 'NONE', ( #216964 ), #145134, .T. ) ;
#53240=EDGE_CURVE ( 'NONE', #198941, #9680, #8907, .T. ) ;
#53277=TOROIDAL_SURFACE ( 'NONE', #140753, 0.6000000000000013101, 0.1000000000000000056 ) ;
#53340=CARTESIAN_POINT ( 'NONE',  ( 20.97250901189795513, 58.98335100983494073, -225.6767934319825031 ) ) ;
#53356=ORIENTED_EDGE ( 'NONE', *, *, #183941, .F. ) ;
#53369=CARTESIAN_POINT ( 'NONE',  ( -20.94999999999999929, 72.93748991853820485, -214.8151857698041738 ) ) ;
#53395=ORIENTED_EDGE ( 'NONE', *, *, #50731, .F. ) ;
#53397=ORIENTED_EDGE ( 'NONE', *, *, #105037, .F. ) ;
#53404=DIRECTION ( 'NONE',  ( 1.000000000000000000, 0.000000000000000000, 0.000000000000000000 ) ) ;
#53416=CIRCLE ( 'NONE', #199161, 12.77499999999999503 ) ;
#53445=EDGE_CURVE ( 'NONE', #68619, #158463, #150304, .T. ) ;
#53489=CIRCLE ( 'NONE', #140984, 0.1000000000000018374 ) ;
#53527=DIRECTION ( 'NONE',  ( 0.000000000000000000, -0.7106264324241465813, 0.7035695228903324772 ) ) ;
#53563=CARTESIAN_POINT ( 'NONE',  ( -21.10320863425827298, 65.53183290861515786, -242.0257079080814435 ) ) ;
#53564=EDGE_CURVE ( 'NONE', #247, #70381, #35520, .T. ) ;
#53566=DIRECTION ( 'NONE',  ( -2.827886303505249259E-16, -0.9667078373770114919, -0.2558827019434133931 ) ) ;
#53631=CARTESIAN_POINT ( 'NONE',  ( 20.95420533658165141, 59.03391012955845696, -225.7910507217099507 ) ) ;
#53636=CARTESIAN_POINT ( 'NONE',  ( 18.59999999999999787, 68.50594083727658301, -224.0235912779512830 ) ) ;
#53650=ORIENTED_EDGE ( 'NONE', *, *, #20855, .T. ) ;
#53669=AXIS2_PLACEMENT_3D ( 'NONE', #50897, #52193, #211290 ) ;
#53679=DIRECTION ( 'NONE',  ( 0.000000000000000000, 0.2617529984165035684, 0.9651348961777156399 ) ) ;
#53696=EDGE_LOOP ( 'NONE', ( #84498, #20078, #169951, #165910 ) ) ;
#53708=CARTESIAN_POINT ( 'NONE',  ( -18.50000000000000000, 63.93636616954134411, -213.0474835168086827 ) ) ;
#53723=DIRECTION ( 'NONE',  ( 1.000000000000000000, 0.000000000000000000, 0.000000000000000000 ) ) ;
#53744=EDGE_CURVE ( 'NONE', #137789, #206482, #66285, .T. ) ;
#53776=VECTOR ( 'NONE', #228915, 1000.000000000000000 ) ;
#53802=AXIS2_PLACEMENT_3D ( 'NONE', #257975, #100205, #194233 ) ;
#53805=CARTESIAN_POINT ( 'NONE',  ( 18.49999999999999289, 62.39550153362034735, -208.7959266050682459 ) ) ;
#53814=VERTEX_POINT ( 'NONE', #241086 ) ;
#53830=EDGE_CURVE ( 'NONE', #211751, #8256, #133939, .T. ) ;
#53838=DIRECTION ( 'NONE',  ( 0.000000000000000000, 0.7092521942343974484, 0.7049548389604062271 ) ) ;
#53854=DIRECTION ( 'NONE',  ( -0.000000000000000000, -0.2617529984165031243, -0.9651348961777157509 ) ) ;
#53875=DIRECTION ( 'NONE',  ( 0.000000000000000000, 0.8430646840892555005, 0.5378121776619452232 ) ) ;
#53911=LINE ( 'NONE', #51307, #239577 ) ;
#53940=VECTOR ( 'NONE', #120194, 1000.000000000000000 ) ;
#53944=CARTESIAN_POINT ( 'NONE',  ( -21.05000000000000071, 68.51069317435826633, -224.1259271199053842 ) ) ;
#53956=ORIENTED_EDGE ( 'NONE', *, *, #64241, .F. ) ;
#53964=ORIENTED_EDGE ( 'NONE', *, *, #133355, .F. ) ;
#53978=EDGE_CURVE ( 'NONE', #167923, #250282, #242487, .T. ) ;
#53991=CARTESIAN_POINT ( 'NONE',  ( -22.16821283564876666, 59.93584560259382243, -233.8765425695785893 ) ) ;
#53996=DIRECTION ( 'NONE',  ( 1.000000000000000000, 0.000000000000000000, 0.000000000000000000 ) ) ;
#54043=ORIENTED_EDGE ( 'NONE', *, *, #244413, .F. ) ;
#54059=DIRECTION ( 'NONE',  ( 0.000000000000000000, 0.2617529984165031243, 0.9651348961777157509 ) ) ;
#54062=DIRECTION ( 'NONE',  ( 0.000000000000000000, 0.2617529984165152257, 0.9651348961777124202 ) ) ;
#54093=CARTESIAN_POINT ( 'NONE',  ( -23.15000000000000213, 86.43238724539048690, -209.5644480942280836 ) ) ;
#54117=CARTESIAN_POINT ( 'NONE',  ( 22.40000000000010516, 64.15556351076629937, -247.1958793361852429 ) ) ;
#54157=VERTEX_POINT ( 'NONE', #170254 ) ;
#54171=ORIENTED_EDGE ( 'NONE', *, *, #63236, .F. ) ;
#54175=DIRECTION ( 'NONE',  ( 1.000000000000000000, 0.000000000000000000, 0.000000000000000000 ) ) ;
#54203=EDGE_CURVE ( 'NONE', #115380, #146108, #50926, .T. ) ;
#54204=AXIS2_PLACEMENT_3D ( 'NONE', #104665, #143816, #65574 ) ;
#54217=DIRECTION ( 'NONE',  ( 0.000000000000000000, -0.7973076739542579450, 0.6035730884107166627 ) ) ;
#54254=EDGE_CURVE ( 'NONE', #43859, #209826, #108932, .T. ) ;
#54278=CARTESIAN_POINT ( 'NONE',  ( 22.40736611211992368, 64.18196446391819165, -247.0985338183330668 ) ) ;
#54294=CARTESIAN_POINT ( 'NONE',  ( 18.59999999999999076, 62.49201502323811752, -208.8221019049098857 ) ) ;
#54303=ADVANCED_FACE ( 'NONE', ( #187218 ), #47025, .T. ) ;
#54320=CYLINDRICAL_SURFACE ( 'NONE', #223031, 0.09999999999999939493 ) ;
#54335=ADVANCED_FACE ( 'NONE', ( #117913 ), #13723, .F. ) ;
#54357=ORIENTED_EDGE ( 'NONE', *, *, #246804, .F. ) ;
#54358=B_SPLINE_CURVE_WITH_KNOTS ( 'NONE', 3,
 ( #29587, #230312, #146908, #51654, #131214, #105188, #184768, #66112, #225159, #215869, #234162, #75129, #232915, #55494, #95927, #33448, #210756, #37278, #154667 ),
 .UNSPECIFIED., .F., .F.,
 ( 4, 3, 3, 3, 3, 3, 4 ),
 ( 0.000000000000000000, 2.646747978908111750E-05, 5.271166642128749541E-05, 9.008788829883769176E-05, 0.0001426648776561031766, 0.0001897378458659604891, 0.0001917382627806266582 ),
 .UNSPECIFIED. ) ;
#54381=EDGE_CURVE ( 'NONE', #87179, #101113, #255084, .T. ) ;
#54388=ORIENTED_EDGE ( 'NONE', *, *, #80520, .F. ) ;
#54437=DIRECTION ( 'NONE',  ( 0.000000000000000000, -0.1071148137998806232, -0.9942466578594150173 ) ) ;
#54450=FACE_OUTER_BOUND ( 'NONE', #162363, .T. ) ;
#54451=ADVANCED_FACE ( 'NONE', ( #42253 ), #43539, .T. ) ;
#54471=CARTESIAN_POINT ( 'NONE',  ( -20.64999999999999858, 78.98983215084128062, -228.7927651294584450 ) ) ;
#54481=ADVANCED_FACE ( 'NONE', ( #23987 ), #134505, .F. ) ;
#54524=DIRECTION ( 'NONE',  ( 0.000000000000000000, -0.3896596508880124654, -0.9209589331071350582 ) ) ;
#54539=LINE ( 'NONE', #235736, #154145 ) ;
#54559=DIRECTION ( 'NONE',  ( 1.000000000000000000, 0.000000000000000000, 0.000000000000000000 ) ) ;
#54560=EDGE_LOOP ( 'NONE', ( #179737, #85210, #174267, #249840 ) ) ;
#54566=ORIENTED_EDGE ( 'NONE', *, *, #194506, .F. ) ;
#54569=CARTESIAN_POINT ( 'NONE',  ( -21.14999999999999858, 65.59307282722802768, -241.8954991560463554 ) ) ;
#54578=EDGE_CURVE ( 'NONE', #124124, #211251, #9440, .T. ) ;
#54596=ADVANCED_FACE ( 'NONE', ( #128208 ), #221803, .T. ) ;
#54606=DIRECTION ( 'NONE',  ( 0.000000000000000000, 0.2617529984164856383, 0.9651348961777204138 ) ) ;
#54615=CARTESIAN_POINT ( 'NONE',  ( -22.47071067811865319, 65.11488425470513164, -243.2801022963548689 ) ) ;
#54621=DIRECTION ( 'NONE',  ( 0.000000000000000000, 0.2617529984166090395, 0.9651348961776869961 ) ) ;
#54625=ORIENTED_EDGE ( 'NONE', *, *, #231550, .F. ) ;
#54635=CARTESIAN_POINT ( 'NONE',  ( 18.49999999999999645, 79.37986612816742138, -196.2658927859692142 ) ) ;
#54640=VERTEX_POINT ( 'NONE', #171229 ) ;
#54641=EDGE_LOOP ( 'NONE', ( #215981, #100446, #215077, #165200, #173762, #188083, #91112, #32826, #45897, #20628 ) ) ;
#54652=ORIENTED_EDGE ( 'NONE', *, *, #104808, .F. ) ;
#54660=LINE ( 'NONE', #212477, #177862 ) ;
#54690=DIRECTION ( 'NONE',  ( 0.000000000000000000, 0.9651348961777379554, -0.2617529984164210233 ) ) ;
#54696=EDGE_LOOP ( 'NONE', ( #82364, #48200, #234366, #227195 ) ) ;
#54734=CARTESIAN_POINT ( 'NONE',  ( -21.05000000000000071, 86.32947205150912851, -209.3293116780858156 ) ) ;
#54766=AXIS2_PLACEMENT_3D ( 'NONE', #166028, #184271, #65608 ) ;
#54776=FACE_OUTER_BOUND ( 'NONE', #1391, .T. ) ;
#54796=CIRCLE ( 'NONE', #200549, 0.1000000000000124678 ) ;
#54807=DIRECTION ( 'NONE',  ( -1.000000000000000000, -0.000000000000000000, -0.000000000000000000 ) ) ;
#54829=PLANE ( 'NONE',  #203600 ) ;
#54834=DIRECTION ( 'NONE',  ( 0.000000000000000000, 0.2617529984164915779, 0.9651348961777189706 ) ) ;
#54852=ORIENTED_EDGE ( 'NONE', *, *, #122772, .F. ) ;
#54869=CARTESIAN_POINT ( 'NONE',  ( 21.05000000000000071, 60.92751661265764795, -225.4207664198654015 ) ) ;
#54935=DIRECTION ( 'NONE',  ( 0.000000000000000000, 0.9651348961777118651, -0.2617529984165174461 ) ) ;
#54942=ORIENTED_EDGE ( 'NONE', *, *, #200928, .T. ) ;
#54964=LINE ( 'NONE', #74595, #181666 ) ;
#54987=CARTESIAN_POINT ( 'NONE',  ( 21.14999999999999858, 61.95748721176698126, -221.7323031544521541 ) ) ;
#55002=AXIS2_PLACEMENT_3D ( 'NONE', #15563, #168234, #69108 ) ;
#55015=LINE ( 'NONE', #158043, #203787 ) ;
#55018=DIRECTION ( 'NONE',  ( 1.000000000000000000, 0.000000000000000000, 0.000000000000000000 ) ) ;
#55028=VECTOR ( 'NONE', #55018, 1000.000000000000000 ) ;
#55076=PLANE ( 'NONE',  #122077 ) ;
#55080=ORIENTED_EDGE ( 'NONE', *, *, #60988, .F. ) ;
#55094=FACE_OUTER_BOUND ( 'NONE', #88084, .T. ) ;
#55096=CARTESIAN_POINT ( 'NONE',  ( -20.64999999999999858, 68.37653524343949130, -222.4633752038642172 ) ) ;
#55097=CARTESIAN_POINT ( 'NONE',  ( -21.64999999999999858, 63.37018259659601682, -222.0118260003222872 ) ) ;
#55100=VERTEX_POINT ( 'NONE', #73097 ) ;
#55118=CARTESIAN_POINT ( 'NONE',  ( 23.14999999999999858, 64.04577702392042227, -222.1950530992138226 ) ) ;
#55120=DIRECTION ( 'NONE',  ( 0.000000000000000000, -0.2617529984164955192, -0.9651348961777178603 ) ) ;
#55134=VERTEX_POINT ( 'NONE', #96448 ) ;
#55141=DIRECTION ( 'NONE',  ( 0.000000000000000000, 0.2617529984165071211, 0.9651348961777146407 ) ) ;
#55161=PLANE ( 'NONE',  #51063 ) ;
#55162=ADVANCED_FACE ( 'NONE', ( #212583 ), #147367, .F. ) ;
#55167=ORIENTED_EDGE ( 'NONE', *, *, #49871, .T. ) ;
#55177=DIRECTION ( 'NONE',  ( 0.000000000000000000, 0.9651348961777157509, -0.2617529984165031243 ) ) ;
#55178=VECTOR ( 'NONE', #6004, 1000.000000000000000 ) ;
#55190=EDGE_CURVE ( 'NONE', #27906, #252932, #155766, .T. ) ;
#55198=TOROIDAL_SURFACE ( 'NONE', #205248, 11.65000000000000036, 0.1000000000000000056 ) ;
#55216=DIRECTION ( 'NONE',  ( 7.304098846218135653E-16, 0.9651348961777157509, -0.2617529984165031243 ) ) ;
#55222=ADVANCED_FACE ( 'NONE', ( #178608 ), #182446, .F. ) ;
#55296=ADVANCED_FACE ( 'NONE', ( #220291 ), #35162, .F. ) ;
#55332=CARTESIAN_POINT ( 'NONE',  ( -23.25000000000000000, 76.00000000001126921, -203.5231074845248997 ) ) ;
#55339=EDGE_CURVE ( 'NONE', #59315, #240058, #132405, .T. ) ;
#55344=DIRECTION ( 'NONE',  ( 0.000000000000000000, -0.2617529984165031243, -0.9651348961777157509 ) ) ;
#55345=CARTESIAN_POINT ( 'NONE',  ( -18.50000000000000000, 79.37986612816742138, -196.2658927859692142 ) ) ;
#55354=CARTESIAN_POINT ( 'NONE',  ( -22.47071067811865319, 65.11488425470513164, -243.2801022963548689 ) ) ;
#55359=CARTESIAN_POINT ( 'NONE',  ( -18.59999999999999787, 68.51069317435826633, -224.1259271199053842 ) ) ;
#55372=DIRECTION ( 'NONE',  ( 2.952720810173289112E-16, 0.9651348961777155289, -0.2617529984165037904 ) ) ;
#55378=DIRECTION ( 'NONE',  ( -1.000000000000000000, 0.000000000000000000, 0.000000000000000000 ) ) ;
#55407=CARTESIAN_POINT ( 'NONE',  ( -18.40000000000000213, 78.24072131640578220, -231.5548844243369331 ) ) ;
#55418=ADVANCED_FACE ( 'NONE', ( #252330 ), #67611, .F. ) ;
#55428=EDGE_LOOP ( 'NONE', ( #240619, #33640, #247681, #186508, #22898 ) ) ;
#55433=CARTESIAN_POINT ( 'NONE',  ( 23.25000000000000000, 81.82295291318693842, -214.8938525951558915 ) ) ;
#55438=DIRECTION ( 'NONE',  ( 0.000000000000000000, 0.2617529984165152257, 0.9651348961777124202 ) ) ;
#55441=ORIENTED_EDGE ( 'NONE', *, *, #225547, .T. ) ;
#55472=DIRECTION ( 'NONE',  ( 0.000000000000000000, 0.9651348961777157509, -0.2617529984165031243 ) ) ;
#55492=ADVANCED_FACE ( 'NONE', ( #138774 ), #157118, .F. ) ;
#55494=CARTESIAN_POINT ( 'NONE',  ( -18.50211644919735932, 67.49401193140450061, -195.5283494629371432 ) ) ;
#55496=CIRCLE ( 'NONE', #13849, 11.90000000000000568 ) ;
#55534=DIRECTION ( 'NONE',  ( 1.000000000000000000, 0.000000000000000000, 0.000000000000000000 ) ) ;
#55546=FACE_OUTER_BOUND ( 'NONE', #63305, .T. ) ;
#55549=AXIS2_PLACEMENT_3D ( 'NONE', #100740, #239018, #36993 ) ;
#55586=AXIS2_PLACEMENT_3D ( 'NONE', #178055, #115483, #78904 ) ;
#55587=CARTESIAN_POINT ( 'NONE',  ( 20.94999999999999929, 76.00000000001126921, -203.5231074845248997 ) ) ;
#55594=CARTESIAN_POINT ( 'NONE',  ( 21.05000000000000071, 77.07318729351892728, -199.5660544101962728 ) ) ;
#55600=ADVANCED_FACE ( 'NONE', ( #145224 ), #76622, .T. ) ;
#55602=CARTESIAN_POINT ( 'NONE',  ( -20.94999999999999929, 79.28653038861995128, -235.9126307598797325 ) ) ;
#55604=VERTEX_POINT ( 'NONE', #162255 ) ;
#55625=ORIENTED_EDGE ( 'NONE', *, *, #130285, .T. ) ;
#55634=ORIENTED_EDGE ( 'NONE', *, *, #50873, .T. ) ;
#55635=AXIS2_PLACEMENT_3D ( 'NONE', #140313, #120797, #219862 ) ;
#55639=ORIENTED_EDGE ( 'NONE', *, *, #213764, .T. ) ;
#55642=EDGE_CURVE ( 'NONE', #128967, #50451, #1848, .T. ) ;
#55660=CYLINDRICAL_SURFACE ( 'NONE', #68794, 0.1000000000000124678 ) ;
#55698=CARTESIAN_POINT ( 'NONE',  ( 21.14999999999999858, 63.99342642423710714, -222.3880800784493772 ) ) ;
#55705=AXIS2_PLACEMENT_3D ( 'NONE', #59619, #218709, #40126 ) ;
#55719=CARTESIAN_POINT ( 'NONE',  ( 21.05000000000000071, 59.13236860818124541, -225.8959333647716505 ) ) ;
#55726=DIRECTION ( 'NONE',  ( 0.000000000000000000, 0.2617529984165120616, 0.9651348961777134194 ) ) ;
#55731=ADVANCED_FACE ( 'NONE', ( #12176 ), #160230, .T. ) ;
#55756=AXIS2_PLACEMENT_3D ( 'NONE', #148662, #66549, #250313 ) ;
#55771=AXIS2_PLACEMENT_3D ( 'NONE', #144324, #79225, #140488 ) ;
#55816=ADVANCED_FACE ( 'NONE', ( #55094 ), #76997, .F. ) ;
#55841=CARTESIAN_POINT ( 'NONE',  ( 18.49999999999999645, 58.44755627554218336, -246.4682640075163818 ) ) ;
#55873=DIRECTION ( 'NONE',  ( -1.000000000000000000, -0.000000000000000000, 0.000000000000000000 ) ) ;
#55878=CARTESIAN_POINT ( 'NONE',  ( 21.05000000000000071, 70.47363787294415260, -228.3418745167492432 ) ) ;
#55886=EDGE_LOOP ( 'NONE', ( #39556, #51141, #217938, #215062 ) ) ;
#55888=EDGE_CURVE ( 'NONE', #16173, #188424, #17301, .T. ) ;
#55902=CIRCLE ( 'NONE', #126674, 0.1000000000000079159 ) ;
#55919=DIRECTION ( 'NONE',  ( 0.7071067811865474617, -0.6824534298470372740, 0.1850873201762209819 ) ) ;
#55928=CIRCLE ( 'NONE', #14289, 0.09999999999999543976 ) ;
#55953=EDGE_CURVE ( 'NONE', #47050, #50777, #101928, .T. ) ;
#55992=DIRECTION ( 'NONE',  ( 0.000000000000000000, -0.9209589331071360574, 0.3896596508880098009 ) ) ;
#56028=CARTESIAN_POINT ( 'NONE',  ( 22.50000000000000000, 59.68594599439719417, -233.9123800762197902 ) ) ;
#56040=EDGE_LOOP ( 'NONE', ( #35, #152823, #137921, #208344 ) ) ;
#56050=CIRCLE ( 'NONE', #126991, 0.1000000000000124678 ) ;
#56077=ORIENTED_EDGE ( 'NONE', *, *, #184297, .F. ) ;
#56079=CARTESIAN_POINT ( 'NONE',  ( -18.59999999999999787, 97.49741144064424248, -225.2667035127916790 ) ) ;
#56093=ORIENTED_EDGE ( 'NONE', *, *, #121777, .F. ) ;
#56097=CARTESIAN_POINT ( 'NONE',  ( -21.14999999999999858, 65.51923798433686841, -242.1677427744926092 ) ) ;
#56110=DIRECTION ( 'NONE',  ( 0.000000000000000000, -0.7092521942343286145, -0.7049548389604757270 ) ) ;
#56134=DIRECTION ( 'NONE',  ( 1.000000000000000000, 0.000000000000000000, 0.000000000000000000 ) ) ;
#56211=ADVANCED_FACE ( 'NONE', ( #174820 ), #212626, .T. ) ;
#56234=CIRCLE ( 'NONE', #156238, 0.09999999999999543976 ) ;
#56248=DIRECTION ( 'NONE',  ( 1.000000000000000000, 0.000000000000000000, -0.000000000000000000 ) ) ;
#56253=ORIENTED_EDGE ( 'NONE', *, *, #33173, .F. ) ;
#56264=( BOUNDED_CURVE ( )  B_SPLINE_CURVE ( 3, ( #132558, #212103, #131264, #33496 ),
 .UNSPECIFIED., .F., .T. ) 
 B_SPLINE_CURVE_WITH_KNOTS ( ( 4, 4 ),
 ( 3.141592653589793116, 4.712388980384689674 ),
 .UNSPECIFIED. ) 
 CURVE ( )  GEOMETRIC_REPRESENTATION_ITEM ( )  RATIONAL_B_SPLINE_CURVE ( ( 1.000000000000000000, 0.8047378541243649375, 0.8047378541243649375, 1.000000000000000000 ) ) 
 REPRESENTATION_ITEM ( '' )  );
#56293=ORIENTED_EDGE ( 'NONE', *, *, #189167, .F. ) ;
#56297=EDGE_CURVE ( 'NONE', #235080, #192701, #247426, .T. ) ;
#56315=AXIS2_PLACEMENT_3D ( 'NONE', #230061, #207952, #110105 ) ;
#56318=FACE_OUTER_BOUND ( 'NONE', #140715, .T. ) ;
#56326=DIRECTION ( 'NONE',  ( 1.000000000000000000, 0.000000000000000000, 0.000000000000000000 ) ) ;
#56369=ADVANCED_FACE ( 'NONE', ( #89251 ), #14670, .T. ) ;
#56372=EDGE_CURVE ( 'NONE', #123814, #155690, #214539, .T. ) ;
#56374=EDGE_CURVE ( 'NONE', #241262, #205787, #232652, .T. ) ;
#56400=FACE_OUTER_BOUND ( 'NONE', #125496, .T. ) ;
#56415=AXIS2_PLACEMENT_3D ( 'NONE', #204652, #185107, #145969 ) ;
#56487=AXIS2_PLACEMENT_3D ( 'NONE', #50591, #187581, #169319 ) ;
#56489=CIRCLE ( 'NONE', #202269, 0.09999999999999939493 ) ;
#56507=ORIENTED_EDGE ( 'NONE', *, *, #120309, .F. ) ;
#56571=( BOUNDED_SURFACE ( )  B_SPLINE_SURFACE ( 3, 2, ( 
 ( #127971, #6728, #185370 ),
 ( #2863, #242762, #64145 ),
 ( #207520, #101949, #181538 ),
 ( #143668, #223198, #203652 ),
 ( #184083, #165831, #5416 ),
 ( #84947, #164538, #244047 ) ),
 .UNSPECIFIED., .F., .F., .F. ) 
 B_SPLINE_SURFACE_WITH_KNOTS ( ( 4, 2, 4 ),
 ( 3, 3 ),
 ( 1.570796326794897668, 2.356194490192346169, 3.141592653589794448 ),
 ( 0.000000000000000000, 1.000000000000000000 ),
 .UNSPECIFIED. ) 
 GEOMETRIC_REPRESENTATION_ITEM ( )  RATIONAL_B_SPLINE_SURFACE ( (
 ( 1.000000000000000000, 0.7071067811865341390, 1.000000000000000000),
 ( 1.000000000000000000, 0.6611148371781488953, 1.000000000000000000),
 ( 1.000000000000000000, 0.6092287576690736950, 1.000000000000000000),
 ( 1.000000000000000000, 0.5278258667062413201, 1.000000000000000000),
 ( 1.000000000000000000, 0.4993418825330954713, 1.000000000000000000),
 ( 1.000000000000000000, 0.4999999999999439337, 1.000000000000000000) ) ) 
 REPRESENTATION_ITEM ( '' )  SURFACE ( )  );
#56580=AXIS2_PLACEMENT_3D ( 'NONE', #188618, #27017, #106490 ) ;
#56600=CARTESIAN_POINT ( 'NONE',  ( -22.50000000000000000, 55.96443555106008461, -232.8914797391818752 ) ) ;
#56608=EDGE_CURVE ( 'NONE', #257242, #121380, #197973, .T. ) ;
#56615=( BOUNDED_SURFACE ( )  B_SPLINE_SURFACE ( 3, 2, ( 
 ( #55407, #1865, #97095 ),
 ( #197512, #218347, #119285 ),
 ( #154581, #16346, #196231 ),
 ( #35909, #115412, #176697 ),
 ( #194983, #17587, #98375 ),
 ( #177977, #257438, #243064 ),
 ( #244344, #3153, #85244 ),
 ( #43594, #126978, #166147 ) ),
 .UNSPECIFIED., .F., .F., .F. ) 
 B_SPLINE_SURFACE_WITH_KNOTS ( ( 4, 2, 2, 4 ),
 ( 3, 3 ),
 ( 0.0001723339234021440737, 0.0002782939632049864602, 0.0003842540030078289010, 0.0005961740826135137825 ),
 ( 0.000000000000000000, 1.000000000000000000 ),
 .UNSPECIFIED. ) 
 GEOMETRIC_REPRESENTATION_ITEM ( )  RATIONAL_B_SPLINE_SURFACE ( (
 ( 1.000000000000000000, 0.9504532311154547664, 1.000000000000000000),
 ( 1.000000000000000000, 0.9506023220708359478, 1.000000000000000000),
 ( 1.000000000000000000, 0.9395774818183325605, 1.000000000000000000),
 ( 1.000000000000000000, 0.9079328464646000407, 1.000000000000000000),
 ( 1.000000000000000000, 0.8875702416213150370, 1.000000000000000000),
 ( 1.000000000000000000, 0.8205919608026237544, 1.000000000000000000),
 ( 1.000000000000000000, 0.7666842783609403300, 1.000000000000000000),
 ( 1.000000000000000000, 0.7071067811864569785, 1.000000000000000000) ) ) 
 REPRESENTATION_ITEM ( '' )  SURFACE ( )  );
#56634=EDGE_CURVE ( 'NONE', #186373, #204719, #56489, .T. ) ;
#56640=DIRECTION ( 'NONE',  ( 1.000000000000000000, 0.000000000000000000, 0.000000000000000000 ) ) ;
#56655=CARTESIAN_POINT ( 'NONE',  ( 22.49999999999999645, 64.05844819680035584, -247.1686437718134641 ) ) ;
#56696=ORIENTED_EDGE ( 'NONE', *, *, #102169, .F. ) ;
#56722=LINE ( 'NONE', #217094, #216268 ) ;
#56738=VERTEX_POINT ( 'NONE', #54635 ) ;
#56762=CARTESIAN_POINT ( 'NONE',  ( -23.25000000000000000, 78.47509609352879068, -238.9045489380306435 ) ) ;
#56778=CIRCLE ( 'NONE', #77634, 0.3999999999999926392 ) ;
#56780=CARTESIAN_POINT ( 'NONE',  ( -20.64999999999999858, 72.62993014539878800, -215.9492192728129965 ) ) ;
#56792=VERTEX_POINT ( 'NONE', #35125 ) ;
#56824=CARTESIAN_POINT ( 'NONE',  ( 18.50016250449482413, 67.49429988484645548, -195.5441618131978316 ) ) ;
#56830=CARTESIAN_POINT ( 'NONE',  ( 20.94999999999999929, 60.06173988932782493, -221.3217724115915814 ) ) ;
#56854=AXIS2_PLACEMENT_3D ( 'NONE', #121928, #64513, #46222 ) ;
#56855=CIRCLE ( 'NONE', #165042, 0.5000000000000014433 ) ;
#56914=CARTESIAN_POINT ( 'NONE',  ( -20.94999999999999929, 68.20313450767837082, -227.8297066677462794 ) ) ;
#56951=CARTESIAN_POINT ( 'NONE',  ( 22.50000000000000000, 59.72530380783945247, -233.9230542583682393 ) ) ;
#56962=CARTESIAN_POINT ( 'NONE',  ( -20.94999999999999929, 76.00000000001126921, -203.5231074845248997 ) ) ;
#56963=DIRECTION ( 'NONE',  ( 1.000000000000000000, 0.000000000000000000, 0.000000000000000000 ) ) ;
#56970=AXIS2_PLACEMENT_3D ( 'NONE', #97022, #194908, #117902 ) ;
#57010=ORIENTED_EDGE ( 'NONE', *, *, #70581, .F. ) ;
#57011=DIRECTION ( 'NONE',  ( 0.000000000000000000, 0.2617529984165152257, 0.9651348961777124202 ) ) ;
#57014=CARTESIAN_POINT ( 'NONE',  ( -20.64999999999999858, 68.70534379447684614, -223.0647885566232560 ) ) ;
#57019=DIRECTION ( 'NONE',  ( -1.000000000000000000, -0.000000000000000000, 0.000000000000000000 ) ) ;
#57024=EDGE_CURVE ( 'NONE', #110447, #188240, #148278, .T. ) ;
#57027=ADVANCED_FACE ( 'NONE', ( #106584 ), #64902, .F. ) ;
#57028=ORIENTED_EDGE ( 'NONE', *, *, #4631, .T. ) ;
#57031=DIRECTION ( 'NONE',  ( -1.000000000000000000, -0.000000000000000000, 0.000000000000000000 ) ) ;
#57053=ORIENTED_EDGE ( 'NONE', *, *, #132475, .T. ) ;
#57065=CIRCLE ( 'NONE', #89835, 11.64999999999998970 ) ;
#57097=DIRECTION ( 'NONE',  ( 1.000000000000000000, 0.000000000000000000, -0.000000000000000000 ) ) ;
#57136=CIRCLE ( 'NONE', #202899, 0.1000000000000090677 ) ;
#57167=EDGE_LOOP ( 'NONE', ( #187514, #107209, #10683, #78764 ) ) ;
#57172=PLANE ( 'NONE',  #191606 ) ;
#57206=EDGE_CURVE ( 'NONE', #25862, #74935, #144152, .T. ) ;
#57255=DIRECTION ( 'NONE',  ( 1.000000000000000000, -2.849773892568378313E-16, 7.728835255496647986E-17 ) ) ;
#57260=VERTEX_POINT ( 'NONE', #76455 ) ;
#57271=DIRECTION ( 'NONE',  ( 0.000000000000000000, 0.2558827019434435912, -0.9667078373770033872 ) ) ;
#57272=CARTESIAN_POINT ( 'NONE',  ( 22.39999999999999503, 65.19201463318205469, -243.3742797652979277 ) ) ;
#57317=CARTESIAN_POINT ( 'NONE',  ( 23.14999999999999858, 68.05808644172607558, -213.7045301755741491 ) ) ;
#57326=CIRCLE ( 'NONE', #90647, 0.1000000000000106498 ) ;
#57366=ORIENTED_EDGE ( 'NONE', *, *, #177505, .T. ) ;
#57381=AXIS2_PLACEMENT_3D ( 'NONE', #119566, #183379, #240783 ) ;
#57385=ORIENTED_EDGE ( 'NONE', *, *, #195818, .T. ) ;
#57399=CARTESIAN_POINT ( 'NONE',  ( 21.05000000000000071, 65.61575147395463148, -242.1939180743342774 ) ) ;
#57409=DIRECTION ( 'NONE',  ( -1.000000000000000000, 0.000000000000000000, 0.000000000000000000 ) ) ;
#57418=DIRECTION ( 'NONE',  ( -0.000000000000000000, 0.9651348961777155289, -0.2617529984165036794 ) ) ;
#57420=FACE_OUTER_BOUND ( 'NONE', #138198, .T. ) ;
#57426=EDGE_CURVE ( 'NONE', #200563, #70381, #183274, .T. ) ;
#57453=DIRECTION ( 'NONE',  ( -1.000000000000000000, -0.000000000000000000, 0.000000000000000000 ) ) ;
#57461=VERTEX_POINT ( 'NONE', #125848 ) ;
#57480=DIRECTION ( 'NONE',  ( 0.000000000000000000, -0.2617529984164955192, -0.9651348961777178603 ) ) ;
#57496=EDGE_CURVE ( 'NONE', #204227, #129114, #67177, .T. ) ;
#57504=CARTESIAN_POINT ( 'NONE',  ( -18.59999999999999787, 61.38756220455727686, -221.6813469827248184 ) ) ;
#57509=EDGE_LOOP ( 'NONE', ( #13300, #219566 ) ) ;
#57518=AXIS2_PLACEMENT_3D ( 'NONE', #253330, #156840, #214223 ) ;
#57529=ORIENTED_EDGE ( 'NONE', *, *, #56634, .T. ) ;
#57554=ORIENTED_EDGE ( 'NONE', *, *, #205642, .F. ) ;
#57600=DIRECTION ( 'NONE',  ( -1.000000000000000000, -0.000000000000000000, 0.000000000000000000 ) ) ;
#57625=ORIENTED_EDGE ( 'NONE', *, *, #63236, .T. ) ;
#57654=CARTESIAN_POINT ( 'NONE',  ( -18.59999999999999787, 61.63293978347611812, -221.5406706031726003 ) ) ;
#57657=EDGE_LOOP ( 'NONE', ( #49969, #235828, #144503 ) ) ;
#57659=CARTESIAN_POINT ( 'NONE',  ( -20.00857864376270001, 63.86602797976523505, -212.9247947273492514 ) ) ;
#57687=LINE ( 'NONE', #218037, #96894 ) ;
#57722=EDGE_LOOP ( 'NONE', ( #101029, #147603, #75963, #184301 ) ) ;
#57724=DIRECTION ( 'NONE',  ( 0.000000000000000000, -0.2617529984165035128, -0.9651348961777155289 ) ) ;
#57763=LINE ( 'NONE', #194751, #237470 ) ;
#57797=FACE_OUTER_BOUND ( 'NONE', #91538, .T. ) ;
#57801=AXIS2_PLACEMENT_3D ( 'NONE', #215618, #190959, #91832 ) ;
#57828=FACE_OUTER_BOUND ( 'NONE', #127829, .T. ) ;
#57857=DIRECTION ( 'NONE',  ( 1.000000000000000000, 0.000000000000000000, 0.000000000000000000 ) ) ;
#57863=CARTESIAN_POINT ( 'NONE',  ( -21.14999999999999858, 60.94483358488582070, -234.0465764481390636 ) ) ;
#57875=ORIENTED_EDGE ( 'NONE', *, *, #124284, .T. ) ;
#57893=DIRECTION ( 'NONE',  ( -1.000000000000000000, -0.000000000000000000, 0.000000000000000000 ) ) ;
#57983=CARTESIAN_POINT ( 'NONE',  ( 20.94999675878240808, 67.49461024981995649, -195.5605382655040216 ) ) ;
#57991=VECTOR ( 'NONE', #188607, 1000.000000000000000 ) ;
#58042=VECTOR ( 'NONE', #221257, 1000.000000000000000 ) ;
#58049=ORIENTED_EDGE ( 'NONE', *, *, #222285, .F. ) ;
#58065=ORIENTED_EDGE ( 'NONE', *, *, #219234, .T. ) ;
#58070=VERTEX_POINT ( 'NONE', #54987 ) ;
#58073=DIRECTION ( 'NONE',  ( 1.000000000000000000, 0.000000000000000000, 0.000000000000000000 ) ) ;
#58082=CARTESIAN_POINT ( 'NONE',  ( -23.15000000000000213, 61.57587952878036219, -212.2000740415318774 ) ) ;
#58085=CARTESIAN_POINT ( 'NONE',  ( -21.05000000000000071, 70.47363787294415260, -228.3418745167492432 ) ) ;
#58103=ADVANCED_FACE ( 'NONE', ( #114986 ), #120167, .T. ) ;
#58159=FACE_OUTER_BOUND ( 'NONE', #211760, .T. ) ;
#58172=DIRECTION ( 'NONE',  ( 0.000000000000000000, -0.2617529984165022361, -0.9651348961777160840 ) ) ;
#58200=VERTEX_POINT ( 'NONE', #75862 ) ;
#58208=CARTESIAN_POINT ( 'NONE',  ( -18.59999999999999787, 59.50933445848280456, -243.9217804674669310 ) ) ;
#58247=DIRECTION ( 'NONE',  ( -1.000000000000000000, -3.348484323767863974E-14, 9.081381425208614860E-15 ) ) ;
#58280=VECTOR ( 'NONE', #166922, 1000.000000000000000 ) ;
#58302=ORIENTED_EDGE ( 'NONE', *, *, #191502, .T. ) ;
#58360=DIRECTION ( 'NONE',  ( 0.000000000000000000, -0.4105728183244014562, -0.9118278131605539460 ) ) ;
#58367=CARTESIAN_POINT ( 'NONE',  ( 21.00000000000000000, 63.35728523183471594, -212.8904317177587870 ) ) ;
#58400=CIRCLE ( 'NONE', #50221, 4.300000000000033573 ) ;
#58410=DIRECTION ( 'NONE',  ( 0.000000000000000000, -0.2617529984164955192, -0.9651348961777178603 ) ) ;
#58420=CIRCLE ( 'NONE', #245892, 0.1999999999999987899 ) ;
#58450=CIRCLE ( 'NONE', #25185, 0.1000000000000124678 ) ;
#58460=ORIENTED_EDGE ( 'NONE', *, *, #195161, .T. ) ;
#58470=ADVANCED_FACE ( 'NONE', ( #256364 ), #81604, .T. ) ;
#58477=LINE ( 'NONE', #200579, #217696 ) ;
#58487=ORIENTED_EDGE ( 'NONE', *, *, #136539, .T. ) ;
#58493=ORIENTED_EDGE ( 'NONE', *, *, #54254, .T. ) ;
#58495=AXIS2_PLACEMENT_3D ( 'NONE', #15817, #233562, #255625 ) ;
#58541=CARTESIAN_POINT ( 'NONE',  ( -22.59999985501179154, 55.87389454177475301, -232.8428744225222431 ) ) ;
#58567=DIRECTION ( 'NONE',  ( 0.000000000000000000, 0.2617529984165034018, 0.9651348961777157509 ) ) ;
#58576=CARTESIAN_POINT ( 'NONE',  ( 19.75857864376268935, 62.46583972339646351, -208.9186153945276487 ) ) ;
#58598=DIRECTION ( 'NONE',  ( 0.000000000000000000, 0.2617529984165050116, 0.9651348961777153068 ) ) ;
#58613=DIRECTION ( 'NONE',  ( 0.000000000000000000, -0.2617529984164915779, -0.9651348961777189706 ) ) ;
#58621=DIRECTION ( 'NONE',  ( 0.000000000000000000, 0.2617529984165152257, 0.9651348961777124202 ) ) ;
#58630=LINE ( 'NONE', #73118, #30028 ) ;
#58696=EDGE_CURVE ( 'NONE', #17708, #164109, #112197, .T. ) ;
#58713=CARTESIAN_POINT ( 'NONE',  ( 21.05000000000000071, 60.90953975616409366, -225.2728109422286877 ) ) ;
#58714=CARTESIAN_POINT ( 'NONE',  ( 20.95083306685154056, 60.84428375453579463, -225.3393541664412112 ) ) ;
#58730=LINE ( 'NONE', #114883, #173501 ) ;
#58753=LINE ( 'NONE', #97872, #5806 ) ;
#58756=DIRECTION ( 'NONE',  ( 1.000000000000000000, 0.000000000000000000, 0.000000000000000000 ) ) ;
#58767=EDGE_LOOP ( 'NONE', ( #254394, #68720, #238674, #146747 ) ) ;
#58799=ORIENTED_EDGE ( 'NONE', *, *, #136539, .F. ) ;
#58815=EDGE_CURVE ( 'NONE', #185762, #85685, #36227, .T. ) ;
#58832=ORIENTED_EDGE ( 'NONE', *, *, #30338, .F. ) ;
#58843=AXIS2_PLACEMENT_3D ( 'NONE', #123391, #38725, #142921 ) ;
#58889=FACE_OUTER_BOUND ( 'NONE', #197846, .T. ) ;
#58912=DIRECTION ( 'NONE',  ( -1.000000000000000000, 3.151514657663852580E-16, -8.547182517843351137E-17 ) ) ;
#58933=EDGE_CURVE ( 'NONE', #184831, #211733, #65233, .T. ) ;
#58958=ORIENTED_EDGE ( 'NONE', *, *, #221345, .T. ) ;
#58963=ORIENTED_EDGE ( 'NONE', *, *, #15009, .F. ) ;
#58974=ORIENTED_EDGE ( 'NONE', *, *, #208638, .F. ) ;
#58982=CARTESIAN_POINT ( 'NONE',  ( 19.90621891164687440, 62.38985952047473660, -208.8167298195660635 ) ) ;
#59089=DIRECTION ( 'NONE',  ( 0.000000000000000000, 0.2617529984165152257, 0.9651348961777124202 ) ) ;
#59115=CIRCLE ( 'NONE', #250683, 0.1000000000000106498 ) ;
#59190=DIRECTION ( 'NONE',  ( 0.000000000000000000, 0.2617529984165152257, 0.9651348961777124202 ) ) ;
#59223=AXIS2_PLACEMENT_3D ( 'NONE', #43282, #19878, #23746 ) ;
#59249=DIRECTION ( 'NONE',  ( -0.000000000000000000, 0.2493442905258256848, 0.9684149032218436481 ) ) ;
#59284=AXIS2_PLACEMENT_3D ( 'NONE', #193939, #58247, #40021 ) ;
#59308=DIRECTION ( 'NONE',  ( -0.7070776581709311559, -0.1850949428989308032, -0.6824815363280924974 ) ) ;
#59315=VERTEX_POINT ( 'NONE', #78458 ) ;
#59329=SPHERICAL_SURFACE ( 'NONE', #100279, 0.1000000000000000056 ) ;
#59332=ORIENTED_EDGE ( 'NONE', *, *, #36342, .F. ) ;
#59336=ORIENTED_EDGE ( 'NONE', *, *, #37158, .T. ) ;
#59342=EDGE_CURVE ( 'NONE', #9358, #65920, #225011, .T. ) ;
#59390=VECTOR ( 'NONE', #143114, 1000.000000000000000 ) ;
#59402=CARTESIAN_POINT ( 'NONE',  ( -23.25000000000000000, 55.89093952297024970, -232.7795287750844579 ) ) ;
#59409=CARTESIAN_POINT ( 'NONE',  ( 20.94999999999999574, 70.62381305392328557, -228.5002045501660746 ) ) ;
#59448=CARTESIAN_POINT ( 'NONE',  ( 21.05000000000000071, 67.23127455305841238, -235.8551265064783991 ) ) ;
#59454=ORIENTED_EDGE ( 'NONE', *, *, #158333, .T. ) ;
#59460=CARTESIAN_POINT ( 'NONE',  ( -20.94999999999999929, 67.49463558145296815, -195.5618716440587548 ) ) ;
#59506=CIRCLE ( 'NONE', #226106, 11.70000000000000817 ) ;
#59517=DIRECTION ( 'NONE',  ( -0.000000000000000000, 0.9651348961777155289, -0.2617529984165036794 ) ) ;
#59528=EDGE_LOOP ( 'NONE', ( #191332, #45662, #50366, #139906 ) ) ;
#59530=DIRECTION ( 'NONE',  ( 1.000000000000000000, 0.000000000000000000, 0.000000000000000000 ) ) ;
#59563=CARTESIAN_POINT ( 'NONE',  ( -21.05000000000000071, 74.92681270650359693, -207.4801605588535551 ) ) ;
#59571=AXIS2_PLACEMENT_3D ( 'NONE', #192043, #251986, #35546 ) ;
#59590=DIRECTION ( 'NONE',  ( -4.448008912761039862E-16, -0.9651348961777161950, 0.2617529984165013479 ) ) ;
#59604=CARTESIAN_POINT ( 'NONE',  ( 21.14999999999999858, 52.81534179157632991, -244.1198638051726277 ) ) ;
#59619=CARTESIAN_POINT ( 'NONE',  ( -23.25000000000000000, 67.23127455305841238, -235.8551265064783991 ) ) ;
#59655=ORIENTED_EDGE ( 'NONE', *, *, #121343, .T. ) ;
#59675=DIRECTION ( 'NONE',  ( 0.000000000000000000, 0.9667078373770114919, 0.2558827019434133931 ) ) ;
#59688=ORIENTED_EDGE ( 'NONE', *, *, #112149, .T. ) ;
#59705=DIRECTION ( 'NONE',  ( 1.000000000000000000, -3.151514657663852580E-16, 8.547182517843351137E-17 ) ) ;
#59719=DIRECTION ( 'NONE',  ( -0.000000000000000000, 0.2617529984165031243, 0.9651348961777157509 ) ) ;
#59756=DIRECTION ( 'NONE',  ( 0.000000000000000000, -0.9999991631930157387, 0.001293682058423061953 ) ) ;
#59868=CARTESIAN_POINT ( 'NONE',  ( 20.85000000000000142, 76.00000000001126921, -203.5231074845248997 ) ) ;
#59904=ADVANCED_FACE ( 'NONE', ( #127570 ), #148426, .T. ) ;
#59923=CARTESIAN_POINT ( 'NONE',  ( -20.85000000000000142, 76.00000000001126921, -203.5231074845248997 ) ) ;
#59933=AXIS2_PLACEMENT_3D ( 'NONE', #241396, #84835, #220542 ) ;
#59950=AXIS2_PLACEMENT_3D ( 'NONE', #136661, #98793, #197921 ) ;
#59966=ADVANCED_FACE ( 'NONE', ( #201496 ), #145376, .T. ) ;
#59988=CARTESIAN_POINT ( 'NONE',  ( 18.59999999999999432, 79.11538813396778380, -196.3722783875038544 ) ) ;
#59995=DIRECTION ( 'NONE',  ( -0.000000000000000000, -0.2617529984165031243, -0.9651348961777157509 ) ) ;
#60012=CIRCLE ( 'NONE', #247469, 7.900000000000013678 ) ;
#60026=DIRECTION ( 'NONE',  ( -0.000000000000000000, 0.9118278131605244141, -0.4105728183244670704 ) ) ;
#60067=EDGE_LOOP ( 'NONE', ( #240823, #180610, #74578, #210304 ) ) ;
#60071=ORIENTED_EDGE ( 'NONE', *, *, #41774, .T. ) ;
#60086=SPHERICAL_SURFACE ( 'NONE', #132696, 0.1000000000000000056 ) ;
#60087=ORIENTED_EDGE ( 'NONE', *, *, #226944, .F. ) ;
#60117=ORIENTED_EDGE ( 'NONE', *, *, #40547, .T. ) ;
#60119=AXIS2_PLACEMENT_3D ( 'NONE', #50549, #169284, #84517 ) ;
#60147=EDGE_LOOP ( 'NONE', ( #251526, #210566, #114599, #244310 ) ) ;
#60150=CARTESIAN_POINT ( 'NONE',  ( 20.94999999999999929, 76.00000000001126921, -203.5231074845248997 ) ) ;
#60170=CARTESIAN_POINT ( 'NONE',  ( 21.05000000000000071, 78.17003882911672008, -228.8770135013149911 ) ) ;
#60188=DIRECTION ( 'NONE',  ( 0.000000000000000000, -0.2617529984164506107, -0.9651348961777299618 ) ) ;
#60231=CARTESIAN_POINT ( 'NONE',  ( -21.14999999999999858, 55.98745301258801987, -232.8057040749261262 ) ) ;
#60248=DIRECTION ( 'NONE',  ( -1.000000000000000000, -2.671448610905051031E-14, -6.406987848362951272E-14 ) ) ;
#60265=CARTESIAN_POINT ( 'NONE',  ( 21.14999999999999858, 64.27847795353595473, -247.1247091181747066 ) ) ;
#60266=ORIENTED_EDGE ( 'NONE', *, *, #163278, .T. ) ;
#60273=TOROIDAL_SURFACE ( 'NONE', #110336, 0.6000000000000009770, 0.1000000000000000056 ) ;
#60286=ORIENTED_EDGE ( 'NONE', *, *, #208781, .F. ) ;
#60297=CARTESIAN_POINT ( 'NONE',  ( 20.97468175916167965, 60.18418091238081757, -221.2464335850836505 ) ) ;
#60341=CIRCLE ( 'NONE', #35269, 0.1000000000000106498 ) ;
#60363=ADVANCED_FACE ( 'NONE', ( #24386 ), #204724, .T. ) ;
#60374=FACE_OUTER_BOUND ( 'NONE', #26128, .T. ) ;
#60383=VERTEX_POINT ( 'NONE', #45206 ) ;
#60402=ORIENTED_EDGE ( 'NONE', *, *, #102395, .T. ) ;
#60413=ORIENTED_EDGE ( 'NONE', *, *, #230150, .F. ) ;
#60420=CARTESIAN_POINT ( 'NONE',  ( 20.93284271247462414, 62.82351852614502974, -207.2177435922979214 ) ) ;
#60444=EDGE_LOOP ( 'NONE', ( #236780, #60087, #159257, #168914 ) ) ;
#60466=CARTESIAN_POINT ( 'NONE',  ( -20.94999675878240808, 67.49461024981995649, -195.5605382655040216 ) ) ;
#60484=VERTEX_POINT ( 'NONE', #26963 ) ;
#60488=ORIENTED_EDGE ( 'NONE', *, *, #12267, .F. ) ;
#60490=DIRECTION ( 'NONE',  ( 1.000000000000000000, 0.000000000000000000, 0.000000000000000000 ) ) ;
#60497=EDGE_CURVE ( 'NONE', #15176, #249034, #121582, .T. ) ;
#60500=DIRECTION ( 'NONE',  ( 0.000000000000000000, -0.9651348961777379554, 0.2617529984164210233 ) ) ;
#60505=DIRECTION ( 'NONE',  ( 1.000000000000000000, 0.000000000000000000, 0.000000000000000000 ) ) ;
#60511=EDGE_CURVE ( 'NONE', #159037, #133646, #17325, .T. ) ;
#60523=DIRECTION ( 'NONE',  ( -1.000000000000000000, 2.849773892568378313E-16, -7.728835255496647986E-17 ) ) ;
#60555=ADVANCED_FACE ( 'NONE', ( #51593 ), #166474, .F. ) ;
#60599=ORIENTED_EDGE ( 'NONE', *, *, #136914, .T. ) ;
#60621=ORIENTED_EDGE ( 'NONE', *, *, #225357, .F. ) ;
#60629=DIRECTION ( 'NONE',  ( 0.000000000000000000, -0.2617529984164856383, -0.9651348961777204138 ) ) ;
#60643=DIRECTION ( 'NONE',  ( -1.000000000000000000, -0.000000000000000000, -0.000000000000000000 ) ) ;
#60649=CARTESIAN_POINT ( 'NONE',  ( -20.54999999999999716, 81.86853375790846599, -214.9828603846715964 ) ) ;
#60669=CARTESIAN_POINT ( 'NONE',  ( 18.49999999999998934, 63.79085327820362039, -209.3815830819285395 ) ) ;
#60671=CARTESIAN_POINT ( 'NONE',  ( -20.94999999999999929, 69.29912324054878070, -228.2305608266744343 ) ) ;
#60729=AXIS2_PLACEMENT_3D ( 'NONE', #20619, #199249, #58410 ) ;
#60747=ORIENTED_EDGE ( 'NONE', *, *, #23159, .T. ) ;
#60802=DIRECTION ( 'NONE',  ( -1.000000000000000000, -0.000000000000000000, -0.000000000000000000 ) ) ;
#60818=CARTESIAN_POINT ( 'NONE',  ( 23.24999999999999289, 63.99342642423710714, -222.3880800784493772 ) ) ;
#60834=EDGE_CURVE ( 'NONE', #101319, #2330, #163581, .T. ) ;
#60861=EDGE_CURVE ( 'NONE', #22560, #171424, #188270, .T. ) ;
#60883=CARTESIAN_POINT ( 'NONE',  ( -20.94999999999999929, 80.82257920297074349, -192.8058055878823609 ) ) ;
#60915=ADVANCED_FACE ( 'NONE', ( #224817 ), #26654, .T. ) ;
#60935=ORIENTED_EDGE ( 'NONE', *, *, #24993, .T. ) ;
#60947=AXIS2_PLACEMENT_3D ( 'NONE', #25321, #164815, #246901 ) ;
#60952=CARTESIAN_POINT ( 'NONE',  ( 23.15000000000000213, 82.67551891922275331, -215.5849511313000164 ) ) ;
#60988=EDGE_CURVE ( 'NONE', #59315, #40380, #115159, .T. ) ;
#60996=DIRECTION ( 'NONE',  ( -1.000000000000000000, 0.000000000000000000, 0.000000000000000000 ) ) ;
#60999=FACE_OUTER_BOUND ( 'NONE', #62974, .T. ) ;
#61017=CARTESIAN_POINT ( 'NONE',  ( 22.39999999999999858, 59.71212129423884818, -233.8158665866020272 ) ) ;
#61034=ORIENTED_EDGE ( 'NONE', *, *, #100871, .F. ) ;
#61044=DIRECTION ( 'NONE',  ( 1.000000000000000000, -6.696968647535681247E-15, 1.816276285041710114E-15 ) ) ;
#61104=LINE ( 'NONE', #237188, #172637 ) ;
#61150=EDGE_CURVE ( 'NONE', #41172, #77258, #183790, .T. ) ;
#61187=CARTESIAN_POINT ( 'NONE',  ( 20.95512820512820440, 58.98414156600839675, -225.6766266970810477 ) ) ;
#61227=DIRECTION ( 'NONE',  ( 1.000000000000000000, 0.000000000000000000, 0.000000000000000000 ) ) ;
#61240=CIRCLE ( 'NONE', #94536, 11.90000000000000213 ) ;
#61317=DIRECTION ( 'NONE',  ( 0.000000000000000000, 0.2617529984165044010, 0.9651348961777154178 ) ) ;
#61358=ADVANCED_FACE ( 'NONE', ( #173265 ), #171969, .F. ) ;
#61360=VERTEX_POINT ( 'NONE', #70293 ) ;
#61400=ORIENTED_EDGE ( 'NONE', *, *, #97112, .T. ) ;
#61401=CARTESIAN_POINT ( 'NONE',  ( -22.45354308602258087, 64.15556329907074939, -247.1958792766958481 ) ) ;
#61409=TOROIDAL_SURFACE ( 'NONE', #186316, 0.4000000000000015210, 0.1000000000000000056 ) ;
#61412=ORIENTED_EDGE ( 'NONE', *, *, #105742, .F. ) ;
#61425=EDGE_CURVE ( 'NONE', #176771, #235080, #139187, .T. ) ;
#61453=DIRECTION ( 'NONE',  ( -1.000000000000000000, 0.000000000000000000, 0.000000000000000000 ) ) ;
#61463=ADVANCED_FACE ( 'NONE', ( #97486 ), #20573, .T. ) ;
#61511=CARTESIAN_POINT ( 'NONE',  ( 23.14999999999999503, 59.07123845373075000, -221.0531397865252075 ) ) ;
#61516=VERTEX_POINT ( 'NONE', #23144 ) ;
#61532=DIRECTION ( 'NONE',  ( 0.000000000000000000, -0.9651348961777028723, 0.2617529984165503087 ) ) ;
#61535=EDGE_CURVE ( 'NONE', #85165, #104826, #130270, .T. ) ;
#61553=CARTESIAN_POINT ( 'NONE',  ( -21.05000000000000071, 68.35681244624936426, -231.7050464529142459 ) ) ;
#61554=CARTESIAN_POINT ( 'NONE',  ( 23.14999999999999503, 59.16775194334852017, -221.0793150863668473 ) ) ;
#61596=CARTESIAN_POINT ( 'NONE',  ( -21.17356465864818560, 61.00651281073072596, -234.2694012202724423 ) ) ;
#61605=CARTESIAN_POINT ( 'NONE',  ( -20.85000000000000142, 62.88396779178383156, -206.9948552354529170 ) ) ;
#61617=DIRECTION ( 'NONE',  ( 1.000000000000000000, -3.151514657663852580E-16, 8.547182517843351137E-17 ) ) ;
#61643=ORIENTED_EDGE ( 'NONE', *, *, #52250, .F. ) ;
#61658=AXIS2_PLACEMENT_3D ( 'NONE', #6706, #186647, #225731 ) ;
#61665=ORIENTED_EDGE ( 'NONE', *, *, #167048, .F. ) ;
#61668=DIRECTION ( 'NONE',  ( 1.000000000000000000, 0.000000000000000000, 0.000000000000000000 ) ) ;
#61721=ORIENTED_EDGE ( 'NONE', *, *, #54578, .T. ) ;
#61751=CARTESIAN_POINT ( 'NONE',  ( -22.48479450179659977, 64.13649931337441501, -247.0866463600959833 ) ) ;
#61754=FILL_AREA_STYLE_COLOUR ( '', #10826 ) ;
#61762=DIRECTION ( 'NONE',  ( 0.000000000000000000, 0.2617529984165152257, 0.9651348961777124202 ) ) ;
#61777=DIRECTION ( 'NONE',  ( -0.000000000000000000, 0.1290532225515619857, 0.9916376685811492120 ) ) ;
#61805=AXIS2_PLACEMENT_3D ( 'NONE', #120135, #139629, #99222 ) ;
#61827=EDGE_LOOP ( 'NONE', ( #149334, #48515, #252387, #19099 ) ) ;
#61865=TOROIDAL_SURFACE ( 'NONE', #211725, 4.099999999999999645, 0.1000000000000000056 ) ;
#61867=CARTESIAN_POINT ( 'NONE',  ( 20.94999999999999929, 67.49462292596868451, -195.5612049585272700 ) ) ;
#61869=DIRECTION ( 'NONE',  ( 0.000000000000000000, -0.9930108503404180276, -0.1180230956474192239 ) ) ;
#61890=DIRECTION ( 'NONE',  ( -0.000000000000000000, 0.2617529984165031243, 0.9651348961777157509 ) ) ;
#61908=EDGE_CURVE ( 'NONE', #97513, #74229, #122275, .T. ) ;
#61976=DIRECTION ( 'NONE',  ( -1.000000000000000000, -8.153259210133937167E-16, -2.158126701439427224E-16 ) ) ;
#61989=DIRECTION ( 'NONE',  ( -1.000000000000000000, 2.849773892568378313E-16, -7.728835255496647986E-17 ) ) ;
#62009=EDGE_CURVE ( 'NONE', #248002, #135164, #163617, .T. ) ;
#62023=CYLINDRICAL_SURFACE ( 'NONE', #47561, 12.87500000000000178 ) ;
#62108=ORIENTED_EDGE ( 'NONE', *, *, #16240, .F. ) ;
#62128=DIRECTION ( 'NONE',  ( 0.000000000000000000, 0.9651348961777157509, -0.2617529984165031243 ) ) ;
#62136=LINE ( 'NONE', #120854, #187882 ) ;
#62150=DIRECTION ( 'NONE',  ( 1.000000000000000000, 0.000000000000000000, 0.000000000000000000 ) ) ;
#62189=DIRECTION ( 'NONE',  ( 0.000000000000000000, 0.3848449534832868446, 0.9229812358755982160 ) ) ;
#62193=VERTEX_POINT ( 'NONE', #112632 ) ;
#62207=CARTESIAN_POINT ( 'NONE',  ( 20.94999999999999929, 64.32322888843472697, -213.0487915999076449 ) ) ;
#62243=CARTESIAN_POINT ( 'NONE',  ( 23.25000000000000000, 73.42097182497056451, -249.7082903213649558 ) ) ;
#62279=ORIENTED_EDGE ( 'NONE', *, *, #10938, .F. ) ;
#62285=DIRECTION ( 'NONE',  ( 0.000000000000000000, -0.9667078373770112698, -0.2558827019434132821 ) ) ;
#62290=CYLINDRICAL_SURFACE ( 'NONE', #144293, 0.09999999999999939493 ) ;
#62318=EDGE_LOOP ( 'NONE', ( #169794, #219290, #112345, #12538, #67977 ) ) ;
#62347=ORIENTED_EDGE ( 'NONE', *, *, #140288, .T. ) ;
#62354=CYLINDRICAL_SURFACE ( 'NONE', #207885, 0.1000000000000018374 ) ;
#62390=DIRECTION ( 'NONE',  ( 1.000000000000000000, 0.000000000000000000, 0.000000000000000000 ) ) ;
#62395=VERTEX_POINT ( 'NONE', #103314 ) ;
#62402=DIRECTION ( 'NONE',  ( 0.000000000000000000, -0.9651348961777157509, 0.2617529984165031243 ) ) ;
#62444=CARTESIAN_POINT ( 'NONE',  ( -20.94999999999999929, 79.37986612816742138, -196.2658927859692142 ) ) ;
#62447=FACE_OUTER_BOUND ( 'NONE', #192112, .T. ) ;
#62450=EDGE_CURVE ( 'NONE', #148169, #226006, #124198, .T. ) ;
#62493=CARTESIAN_POINT ( 'NONE',  ( -20.64999999999999858, 82.09643798151613225, -215.4278993322501208 ) ) ;
#62498=DIRECTION ( 'NONE',  ( -1.000000000000000000, -0.000000000000000000, -0.000000000000000000 ) ) ;
#62503=DIRECTION ( 'NONE',  ( -0.000000000000000000, 0.9651348961777157509, -0.2617529984165031243 ) ) ;
#62510=AXIS2_PLACEMENT_3D ( 'NONE', #141758, #201741, #28282 ) ;
#62547=DIRECTION ( 'NONE',  ( 1.000000000000000000, 0.000000000000000000, 0.000000000000000000 ) ) ;
#62550=DIRECTION ( 'NONE',  ( -1.000000000000000000, -0.000000000000000000, -0.000000000000000000 ) ) ;
#62562=VECTOR ( 'NONE', #156005, 1000.000000000000000 ) ;
#62567=ORIENTED_EDGE ( 'NONE', *, *, #222631, .T. ) ;
#62602=AXIS2_PLACEMENT_3D ( 'NONE', #113837, #13468, #53875 ) ;
#62610=CIRCLE ( 'NONE', #124970, 0.09999999999999939493 ) ;
#62616=ORIENTED_EDGE ( 'NONE', *, *, #121216, .T. ) ;
#62633=AXIS2_PLACEMENT_3D ( 'NONE', #117462, #237403, #97852 ) ;
#62636=EDGE_CURVE ( 'NONE', #8746, #146536, #72011, .T. ) ;
#62647=CARTESIAN_POINT ( 'NONE',  ( -21.65000000000000213, 62.98412863812492901, -221.9071248009556712 ) ) ;
#62650=AXIS2_PLACEMENT_3D ( 'NONE', #73364, #98002, #95458 ) ;
#62653=EDGE_CURVE ( 'NONE', #38302, #204155, #190595, .T. ) ;
#62656=AXIS2_PLACEMENT_3D ( 'NONE', #29200, #69578, #49996 ) ;
#62695=VERTEX_POINT ( 'NONE', #233567 ) ;
#62699=ORIENTED_EDGE ( 'NONE', *, *, #128120, .F. ) ;
#62718=CARTESIAN_POINT ( 'NONE',  ( -23.15000000000000213, 70.60814576644823148, -215.7631455941064189 ) ) ;
#62720=AXIS2_PLACEMENT_3D ( 'NONE', #111225, #172536, #12151 ) ;
#62724=DIRECTION ( 'NONE',  ( 0.000000000000000000, 0.9651348961777379554, -0.2617529984164210233 ) ) ;
#62730=CARTESIAN_POINT ( 'NONE',  ( 18.49999999999999289, 67.49463558145296815, -195.5618716440587548 ) ) ;
#62742=CARTESIAN_POINT ( 'NONE',  ( -18.50000000000000000, 70.08587962373172786, -198.1273832143211848 ) ) ;
#62761=CARTESIAN_POINT ( 'NONE',  ( 22.39999999999999858, 65.09550114356429162, -243.3481044654562879 ) ) ;
#62794=CARTESIAN_POINT ( 'NONE',  ( -23.25000000000000000, 75.45031870333662027, -205.5498907664980948 ) ) ;
#62808=DIRECTION ( 'NONE',  ( -1.000000000000000000, 0.000000000000000000, 0.000000000000000000 ) ) ;
#62829=ORIENTED_EDGE ( 'NONE', *, *, #210993, .T. ) ;
#62970=ORIENTED_EDGE ( 'NONE', *, *, #102395, .F. ) ;
#62974=EDGE_LOOP ( 'NONE', ( #210789, #30158, #234038, #64578 ) ) ;
#63040=CARTESIAN_POINT ( 'NONE',  ( 22.50000000000000000, 64.08545097430041437, -247.0723585184913986 ) ) ;
#63062=ORIENTED_EDGE ( 'NONE', *, *, #28576, .T. ) ;
#63080=DIRECTION ( 'NONE',  ( 1.000000000000000000, -1.772924042024179204E-16, 4.808324575169891715E-17 ) ) ;
#63082=CARTESIAN_POINT ( 'NONE',  ( -18.59999999999999787, 66.46020053479900014, -223.7494053730254961 ) ) ;
#63119=DIRECTION ( 'NONE',  ( -0.4999999999999799050, 0.2266847461454426782, 0.8358313381687697552 ) ) ;
#63135=DIRECTION ( 'NONE',  ( -1.000000000000000000, 0.000000000000000000, 0.000000000000000000 ) ) ;
#63139=CARTESIAN_POINT ( 'NONE',  ( -18.50000000000000000, 67.23127455305841238, -235.8551265064783991 ) ) ;
#63147=DIRECTION ( 'NONE',  ( 1.000000000000000000, 0.000000000000000000, 0.000000000000000000 ) ) ;
#63162=CARTESIAN_POINT ( 'NONE',  ( 21.05000000000000071, 60.91865828504416669, -234.1430899377568267 ) ) ;
#63188=ORIENTED_EDGE ( 'NONE', *, *, #198687, .T. ) ;
#63236=EDGE_CURVE ( 'NONE', #123166, #255232, #255285, .T. ) ;
#63240=ORIENTED_EDGE ( 'NONE', *, *, #53240, .T. ) ;
#63279=DIRECTION ( 'NONE',  ( 1.000000000000000000, 0.000000000000000000, 0.000000000000000000 ) ) ;
#63285=ORIENTED_EDGE ( 'NONE', *, *, #8141, .T. ) ;
#63305=EDGE_LOOP ( 'NONE', ( #221275, #144874, #176299, #155264 ) ) ;
#63316=FACE_OUTER_BOUND ( 'NONE', #67630, .T. ) ;
#63324=AXIS2_PLACEMENT_3D ( 'NONE', #55587, #133876, #32238 ) ;
#63372=EDGE_CURVE ( 'NONE', #163468, #192701, #188897, .T. ) ;
#63391=DIRECTION ( 'NONE',  ( -1.000000000000000000, -0.000000000000000000, 0.000000000000000000 ) ) ;
#63422=AXIS2_PLACEMENT_3D ( 'NONE', #173424, #170858, #35183 ) ;
#63431=FACE_OUTER_BOUND ( 'NONE', #229371, .T. ) ;
#63445=VECTOR ( 'NONE', #212974, 999.9999999999998863 ) ;
#63498=ORIENTED_EDGE ( 'NONE', *, *, #63548, .T. ) ;
#63503=ORIENTED_EDGE ( 'NONE', *, *, #135606, .T. ) ;
#63516=CARTESIAN_POINT ( 'NONE',  ( 18.40000000000000213, 86.98067499225015808, -199.3289525933215032 ) ) ;
#63526=DIRECTION ( 'NONE',  ( -0.000000000000000000, 0.2617529984165031243, 0.9651348961777157509 ) ) ;
#63531=LINE ( 'NONE', #43980, #224811 ) ;
#63542=DIRECTION ( 'NONE',  ( -1.000000000000000000, 2.849773892568378313E-16, -7.728835255496647986E-17 ) ) ;
#63548=EDGE_CURVE ( 'NONE', #248822, #45881, #176445, .T. ) ;
#63643=VERTEX_POINT ( 'NONE', #111071 ) ;
#63646=CARTESIAN_POINT ( 'NONE',  ( -23.15000000000000213, 61.47936603916258491, -212.1738987416902376 ) ) ;
#63678=FACE_OUTER_BOUND ( 'NONE', #15909, .T. ) ;
#63682=CARTESIAN_POINT ( 'NONE',  ( 20.85000000000000142, 64.65966496992308521, -200.4475097531309586 ) ) ;
#63697=CIRCLE ( 'NONE', #42863, 0.09999999999999395484 ) ;
#63698=EDGE_CURVE ( 'NONE', #219655, #204834, #64182, .T. ) ;
#63700=DIRECTION ( 'NONE',  ( 0.000000000000000000, 0.2534589355813222089, 0.9673461469267261581 ) ) ;
#63703=EDGE_CURVE ( 'NONE', #159037, #178237, #255659, .T. ) ;
#63721=ADVANCED_BREP_SHAPE_REPRESENTATION ( '', ( #18376, #2425 ), #89914 ) ;
#63759=CIRCLE ( 'NONE', #146940, 0.09999999999998657185 ) ;
#63764=EDGE_LOOP ( 'NONE', ( #122974, #13901, #199862 ) ) ;
#63781=ORIENTED_EDGE ( 'NONE', *, *, #149145, .F. ) ;
#63803=AXIS2_PLACEMENT_3D ( 'NONE', #127780, #106912, #185178 ) ;
#63824=EDGE_CURVE ( 'NONE', #44180, #122792, #234883, .T. ) ;
#63847=LINE ( 'NONE', #123828, #16163 ) ;
#63878=DIRECTION ( 'NONE',  ( 0.000000000000000000, 0.2617529984164915779, 0.9651348961777187485 ) ) ;
#63891=CARTESIAN_POINT ( 'NONE',  ( -20.85000000000000142, 79.19526988099229925, -196.1889237952725296 ) ) ;
#63893=ORIENTED_EDGE ( 'NONE', *, *, #128126, .F. ) ;
#63894=ORIENTED_EDGE ( 'NONE', *, *, #14740, .T. ) ;
#63905=CARTESIAN_POINT ( 'NONE',  ( -21.05000000000000071, 62.82351852614503684, -207.2177435922979214 ) ) ;
#63906=ORIENTED_EDGE ( 'NONE', *, *, #216847, .F. ) ;
#63918=CARTESIAN_POINT ( 'NONE',  ( -18.50000000000000000, 76.00000000001126921, -203.5231074845248997 ) ) ;
#63934=ORIENTED_EDGE ( 'NONE', *, *, #196733, .F. ) ;
#63954=DIRECTION ( 'NONE',  ( 1.000000000000000000, 0.000000000000000000, 0.000000000000000000 ) ) ;
#63993=ORIENTED_EDGE ( 'NONE', *, *, #215601, .T. ) ;
#64017=ORIENTED_EDGE ( 'NONE', *, *, #167730, .T. ) ;
#64037=CARTESIAN_POINT ( 'NONE',  ( 18.49999999999999645, 68.68284540823283635, -224.2482512540334767 ) ) ;
#64075=EDGE_LOOP ( 'NONE', ( #88136, #145168, #190413, #209112 ) ) ;
#64099=ORIENTED_EDGE ( 'NONE', *, *, #226155, .T. ) ;
#64126=FACE_OUTER_BOUND ( 'NONE', #103441, .T. ) ;
#64143=CIRCLE ( 'NONE', #176752, 0.1999999999999981515 ) ;
#64145=CARTESIAN_POINT ( 'NONE',  ( -20.85000000106584750, 62.86809779110723184, -207.0533710558943881 ) ) ;
#64152=DIRECTION ( 'NONE',  ( 1.000000000000000000, -1.809991526360996944E-16, 4.908854824437060108E-17 ) ) ;
#64175=CIRCLE ( 'NONE', #22677, 0.1000000000000124678 ) ;
#64182=CIRCLE ( 'NONE', #114239, 0.1000000000000124678 ) ;
#64239=SPHERICAL_SURFACE ( 'NONE', #243065, 0.1000000000000000056 ) ;
#64241=EDGE_CURVE ( 'NONE', #65719, #206526, #85159, .T. ) ;
#64242=EDGE_CURVE ( 'NONE', #193922, #157057, #68789, .T. ) ;
#64266=CARTESIAN_POINT ( 'NONE',  ( 20.85000000000000142, 79.15532900748003442, -196.2806010913881778 ) ) ;
#64272=AXIS2_PLACEMENT_3D ( 'NONE', #41108, #236695, #99742 ) ;
#64288=CARTESIAN_POINT ( 'NONE',  ( 20.94999999999999574, 70.56573376625485139, -228.3808404818380779 ) ) ;
#64327=AXIS2_PLACEMENT_3D ( 'NONE', #39975, #119490, #199019 ) ;
#64341=CARTESIAN_POINT ( 'NONE',  ( -20.88420186297724257, 67.49234744263520724, -195.4268335588911611 ) ) ;
#64351=DIRECTION ( 'NONE',  ( -1.000000000000000000, -0.000000000000000000, 0.000000000000000000 ) ) ;
#64353=AXIS2_PLACEMENT_3D ( 'NONE', #227530, #167591, #28087 ) ;
#64355=DIRECTION ( 'NONE',  ( 0.000000000000000000, -0.2617529984165028467, -0.9651348961777157509 ) ) ;
#64445=DIRECTION ( 'NONE',  ( 1.000000000000000000, 0.000000000000000000, 0.000000000000000000 ) ) ;
#64455=ADVANCED_FACE ( 'NONE', ( #239414 ), #82855, .F. ) ;
#64459=AXIS2_PLACEMENT_3D ( 'NONE', #147587, #73220, #31530 ) ;
#64466=ORIENTED_EDGE ( 'NONE', *, *, #221477, .T. ) ;
#64488=DIRECTION ( 'NONE',  ( -1.836970198721030181E-16, -0.9651348961777157509, 0.2617529984165031243 ) ) ;
#64513=DIRECTION ( 'NONE',  ( 0.000000000000000000, -0.9209589331071360574, 0.3896596508880098009 ) ) ;
#64537=VERTEX_POINT ( 'NONE', #20382 ) ;
#64578=ORIENTED_EDGE ( 'NONE', *, *, #191502, .F. ) ;
#64583=ORIENTED_EDGE ( 'NONE', *, *, #52665, .T. ) ;
#64591=ORIENTED_EDGE ( 'NONE', *, *, #25441, .T. ) ;
#64593=DIRECTION ( 'NONE',  ( 1.000000000000000000, 0.000000000000000000, 0.000000000000000000 ) ) ;
#64720=CARTESIAN_POINT ( 'NONE',  ( -1.739115166359751801E-14, 61.57587952878036930, -212.2000740415318774 ) ) ;
#64748=CARTESIAN_POINT ( 'NONE',  ( -20.94999999999999929, 62.99095723518624368, -207.1734234082435080 ) ) ;
#64788=AXIS2_PLACEMENT_3D ( 'NONE', #15193, #12635, #33505 ) ;
#64799=CIRCLE ( 'NONE', #114893, 0.1999999999999945155 ) ;
#64808=ORIENTED_EDGE ( 'NONE', *, *, #9901, .F. ) ;
#64827=LINE ( 'NONE', #122250, #2217 ) ;
#64872=ORIENTED_EDGE ( 'NONE', *, *, #8795, .T. ) ;
#64884=CARTESIAN_POINT ( 'NONE',  ( -18.50000000000000000, 66.46020053479900014, -223.7494053730254961 ) ) ;
#64902=CYLINDRICAL_SURFACE ( 'NONE', #160782, 0.1000000000000124678 ) ;
#65036=CARTESIAN_POINT ( 'NONE',  ( 21.05000005001233276, 61.85690724456019041, -221.7796802661272295 ) ) ;
#65048=LINE ( 'NONE', #125038, #165426 ) ;
#65055=EDGE_CURVE ( 'NONE', #85165, #9680, #22014, .T. ) ;
#65061=EDGE_CURVE ( 'NONE', #204227, #234655, #20735, .T. ) ;
#65100=ORIENTED_EDGE ( 'NONE', *, *, #142629, .T. ) ;
#65179=DIRECTION ( 'NONE',  ( 0.000000000000000000, 0.9651348961777157509, -0.2617529984165031243 ) ) ;
#65199=CARTESIAN_POINT ( 'NONE',  ( 20.85000000000000142, 87.24382154048164750, -206.5725299160771726 ) ) ;
#65223=EDGE_CURVE ( 'NONE', #180985, #17556, #3710, .T. ) ;
#65224=CARTESIAN_POINT ( 'NONE',  ( -18.52309608778520555, 87.06385610752170123, -199.5665633308501299 ) ) ;
#65233=CIRCLE ( 'NONE', #252668, 0.09999999999999685529 ) ;
#65241=EDGE_LOOP ( 'NONE', ( #93495, #193339, #193947, #224083, #162843 ) ) ;
#65253=CARTESIAN_POINT ( 'NONE',  ( 21.14999999999999858, 67.23127455305841238, -235.8551265064783991 ) ) ;
#65276=EDGE_CURVE ( 'NONE', #191700, #248135, #71418, .T. ) ;
#65280=EDGE_CURVE ( 'NONE', #248032, #68619, #191376, .T. ) ;
#65299=CYLINDRICAL_SURFACE ( 'NONE', #249314, 0.8750000000000007772 ) ;
#65307=CARTESIAN_POINT ( 'NONE',  ( 20.94999999999999574, 59.13236860818124541, -225.8959333647716505 ) ) ;
#65310=AXIS2_PLACEMENT_3D ( 'NONE', #71065, #112741, #154470 ) ;
#65325=ADVANCED_FACE ( 'NONE', ( #110514 ), #92231, .F. ) ;
#65375=FACE_BOUND ( 'NONE', #178636, .T. ) ;
#65394=VERTEX_POINT ( 'NONE', #235591 ) ;
#65421=CARTESIAN_POINT ( 'NONE',  ( -21.04999999999999716, 65.56240296622316066, -242.0762802233569744 ) ) ;
#65429=ORIENTED_EDGE ( 'NONE', *, *, #99608, .T. ) ;
#65439=FACE_OUTER_BOUND ( 'NONE', #252595, .T. ) ;
#65468=FACE_OUTER_BOUND ( 'NONE', #19907, .T. ) ;
#65482=FACE_OUTER_BOUND ( 'NONE', #199288, .T. ) ;
#65488=DIRECTION ( 'NONE',  ( 0.000000000000000000, 0.2617529984164955192, 0.9651348961777178603 ) ) ;
#65520=LINE ( 'NONE', #218158, #23919 ) ;
#65558=EDGE_LOOP ( 'NONE', ( #198056, #90754, #196003, #138392 ) ) ;
#65574=DIRECTION ( 'NONE',  ( -3.265361837132813093E-16, -0.9651348961777155289, 0.2617529984165037904 ) ) ;
#65590=DIRECTION ( 'NONE',  ( 2.915501640297154283E-16, 0.9651348961777159730, -0.2617529984165023471 ) ) ;
#65603=PRESENTATION_STYLE_ASSIGNMENT (( #225930 ) ) ;
#65608=DIRECTION ( 'NONE',  ( 0.000000000000000000, 0.2617529984165152257, 0.9651348961777124202 ) ) ;
#65622=CARTESIAN_POINT ( 'NONE',  ( -20.94999999999999929, 68.48451787451661232, -224.2224406095231757 ) ) ;
#65626=DIRECTION ( 'NONE',  ( 1.000000000000000000, 0.000000000000000000, 0.000000000000000000 ) ) ;
#65629=DIRECTION ( 'NONE',  ( 0.000000000000000000, 0.2617529984165031243, 0.9651348961777157509 ) ) ;
#65646=ORIENTED_EDGE ( 'NONE', *, *, #241465, .T. ) ;
#65687=DIRECTION ( 'NONE',  ( 1.000000000000000000, 0.000000000000000000, 0.000000000000000000 ) ) ;
#65694=EDGE_CURVE ( 'NONE', #143687, #51386, #90187, .T. ) ;
#65711=DIRECTION ( 'NONE',  ( 0.000000000000000000, 0.2617529984165152257, 0.9651348961777124202 ) ) ;
#65715=CARTESIAN_POINT ( 'NONE',  ( -18.60000000000000497, 86.99328926435038056, -199.3739562671294721 ) ) ;
#65719=VERTEX_POINT ( 'NONE', #69825 ) ;
#65724=CARTESIAN_POINT ( 'NONE',  ( 22.42357213249528769, 59.79992344103889934, -233.9423457344157953 ) ) ;
#65744=CARTESIAN_POINT ( 'NONE',  ( -20.54999999999999716, 66.33592547490526670, -222.9197737850312251 ) ) ;
#65746=CARTESIAN_POINT ( 'NONE',  ( 21.07954763557365396, 61.10541173128874703, -234.2619947598618069 ) ) ;
#65769=LINE ( 'NONE', #224832, #47287 ) ;
#65776=AXIS2_PLACEMENT_3D ( 'NONE', #31949, #168910, #29392 ) ;
#65802=ADVANCED_FACE ( 'NONE', ( #116630 ), #175349, .T. ) ;
#65811=AXIS2_PLACEMENT_3D ( 'NONE', #231498, #11155, #151977 ) ;
#65866=EDGE_CURVE ( 'NONE', #110678, #242581, #110886, .T. ) ;
#65888=CARTESIAN_POINT ( 'NONE',  ( 23.15000000000000213, 86.43238724539048690, -209.5644480942280836 ) ) ;
#65920=VERTEX_POINT ( 'NONE', #125613 ) ;
#65922=DIRECTION ( 'NONE',  ( 0.000000000000000000, 0.2617529984164915779, 0.9651348961777187485 ) ) ;
#65935=DIRECTION ( 'NONE',  ( 0.000000000000000000, 0.2617529984165035128, 0.9651348961777155289 ) ) ;
#65965=SURFACE_SIDE_STYLE ('',( #247154 ) ) ;
#65978=ORIENTED_EDGE ( 'NONE', *, *, #101668, .F. ) ;
#65988=CARTESIAN_POINT ( 'NONE',  ( -20.94999999999999929, 68.13014604066189861, -227.7202878558733516 ) ) ;
#66002=CIRCLE ( 'NONE', #178460, 0.1000000000000124678 ) ;
#66020=DIRECTION ( 'NONE',  ( 2.465190328815662439E-32, -0.2617529984165030132, -0.9651348961777158619 ) ) ;
#66036=VECTOR ( 'NONE', #49048, 1000.000000000000000 ) ;
#66050=CARTESIAN_POINT ( 'NONE',  ( -20.85000000000000142, 70.17424292862648372, -198.1782849070719124 ) ) ;
#66051=CARTESIAN_POINT ( 'NONE',  ( 20.94999999999999929, 86.19075908668452257, -209.4719249499869136 ) ) ;
#66073=CIRCLE ( 'NONE', #45229, 0.09999999999999939493 ) ;
#66112=CARTESIAN_POINT ( 'NONE',  ( -18.54148534481894472, 67.49261718274587452, -195.4446851895584416 ) ) ;
#66196=VERTEX_POINT ( 'NONE', #18517 ) ;
#66198=FACE_OUTER_BOUND ( 'NONE', #180819, .T. ) ;
#66209=EDGE_CURVE ( 'NONE', #101793, #252329, #177622, .T. ) ;
#66226=DIRECTION ( 'NONE',  ( 0.000000000000000000, 0.2617529984164506107, 0.9651348961777299618 ) ) ;
#66282=CIRCLE ( 'NONE', #91226, 0.1000000000000033779 ) ;
#66285=LINE ( 'NONE', #106660, #21751 ) ;
#66286=DIRECTION ( 'NONE',  ( 0.000000000000000000, 0.2617529984165152257, 0.9651348961777124202 ) ) ;
#66288=CARTESIAN_POINT ( 'NONE',  ( 18.59999999999999076, 63.53162788017662166, -224.4728618886983043 ) ) ;
#66289=CARTESIAN_POINT ( 'NONE',  ( 21.05000000000000071, 58.88961935843800433, -225.7942249309140834 ) ) ;
#66294=LINE ( 'NONE', #226628, #113364 ) ;
#66296=EDGE_LOOP ( 'NONE', ( #192303, #5912 ) ) ;
#66315=AXIS2_PLACEMENT_3D ( 'NONE', #214805, #193987, #253924 ) ;
#66323=ADVANCED_FACE ( 'NONE', ( #7617 ), #87134, .F. ) ;
#66331=CARTESIAN_POINT ( 'NONE',  ( -21.05000000000000071, 79.03126467873600802, -235.8703919547671717 ) ) ;
#66369=CARTESIAN_POINT ( 'NONE',  ( -21.14999999999999858, 65.51923798433686841, -242.1677427744926092 ) ) ;
#66376=AXIS2_PLACEMENT_3D ( 'NONE', #240101, #154488, #100545 ) ;
#66401=CARTESIAN_POINT ( 'NONE',  ( -23.15000000000000213, 76.00000000001126921, -203.5231074845248997 ) ) ;
#66422=DIRECTION ( 'NONE',  ( 6.484947573744954877E-15, -0.7973076739542579450, 0.6035730884107166627 ) ) ;
#66426=DIRECTION ( 'NONE',  ( -1.000000000000000000, -0.000000000000000000, -0.000000000000000000 ) ) ;
#66434=ORIENTED_EDGE ( 'NONE', *, *, #176685, .F. ) ;
#66450=DIRECTION ( 'NONE',  ( 2.557131231893036985E-16, 0.7049548389605067023, -0.7092521942342977503 ) ) ;
#66454=CARTESIAN_POINT ( 'NONE',  ( 21.12757541349815682, 60.98223810379111853, -234.1656810015468579 ) ) ;
#66472=LINE ( 'NONE', #185134, #221602 ) ;
#66473=DIRECTION ( 'NONE',  ( 0.000000000000000000, -0.2617529984164856383, -0.9651348961777204138 ) ) ;
#66479=VECTOR ( 'NONE', #38459, 1000.000000000000000 ) ;
#66487=DIRECTION ( 'NONE',  ( 1.000000000000000000, 0.000000000000000000, -0.000000000000000000 ) ) ;
#66494=CIRCLE ( 'NONE', #249662, 0.5000000000000051070 ) ;
#66510=TOROIDAL_SURFACE ( 'NONE', #8257, 12.97499999999999609, 0.1000000000000000056 ) ;
#66528=CARTESIAN_POINT ( 'NONE',  ( 18.49999999999999289, 63.84457430183214655, -209.3417490372068528 ) ) ;
#66545=CARTESIAN_POINT ( 'NONE',  ( -22.50000000000088463, 64.13793881490383342, -247.0875655909796649 ) ) ;
#66546=ORIENTED_EDGE ( 'NONE', *, *, #112336, .F. ) ;
#66549=DIRECTION ( 'NONE',  ( -1.000000000000000000, 0.000000000000000000, 0.000000000000000000 ) ) ;
#66571=DIRECTION ( 'NONE',  ( 0.000000000000000000, -0.2617529984165026247, -0.9651348961777158619 ) ) ;
#66573=LINE ( 'NONE', #31329, #207090 ) ;
#66604=CARTESIAN_POINT ( 'NONE',  ( -18.39999999999999858, 78.23214007969471595, -231.5865251354359771 ) ) ;
#66608=CARTESIAN_POINT ( 'NONE',  ( 23.24999999999999645, 67.23127455305841238, -235.8551265064783991 ) ) ;
#66717=CARTESIAN_POINT ( 'NONE',  ( -21.05000000000000071, 65.49889199258218753, -241.8691648588935266 ) ) ;
#66723=DIRECTION ( 'NONE',  ( 0.000000000000000000, -0.2617529984164856383, -0.9651348961777204138 ) ) ;
#66729=SPHERICAL_SURFACE ( 'NONE', #194971, 0.1000000000000000056 ) ;
#66738=ADVANCED_FACE ( 'NONE', ( #223766 ), #103810, .T. ) ;
#66747=AXIS2_PLACEMENT_3D ( 'NONE', #62761, #143579, #4063 ) ;
#66770=PLANE ( 'NONE',  #4452 ) ;
#66781=ORIENTED_EDGE ( 'NONE', *, *, #129287, .T. ) ;
#66786=VERTEX_POINT ( 'NONE', #122125 ) ;
#66790=DIRECTION ( 'NONE',  ( 1.000000000000000000, -0.000000000000000000, -0.000000000000000000 ) ) ;
#66796=EDGE_CURVE ( 'NONE', #134353, #60484, #11672, .T. ) ;
#66808=EDGE_LOOP ( 'NONE', ( #233323, #174179, #91849, #178028 ) ) ;
#66842=ORIENTED_EDGE ( 'NONE', *, *, #225224, .T. ) ;
#66847=VERTEX_POINT ( 'NONE', #210636 ) ;
#66884=VERTEX_POINT ( 'NONE', #253596 ) ;
#66924=EDGE_LOOP ( 'NONE', ( #192941, #131822, #28050, #90085 ) ) ;
#66996=AXIS2_PLACEMENT_3D ( 'NONE', #8688, #186042, #227721 ) ;
#67003=CYLINDRICAL_SURFACE ( 'NONE', #180224, 0.09999999999999939493 ) ;
#67010=CARTESIAN_POINT ( 'NONE',  ( 22.37643362114956247, 59.84542367231799176, -233.9546800015663166 ) ) ;
#67011=CARTESIAN_POINT ( 'NONE',  ( -18.59999999999999787, 80.80934863333322937, -192.8037999715871535 ) ) ;
#67016=ADVANCED_FACE ( 'NONE', ( #143927 ), #145206, .T. ) ;
#67032=DIRECTION ( 'NONE',  ( 0.000000000000000000, -0.2617529984165031243, -0.9651348961777157509 ) ) ;
#67047=ORIENTED_EDGE ( 'NONE', *, *, #247502, .F. ) ;
#67062=CARTESIAN_POINT ( 'NONE',  ( 20.94999999999999929, 78.04167338765999773, -195.9950552943387265 ) ) ;
#67067=AXIS2_PLACEMENT_3D ( 'NONE', #247631, #148540, #199267 ) ;
#67070=VERTEX_POINT ( 'NONE', #8293 ) ;
#67083=FACE_OUTER_BOUND ( 'NONE', #153121, .T. ) ;
#67095=EDGE_CURVE ( 'NONE', #171580, #66786, #253251, .T. ) ;
#67153=CARTESIAN_POINT ( 'NONE',  ( 23.14999999999999503, 61.45319073932094511, -212.2704122313080006 ) ) ;
#67164=EDGE_CURVE ( 'NONE', #161458, #193922, #124277, .T. ) ;
#67176=DIRECTION ( 'NONE',  ( 0.000000000000000000, 0.2617529984165024026, 0.9651348961777158619 ) ) ;
#67177=LINE ( 'NONE', #108867, #98518 ) ;
#67182=DIRECTION ( 'NONE',  ( -1.000000000000000000, 3.151514657663852580E-16, -8.547182517843351137E-17 ) ) ;
#67216=CARTESIAN_POINT ( 'NONE',  ( -20.94999999999999929, 66.97496366775517629, -235.8217698210967512 ) ) ;
#67254=EDGE_LOOP ( 'NONE', ( #58065, #210217, #30303, #139190 ) ) ;
#67273=ADVANCED_FACE ( 'NONE', ( #134619 ), #82532, .T. ) ;
#67283=AXIS2_PLACEMENT_3D ( 'NONE', #146816, #71170, #192383 ) ;
#67295=LINE ( 'NONE', #226346, #21761 ) ;
#67296=DIRECTION ( 'NONE',  ( 1.000000000000000000, 0.000000000000000000, 0.000000000000000000 ) ) ;
#67316=DIRECTION ( 'NONE',  ( 0.000000000000000000, -0.2617529984165031243, -0.9651348961777157509 ) ) ;
#67354=ADVANCED_FACE ( 'NONE', ( #100613 ), #219309, .T. ) ;
#67365=EDGE_CURVE ( 'NONE', #22691, #11008, #244874, .T. ) ;
#67379=CARTESIAN_POINT ( 'NONE',  ( 21.14999999999999503, 64.27847795353595473, -247.1247091181747066 ) ) ;
#67412=ORIENTED_EDGE ( 'NONE', *, *, #90569, .F. ) ;
#67453=AXIS2_PLACEMENT_3D ( 'NONE', #583, #59249, #219642 ) ;
#67454=LINE ( 'NONE', #64884, #152089 ) ;
#67473=DIRECTION ( 'NONE',  ( 0.000000000000000000, 0.2617529984165035684, 0.9651348961777156399 ) ) ;
#67495=ORIENTED_EDGE ( 'NONE', *, *, #96991, .T. ) ;
#67540=AXIS2_PLACEMENT_3D ( 'NONE', #246066, #205628, #86949 ) ;
#67541=ADVANCED_FACE ( 'NONE', ( #82700 ), #41071, .F. ) ;
#67563=CARTESIAN_POINT ( 'NONE',  ( -21.05000000000000071, 60.94483358488582070, -234.0465764481390636 ) ) ;
#67580=DIRECTION ( 'NONE',  ( 2.952720810173289112E-16, 0.9651348961777157509, -0.2617529984165031243 ) ) ;
#67585=ORIENTED_EDGE ( 'NONE', *, *, #130920, .F. ) ;
#67596=EDGE_CURVE ( 'NONE', #251815, #56792, #207856, .T. ) ;
#67611=PLANE ( 'NONE',  #114226 ) ;
#67613=DIRECTION ( 'NONE',  ( -1.000000000000000000, -0.000000000000000000, 0.000000000000000000 ) ) ;
#67628=CARTESIAN_POINT ( 'NONE',  ( 20.94999999999999929, 79.37986612816742138, -196.2658927859692142 ) ) ;
#67630=EDGE_LOOP ( 'NONE', ( #232992, #250640, #34590, #252001 ) ) ;
#67635=ORIENTED_EDGE ( 'NONE', *, *, #41883, .T. ) ;
#67642=FACE_OUTER_BOUND ( 'NONE', #115415, .T. ) ;
#67658=CARTESIAN_POINT ( 'NONE',  ( 21.05000000000000071, 67.23127455305841238, -235.8551265064783991 ) ) ;
#67667=ADVANCED_FACE ( 'NONE', ( #48740 ), #128300, .T. ) ;
#67669=EDGE_LOOP ( 'NONE', ( #135664, #223532, #14321 ) ) ;
#67696=CARTESIAN_POINT ( 'NONE',  ( -18.50000000000000000, 59.16775194334852728, -221.0793150863668473 ) ) ;
#67710=DIRECTION ( 'NONE',  ( 0.000000000000000000, 0.2617529984165185009, 0.9651348961777115321 ) ) ;
#67731=DIRECTION ( 'NONE',  ( 1.000000000000000000, 0.000000000000000000, 0.000000000000000000 ) ) ;
#67738=CARTESIAN_POINT ( 'NONE',  ( 21.13498764882293557, 60.96169324425918035, -234.1564776252124886 ) ) ;
#67763=ORIENTED_EDGE ( 'NONE', *, *, #156696, .T. ) ;
#67790=EDGE_CURVE ( 'NONE', #162955, #248032, #140431, .T. ) ;
#67792=CARTESIAN_POINT ( 'NONE',  ( -20.54999999999999716, 70.80971041069356886, -215.3055740759912453 ) ) ;
#67842=DIRECTION ( 'NONE',  ( 1.000000000000000000, 0.000000000000000000, 0.000000000000000000 ) ) ;
#67854=CARTESIAN_POINT ( 'NONE',  ( -20.54999999999999716, 82.09643798151613225, -215.4278993322501208 ) ) ;
#67884=DIRECTION ( 'NONE',  ( 1.000000000000000000, -2.849773892568378313E-16, 7.728835255496647986E-17 ) ) ;
#67893=ADVANCED_FACE ( 'NONE', ( #177720 ), #182336, .T. ) ;
#67905=CARTESIAN_POINT ( 'NONE',  ( 18.59999999999999076, 68.48451787451661232, -224.2224406095231757 ) ) ;
#67929=CARTESIAN_POINT ( 'NONE',  ( -23.15000000000000213, 67.23127455305841238, -235.8551265064783991 ) ) ;
#67953=CARTESIAN_POINT ( 'NONE',  ( 23.24999999999999289, 61.57587952878035509, -212.2000740415318774 ) ) ;
#67955=DIRECTION ( 'NONE',  ( 0.000000000000000000, -0.2617529984165152257, -0.9651348961777124202 ) ) ;
#67967=CARTESIAN_POINT ( 'NONE',  ( -18.59999999999999787, 78.06784868750165174, -195.8985418047209350 ) ) ;
#67977=ORIENTED_EDGE ( 'NONE', *, *, #252174, .T. ) ;
#67989=ORIENTED_EDGE ( 'NONE', *, *, #62636, .F. ) ;
#68005=FACE_OUTER_BOUND ( 'NONE', #247383, .T. ) ;
#68015=CARTESIAN_POINT ( 'NONE',  ( 23.14999999999999858, 67.23127455305841238, -235.8551265064783991 ) ) ;
#68074=ORIENTED_EDGE ( 'NONE', *, *, #18641, .F. ) ;
#68077=CARTESIAN_POINT ( 'NONE',  ( -18.59999999999999787, 59.19392724319018129, -220.9828015967491126 ) ) ;
#68100=ORIENTED_EDGE ( 'NONE', *, *, #135245, .F. ) ;
#68107=AXIS2_PLACEMENT_3D ( 'NONE', #181934, #78947, #80219 ) ;
#68121=VERTEX_POINT ( 'NONE', #8050 ) ;
#68144=VECTOR ( 'NONE', #62547, 1000.000000000000000 ) ;
#68161=DIRECTION ( 'NONE',  ( 0.000000000000000000, 0.2617529984164915779, 0.9651348961777187485 ) ) ;
#68168=ORIENTED_EDGE ( 'NONE', *, *, #87150, .F. ) ;
#68180=CIRCLE ( 'NONE', #134790, 0.5000000000000087708 ) ;
#68210=DIRECTION ( 'NONE',  ( 0.000000000000000000, 0.2617529984165152257, 0.9651348961777124202 ) ) ;
#68268=EDGE_CURVE ( 'NONE', #173665, #19956, #150137, .T. ) ;
#68270=LINE ( 'NONE', #202960, #27395 ) ;
#68283=LINE ( 'NONE', #162256, #136464 ) ;
#68285=DIRECTION ( 'NONE',  ( 0.000000000000000000, 0.2617529984165152257, 0.9651348961777124202 ) ) ;
#68306=DIRECTION ( 'NONE',  ( 0.000000000000000000, -0.2617529984162567103, -0.9651348961777825863 ) ) ;
#68332=ORIENTED_EDGE ( 'NONE', *, *, #94314, .F. ) ;
#68349=DIRECTION ( 'NONE',  ( 1.000000000000000000, 0.000000000000000000, 0.000000000000000000 ) ) ;
#68409=CARTESIAN_POINT ( 'NONE',  ( -18.39999999999999858, 86.99291436658650412, -199.6658631664729739 ) ) ;
#68434=ORIENTED_EDGE ( 'NONE', *, *, #257363, .F. ) ;
#68458=VECTOR ( 'NONE', #134464, 1000.000000000000000 ) ;
#68486=EDGE_CURVE ( 'NONE', #40333, #65719, #199080, .T. ) ;
#68489=EDGE_CURVE ( 'NONE', #255081, #9432, #7740, .T. ) ;
#68531=VECTOR ( 'NONE', #151125, 1000.000000000000000 ) ;
#68532=FACE_BOUND ( 'NONE', #169258, .T. ) ;
#68619=VERTEX_POINT ( 'NONE', #71578 ) ;
#68622=DIRECTION ( 'NONE',  ( 1.000000000000000000, 0.000000000000000000, 0.000000000000000000 ) ) ;
#68643=ORIENTED_EDGE ( 'NONE', *, *, #54381, .F. ) ;
#68673=CARTESIAN_POINT ( 'NONE',  ( 18.60000000000000142, 86.96699927712943179, -199.3055931863049466 ) ) ;
#68682=CARTESIAN_POINT ( 'NONE',  ( -20.85000000000000142, 86.58125133469155799, -209.3975964148341973 ) ) ;
#68687=PLANE ( 'NONE',  #231778 ) ;
#68693=CARTESIAN_POINT ( 'NONE',  ( -21.05000000000000071, 64.27836561112391678, -247.1251233467904171 ) ) ;
#68696=ORIENTED_EDGE ( 'NONE', *, *, #3754, .F. ) ;
#68720=ORIENTED_EDGE ( 'NONE', *, *, #26137, .F. ) ;
#68751=CIRCLE ( 'NONE', #156080, 0.09999999999999868716 ) ;
#68764=LINE ( 'NONE', #53041, #251246 ) ;
#68771=DIRECTION ( 'NONE',  ( 1.000000000000000000, 0.000000000000000000, 0.000000000000000000 ) ) ;
#68789=LINE ( 'NONE', #148321, #122641 ) ;
#68794=AXIS2_PLACEMENT_3D ( 'NONE', #115681, #152265, #133945 ) ;
#68803=EDGE_LOOP ( 'NONE', ( #71682, #160437, #227868, #103393, #23047 ) ) ;
#68822=ORIENTED_EDGE ( 'NONE', *, *, #201783, .F. ) ;
#68829=CARTESIAN_POINT ( 'NONE',  ( -21.05000000000000071, 60.94483358488582070, -234.0465764481390636 ) ) ;
#68830=SPHERICAL_SURFACE ( 'NONE', #191582, 0.1000000000000000056 ) ;
#68837=DIRECTION ( 'NONE',  ( -1.000000000000000000, -0.000000000000000000, 0.000000000000000000 ) ) ;
#68845=ORIENTED_EDGE ( 'NONE', *, *, #156886, .F. ) ;
#68865=CARTESIAN_POINT ( 'NONE',  ( -20.64999999999999858, 68.66552716081216090, -214.3300732090495444 ) ) ;
#68885=ORIENTED_EDGE ( 'NONE', *, *, #172828, .F. ) ;
#68886=LINE ( 'NONE', #32340, #103168 ) ;
#68896=DIRECTION ( 'NONE',  ( -1.000000000000000000, 0.000000000000000000, 0.000000000000000000 ) ) ;
#68905=AXIS2_PLACEMENT_3D ( 'NONE', #243466, #201768, #199224 ) ;
#68913=ORIENTED_EDGE ( 'NONE', *, *, #252911, .T. ) ;
#68920=CARTESIAN_POINT ( 'NONE',  ( -22.50000000000000000, 64.08545097430041437, -247.0723585184913986 ) ) ;
#68937=DIRECTION ( 'NONE',  ( -5.603264701231745086E-32, 0.2617529984165030132, 0.9651348961777158619 ) ) ;
#68989=DIRECTION ( 'NONE',  ( -1.000000000000000000, -0.000000000000000000, -0.000000000000000000 ) ) ;
#69014=FACE_OUTER_BOUND ( 'NONE', #7290, .T. ) ;
#69018=DIRECTION ( 'NONE',  ( 0.000000000000000000, 0.2617529984165024026, 0.9651348961777159730 ) ) ;
#69025=CARTESIAN_POINT ( 'NONE',  ( 20.94999999999999929, 79.19526988099229925, -196.1889237952725296 ) ) ;
#69031=DIRECTION ( 'NONE',  ( -1.000000000000000000, 2.849773892568378313E-16, -7.728835255496647986E-17 ) ) ;
#69053=CYLINDRICAL_SURFACE ( 'NONE', #179169, 11.75000000000000178 ) ;
#69075=DIRECTION ( 'NONE',  ( 0.000000000000000000, 0.9942466578594195692, -0.1071148137998398919 ) ) ;
#69084=ORIENTED_EDGE ( 'NONE', *, *, #143173, .T. ) ;
#69100=CIRCLE ( 'NONE', #56415, 12.97499999999998366 ) ;
#69108=DIRECTION ( 'NONE',  ( 0.000000000000000000, -0.2558827019434435912, 0.9667078373770033872 ) ) ;
#69137=CARTESIAN_POINT ( 'NONE',  ( 23.24999999999999645, 72.23597390491818260, -202.5022707907005497 ) ) ;
#69156=ORIENTED_EDGE ( 'NONE', *, *, #96598, .F. ) ;
#69182=CYLINDRICAL_SURFACE ( 'NONE', #99310, 0.1000000000000124678 ) ;
#69185=CYLINDRICAL_SURFACE ( 'NONE', #41168, 0.1000000000000124678 ) ;
#69187=ADVANCED_FACE ( 'NONE', ( #169758 ), #151641, .F. ) ;
#69194=FACE_OUTER_BOUND ( 'NONE', #89985, .T. ) ;
#69235=DIRECTION ( 'NONE',  ( 0.000000000000000000, -0.2617529984165031243, -0.9651348961777157509 ) ) ;
#69294=VECTOR ( 'NONE', #79233, 999.9999999999998863 ) ;
#69306=DIRECTION ( 'NONE',  ( 1.000000000000000000, 0.000000000000000000, 0.000000000000000000 ) ) ;
#69316=ORIENTED_EDGE ( 'NONE', *, *, #221565, .F. ) ;
#69328=DIRECTION ( 'NONE',  ( 0.000000000000000000, 0.9651348961777189706, -0.2617529984164915779 ) ) ;
#69335=AXIS2_PLACEMENT_3D ( 'NONE', #43704, #61989, #224886 ) ;
#69358=CARTESIAN_POINT ( 'NONE',  ( 23.15000000000000213, 78.00142589229885459, -228.9845759368473637 ) ) ;
#69388=CARTESIAN_POINT ( 'NONE',  ( -21.05000000000000071, 60.94483358488582070, -234.0465764481390636 ) ) ;
#69420=ORIENTED_EDGE ( 'NONE', *, *, #85633, .T. ) ;
#69518=ORIENTED_EDGE ( 'NONE', *, *, #60861, .F. ) ;
#69578=DIRECTION ( 'NONE',  ( -1.000000000000000000, -0.000000000000000000, -0.000000000000000000 ) ) ;
#69581=FACE_OUTER_BOUND ( 'NONE', #127524, .T. ) ;
#69610=ORIENTED_EDGE ( 'NONE', *, *, #131174, .F. ) ;
#69621=CARTESIAN_POINT ( 'NONE',  ( 22.47071067811865319, 67.23127455305841238, -235.8551265064783991 ) ) ;
#69638=CARTESIAN_POINT ( 'NONE',  ( -23.15000000000000213, 86.43238724539048690, -209.5644480942280836 ) ) ;
#69663=CARTESIAN_POINT ( 'NONE',  ( -20.94999999999999929, 79.11538813396778380, -196.3722783875038544 ) ) ;
#69666=DIRECTION ( 'NONE',  ( 1.000000000000000000, 0.000000000000000000, 0.000000000000000000 ) ) ;
#69688=CARTESIAN_POINT ( 'NONE',  ( -21.05000000000000071, 62.82351852614503684, -207.2177435922979214 ) ) ;
#69722=CARTESIAN_POINT ( 'NONE',  ( -21.14999999999999858, 60.91865828504416669, -234.1430899377568551 ) ) ;
#69748=AXIS2_PLACEMENT_3D ( 'NONE', #196845, #23391, #58613 ) ;
#69755=EDGE_CURVE ( 'NONE', #141218, #5530, #172876, .T. ) ;
#69767=DIRECTION ( 'NONE',  ( 0.000000000000000000, 0.2617529984164955192, 0.9651348961777178603 ) ) ;
#69786=CIRCLE ( 'NONE', #40771, 7.800000000000005151 ) ;
#69793=ADVANCED_FACE ( 'NONE', ( #15495 ), #27104, .T. ) ;
#69797=CARTESIAN_POINT ( 'NONE',  ( 21.05000000000000071, 74.95298800634525094, -207.3836470692357636 ) ) ;
#69819=TOROIDAL_SURFACE ( 'NONE', #190623, 11.65000000000000036, 0.1000000000000000056 ) ;
#69825=CARTESIAN_POINT ( 'NONE',  ( 23.24999999999999645, 68.28935379556426710, -213.7087130192904567 ) ) ;
#69857=LINE ( 'NONE', #249758, #53776 ) ;
#69927=LINE ( 'NONE', #211996, #66036 ) ;
#69934=CARTESIAN_POINT ( 'NONE',  ( 21.05000000000000071, 67.23127455305841238, -235.8551265064783991 ) ) ;
#69945=VERTEX_POINT ( 'NONE', #76713 ) ;
#69959=DIRECTION ( 'NONE',  ( 1.000000000000000000, 0.000000000000000000, 0.000000000000000000 ) ) ;
#69965=DIRECTION ( 'NONE',  ( 0.000000000000000000, -0.6035730884107395333, -0.7973076739542406255 ) ) ;
#69969=EDGE_CURVE ( 'NONE', #126077, #153125, #47904, .T. ) ;
#69972=EDGE_CURVE ( 'NONE', #139316, #28102, #118680, .T. ) ;
#69973=CARTESIAN_POINT ( 'NONE',  ( 18.49362639424904131, 86.88399968321819244, -199.4661394926152411 ) ) ;
#69974=VERTEX_POINT ( 'NONE', #136687 ) ;
#69978=CARTESIAN_POINT ( 'NONE',  ( -23.25000000000000000, 76.00000000001126921, -203.5231074845248997 ) ) ;
#69988=TOROIDAL_SURFACE ( 'NONE', #215685, 12.77499999999999858, 0.1000000000000000056 ) ;
#69989=CARTESIAN_POINT ( 'NONE',  ( -21.05000000000000071, 68.59681812508419796, -224.1344059333694361 ) ) ;
#69990=FACE_OUTER_BOUND ( 'NONE', #246121, .T. ) ;
#69992=ORIENTED_EDGE ( 'NONE', *, *, #225709, .F. ) ;
#70076=DIRECTION ( 'NONE',  ( 0.000000000000000000, -0.2617529984165152257, -0.9651348961777124202 ) ) ;
#70094=ORIENTED_EDGE ( 'NONE', *, *, #205337, .F. ) ;
#70149=AXIS2_PLACEMENT_3D ( 'NONE', #9, #83375, #102950 ) ;
#70163=VERTEX_POINT ( 'NONE', #149561 ) ;
#70166=CARTESIAN_POINT ( 'NONE',  ( -20.64999999999999858, 63.46669608621377279, -222.0380013001639270 ) ) ;
#70195=CIRCLE ( 'NONE', #136786, 0.09999999999999949207 ) ;
#70196=CARTESIAN_POINT ( 'NONE',  ( -21.05439746398122836, 57.72057112225034814, -226.0333164516449074 ) ) ;
#70215=AXIS2_PLACEMENT_3D ( 'NONE', #112276, #250473, #251764 ) ;
#70229=CIRCLE ( 'NONE', #207586, 0.09999999999999939493 ) ;
#70230=ORIENTED_EDGE ( 'NONE', *, *, #81122, .T. ) ;
#70239=EDGE_CURVE ( 'NONE', #211510, #160294, #2290, .T. ) ;
#70249=DIRECTION ( 'NONE',  ( 0.000000000000000000, 0.2534589355813222089, 0.9673461469267261581 ) ) ;
#70261=ORIENTED_EDGE ( 'NONE', *, *, #31082, .F. ) ;
#70267=CYLINDRICAL_SURFACE ( 'NONE', #133252, 0.1000000000000018374 ) ;
#70272=TOROIDAL_SURFACE ( 'NONE', #41042, 0.2000000000000000111, 0.1000000000000000056 ) ;
#70279=EDGE_CURVE ( 'NONE', #156295, #104826, #202053, .T. ) ;
#70280=EDGE_LOOP ( 'NONE', ( #199623, #238604, #130410 ) ) ;
#70293=CARTESIAN_POINT ( 'NONE',  ( -22.39999999999999858, 64.18196446391819165, -247.0985338183330668 ) ) ;
#70306=CARTESIAN_POINT ( 'NONE',  ( 21.05000000000000071, 62.99095723518624368, -207.1734234082435080 ) ) ;
#70342=CARTESIAN_POINT ( 'NONE',  ( 21.08198257630413508, 61.09658931423916073, -234.2666139183525615 ) ) ;
#70371=CARTESIAN_POINT ( 'NONE',  ( 20.97107704358301916, 60.90557777443898146, -225.2713797486721887 ) ) ;
#70381=VERTEX_POINT ( 'NONE', #16465 ) ;
#70398=CARTESIAN_POINT ( 'NONE',  ( 23.14999999999999858, 67.44464249442897597, -214.0562211244547655 ) ) ;
#70415=CARTESIAN_POINT ( 'NONE',  ( 18.50000000000000000, 78.21920797885123022, -231.3255576768048911 ) ) ;
#70417=AXIS2_PLACEMENT_3D ( 'NONE', #124292, #79984, #142543 ) ;
#70419=CARTESIAN_POINT ( 'NONE',  ( -18.50000000000000000, 80.78317333349157536, -192.9003134612048882 ) ) ;
#70430=VERTEX_POINT ( 'NONE', #121962 ) ;
#70434=ORIENTED_EDGE ( 'NONE', *, *, #36684, .F. ) ;
#70442=CIRCLE ( 'NONE', #249475, 12.97499999999999076 ) ;
#70457=DIRECTION ( 'NONE',  ( 0.000000000000000000, 0.9673461469267252699, -0.2534589355813257061 ) ) ;
#70469=DIRECTION ( 'NONE',  ( 0.000000000000000000, 0.2617529984162567103, 0.9651348961777825863 ) ) ;
#70491=ORIENTED_EDGE ( 'NONE', *, *, #230696, .T. ) ;
#70495=EDGE_LOOP ( 'NONE', ( #124187, #163688, #178657, #68074, #225567 ) ) ;
#70522=LINE ( 'NONE', #110895, #229743 ) ;
#70553=FACE_OUTER_BOUND ( 'NONE', #138825, .T. ) ;
#70577=DIRECTION ( 'NONE',  ( 1.000000000000000000, 0.000000000000000000, 0.000000000000000000 ) ) ;
#70581=EDGE_CURVE ( 'NONE', #89267, #7014, #123132, .T. ) ;
#70583=EDGE_LOOP ( 'NONE', ( #256837, #22973, #144649, #219792, #84746 ) ) ;
#70606=ORIENTED_EDGE ( 'NONE', *, *, #190639, .F. ) ;
#70607=CARTESIAN_POINT ( 'NONE',  ( 20.94999999999999929, 64.75617845954087670, -200.4736850529726269 ) ) ;
#70615=CARTESIAN_POINT ( 'NONE',  ( -21.78635804494510708, 60.41499726328847686, -234.1090742605158539 ) ) ;
#70617=CYLINDRICAL_SURFACE ( 'NONE', #205487, 0.09999999999999543976 ) ;
#70643=CARTESIAN_POINT ( 'NONE',  ( -21.05000000000000071, 67.63082410804655353, -211.8415745842588649 ) ) ;
#70647=CARTESIAN_POINT ( 'NONE',  ( -18.59999999999999787, 65.50527602196416410, -248.6645148362614748 ) ) ;
#70655=CARTESIAN_POINT ( 'NONE',  ( 20.95325940946048249, 59.05480421347601805, -225.7998712302227773 ) ) ;
#70668=ORIENTED_EDGE ( 'NONE', *, *, #50873, .F. ) ;
#70682=ORIENTED_EDGE ( 'NONE', *, *, #170043, .F. ) ;
#70725=ORIENTED_EDGE ( 'NONE', *, *, #153100, .T. ) ;
#70734=EDGE_CURVE ( 'NONE', #111271, #88487, #222010, .T. ) ;
#70761=DIRECTION ( 'NONE',  ( 1.000000000000000000, 0.000000000000000000, 0.000000000000000000 ) ) ;
#70809=EDGE_CURVE ( 'NONE', #170116, #242049, #85059, .T. ) ;
#70810=VERTEX_POINT ( 'NONE', #146338 ) ;
#70856=ORIENTED_EDGE ( 'NONE', *, *, #108037, .T. ) ;
#70858=DIRECTION ( 'NONE',  ( 0.000000000000000000, -0.2617529984165031243, -0.9651348961777157509 ) ) ;
#70874=DIRECTION ( 'NONE',  ( 2.952720810173290098E-16, 0.9651348961777149738, -0.2617529984165062884 ) ) ;
#70875=DIRECTION ( 'NONE',  ( 1.000000000000000000, 0.000000000000000000, 0.000000000000000000 ) ) ;
#70911=CARTESIAN_POINT ( 'NONE',  ( 22.39999999999999503, 64.25313205997782973, -247.2214437328673853 ) ) ;
#70953=AXIS2_PLACEMENT_3D ( 'NONE', #214415, #215689, #115318 ) ;
#70980=AXIS2_PLACEMENT_3D ( 'NONE', #169175, #206985, #8786 ) ;
#70993=AXIS2_PLACEMENT_3D ( 'NONE', #51266, #30471, #68306 ) ;
#71011=CYLINDRICAL_SURFACE ( 'NONE', #233711, 0.5000000000000014433 ) ;
#71035=AXIS2_PLACEMENT_3D ( 'NONE', #28281, #69959, #246011 ) ;
#71065=CARTESIAN_POINT ( 'NONE',  ( 20.04142135623730070, 52.91185528119410009, -244.1460391050142675 ) ) ;
#71082=FACE_OUTER_BOUND ( 'NONE', #76735, .T. ) ;
#71087=CARTESIAN_POINT ( 'NONE',  ( -20.94999999999999929, 67.23127455305841238, -235.8551265064783991 ) ) ;
#71123=DIRECTION ( 'NONE',  ( 0.000000000000000000, 0.7106264324241517993, -0.7035695228903270371 ) ) ;
#71155=CARTESIAN_POINT ( 'NONE',  ( -20.94999999999999929, 86.19075908668452257, -209.4719249499869136 ) ) ;
#71170=DIRECTION ( 'NONE',  ( 0.000000000000000000, -0.9651348961777158619, 0.2617529984165028467 ) ) ;
#71186=CARTESIAN_POINT ( 'NONE',  ( 20.94999999999999574, 70.44746257310249860, -228.4383880063670347 ) ) ;
#71194=AXIS2_PLACEMENT_3D ( 'NONE', #49147, #148251, #254683 ) ;
#71245=EDGE_CURVE ( 'NONE', #249371, #41329, #56264, .T. ) ;
#71310=CYLINDRICAL_SURFACE ( 'NONE', #71194, 0.5000000000000014433 ) ;
#71316=CARTESIAN_POINT ( 'NONE',  ( 18.50211644919734866, 67.49401193140447219, -195.5283494629371148 ) ) ;
#71320=CARTESIAN_POINT ( 'NONE',  ( 18.49505816908823874, 86.88289224156976331, -199.4521454443379582 ) ) ;
#71321=SPHERICAL_SURFACE ( 'NONE', #226089, 0.1000000000000000056 ) ;
#71357=FACE_OUTER_BOUND ( 'NONE', #144186, .T. ) ;
#71361=AXIS2_PLACEMENT_3D ( 'NONE', #175612, #16539, #230437 ) ;
#71404=ORIENTED_EDGE ( 'NONE', *, *, #75838, .F. ) ;
#71411=EDGE_LOOP ( 'NONE', ( #206859, #112957, #241737, #107551 ) ) ;
#71414=DIRECTION ( 'NONE',  ( 0.000000000000000000, 0.2617529984165152257, 0.9651348961777124202 ) ) ;
#71418=LINE ( 'NONE', #89657, #106571 ) ;
#71470=FACE_OUTER_BOUND ( 'NONE', #11449, .T. ) ;
#71475=DIRECTION ( 'NONE',  ( -2.602085213965226419E-14, 0.2617529984165031243, 0.9651348961777157509 ) ) ;
#71483=AXIS2_PLACEMENT_3D ( 'NONE', #69358, #75464, #247968 ) ;
#71500=ORIENTED_EDGE ( 'NONE', *, *, #244745, .F. ) ;
#71528=DIRECTION ( 'NONE',  ( 0.000000000000000000, 0.1144908148674362580, 0.9934243067848653741 ) ) ;
#71541=EDGE_CURVE ( 'NONE', #221590, #217985, #185798, .T. ) ;
#71578=CARTESIAN_POINT ( 'NONE',  ( 21.05000000000000071, 67.44464249442897597, -214.0562211244547655 ) ) ;
#71598=CARTESIAN_POINT ( 'NONE',  ( -20.85000000000000142, 62.86885547537413288, -207.0505773246641752 ) ) ;
#71610=FACE_OUTER_BOUND ( 'NONE', #139794, .T. ) ;
#71648=ORIENTED_EDGE ( 'NONE', *, *, #106783, .T. ) ;
#71652=VERTEX_POINT ( 'NONE', #93113 ) ;
#71665=CARTESIAN_POINT ( 'NONE',  ( -1.739115166359751801E-14, 62.49201502323813173, -208.8221019049098857 ) ) ;
#71675=ADVANCED_FACE ( 'NONE', ( #91838 ), #33194, .F. ) ;
#71681=CARTESIAN_POINT ( 'NONE',  ( 18.42555734704283665, 78.24001024381558977, -231.5466501076114980 ) ) ;
#71682=ORIENTED_EDGE ( 'NONE', *, *, #73348, .T. ) ;
#71693=EDGE_LOOP ( 'NONE', ( #226607, #34630, #202256 ) ) ;
#71734=EDGE_CURVE ( 'NONE', #81173, #217285, #247041, .T. ) ;
#71740=CARTESIAN_POINT ( 'NONE',  ( -20.00857864376270001, 63.74333919030581086, -212.9951329171253747 ) ) ;
#71768=CYLINDRICAL_SURFACE ( 'NONE', #85920, 0.09999999999999939493 ) ;
#71788=DIRECTION ( 'NONE',  ( 0.000000000000000000, -0.2617529984165036239, -0.9651348961777156399 ) ) ;
#71802=CIRCLE ( 'NONE', #55002, 0.1000000000000066530 ) ;
#71811=AXIS2_PLACEMENT_3D ( 'NONE', #53636, #94031, #250540 ) ;
#71818=ORIENTED_EDGE ( 'NONE', *, *, #249901, .T. ) ;
#71822=CARTESIAN_POINT ( 'NONE',  ( -20.54999999999999716, 76.00000000001126921, -203.5231074845248997 ) ) ;
#71863=CARTESIAN_POINT ( 'NONE',  ( -18.59999999999999787, 76.00000000001126921, -203.5231074845248997 ) ) ;
#71884=FACE_OUTER_BOUND ( 'NONE', #93610, .T. ) ;
#71906=CIRCLE ( 'NONE', #113409, 0.09999999999999939493 ) ;
#71936=AXIS2_PLACEMENT_3D ( 'NONE', #99124, #18325, #39202 ) ;
#72004=ORIENTED_EDGE ( 'NONE', *, *, #13473, .T. ) ;
#72011=CIRCLE ( 'NONE', #159495, 0.1000000000000124678 ) ;
#72032=EDGE_CURVE ( 'NONE', #172976, #222651, #140404, .T. ) ;
#72038=DIRECTION ( 'NONE',  ( 1.000000000000000000, -7.049440681616512959E-16, 1.911869773728117674E-16 ) ) ;
#72069=CARTESIAN_POINT ( 'NONE',  ( 23.14999999999999858, 76.00000000001126921, -203.5231074845248997 ) ) ;
#72090=VERTEX_POINT ( 'NONE', #38006 ) ;
#72209=ORIENTED_EDGE ( 'NONE', *, *, #95518, .F. ) ;
#72240=DIRECTION ( 'NONE',  ( 0.000000000000000000, 0.9651348961777157509, -0.2617529984165031243 ) ) ;
#72258=VERTEX_POINT ( 'NONE', #99210 ) ;
#72262=DIRECTION ( 'NONE',  ( 1.000000000000000000, 0.000000000000000000, -0.000000000000000000 ) ) ;
#72278=SPHERICAL_SURFACE ( 'NONE', #205587, 0.1000000000000000056 ) ;
#72292=FACE_OUTER_BOUND ( 'NONE', #123070, .T. ) ;
#72323=CARTESIAN_POINT ( 'NONE',  ( 23.14999999999999858, 67.55989888862310977, -211.9120700681549465 ) ) ;
#72328=ADVANCED_FACE ( 'NONE', ( #71357 ), #249977, .F. ) ;
#72359=CARTESIAN_POINT ( 'NONE',  ( 21.14999999999999858, 60.09787988008869775, -221.2279614330287245 ) ) ;
#72380=CARTESIAN_POINT ( 'NONE',  ( 20.94999999999999929, 82.09643798151613225, -215.4278993322501208 ) ) ;
#72399=EDGE_LOOP ( 'NONE', ( #253521, #198814, #75314, #256080 ) ) ;
#72401=AXIS2_PLACEMENT_3D ( 'NONE', #72323, #28075, #90571 ) ;
#72424=CARTESIAN_POINT ( 'NONE',  ( 23.24999999999999645, 67.23127455305841238, -235.8551265064783991 ) ) ;
#72443=AXIS2_PLACEMENT_3D ( 'NONE', #221786, #43188, #103135 ) ;
#72465=ORIENTED_EDGE ( 'NONE', *, *, #225709, .T. ) ;
#72467=AXIS2_PLACEMENT_3D ( 'NONE', #91192, #52040, #170780 ) ;
#72489=CARTESIAN_POINT ( 'NONE',  ( -21.05000000000000071, 69.29912324054878070, -228.2305608266744343 ) ) ;
#72510=VECTOR ( 'NONE', #192021, 1000.000000000000000 ) ;
#72531=CARTESIAN_POINT ( 'NONE',  ( -20.64999999999999858, 78.50726470275243685, -228.6618886302502176 ) ) ;
#72546=CARTESIAN_POINT ( 'NONE',  ( -22.50000000000000000, 55.89093952297024970, -232.7795287750844579 ) ) ;
#72555=EDGE_LOOP ( 'NONE', ( #169930, #145772, #203598 ) ) ;
#72579=ORIENTED_EDGE ( 'NONE', *, *, #26774, .T. ) ;
#72590=EDGE_CURVE ( 'NONE', #159923, #217493, #44376, .T. ) ;
#72617=EDGE_CURVE ( 'NONE', #129900, #11577, #256692, .T. ) ;
#72623=ORIENTED_EDGE ( 'NONE', *, *, #119763, .T. ) ;
#72677=DIRECTION ( 'NONE',  ( 1.000000000000000000, 0.000000000000000000, 0.000000000000000000 ) ) ;
#72681=LINE ( 'NONE', #29708, #144815 ) ;
#72701=VERTEX_POINT ( 'NONE', #243233 ) ;
#72703=CARTESIAN_POINT ( 'NONE',  ( 18.49999999999999289, 58.01113881014391893, -224.9619361160449387 ) ) ;
#72715=CARTESIAN_POINT ( 'NONE',  ( -20.64999999999999858, 78.50726470275243685, -228.6618886302502176 ) ) ;
#72739=ADVANCED_FACE ( 'NONE', ( #227529 ), #211135, .F. ) ;
#72740=VERTEX_POINT ( 'NONE', #188406 ) ;
#72753=ORIENTED_EDGE ( 'NONE', *, *, #209491, .F. ) ;
#72769=CARTESIAN_POINT ( 'NONE',  ( -20.94684162445269848, 57.68176035244419353, -226.1764194146458635 ) ) ;
#72783=DIRECTION ( 'NONE',  ( 0.000000000000000000, 0.2617529984165031243, 0.9651348961777157509 ) ) ;
#72809=DIRECTION ( 'NONE',  ( 0.000000000000000000, -0.2617529984165032908, -0.9651348961777156399 ) ) ;
#72822=CIRCLE ( 'NONE', #218502, 0.1000000000000106498 ) ;
#72828=CIRCLE ( 'NONE', #206070, 0.09999999999999123479 ) ;
#72836=ORIENTED_EDGE ( 'NONE', *, *, #161557, .F. ) ;
#72862=CARTESIAN_POINT ( 'NONE',  ( -22.39999999999999858, 64.25313205997782973, -247.2214437328673853 ) ) ;
#72866=DIRECTION ( 'NONE',  ( 1.000000000000000000, 7.049440681616512959E-16, -1.911869773728115455E-16 ) ) ;
#72871=ORIENTED_EDGE ( 'NONE', *, *, #135989, .T. ) ;
#72897=DIRECTION ( 'NONE',  ( -1.000000000000000000, -0.000000000000000000, -0.000000000000000000 ) ) ;
#72929=VERTEX_POINT ( 'NONE', #177858 ) ;
#72930=CYLINDRICAL_SURFACE ( 'NONE', #245198, 0.1000000000000124678 ) ;
#72941=CARTESIAN_POINT ( 'NONE',  ( 20.87631937322885278, 59.10889048783243993, -225.7987040349840697 ) ) ;
#72972=CYLINDRICAL_SURFACE ( 'NONE', #187325, 0.09999999999999939493 ) ;
#72978=FACE_OUTER_BOUND ( 'NONE', #157253, .T. ) ;
#73000=DIRECTION ( 'NONE',  ( 0.000000000000000000, -0.2617529984165152257, -0.9651348961777124202 ) ) ;
#73040=AXIS2_PLACEMENT_3D ( 'NONE', #80564, #256609, #160165 ) ;
#73056=EDGE_CURVE ( 'NONE', #129974, #103686, #15528, .T. ) ;
#73057=ORIENTED_EDGE ( 'NONE', *, *, #251875, .T. ) ;
#73071=ADVANCED_FACE ( 'NONE', ( #145111 ), #194604, .T. ) ;
#73094=VECTOR ( 'NONE', #195408, 1000.000000000000000 ) ;
#73097=CARTESIAN_POINT ( 'NONE',  ( -18.50000000000000000, 79.11538813396778380, -196.3722783875038544 ) ) ;
#73103=CARTESIAN_POINT ( 'NONE',  ( -23.15000000000000213, 86.27712145182582049, -209.5223386573213702 ) ) ;
#73118=CARTESIAN_POINT ( 'NONE',  ( 18.49999999999998934, 66.44571689960341132, -213.7280413126916017 ) ) ;
#73132=CARTESIAN_POINT ( 'NONE',  ( 22.39999999999999503, 55.96127771274635876, -232.9022175645438892 ) ) ;
#73171=ORIENTED_EDGE ( 'NONE', *, *, #46014, .T. ) ;
#73198=ORIENTED_EDGE ( 'NONE', *, *, #63372, .T. ) ;
#73220=DIRECTION ( 'NONE',  ( 1.000000000000000000, 0.000000000000000000, 0.000000000000000000 ) ) ;
#73221=CARTESIAN_POINT ( 'NONE',  ( 20.95575313997065336, 58.98169444576728893, -225.7211617421326650 ) ) ;
#73229=CARTESIAN_POINT ( 'NONE',  ( -18.59999999999999787, 63.74333919030581086, -212.9951329171253747 ) ) ;
#73237=ORIENTED_EDGE ( 'NONE', *, *, #216847, .T. ) ;
#73246=CIRCLE ( 'NONE', #48256, 0.1000000000000124678 ) ;
#73248=CARTESIAN_POINT ( 'NONE',  ( 18.59999999999999432, 68.22930980752001062, -227.7331931781284879 ) ) ;
#73348=EDGE_CURVE ( 'NONE', #38351, #182549, #136274, .T. ) ;
#73363=CARTESIAN_POINT ( 'NONE',  ( -20.94999999999999929, 72.06821323333463170, -225.0920403225231610 ) ) ;
#73364=CARTESIAN_POINT ( 'NONE',  ( -20.54999999999999716, 76.00000000001126921, -203.5231074845248997 ) ) ;
#73431=CARTESIAN_POINT ( 'NONE',  ( 18.59999999999999432, 80.78317333349157536, -192.9003134612048882 ) ) ;
#73433=CARTESIAN_POINT ( 'NONE',  ( 20.94999999999999574, 72.05339752741123505, -225.0867394276846483 ) ) ;
#73458=EDGE_CURVE ( 'NONE', #84528, #125683, #15719, .T. ) ;
#73464=VECTOR ( 'NONE', #173034, 1000.000000000000114 ) ;
#73494=CARTESIAN_POINT ( 'NONE',  ( 21.05000000000000071, 82.57900542960499024, -215.5587758314583766 ) ) ;
#73513=AXIS2_PLACEMENT_3D ( 'NONE', #194936, #191095, #230190 ) ;
#73557=CARTESIAN_POINT ( 'NONE',  ( -21.46681500593047431, 60.61285123220599758, -234.0601523988342194 ) ) ;
#73566=VERTEX_POINT ( 'NONE', #174715 ) ;
#73578=CIRCLE ( 'NONE', #194382, 0.1999999999999945155 ) ;
#73590=DIRECTION ( 'NONE',  ( -1.000000000000000000, -0.000000000000000000, 0.000000000000000000 ) ) ;
#73620=CARTESIAN_POINT ( 'NONE',  ( 18.49999999999999645, 76.00000000001126921, -203.5231074845248997 ) ) ;
#73716=CARTESIAN_POINT ( 'NONE',  ( -18.49499033040906681, 78.22449947793296587, -231.3784013806107112 ) ) ;
#73734=CARTESIAN_POINT ( 'NONE',  ( -23.25000000000000000, 79.24821784679178904, -196.3217825494968736 ) ) ;
#73793=AXIS2_PLACEMENT_3D ( 'NONE', #189698, #167589, #69767 ) ;
#73796=DIRECTION ( 'NONE',  ( -4.391705002472931063E-16, -0.9651348961777154178, 0.2617529984165040680 ) ) ;
#73828=CARTESIAN_POINT ( 'NONE',  ( 18.59999999999999787, 86.87366311306882949, -199.3414869250131858 ) ) ;
#73870=VERTEX_POINT ( 'NONE', #198718 ) ;
#73874=FACE_OUTER_BOUND ( 'NONE', #10953, .T. ) ;
#73882=CARTESIAN_POINT ( 'NONE',  ( 22.49231231312462853, 55.97148680618423100, -232.8646322987703456 ) ) ;
#73936=EDGE_CURVE ( 'NONE', #250542, #193798, #140967, .T. ) ;
#73949=AXIS2_PLACEMENT_3D ( 'NONE', #63891, #43051, #143422 ) ;
#74049=AXIS2_PLACEMENT_3D ( 'NONE', #184677, #243371, #244653 ) ;
#74123=ADVANCED_FACE ( 'NONE', ( #164738 ), #141319, .F. ) ;
#74132=CARTESIAN_POINT ( 'NONE',  ( 18.59999999999999076, 68.51069317435826633, -224.1259271199053842 ) ) ;
#74161=CARTESIAN_POINT ( 'NONE',  ( 21.05000000000000071, 62.86885547537412577, -207.0505773246641752 ) ) ;
#74165=CARTESIAN_POINT ( 'NONE',  ( -18.50000000000000000, 61.53642629385834795, -221.5144953033309321 ) ) ;
#74175=DIRECTION ( 'NONE',  ( 0.000000000000000000, 0.2617529984165152257, 0.9651348961777124202 ) ) ;
#74191=DIRECTION ( 'NONE',  ( -1.000000000000000000, -0.000000000000000000, 0.000000000000000000 ) ) ;
#74207=DIRECTION ( 'NONE',  ( 1.000000000000000000, 8.153259210133938153E-16, 2.158126701439427964E-16 ) ) ;
#74227=CARTESIAN_POINT ( 'NONE',  ( 20.86036036209928923, 58.98722522104349508, -225.6759763284424309 ) ) ;
#74229=VERTEX_POINT ( 'NONE', #108181 ) ;
#74244=ORIENTED_EDGE ( 'NONE', *, *, #33820, .T. ) ;
#74266=FACE_OUTER_BOUND ( 'NONE', #144228, .T. ) ;
#74272=ORIENTED_EDGE ( 'NONE', *, *, #938, .F. ) ;
#74276=ORIENTED_EDGE ( 'NONE', *, *, #243109, .F. ) ;
#74294=CIRCLE ( 'NONE', #86695, 0.1000000000000124678 ) ;
#74302=ORIENTED_EDGE ( 'NONE', *, *, #133771, .T. ) ;
#74312=DIRECTION ( 'NONE',  ( 7.304098846218135653E-16, 0.9651348961777157509, -0.2617529984165031243 ) ) ;
#74403=CARTESIAN_POINT ( 'NONE',  ( 18.49999999999999289, 63.83083047455526327, -209.3924252461221158 ) ) ;
#74410=ADVANCED_FACE ( 'NONE', ( #233279 ), #72930, .T. ) ;
#74432=CARTESIAN_POINT ( 'NONE',  ( -21.14999999999999858, 55.91711482281189660, -232.6830152854666949 ) ) ;
#74444=DIRECTION ( 'NONE',  ( -6.938893903907221278E-15, -0.9651348961777157509, 0.2617529984165028467 ) ) ;
#74453=EDGE_CURVE ( 'NONE', #12569, #232481, #136701, .T. ) ;
#74454=CARTESIAN_POINT ( 'NONE',  ( -21.05000000000000071, 68.35681244624936426, -231.7050464529142459 ) ) ;
#74482=AXIS2_PLACEMENT_3D ( 'NONE', #146011, #26089, #222979 ) ;
#74483=ORIENTED_EDGE ( 'NONE', *, *, #26774, .F. ) ;
#74489=VERTEX_POINT ( 'NONE', #76730 ) ;
#74492=ORIENTED_EDGE ( 'NONE', *, *, #235169, .T. ) ;
#74499=VECTOR ( 'NONE', #500, 1000.000000000000000 ) ;
#74511=CARTESIAN_POINT ( 'NONE',  ( -23.25000000000000000, 66.21323668544584962, -222.9901119748073484 ) ) ;
#74559=PLANE ( 'NONE',  #42772 ) ;
#74574=ORIENTED_EDGE ( 'NONE', *, *, #226155, .F. ) ;
#74578=ORIENTED_EDGE ( 'NONE', *, *, #206068, .F. ) ;
#74582=B_SPLINE_CURVE_WITH_KNOTS ( 'NONE', 3,
 ( #210943, #130109, #114410, #32336 ),
 .UNSPECIFIED., .F., .F.,
 ( 4, 4 ),
 ( 3.469446951953614189E-18, 0.0001058379652594699388 ),
 .UNSPECIFIED. ) ;
#74595=CARTESIAN_POINT ( 'NONE',  ( -21.05000000000000071, 68.20313450767837082, -227.8297066677462794 ) ) ;
#74596=EDGE_LOOP ( 'NONE', ( #237130, #251550, #19463, #125877 ) ) ;
#74605=( BOUNDED_SURFACE ( )  B_SPLINE_SURFACE ( 3, 2, ( 
 ( #251532, #169485, #70371 ),
 ( #211132, #89885, #131590 ),
 ( #14238, #95027, #11667 ),
 ( #174629, #33826, #152470 ),
 ( #93747, #189006, #208586 ),
 ( #12956, #110740, #173342 ),
 ( #254090, #109446, #153780 ),
 ( #149897, #250257, #194157 ),
 ( #190301, #130299, #252812 ),
 ( #248992, #75498, #50745 ),
 ( #72941, #91187, #74227 ),
 ( #233288, #15525, #53340 ) ),
 .UNSPECIFIED., .F., .F., .F. ) 
 B_SPLINE_SURFACE_WITH_KNOTS ( ( 4, 2, 2, 2, 2, 4 ),
 ( 3, 3 ),
 ( 3.174653483277205090, 3.943930578431713574, 4.713207673586222057, 5.482484768740730985, 5.867123316317985449, 6.251761863895239912 ),
 ( 0.000000000000000000, 1.000000000000000000 ),
 .UNSPECIFIED. ) 
 GEOMETRIC_REPRESENTATION_ITEM ( )  RATIONAL_B_SPLINE_SURFACE ( (
 ( 1.000000000000000000, 0.8659465255642661008, 1.000000000000000000),
 ( 1.000000000000000000, 0.8648614068561133461, 1.000000000000000000),
 ( 1.000000000000000000, 0.8489031841225879171, 1.000000000000000000),
 ( 1.000000000000000000, 0.7927507630259206239, 1.000000000000000000),
 ( 1.000000000000000000, 0.7523013859064423547, 1.000000000000000000),
 ( 1.000000000000000000, 0.6616226951140901091, 1.000000000000000000),
 ( 1.000000000000000000, 0.6112214368715968016, 1.000000000000000000),
 ( 1.000000000000000000, 0.5507684314502028222, 1.000000000000000000),
 ( 1.000000000000000000, 0.5333267243212502784, 1.000000000000000000),
 ( 1.000000000000000000, 0.5084565446419482271, 1.000000000000000000),
 ( 1.000000000000000000, 0.5010722703496404140, 1.000000000000000000),
 ( 1.000000000000000000, 0.5001234037138357902, 1.000000000000000000) ) ) 
 REPRESENTATION_ITEM ( '' )  SURFACE ( )  );
#74609=ORIENTED_EDGE ( 'NONE', *, *, #179627, .F. ) ;
#74617=DIRECTION ( 'NONE',  ( 0.000000000000000000, 0.2617529984165029577, 0.9651348961777157509 ) ) ;
#74664=DIRECTION ( 'NONE',  ( 1.000000000000000000, 0.000000000000000000, 0.000000000000000000 ) ) ;
#74706=EDGE_LOOP ( 'NONE', ( #146409, #253012, #128518 ) ) ;
#74710=VERTEX_POINT ( 'NONE', #112311 ) ;
#74753=TOROIDAL_SURFACE ( 'NONE', #153872, 0.6000000000000004219, 0.1000000000000000056 ) ;
#74771=EDGE_CURVE ( 'NONE', #38549, #85926, #194930, .T. ) ;
#74879=CARTESIAN_POINT ( 'NONE',  ( -22.39999999999999858, 59.71212129423881976, -233.8158665866020272 ) ) ;
#74906=CARTESIAN_POINT ( 'NONE',  ( 18.49999999999999289, 70.37092869010230345, -198.1237041667535550 ) ) ;
#74927=FACE_OUTER_BOUND ( 'NONE', #55886, .T. ) ;
#74935=VERTEX_POINT ( 'NONE', #242510 ) ;
#74956=AXIS2_PLACEMENT_3D ( 'NONE', #247164, #191083, #209325 ) ;
#74960=DIRECTION ( 'NONE',  ( 0.000000000000000000, -0.2617529984164955192, -0.9651348961777178603 ) ) ;
#75015=CARTESIAN_POINT ( 'NONE',  ( -21.05000000000000071, 67.23127455305841238, -235.8551265064783991 ) ) ;
#75032=CARTESIAN_POINT ( 'NONE',  ( 18.59999999999999076, 80.78317333349157536, -192.9003134612049166 ) ) ;
#75033=ORIENTED_EDGE ( 'NONE', *, *, #234538, .F. ) ;
#75034=LINE ( 'NONE', #197504, #17398 ) ;
#75076=CARTESIAN_POINT ( 'NONE',  ( -18.50000000000000000, 64.18627039993180006, -224.3513032416919089 ) ) ;
#75082=EDGE_CURVE ( 'NONE', #157057, #14440, #88554, .T. ) ;
#75091=CARTESIAN_POINT ( 'NONE',  ( 22.57320508075688181, 55.89093952297025680, -232.7795287750844864 ) ) ;
#75115=ORIENTED_EDGE ( 'NONE', *, *, #162628, .F. ) ;
#75116=EDGE_LOOP ( 'NONE', ( #197928, #196458, #96394, #105342, #120324, #95359, #257627, #126904, #100079, #172947, #169514 ) ) ;
#75129=CARTESIAN_POINT ( 'NONE',  ( -18.51024323315077424, 67.49344847133114911, -195.4961807846321733 ) ) ;
#75133=CARTESIAN_POINT ( 'NONE',  ( -23.15000000000000213, 78.08573236070779444, -228.9307947190811774 ) ) ;
#75134=AXIS2_PLACEMENT_3D ( 'NONE', #10616, #133127, #212671 ) ;
#75149=DIRECTION ( 'NONE',  ( 7.589415207398576792E-15, 0.9651348961777157509, -0.2617529984165031243 ) ) ;
#75152=CARTESIAN_POINT ( 'NONE',  ( -20.64999999999999858, 75.47649400317826007, -205.4533772768803317 ) ) ;
#75159=CARTESIAN_POINT ( 'NONE',  ( 22.49806830649814060, 55.96728299348496449, -232.8804964729971232 ) ) ;
#75171=VERTEX_POINT ( 'NONE', #15477 ) ;
#75180=ORIENTED_EDGE ( 'NONE', *, *, #163044, .F. ) ;
#75187=ORIENTED_EDGE ( 'NONE', *, *, #83754, .T. ) ;
#75212=CARTESIAN_POINT ( 'NONE',  ( 20.94999999999999929, 79.34051597037932879, -196.3602670448451875 ) ) ;
#75234=DIRECTION ( 'NONE',  ( -1.000000000000000000, -0.000000000000000000, -0.000000000000000000 ) ) ;
#75236=EDGE_LOOP ( 'NONE', ( #221483, #84994, #151118, #87077 ) ) ;
#75312=EDGE_CURVE ( 'NONE', #229783, #133438, #105206, .T. ) ;
#75314=ORIENTED_EDGE ( 'NONE', *, *, #17876, .F. ) ;
#75330=CIRCLE ( 'NONE', #162798, 0.1000000000000124678 ) ;
#75341=DIRECTION ( 'NONE',  ( 0.000000000000000000, 0.9651348961777157509, -0.2617529984165031243 ) ) ;
#75342=EDGE_CURVE ( 'NONE', #136435, #87098, #134745, .T. ) ;
#75363=DIRECTION ( 'NONE',  ( -1.000000000000000000, -0.000000000000000000, -0.000000000000000000 ) ) ;
#75377=DIRECTION ( 'NONE',  ( 0.000000000000000000, 0.2617529984165027912, 0.9651348961777157509 ) ) ;
#75389=EDGE_LOOP ( 'NONE', ( #172305, #246213, #118565, #53152 ) ) ;
#75401=DIRECTION ( 'NONE',  ( 0.000000000000000000, 0.2617529984164506107, 0.9651348961777299618 ) ) ;
#75464=DIRECTION ( 'NONE',  ( 0.000000000000000000, -0.5378121776619205763, 0.8430646840892713767 ) ) ;
#75498=CARTESIAN_POINT ( 'NONE',  ( 20.72390388899077607, 58.97664953679249322, -225.8337075495444992 ) ) ;
#75546=AXIS2_PLACEMENT_3D ( 'NONE', #194926, #18829, #16298 ) ;
#75554=ORIENTED_EDGE ( 'NONE', *, *, #234032, .T. ) ;
#75602=DIRECTION ( 'NONE',  ( 0.000000000000000000, 0.2617529984165152257, 0.9651348961777124202 ) ) ;
#75671=CARTESIAN_POINT ( 'NONE',  ( 22.39999999999999503, 55.86476422312859569, -232.8760422647022494 ) ) ;
#75680=CIRCLE ( 'NONE', #75845, 0.1000000000000022676 ) ;
#75689=DIRECTION ( 'NONE',  ( 0.000000000000000000, -0.7106264324241464703, 0.7035695228903324772 ) ) ;
#75708=DIRECTION ( 'NONE',  ( 0.000000000000000000, -0.2558827019434133376, 0.9667078373770113808 ) ) ;
#75713=CARTESIAN_POINT ( 'NONE',  ( 21.14999999999999858, 65.51923798433685420, -242.1677427744926092 ) ) ;
#75730=AXIS2_PLACEMENT_3D ( 'NONE', #234379, #192705, #37491 ) ;
#75773=EDGE_CURVE ( 'NONE', #96108, #19722, #111052, .T. ) ;
#75776=DIRECTION ( 'NONE',  ( -1.000000000000000000, -0.000000000000000000, 0.000000000000000000 ) ) ;
#75810=DIRECTION ( 'NONE',  ( 0.000000000000000000, 0.2617529984165030688, 0.9651348961777158619 ) ) ;
#75819=ORIENTED_EDGE ( 'NONE', *, *, #44679, .T. ) ;
#75838=EDGE_CURVE ( 'NONE', #159923, #249034, #193179, .T. ) ;
#75845=AXIS2_PLACEMENT_3D ( 'NONE', #149120, #126969, #26606 ) ;
#75862=CARTESIAN_POINT ( 'NONE',  ( 23.14999999999999858, 65.17014820068582992, -222.4427298839669618 ) ) ;
#75881=ADVANCED_FACE ( 'NONE', ( #10679 ), #254270, .T. ) ;
#75895=EDGE_CURVE ( 'NONE', #250282, #138432, #180032, .T. ) ;
#75905=ORIENTED_EDGE ( 'NONE', *, *, #26096, .T. ) ;
#75914=DIRECTION ( 'NONE',  ( -0.000000000000000000, -0.2617529984165028467, -0.9651348961777159730 ) ) ;
#75927=CIRCLE ( 'NONE', #50762, 7.799999999999997158 ) ;
#75963=ORIENTED_EDGE ( 'NONE', *, *, #32683, .F. ) ;
#75965=ADVANCED_FACE ( 'NONE', ( #120078 ), #199606, .F. ) ;
#75997=ADVANCED_FACE ( 'NONE', ( #181321 ), #161764, .F. ) ;
#76002=DIRECTION ( 'NONE',  ( 1.000000000000000000, 0.000000000000000000, 0.000000000000000000 ) ) ;
#76031=DIRECTION ( 'NONE',  ( 0.000000000000000000, 0.2617529984165152257, 0.9651348961777124202 ) ) ;
#76032=AXIS2_PLACEMENT_3D ( 'NONE', #7015, #86525, #27903 ) ;
#76073=VERTEX_POINT ( 'NONE', #207302 ) ;
#76079=CIRCLE ( 'NONE', #47034, 0.09999999999999939493 ) ;
#76081=CARTESIAN_POINT ( 'NONE',  ( -23.25000000000000000, 70.29876110920605470, -198.0544810472949564 ) ) ;
#76108=EDGE_LOOP ( 'NONE', ( #40709, #22862, #237395, #195258 ) ) ;
#76111=EDGE_CURVE ( 'NONE', #237933, #225653, #171138, .T. ) ;
#76112=LINE ( 'NONE', #77383, #178125 ) ;
#76113=EDGE_LOOP ( 'NONE', ( #251736, #133258, #250038, #29229 ) ) ;
#76120=ADVANCED_FACE ( 'NONE', ( #242550 ), #243833, .T. ) ;
#76122=CARTESIAN_POINT ( 'NONE',  ( 20.12500000000000000, 63.38346053167636995, -212.7939182281409956 ) ) ;
#76124=AXIS2_PLACEMENT_3D ( 'NONE', #72380, #52782, #34542 ) ;
#76125=CARTESIAN_POINT ( 'NONE',  ( -21.44999999999999929, 65.69978428250288971, -213.4221254243406065 ) ) ;
#76126=ORIENTED_EDGE ( 'NONE', *, *, #134751, .T. ) ;
#76144=EDGE_CURVE ( 'NONE', #254106, #136435, #137933, .T. ) ;
#76145=ADVANCED_FACE ( 'NONE', ( #92455 ), #74605, .T. ) ;
#76158=CYLINDRICAL_SURFACE ( 'NONE', #234201, 0.09999999999999939493 ) ;
#76162=FACE_OUTER_BOUND ( 'NONE', #181156, .T. ) ;
#76168=AXIS2_PLACEMENT_3D ( 'NONE', #150834, #230369, #118128 ) ;
#76248=LINE ( 'NONE', #39733, #207230 ) ;
#76278=DIRECTION ( 'NONE',  ( 1.000000000000000000, 0.000000000000000000, 0.000000000000000000 ) ) ;
#76294=DIRECTION ( 'NONE',  ( 0.000000000000000000, -0.9651348961777157509, 0.2617529984165031243 ) ) ;
#76330=ORIENTED_EDGE ( 'NONE', *, *, #161371, .T. ) ;
#76337=CARTESIAN_POINT ( 'NONE',  ( -20.94999999999999929, 77.07318729351892728, -199.5660544101962728 ) ) ;
#76347=EDGE_LOOP ( 'NONE', ( #44097, #163749, #68332, #35156 ) ) ;
#76352=LINE ( 'NONE', #178061, #31395 ) ;
#76364=DIRECTION ( 'NONE',  ( 1.000000000000000000, 0.000000000000000000, 0.000000000000000000 ) ) ;
#76407=AXIS2_PLACEMENT_3D ( 'NONE', #122166, #77882, #99992 ) ;
#76413=EDGE_CURVE ( 'NONE', #43432, #101652, #87858, .T. ) ;
#76429=DIRECTION ( 'NONE',  ( 1.000000000000000000, 0.000000000000000000, 0.000000000000000000 ) ) ;
#76443=ORIENTED_EDGE ( 'NONE', *, *, #61425, .F. ) ;
#76455=CARTESIAN_POINT ( 'NONE',  ( -20.94999999999999929, 86.10439672154322466, -209.4215112426525138 ) ) ;
#76473=LINE ( 'NONE', #158616, #146743 ) ;
#76556=EDGE_CURVE ( 'NONE', #175607, #226006, #206316, .T. ) ;
#76557=CARTESIAN_POINT ( 'NONE',  ( -20.64999999999999858, 66.26558728512915764, -222.7970849955717938 ) ) ;
#76611=ORIENTED_EDGE ( 'NONE', *, *, #115605, .T. ) ;
#76614=CARTESIAN_POINT ( 'NONE',  ( -23.15000000000000213, 62.92003201576280702, -207.2439188921395896 ) ) ;
#76621=DIRECTION ( 'NONE',  ( 0.000000000000000000, 0.2617529984164856383, 0.9651348961777204138 ) ) ;
#76622=TOROIDAL_SURFACE ( 'NONE', #84977, 0.2000000000000000111, 0.1000000000000000056 ) ;
#76660=DIRECTION ( 'NONE',  ( 1.000000000000000000, 0.000000000000000000, 0.000000000000000000 ) ) ;
#76669=DIRECTION ( 'NONE',  ( 0.000000000000000000, -0.2617529984165031243, -0.9651348961777157509 ) ) ;
#76677=EDGE_CURVE ( 'NONE', #45881, #250378, #118137, .T. ) ;
#76707=DIRECTION ( 'NONE',  ( 4.239556034732056743E-17, 0.3848449534832867891, 0.9229812358755983270 ) ) ;
#76713=CARTESIAN_POINT ( 'NONE',  ( 21.05000000000000071, 56.01362831242965967, -232.7091905853083347 ) ) ;
#76725=EDGE_LOOP ( 'NONE', ( #3927, #205234, #70491, #125196 ) ) ;
#76730=CARTESIAN_POINT ( 'NONE',  ( -20.54999999999999716, 65.86663596189677605, -213.5709895136416776 ) ) ;
#76735=EDGE_LOOP ( 'NONE', ( #130727, #235649, #111843, #252393 ) ) ;
#76810=CARTESIAN_POINT ( 'NONE',  ( 23.15000000000000213, 78.47509609352879068, -238.9045489380306435 ) ) ;
#76817=EDGE_CURVE ( 'NONE', #85530, #242990, #123277, .T. ) ;
#76846=CARTESIAN_POINT ( 'NONE',  ( -22.48660254037843487, 55.97436536266719997, -232.8539608197349651 ) ) ;
#76885=AXIS2_PLACEMENT_3D ( 'NONE', #227401, #64488, #246960 ) ;
#76922=FACE_OUTER_BOUND ( 'NONE', #112750, .T. ) ;
#76927=VERTEX_POINT ( 'NONE', #249656 ) ;
#76975=CARTESIAN_POINT ( 'NONE',  ( 21.07928932188134041, 65.47931918658339612, -241.9371126717067568 ) ) ;
#76997=TOROIDAL_SURFACE ( 'NONE', #156143, 0.2000000000000000111, 0.1000000000000000056 ) ;
#77024=LINE ( 'NONE', #236103, #191937 ) ;
#77029=CARTESIAN_POINT ( 'NONE',  ( 20.94999999999999929, 76.00000000001126921, -203.5231074845248997 ) ) ;
#77065=EDGE_LOOP ( 'NONE', ( #257068, #205945, #151663, #18811 ) ) ;
#77068=( GEOMETRIC_REPRESENTATION_CONTEXT ( 3 ) GLOBAL_UNCERTAINTY_ASSIGNED_CONTEXT ( ( #32124 ) ) GLOBAL_UNIT_ASSIGNED_CONTEXT ( ( #107297, #143845, #184266 ) ) REPRESENTATION_CONTEXT ( 'NONE', 'WORKASPACE' ) );
#77070=ORIENTED_EDGE ( 'NONE', *, *, #238577, .F. ) ;
#77130=CARTESIAN_POINT ( 'NONE',  ( 18.59999999999999076, 62.96704557978079464, -212.5773704035085814 ) ) ;
#77133=DIRECTION ( 'NONE',  ( 1.000000000000000000, 0.000000000000000000, 0.000000000000000000 ) ) ;
#77147=VECTOR ( 'NONE', #74191, 1000.000000000000000 ) ;
#77157=CARTESIAN_POINT ( 'NONE',  ( -20.94999999999999929, 79.23417978893665747, -236.1056577391152587 ) ) ;
#77165=EDGE_LOOP ( 'NONE', ( #257639, #196502, #165707, #140681 ) ) ;
#77172=CARTESIAN_POINT ( 'NONE',  ( -21.05000000000000071, 68.58368164137472434, -224.2353459317783120 ) ) ;
#77193=DIRECTION ( 'NONE',  ( -0.000000000000000000, -0.2617529984165031243, -0.9651348961777157509 ) ) ;
#77199=AXIS2_PLACEMENT_3D ( 'NONE', #13656, #248419, #131032 ) ;
#77233=AXIS2_PLACEMENT_3D ( 'NONE', #104338, #82198, #161799 ) ;
#77245=ORIENTED_EDGE ( 'NONE', *, *, #212202, .T. ) ;
#77258=VERTEX_POINT ( 'NONE', #139943 ) ;
#77262=ADVANCED_FACE ( 'NONE', ( #74266 ), #91238, .F. ) ;
#77274=AXIS2_PLACEMENT_3D ( 'NONE', #128975, #226774, #170714 ) ;
#77282=CARTESIAN_POINT ( 'NONE',  ( 19.94784844284945180, 62.39243729835731500, -208.9482361014044329 ) ) ;
#77283=VERTEX_POINT ( 'NONE', #70419 ) ;
#77293=CARTESIAN_POINT ( 'NONE',  ( 20.94999999999999929, 78.08573236070779444, -228.9307947190811774 ) ) ;
#77317=VECTOR ( 'NONE', #141224, 1000.000000000000000 ) ;
#77327=ORIENTED_EDGE ( 'NONE', *, *, #142924, .F. ) ;
#77353=DIRECTION ( 'NONE',  ( 0.000000000000000000, 0.2617529984165152257, 0.9651348961777124202 ) ) ;
#77364=ORIENTED_EDGE ( 'NONE', *, *, #2175, .F. ) ;
#77383=CARTESIAN_POINT ( 'NONE',  ( 23.25000000000000000, 81.75190851390706825, -227.2043352493130612 ) ) ;
#77393=CYLINDRICAL_SURFACE ( 'NONE', #94927, 12.87500000000000178 ) ;
#77405=CARTESIAN_POINT ( 'NONE',  ( 20.85000000000000142, 62.88396779178381735, -206.9948552354529170 ) ) ;
#77436=AXIS2_PLACEMENT_3D ( 'NONE', #137928, #40163, #179657 ) ;
#77438=CARTESIAN_POINT ( 'NONE',  ( -22.50000000000000000, 64.09252369393823301, -247.0744076673471170 ) ) ;
#77451=FACE_OUTER_BOUND ( 'NONE', #175579, .T. ) ;
#77452=VERTEX_POINT ( 'NONE', #98890 ) ;
#77463=CARTESIAN_POINT ( 'NONE',  ( 20.94999999999999929, 76.00000000001126921, -203.5231074845248997 ) ) ;
#77469=ORIENTED_EDGE ( 'NONE', *, *, #180549, .T. ) ;
#77495=CARTESIAN_POINT ( 'NONE',  ( -21.76363531954647357, 65.30006722027489729, -242.5976422560627270 ) ) ;
#77501=CIRCLE ( 'NONE', #11072, 0.1000000000000079159 ) ;
#77510=CARTESIAN_POINT ( 'NONE',  ( 22.59999954896768770, 64.16406410971224261, -247.1982632919209379 ) ) ;
#77536=ORIENTED_EDGE ( 'NONE', *, *, #91200, .T. ) ;
#77539=CARTESIAN_POINT ( 'NONE',  ( 20.90851465518105812, 67.49261718274587452, -195.4446851895584416 ) ) ;
#77575=ORIENTED_EDGE ( 'NONE', *, *, #202867, .F. ) ;
#77612=DIRECTION ( 'NONE',  ( 0.000000000000000000, 0.9229812358756199764, -0.3848449534832346086 ) ) ;
#77627=CARTESIAN_POINT ( 'NONE',  ( 18.59999999999996945, 70.22659352830977753, -197.9852579278363578 ) ) ;
#77634=AXIS2_PLACEMENT_3D ( 'NONE', #131055, #50220, #129771 ) ;
#77636=CARTESIAN_POINT ( 'NONE',  ( -21.05000000000000071, 68.49522935589659767, -224.1230159437372436 ) ) ;
#77663=DIRECTION ( 'NONE',  ( 0.000000000000000000, -0.2617529984164955192, -0.9651348961777178603 ) ) ;
#77674=EDGE_CURVE ( 'NONE', #79203, #242569, #76473, .T. ) ;
#77700=DIRECTION ( 'NONE',  ( 0.000000000000000000, -0.2617529984164506107, -0.9651348961777299618 ) ) ;
#77704=ADVANCED_FACE ( 'NONE', ( #98568 ), #142663, .T. ) ;
#77742=CARTESIAN_POINT ( 'NONE',  ( -23.15000000000000213, 78.98983215084128062, -228.7927651294584450 ) ) ;
#77750=DIRECTION ( 'NONE',  ( 0.000000000000000000, 0.2617529984165034018, 0.9651348961777157509 ) ) ;
#77754=ORIENTED_EDGE ( 'NONE', *, *, #97075, .T. ) ;
#77790=PLANE ( 'NONE',  #219146 ) ;
#77826=LINE ( 'NONE', #42555, #237750 ) ;
#77841=VERTEX_POINT ( 'NONE', #51313 ) ;
#77847=ADVANCED_FACE ( 'NONE', ( #254648 ), #55161, .F. ) ;
#77851=CARTESIAN_POINT ( 'NONE',  ( -20.94999999999999929, 57.72708596674832648, -226.0092949359174952 ) ) ;
#77879=CARTESIAN_POINT ( 'NONE',  ( -20.64999999999999858, 67.23127455305841238, -235.8551265064783991 ) ) ;
#77882=DIRECTION ( 'NONE',  ( 1.000000000000000000, -2.849773892568378313E-16, 7.728835255496647986E-17 ) ) ;
#77894=FACE_OUTER_BOUND ( 'NONE', #174702, .T. ) ;
#77901=DIRECTION ( 'NONE',  ( 1.000000000000000000, 0.000000000000000000, 0.000000000000000000 ) ) ;
#77923=ORIENTED_EDGE ( 'NONE', *, *, #112149, .F. ) ;
#77940=DIRECTION ( 'NONE',  ( 2.259780016855445309E-14, -0.9118278131605127568, 0.4105728183244933271 ) ) ;
#77989=VERTEX_POINT ( 'NONE', #237693 ) ;
#77995=ORIENTED_EDGE ( 'NONE', *, *, #121036, .T. ) ;
#78002=EDGE_LOOP ( 'NONE', ( #142090, #162282, #81557 ) ) ;
#78006=AXIS2_PLACEMENT_3D ( 'NONE', #243502, #119725, #203091 ) ;
#78041=ADVANCED_FACE ( 'NONE', ( #201125 ), #177745, .T. ) ;
#78059=ORIENTED_EDGE ( 'NONE', *, *, #7, .T. ) ;
#78060=ORIENTED_EDGE ( 'NONE', *, *, #204960, .F. ) ;
#78065=VERTEX_POINT ( 'NONE', #196011 ) ;
#78139=LINE ( 'NONE', #220253, #225561 ) ;
#78166=AXIS2_PLACEMENT_3D ( 'NONE', #544, #121806, #219591 ) ;
#78191=EDGE_CURVE ( 'NONE', #177586, #204227, #63759, .T. ) ;
#78201=EDGE_CURVE ( 'NONE', #4469, #20618, #26355, .T. ) ;
#78227=CYLINDRICAL_SURFACE ( 'NONE', #42312, 0.1000000000000124678 ) ;
#78238=TOROIDAL_SURFACE ( 'NONE', #257253, 0.6000000000000004219, 0.1000000000000000056 ) ;
#78239=CARTESIAN_POINT ( 'NONE',  ( 21.14999999999999858, 55.91711482281188950, -232.6830152854666949 ) ) ;
#78315=CARTESIAN_POINT ( 'NONE',  ( 18.59999999999999787, 80.69087520990402140, -192.8618289658565743 ) ) ;
#78338=CIRCLE ( 'NONE', #165859, 0.5000000000000014433 ) ;
#78358=ORIENTED_EDGE ( 'NONE', *, *, #65061, .F. ) ;
#78359=DIRECTION ( 'NONE',  ( 0.000000000000000000, 0.2617529984165031243, 0.9651348961777157509 ) ) ;
#78365=ORIENTED_EDGE ( 'NONE', *, *, #28139, .T. ) ;
#78386=CARTESIAN_POINT ( 'NONE',  ( 21.05543885634738288, 61.95077084394885247, -221.7984674804167184 ) ) ;
#78431=ORIENTED_EDGE ( 'NONE', *, *, #188020, .F. ) ;
#78439=DIRECTION ( 'NONE',  ( -1.836970198721029934E-16, -0.9651348961777157509, 0.2617529984165031243 ) ) ;
#78458=CARTESIAN_POINT ( 'NONE',  ( 21.05000000000000071, 82.57900542960499024, -215.5587758314583766 ) ) ;
#78467=DIRECTION ( 'NONE',  ( -1.000000000000000000, 0.000000000000000000, 0.000000000000000000 ) ) ;
#78476=VECTOR ( 'NONE', #36615, 1000.000000000000000 ) ;
#78491=CARTESIAN_POINT ( 'NONE',  ( 18.60000000000000142, 86.99328439831825222, -199.3739436137589678 ) ) ;
#78495=EDGE_LOOP ( 'NONE', ( #158572, #252460, #15266, #208167 ) ) ;
#78527=CARTESIAN_POINT ( 'NONE',  ( 18.59999999999999787, 80.78317333349157536, -192.9003134612049166 ) ) ;
#78531=AXIS2_PLACEMENT_3D ( 'NONE', #88469, #7691, #71528 ) ;
#78536=ORIENTED_EDGE ( 'NONE', *, *, #16654, .T. ) ;
#78600=DIRECTION ( 'NONE',  ( -1.000000000000000000, -0.000000000000000000, -0.000000000000000000 ) ) ;
#78620=LINE ( 'NONE', #159464, #257147 ) ;
#78641=AXIS2_PLACEMENT_3D ( 'NONE', #176645, #35849, #140039 ) ;
#78660=ORIENTED_EDGE ( 'NONE', *, *, #70581, .T. ) ;
#78702=DIRECTION ( 'NONE',  ( 1.000000000000000000, -0.000000000000000000, -0.000000000000000000 ) ) ;
#78723=VERTEX_POINT ( 'NONE', #49604 ) ;
#78764=ORIENTED_EDGE ( 'NONE', *, *, #181141, .F. ) ;
#78772=VERTEX_POINT ( 'NONE', #252929 ) ;
#78781=CARTESIAN_POINT ( 'NONE',  ( 21.07946286933444213, 65.50061980461839539, -241.9434290563612535 ) ) ;
#78791=EDGE_CURVE ( 'NONE', #109963, #242049, #247083, .T. ) ;
#78793=DIRECTION ( 'NONE',  ( -0.7071067811865474617, 0.6824534298470372740, -0.1850873201762208153 ) ) ;
#78838=TOROIDAL_SURFACE ( 'NONE', #20616, 11.65000000000000036, 0.1000000000000000056 ) ;
#78866=ORIENTED_EDGE ( 'NONE', *, *, #153507, .F. ) ;
#78900=CARTESIAN_POINT ( 'NONE',  ( -18.50000000000000000, 61.43991280424057777, -221.4883200034892923 ) ) ;
#78904=DIRECTION ( 'NONE',  ( 0.000000000000000000, 0.2617529984164506107, 0.9651348961777299618 ) ) ;
#78924=EDGE_CURVE ( 'NONE', #73566, #69974, #34411, .T. ) ;
#78947=DIRECTION ( 'NONE',  ( 1.713247197920696616E-14, -0.9121259477928120862, 0.4099100576505341209 ) ) ;
#78959=CARTESIAN_POINT ( 'NONE',  ( 21.05000000000000071, 86.10439672154322466, -209.4215112426525138 ) ) ;
#78991=EDGE_CURVE ( 'NONE', #245391, #111271, #122099, .T. ) ;
#79058=VERTEX_POINT ( 'NONE', #208066 ) ;
#79082=AXIS2_PLACEMENT_3D ( 'NONE', #42507, #200311, #65935 ) ;
#79091=FACE_OUTER_BOUND ( 'NONE', #157262, .T. ) ;
#79096=VERTEX_POINT ( 'NONE', #86792 ) ;
#79124=AXIS2_PLACEMENT_3D ( 'NONE', #211142, #170787, #191616 ) ;
#79140=FACE_OUTER_BOUND ( 'NONE', #36942, .T. ) ;
#79143=CIRCLE ( 'NONE', #220804, 0.1000000000000124678 ) ;
#79158=CARTESIAN_POINT ( 'NONE',  ( 21.05000000000000071, 59.06422320270096549, -225.9139711108258552 ) ) ;
#79160=ORIENTED_EDGE ( 'NONE', *, *, #40311, .T. ) ;
#79167=CIRCLE ( 'NONE', #62633, 0.1999999999999987899 ) ;
#79168=DIRECTION ( 'NONE',  ( -1.000000000000000000, 2.849773892568378313E-16, -7.728835255496647986E-17 ) ) ;
#79198=VERTEX_POINT ( 'NONE', #55345 ) ;
#79203=VERTEX_POINT ( 'NONE', #94504 ) ;
#79218=FACE_OUTER_BOUND ( 'NONE', #121161, .T. ) ;
#79225=DIRECTION ( 'NONE',  ( 1.000000000000000000, 0.000000000000000000, 0.000000000000000000 ) ) ;
#79231=CARTESIAN_POINT ( 'NONE',  ( 20.85000000000000142, 62.88396779178383156, -206.9948552354529170 ) ) ;
#79233=DIRECTION ( 'NONE',  ( -4.408576920032447972E-17, 0.1290532225515392262, 0.9916376685811522096 ) ) ;
#79238=ORIENTED_EDGE ( 'NONE', *, *, #63824, .F. ) ;
#79288=LINE ( 'NONE', #240954, #244985 ) ;
#79292=ORIENTED_EDGE ( 'NONE', *, *, #201471, .T. ) ;
#79327=ADVANCED_FACE ( 'NONE', ( #243003 ), #181761, .T. ) ;
#79328=AXIS2_PLACEMENT_3D ( 'NONE', #204474, #47972, #107957 ) ;
#79374=DIRECTION ( 'NONE',  ( -0.000000000000000000, -0.2617529984165031243, -0.9651348961777157509 ) ) ;
#79428=DIRECTION ( 'NONE',  ( -1.000000000000000000, 2.849773892568378313E-16, -7.728835255496647986E-17 ) ) ;
#79442=ADVANCED_FACE ( 'NONE', ( #150346 ), #219196, .T. ) ;
#79444=AXIS2_PLACEMENT_3D ( 'NONE', #237287, #20821, #217685 ) ;
#79445=CARTESIAN_POINT ( 'NONE',  ( 20.94999999999999929, 76.00000000001126921, -203.5231074845248997 ) ) ;
#79461=CIRCLE ( 'NONE', #137710, 11.80000000000000071 ) ;
#79523=CARTESIAN_POINT ( 'NONE',  ( 23.15000000000000213, 82.57900542960499024, -215.5587758314583766 ) ) ;
#79537=DIRECTION ( 'NONE',  ( 0.000000000000000000, -0.2617529984165152257, -0.9651348961777124202 ) ) ;
#79542=CARTESIAN_POINT ( 'NONE',  ( -23.15000000000000213, 55.98745301258801987, -232.8057040749261262 ) ) ;
#79592=DIRECTION ( 'NONE',  ( -0.000000000000000000, -0.1290532225515392817, -0.9916376685811522096 ) ) ;
#79595=AXIS2_PLACEMENT_3D ( 'NONE', #226021, #163517, #146499 ) ;
#79607=TOROIDAL_SURFACE ( 'NONE', #196318, 11.65000000000000036, 0.1000000000000000056 ) ;
#79612=AXIS2_PLACEMENT_3D ( 'NONE', #171478, #206713, #33250 ) ;
#79624=ORIENTED_EDGE ( 'NONE', *, *, #66209, .T. ) ;
#79642=CARTESIAN_POINT ( 'NONE',  ( -18.59999999999999787, 70.22659352830977753, -197.9852579278363578 ) ) ;
#79699=AXIS2_PLACEMENT_3D ( 'NONE', #103794, #182085, #102501 ) ;
#79704=EDGE_LOOP ( 'NONE', ( #78358, #97462, #68913, #242905 ) ) ;
#79715=DIRECTION ( 'NONE',  ( 0.000000000000000000, -0.2558827019433787542, 0.9667078373770204847 ) ) ;
#79734=AXIS2_PLACEMENT_3D ( 'NONE', #115465, #174209, #32109 ) ;
#79749=CARTESIAN_POINT ( 'NONE',  ( 22.47071067811864964, 65.11488425470513164, -243.2801022963548689 ) ) ;
#79768=CARTESIAN_POINT ( 'NONE',  ( -23.25000000000000000, 70.22889768795992893, -198.1282601183952750 ) ) ;
#79809=DIRECTION ( 'NONE',  ( 0.000000000000000000, 0.2617529984165025692, 0.9651348961777157509 ) ) ;
#79810=CARTESIAN_POINT ( 'NONE',  ( -23.15000000000000213, 76.00000000001126921, -203.5231074845248997 ) ) ;
#79821=AXIS2_PLACEMENT_3D ( 'NONE', #228309, #246565, #28865 ) ;
#79834=CARTESIAN_POINT ( 'NONE',  ( 19.83283456528360489, 62.39550153346884542, -208.7959266056268461 ) ) ;
#79846=CARTESIAN_POINT ( 'NONE',  ( 21.05000000000000071, 60.15342460706035865, -221.3466381063981032 ) ) ;
#79863=EDGE_CURVE ( 'NONE', #35438, #121064, #31973, .T. ) ;
#79885=DIRECTION ( 'NONE',  ( 1.000000000000000000, 0.000000000000000000, 0.000000000000000000 ) ) ;
#79914=EDGE_LOOP ( 'NONE', ( #85784, #179058, #88520, #210265 ) ) ;
#79915=ORIENTED_EDGE ( 'NONE', *, *, #96991, .F. ) ;
#79922=EDGE_CURVE ( 'NONE', #234918, #228033, #114758, .T. ) ;
#79973=ADVANCED_FACE ( 'NONE', ( #151339 ), #150051, .T. ) ;
#79980=CARTESIAN_POINT ( 'NONE',  ( -23.15000000000000213, 59.07123845373075710, -221.0531397865252075 ) ) ;
#79984=DIRECTION ( 'NONE',  ( -0.000000000000000000, -0.2617529984165031243, -0.9651348961777157509 ) ) ;
#79990=DIRECTION ( 'NONE',  ( -1.000000000000000000, 0.000000000000000000, 0.000000000000000000 ) ) ;
#79993=AXIS2_PLACEMENT_3D ( 'NONE', #16611, #111849, #171854 ) ;
#80004=ORIENTED_EDGE ( 'NONE', *, *, #198860, .F. ) ;
#80035=ORIENTED_EDGE ( 'NONE', *, *, #101479, .F. ) ;
#80044=DIRECTION ( 'NONE',  ( -1.836970198721029934E-16, -0.9651348961777157509, 0.2617529984165031243 ) ) ;
#80083=ORIENTED_EDGE ( 'NONE', *, *, #112848, .T. ) ;
#80099=ADVANCED_FACE ( 'NONE', ( #201998 ), #237279, .F. ) ;
#80129=DIRECTION ( 'NONE',  ( -1.836970198721029934E-16, -0.9651348961777157509, 0.2617529984165031243 ) ) ;
#80133=DIRECTION ( 'NONE',  ( 1.000000000000000000, 0.000000000000000000, 0.000000000000000000 ) ) ;
#80144=CIRCLE ( 'NONE', #63422, 0.09999999999999935330 ) ;
#80169=EDGE_CURVE ( 'NONE', #27906, #18097, #65048, .T. ) ;
#80219=DIRECTION ( 'NONE',  ( -2.428612866367309808E-13, 0.4099100576505548821, 0.9121259477928028714 ) ) ;
#80285=ADVANCED_FACE ( 'NONE', ( #212282 ), #36634, .F. ) ;
#80352=AXIS2_PLACEMENT_3D ( 'NONE', #139563, #19649, #18354 ) ;
#80369=CARTESIAN_POINT ( 'NONE',  ( 21.30000000000002558, 67.23127455305841238, -235.8551265064783991 ) ) ;
#80407=FACE_OUTER_BOUND ( 'NONE', #231228, .T. ) ;
#80424=CIRCLE ( 'NONE', #138866, 0.1999999999999987899 ) ;
#80465=B_SPLINE_CURVE_WITH_KNOTS ( 'NONE', 3,
 ( #163842, #162572, #202954, #221222, #178293, #42604 ),
 .UNSPECIFIED., .F., .F.,
 ( 4, 2, 4 ),
 ( 0.000000000000000000, 0.0001496588209255873239, 0.0002993176418511746479 ),
 .UNSPECIFIED. ) ;
#80487=CARTESIAN_POINT ( 'NONE',  ( 18.31572054635522306, 87.00872412986319659, -199.4107252354332616 ) ) ;
#80490=DIRECTION ( 'NONE',  ( 1.000000000000000000, 0.000000000000000000, 0.000000000000000000 ) ) ;
#80507=DIRECTION ( 'NONE',  ( 0.000000000000000000, 0.2617529984165152257, 0.9651348961777124202 ) ) ;
#80508=VECTOR ( 'NONE', #168225, 1000.000000000000114 ) ;
#80520=EDGE_CURVE ( 'NONE', #110463, #51771, #119825, .T. ) ;
#80533=DIRECTION ( 'NONE',  ( -1.000000000000000000, -0.000000000000000000, -0.000000000000000000 ) ) ;
#80561=ORIENTED_EDGE ( 'NONE', *, *, #70809, .T. ) ;
#80564=CARTESIAN_POINT ( 'NONE',  ( 18.60000000000000142, 78.21362219944482774, -231.2727646510690249 ) ) ;
#80577=LINE ( 'NONE', #19358, #106534 ) ;
#80586=AXIS2_PLACEMENT_3D ( 'NONE', #65307, #141014, #79715 ) ;
#80590=EDGE_LOOP ( 'NONE', ( #228126, #16161, #39967, #184037 ) ) ;
#80604=CARTESIAN_POINT ( 'NONE',  ( 18.59999999999999076, 70.22889768795992893, -198.1282601183952750 ) ) ;
#80613=EDGE_LOOP ( 'NONE', ( #10596, #43386, #125595, #250018 ) ) ;
#80618=EDGE_CURVE ( 'NONE', #216635, #151423, #7365, .T. ) ;
#80638=CARTESIAN_POINT ( 'NONE',  ( 20.94999999999999574, 60.83337574417771521, -225.3422414619149095 ) ) ;
#80670=AXIS2_PLACEMENT_3D ( 'NONE', #132467, #115459, #175468 ) ;
#80674=EDGE_CURVE ( 'NONE', #46658, #15410, #195016, .T. ) ;
#80678=ORIENTED_EDGE ( 'NONE', *, *, #31768, .F. ) ;
#80687=CARTESIAN_POINT ( 'NONE',  ( 21.05000000000000071, 58.86929801030535714, -225.7185417581880529 ) ) ;
#80745=PLANE ( 'NONE',  #84399 ) ;
#80775=DIRECTION ( 'NONE',  ( -0.000000000000000000, -0.2617529984165031243, -0.9651348961777157509 ) ) ;
#80777=AXIS2_PLACEMENT_3D ( 'NONE', #256512, #54524, #33733 ) ;
#80789=ORIENTED_EDGE ( 'NONE', *, *, #75082, .F. ) ;
#80793=ADVANCED_FACE ( 'NONE', ( #182805 ), #100639, .T. ) ;
#80828=AXIS2_PLACEMENT_3D ( 'NONE', #63918, #224263, #209510 ) ;
#80849=FACE_OUTER_BOUND ( 'NONE', #184994, .T. ) ;
#80894=AXIS2_PLACEMENT_3D ( 'NONE', #62493, #13737, #127596 ) ;
#80909=DIRECTION ( 'NONE',  ( -0.000000000000000000, 0.2617529984165031243, 0.9651348961777157509 ) ) ;
#80913=ORIENTED_EDGE ( 'NONE', *, *, #172473, .F. ) ;
#80993=CYLINDRICAL_SURFACE ( 'NONE', #40462, 11.79999999999999361 ) ;
#81010=ORIENTED_EDGE ( 'NONE', *, *, #9939, .F. ) ;
#81026=DIRECTION ( 'NONE',  ( 0.000000000000000000, 0.2617529984165031243, 0.9651348961777157509 ) ) ;
#81059=DIRECTION ( 'NONE',  ( 0.000000000000000000, -0.7035695228903323661, -0.7106264324241465813 ) ) ;
#81081=DIRECTION ( 'NONE',  ( 3.265361837132813093E-16, 0.9651348961777157509, -0.2617529984165031243 ) ) ;
#81097=ORIENTED_EDGE ( 'NONE', *, *, #112206, .T. ) ;
#81122=EDGE_CURVE ( 'NONE', #162715, #43706, #157813, .T. ) ;
#81126=CARTESIAN_POINT ( 'NONE',  ( 19.75857864376269291, 62.39550153362034024, -208.7959266050682459 ) ) ;
#81130=EDGE_CURVE ( 'NONE', #122630, #53814, #178646, .T. ) ;
#81140=ADVANCED_FACE ( 'NONE', ( #221574 ), #95222, .F. ) ;
#81173=VERTEX_POINT ( 'NONE', #181210 ) ;
#81214=AXIS2_PLACEMENT_3D ( 'NONE', #255309, #59705, #235792 ) ;
#81228=DIRECTION ( 'NONE',  ( 1.000000000000000000, 0.000000000000000000, 0.000000000000000000 ) ) ;
#81240=AXIS2_PLACEMENT_3D ( 'NONE', #32526, #247683, #169473 ) ;
#81260=AXIS2_PLACEMENT_3D ( 'NONE', #224954, #120772, #46325 ) ;
#81283=CARTESIAN_POINT ( 'NONE',  ( -22.42253884134832020, 64.18009035189511735, -247.0980616929964242 ) ) ;
#81286=CARTESIAN_POINT ( 'NONE',  ( 21.05000000000000426, 65.59652053147743800, -241.9470453418952900 ) ) ;
#81294=CARTESIAN_POINT ( 'NONE',  ( -20.93975676684922504, 67.49344847133114911, -195.4961807846321733 ) ) ;
#81298=CARTESIAN_POINT ( 'NONE',  ( -21.45000000000000284, 65.35370752038342346, -213.3282663891675952 ) ) ;
#81324=EDGE_LOOP ( 'NONE', ( #55634, #1965, #136923, #165781, #14214, #510, #32460, #134907, #231049, #63062, #173407 ) ) ;
#81333=PLANE ( 'NONE',  #94990 ) ;
#81367=DIRECTION ( 'NONE',  ( 0.000000000000000000, 0.2617529984165034573, 0.9651348961777156399 ) ) ;
#81369=CARTESIAN_POINT ( 'NONE',  ( -18.50000000000000000, 67.23127455305841238, -235.8551265064783991 ) ) ;
#81382=CARTESIAN_POINT ( 'NONE',  ( 20.88420186297724257, 67.49234744263520724, -195.4268335588911611 ) ) ;
#81393=VERTEX_POINT ( 'NONE', #250154 ) ;
#81401=CARTESIAN_POINT ( 'NONE',  ( 21.14999999999999858, 61.98366251160864238, -221.6357896648344195 ) ) ;
#81421=CARTESIAN_POINT ( 'NONE',  ( -20.54999999999999716, 78.50726470275243685, -228.6618886302502176 ) ) ;
#81433=ORIENTED_EDGE ( 'NONE', *, *, #180410, .F. ) ;
#81485=CARTESIAN_POINT ( 'NONE',  ( 23.24999999999999289, 67.55989888862310977, -211.9120700681549465 ) ) ;
#81557=ORIENTED_EDGE ( 'NONE', *, *, #194139, .F. ) ;
#81592=ORIENTED_EDGE ( 'NONE', *, *, #256793, .T. ) ;
#81604=CYLINDRICAL_SURFACE ( 'NONE', #81761, 0.09999999999999935330 ) ;
#81620=ORIENTED_EDGE ( 'NONE', *, *, #87605, .F. ) ;
#81628=ORIENTED_EDGE ( 'NONE', *, *, #212877, .T. ) ;
#81660=CARTESIAN_POINT ( 'NONE',  ( -23.15000000000000213, 52.81534179157633702, -244.1198638051726277 ) ) ;
#81681=CARTESIAN_POINT ( 'NONE',  ( 18.52165635395197185, 78.22063626114007207, -231.5569302423936335 ) ) ;
#81725=DIRECTION ( 'NONE',  ( 0.000000000000000000, 0.2558827019433787542, -0.9667078373770204847 ) ) ;
#81761=AXIS2_PLACEMENT_3D ( 'NONE', #58208, #38673, #240726 ) ;
#81764=CYLINDRICAL_SURFACE ( 'NONE', #111965, 0.1000000000000124678 ) ;
#81778=B_SPLINE_CURVE_WITH_KNOTS ( 'NONE', 3,
 ( #191885, #129311, #14528, #112331, #232289, #168488, #48481, #70655, #207582, #53631, #113600, #211419, #130582, #92738, #251821, #212712, #151463, #73221, #34105, #208850, #150176, #133167 ),
 .UNSPECIFIED., .F., .F.,
 ( 4, 3, 3, 3, 3, 3, 3, 4 ),
 ( 0.000000000000000000, 7.307836821082208987E-06, 4.161455748548728312E-05, 7.576591810647690176E-05, 0.0001098090429817481030, 0.0001438003617351081207, 0.0001777914035423621027, 0.0002117966137402666057 ),
 .UNSPECIFIED. ) ;
#81807=LINE ( 'NONE', #161405, #139670 ) ;
#81814=AXIS2_PLACEMENT_3D ( 'NONE', #199586, #60026, #5171 ) ;
#81815=CARTESIAN_POINT ( 'NONE',  ( -21.64999999999999858, 63.34400729675436281, -222.1083394899400503 ) ) ;
#81821=ORIENTED_EDGE ( 'NONE', *, *, #103532, .F. ) ;
#81838=CARTESIAN_POINT ( 'NONE',  ( -21.05000000000000071, 76.00000000001126921, -203.5231074845248997 ) ) ;
#81854=CARTESIAN_POINT ( 'NONE',  ( -22.00411653889203834, 65.23707900167231344, -242.8297538143244481 ) ) ;
#81875=VECTOR ( 'NONE', #36872, 1000.000000000000000 ) ;
#81924=DIRECTION ( 'NONE',  ( 0.7071067811865474617, -0.6824534298470372740, 0.1850873201762209819 ) ) ;
#81945=ORIENTED_EDGE ( 'NONE', *, *, #145996, .T. ) ;
#81954=CARTESIAN_POINT ( 'NONE',  ( 20.95512820512820085, 58.98414156600839675, -225.6766266970810193 ) ) ;
#81961=ORIENTED_EDGE ( 'NONE', *, *, #7633, .T. ) ;
#81980=DIRECTION ( 'NONE',  ( 0.000000000000000000, -0.9651348961777157509, 0.2617529984165031243 ) ) ;
#82027=CARTESIAN_POINT ( 'NONE',  ( -20.94999999999999929, 86.30329675166747450, -209.4258251677035787 ) ) ;
#82048=AXIS2_PLACEMENT_3D ( 'NONE', #163414, #242932, #223363 ) ;
#82087=CARTESIAN_POINT ( 'NONE',  ( -20.54999999999999716, 67.23127455305841238, -235.8551265064783991 ) ) ;
#82104=ORIENTED_EDGE ( 'NONE', *, *, #164073, .F. ) ;
#82111=AXIS2_PLACEMENT_3D ( 'NONE', #224654, #51135, #108573 ) ;
#82116=VERTEX_POINT ( 'NONE', #46176 ) ;
#82124=DIRECTION ( 'NONE',  ( 1.000000000000000000, 0.000000000000000000, 0.000000000000000000 ) ) ;
#82125=VERTEX_POINT ( 'NONE', #86565 ) ;
#82181=EDGE_LOOP ( 'NONE', ( #254038, #185214, #91899, #189670 ) ) ;
#82184=CARTESIAN_POINT ( 'NONE',  ( 18.39999999999999858, 78.24390740893980478, -231.6169762517609172 ) ) ;
#82190=ADVANCED_FACE ( 'NONE', ( #121886 ), #116454, .F. ) ;
#82198=DIRECTION ( 'NONE',  ( -1.000000000000000000, 3.151514657663852580E-16, -8.547182517843351137E-17 ) ) ;
#82210=CARTESIAN_POINT ( 'NONE',  ( 21.04999999999908411, 61.94334680800506732, -221.8238859006714279 ) ) ;
#82213=DIRECTION ( 'NONE',  ( 1.000000000000000000, 0.000000000000000000, 0.000000000000000000 ) ) ;
#82218=FACE_OUTER_BOUND ( 'NONE', #158466, .T. ) ;
#82256=EDGE_LOOP ( 'NONE', ( #229246, #233239, #47079, #102173 ) ) ;
#82285=EDGE_CURVE ( 'NONE', #88353, #135481, #25073, .T. ) ;
#82339=DIRECTION ( 'NONE',  ( 0.000000000000000000, -0.2617529984165031243, -0.9651348961777157509 ) ) ;
#82348=DIRECTION ( 'NONE',  ( 0.000000000000000000, 0.2617529984165028467, 0.9651348961777159730 ) ) ;
#82364=ORIENTED_EDGE ( 'NONE', *, *, #228860, .F. ) ;
#82404=CIRCLE ( 'NONE', #24771, 4.150000000000003020 ) ;
#82408=CARTESIAN_POINT ( 'NONE',  ( 21.14999999999999858, 60.09787988008870485, -221.2279614330287245 ) ) ;
#82442=ORIENTED_EDGE ( 'NONE', *, *, #75838, .T. ) ;
#82461=ORIENTED_EDGE ( 'NONE', *, *, #109401, .T. ) ;
#82474=LINE ( 'NONE', #50741, #26383 ) ;
#82519=VERTEX_POINT ( 'NONE', #124154 ) ;
#82523=EDGE_LOOP ( 'NONE', ( #133063, #21287, #89815, #100154 ) ) ;
#82527=DIRECTION ( 'NONE',  ( 0.000000000000000000, -0.9651348961777053148, 0.2617529984165415380 ) ) ;
#82529=ORIENTED_EDGE ( 'NONE', *, *, #236152, .F. ) ;
#82532=TOROIDAL_SURFACE ( 'NONE', #7554, 11.90000000000000391, 0.1000000000000000056 ) ;
#82567=CARTESIAN_POINT ( 'NONE',  ( 21.05000000000000071, 65.61575147395463148, -242.1939180743342774 ) ) ;
#82572=DIRECTION ( 'NONE',  ( 0.000000000000000000, -0.9651348961777157509, 0.2617529984165031243 ) ) ;
#82573=EDGE_CURVE ( 'NONE', #73566, #82125, #209781, .T. ) ;
#82582=DIRECTION ( 'NONE',  ( -2.561896900575096011E-15, 0.3589373870825449120, -0.9333616406058026227 ) ) ;
#82586=CARTESIAN_POINT ( 'NONE',  ( -22.50000000000000000, 67.23127455305841238, -235.8551265064783991 ) ) ;
#82590=DIRECTION ( 'NONE',  ( 1.000000000000000000, 0.000000000000000000, 0.000000000000000000 ) ) ;
#82654=DIRECTION ( 'NONE',  ( 0.000000000000000000, -0.2617529984165034573, -0.9651348961777156399 ) ) ;
#82656=EDGE_CURVE ( 'NONE', #217285, #40334, #137620, .T. ) ;
#82668=CARTESIAN_POINT ( 'NONE',  ( 20.94403535211772294, 67.49374512151688066, -195.5131169347613991 ) ) ;
#82674=CIRCLE ( 'NONE', #3590, 0.5000000000000014433 ) ;
#82677=FACE_OUTER_BOUND ( 'NONE', #108682, .T. ) ;
#82683=CARTESIAN_POINT ( 'NONE',  ( 21.05000000000000071, 72.02722222756959525, -225.1832529173024398 ) ) ;
#82700=FACE_OUTER_BOUND ( 'NONE', #23573, .T. ) ;
#82738=DIRECTION ( 'NONE',  ( 0.000000000000000000, -0.9651348961777157509, 0.2617529984165031243 ) ) ;
#82753=CARTESIAN_POINT ( 'NONE',  ( 21.30000000000002558, 67.23127455305841238, -235.8551265064783991 ) ) ;
#82770=CARTESIAN_POINT ( 'NONE',  ( -18.46907102845853643, 86.89089698701586428, -199.5596099339830971 ) ) ;
#82831=CARTESIAN_POINT ( 'NONE',  ( -23.25000000000000000, 52.81534179157633702, -244.1198638051726277 ) ) ;
#82833=CIRCLE ( 'NONE', #116216, 4.300000000000033573 ) ;
#82840=CARTESIAN_POINT ( 'NONE',  ( -21.14999999999999858, 78.47509609352879068, -238.9045489380306435 ) ) ;
#82845=CARTESIAN_POINT ( 'NONE',  ( 21.05000000000000071, 65.49889199258218753, -241.8691648588935266 ) ) ;
#82855=CYLINDRICAL_SURFACE ( 'NONE', #81260, 2.000000000000013323 ) ;
#82869=EDGE_CURVE ( 'NONE', #92030, #209902, #89484, .T. ) ;
#82894=ADVANCED_FACE ( 'NONE', ( #248570 ), #233358, .F. ) ;
#82941=AXIS2_PLACEMENT_3D ( 'NONE', #25044, #146232, #5420 ) ;
#82961=EDGE_LOOP ( 'NONE', ( #85980, #104811, #212286, #150684 ) ) ;
#82970=FACE_OUTER_BOUND ( 'NONE', #6969, .T. ) ;
#83027=EDGE_CURVE ( 'NONE', #197069, #204834, #137814, .T. ) ;
#83126=EDGE_LOOP ( 'NONE', ( #14244, #131605, #32771, #129811 ) ) ;
#83156=CIRCLE ( 'NONE', #199752, 0.1000000000000124678 ) ;
#83170=ORIENTED_EDGE ( 'NONE', *, *, #44679, .F. ) ;
#83200=ORIENTED_EDGE ( 'NONE', *, *, #200928, .F. ) ;
#83220=CARTESIAN_POINT ( 'NONE',  ( 20.94999999999999929, 63.43511439055885148, -224.4466865888566360 ) ) ;
#83222=DIRECTION ( 'NONE',  ( 0.000000000000000000, -0.2617529984165023471, -0.9651348961777159730 ) ) ;
#83243=DIRECTION ( 'NONE',  ( -0.000000000000000000, 0.9651348961777158619, -0.2617529984165031243 ) ) ;
#83297=DIRECTION ( 'NONE',  ( 1.000000000000000000, 0.000000000000000000, 0.000000000000000000 ) ) ;
#83298=DIRECTION ( 'NONE',  ( 1.000000000000000000, 0.000000000000000000, 0.000000000000000000 ) ) ;
#83312=LINE ( 'NONE', #82027, #242554 ) ;
#83323=CYLINDRICAL_SURFACE ( 'NONE', #111041, 11.75000000000000178 ) ;
#83330=LINE ( 'NONE', #178649, #160462 ) ;
#83375=DIRECTION ( 'NONE',  ( -1.000000000000000000, -0.000000000000000000, -0.000000000000000000 ) ) ;
#83421=EDGE_LOOP ( 'NONE', ( #145863, #201023, #184788, #244538, #57010 ) ) ;
#83462=CARTESIAN_POINT ( 'NONE',  ( -23.15000000000000213, 78.47509609352879068, -238.9045489380306435 ) ) ;
#83468=CARTESIAN_POINT ( 'NONE',  ( 18.54116936837188234, 78.20986773458183450, -231.5294484859616375 ) ) ;
#83471=EDGE_CURVE ( 'NONE', #159456, #130340, #20772, .T. ) ;
#83479=DIRECTION ( 'NONE',  ( -1.000000000000000000, 3.151514657663852580E-16, -8.547182517843351137E-17 ) ) ;
#83491=AXIS2_PLACEMENT_3D ( 'NONE', #210451, #207894, #189601 ) ;
#83530=DIRECTION ( 'NONE',  ( 1.000000000000000000, -2.849773892568378313E-16, 7.728835255496647986E-17 ) ) ;
#83584=CIRCLE ( 'NONE', #141864, 0.1000000000000047656 ) ;
#83654=ORIENTED_EDGE ( 'NONE', *, *, #120412, .T. ) ;
#83661=CIRCLE ( 'NONE', #212717, 0.1000000000000124678 ) ;
#83678=DIRECTION ( 'NONE',  ( -1.000000000000000000, -0.000000000000000000, 0.000000000000000000 ) ) ;
#83689=AXIS2_PLACEMENT_3D ( 'NONE', #239271, #4492, #243113 ) ;
#83699=( BOUNDED_SURFACE ( )  B_SPLINE_SURFACE ( 3, 2, ( 
 ( #123572, #201818, #61017 ),
 ( #199266, #20639, #200537 ),
 ( #137978, #101384, #143111 ),
 ( #179708, #1017, #220107 ) ),
 .UNSPECIFIED., .F., .F., .T. ) 
 B_SPLINE_SURFACE_WITH_KNOTS ( ( 4, 4 ),
 ( 3, 3 ),
 ( 0.04058434257139476031, 0.04256401539001600232 ),
 ( 0.000000000000000000, 1.000000000000000000 ),
 .UNSPECIFIED. ) 
 GEOMETRIC_REPRESENTATION_ITEM ( )  RATIONAL_B_SPLINE_SURFACE ( (
 ( 1.000000000000000000, 0.7103081912008184506, 1.000000000000000000),
 ( 1.000000000000000000, 0.7104998333554868317, 1.000000000000000000),
 ( 1.000000000000000000, 0.7107238315755806113, 1.000000000000000000),
 ( 1.000000000000000000, 0.7110073749539497223, 1.000000000000000000) ) ) 
 REPRESENTATION_ITEM ( '' )  SURFACE ( )  );
#83711=CARTESIAN_POINT ( 'NONE',  ( -18.59999999999999787, 70.22659352830977753, -197.9852579278363578 ) ) ;
#83754=EDGE_CURVE ( 'NONE', #29044, #233526, #81778, .T. ) ;
#83760=ORIENTED_EDGE ( 'NONE', *, *, #106822, .T. ) ;
#83782=ORIENTED_EDGE ( 'NONE', *, *, #218707, .F. ) ;
#83812=EDGE_CURVE ( 'NONE', #4584, #150591, #29340, .T. ) ;
#83821=FACE_OUTER_BOUND ( 'NONE', #87902, .T. ) ;
#83825=DIRECTION ( 'NONE',  ( 0.000000000000000000, -0.9667078373770112698, -0.2558827019434132821 ) ) ;
#83849=EDGE_CURVE ( 'NONE', #49363, #36582, #79167, .T. ) ;
#83851=CARTESIAN_POINT ( 'NONE',  ( -20.87600722750343252, 67.49230083716666684, -195.4236814984208763 ) ) ;
#83858=AXIS2_PLACEMENT_3D ( 'NONE', #183012, #242957, #43491 ) ;
#83867=CARTESIAN_POINT ( 'NONE',  ( -20.64999999999999858, 78.89331866122350334, -228.7665898296168052 ) ) ;
#83910=DIRECTION ( 'NONE',  ( 0.000000000000000000, -0.2617529984164955192, -0.9651348961777178603 ) ) ;
#83933=ORIENTED_EDGE ( 'NONE', *, *, #37178, .T. ) ;
#83943=CARTESIAN_POINT ( 'NONE',  ( 21.00000000000000000, 63.38346053167636995, -212.7939182281409956 ) ) ;
#83949=CIRCLE ( 'NONE', #229745, 4.149999999999999467 ) ;
#83969=DIRECTION ( 'NONE',  ( 0.000000000000000000, -0.2617529984164915779, -0.9651348961777189706 ) ) ;
#83982=AXIS2_PLACEMENT_3D ( 'NONE', #69638, #110026, #210434 ) ;
#84030=DIRECTION ( 'NONE',  ( 0.000000000000000000, -0.2617529984165031243, -0.9651348961777157509 ) ) ;
#84050=VECTOR ( 'NONE', #563, 1000.000000000000000 ) ;
#84055=EDGE_CURVE ( 'NONE', #61516, #6907, #10359, .T. ) ;
#84076=ADVANCED_FACE ( 'NONE', ( #49470 ), #69053, .T. ) ;
#84079=CYLINDRICAL_SURFACE ( 'NONE', #172089, 7.900000000000010125 ) ;
#84089=DIRECTION ( 'NONE',  ( -2.952720810173289112E-16, -0.9651348961777157509, 0.2617529984165031243 ) ) ;
#84091=CARTESIAN_POINT ( 'NONE',  ( 21.30000000000002558, 67.23127455305841238, -235.8551265064783991 ) ) ;
#84124=ORIENTED_EDGE ( 'NONE', *, *, #168996, .T. ) ;
#84134=ORIENTED_EDGE ( 'NONE', *, *, #37874, .T. ) ;
#84136=DIRECTION ( 'NONE',  ( 0.000000000000000000, 0.2617529984165026247, 0.9651348961777158619 ) ) ;
#84167=EDGE_LOOP ( 'NONE', ( #197826, #43934, #246599, #137802 ) ) ;
#84186=CARTESIAN_POINT ( 'NONE',  ( 21.05000000000000071, 61.00122447389660607, -225.2976766370351527 ) ) ;
#84200=TOROIDAL_SURFACE ( 'NONE', #230008, 6.258578643762712446, 0.1000000000000000056 ) ;
#84218=EDGE_CURVE ( 'NONE', #144320, #155936, #197947, .T. ) ;
#84226=DIRECTION ( 'NONE',  ( 1.000000000000000000, -7.049440681616512959E-16, 1.911869773728117674E-16 ) ) ;
#84229=CARTESIAN_POINT ( 'NONE',  ( 18.50000000000000355, 78.21986117685452200, -231.3317312752311068 ) ) ;
#84306=PRODUCT_DEFINITION_CONTEXT ( 'detailed design', #10884, 'design' ) ;
#84318=VERTEX_POINT ( 'NONE', #162696 ) ;
#84344=DIRECTION ( 'NONE',  ( 0.000000000000000000, 0.2617529984164856383, 0.9651348961777204138 ) ) ;
#84356=LINE ( 'NONE', #140523, #226989 ) ;
#84395=VERTEX_POINT ( 'NONE', #204365 ) ;
#84397=AXIS2_PLACEMENT_3D ( 'NONE', #133638, #80044, #20124 ) ;
#84399=AXIS2_PLACEMENT_3D ( 'NONE', #140739, #255500, #179886 ) ;
#84408=CARTESIAN_POINT ( 'NONE',  ( 22.50000000000000000, 55.96169194136206215, -232.9023299069559130 ) ) ;
#84469=ADVANCED_FACE ( 'NONE', ( #194785 ), #71310, .F. ) ;
#84472=CARTESIAN_POINT ( 'NONE',  ( 20.94999999999999929, 76.00000000001126921, -203.5231074845248997 ) ) ;
#84493=ORIENTED_EDGE ( 'NONE', *, *, #43314, .T. ) ;
#84498=ORIENTED_EDGE ( 'NONE', *, *, #201783, .T. ) ;
#84512=VERTEX_POINT ( 'NONE', #95647 ) ;
#84517=DIRECTION ( 'NONE',  ( 0.000000000000000000, 0.2617529984165031243, 0.9651348961777157509 ) ) ;
#84518=AXIS2_PLACEMENT_3D ( 'NONE', #201912, #104066, #140645 ) ;
#84528=VERTEX_POINT ( 'NONE', #126103 ) ;
#84552=CARTESIAN_POINT ( 'NONE',  ( 21.04999999999999716, 61.94813849985776244, -221.8062180090915376 ) ) ;
#84595=EDGE_CURVE ( 'NONE', #145620, #61360, #86965, .T. ) ;
#84598=AXIS2_PLACEMENT_3D ( 'NONE', #90542, #247044, #170137 ) ;
#84630=CARTESIAN_POINT ( 'NONE',  ( -23.15000000000000213, 66.33592547490526670, -222.9197737850312251 ) ) ;
#84661=CARTESIAN_POINT ( 'NONE',  ( -21.05000000000000071, 68.48451787451661232, -224.2224406095231757 ) ) ;
#84677=ADVANCED_FACE ( 'NONE', ( #176498 ), #196249, .F. ) ;
#84690=LINE ( 'NONE', #221654, #10891 ) ;
#84691=TOROIDAL_SURFACE ( 'NONE', #176335, 7.791421356237335338, 0.1000000000000000056 ) ;
#84730=EDGE_CURVE ( 'NONE', #231688, #177774, #38263, .T. ) ;
#84746=ORIENTED_EDGE ( 'NONE', *, *, #76144, .F. ) ;
#84810=( BOUNDED_CURVE ( )  B_SPLINE_CURVE ( 3, ( #77405, #196098, #60420, #199960 ),
 .UNSPECIFIED., .F., .F. ) 
 B_SPLINE_CURVE_WITH_KNOTS ( ( 4, 4 ),
 ( 4.712388980384690562, 6.283185307179586232 ),
 .UNSPECIFIED. ) 
 CURVE ( )  GEOMETRIC_REPRESENTATION_ITEM ( )  RATIONAL_B_SPLINE_CURVE ( ( 1.000000000000000000, 0.8047378541243652705, 0.8047378541243652705, 1.000000000000000000 ) ) 
 REPRESENTATION_ITEM ( '' )  );
#84833=LINE ( 'NONE', #124013, #183912 ) ;
#84835=DIRECTION ( 'NONE',  ( 0.000000000000000000, -0.2617529984165031243, -0.9651348961777158619 ) ) ;
#84906=VECTOR ( 'NONE', #18360, 1000.000000000000000 ) ;
#84922=ORIENTED_EDGE ( 'NONE', *, *, #84730, .F. ) ;
#84947=CARTESIAN_POINT ( 'NONE',  ( -21.05000000000000071, 62.99095723518624368, -207.1734234082435364 ) ) ;
#84948=ORIENTED_EDGE ( 'NONE', *, *, #36449, .T. ) ;
#84977=AXIS2_PLACEMENT_3D ( 'NONE', #222177, #106083, #141377 ) ;
#84994=ORIENTED_EDGE ( 'NONE', *, *, #12267, .T. ) ;
#85013=CARTESIAN_POINT ( 'NONE',  ( 20.94999999999999574, 79.23417978893664326, -236.1056577391152587 ) ) ;
#85019=CARTESIAN_POINT ( 'NONE',  ( 21.05000000000000071, 76.00000000001126921, -203.5231074845248997 ) ) ;
#85050=DIRECTION ( 'NONE',  ( 0.000000000000000000, 0.2617529984165032908, 0.9651348961777156399 ) ) ;
#85059=LINE ( 'NONE', #244155, #239839 ) ;
#85067=CARTESIAN_POINT ( 'NONE',  ( 18.49999999999999645, 76.00000000001126921, -203.5231074845248997 ) ) ;
#85091=DIRECTION ( 'NONE',  ( 0.000000000000000000, 0.2617529984165030132, 0.9651348961777157509 ) ) ;
#85111=CARTESIAN_POINT ( 'NONE',  ( -23.15000000000000213, 66.21323668544584962, -222.9901119748073484 ) ) ;
#85149=ORIENTED_EDGE ( 'NONE', *, *, #52920, .T. ) ;
#85152=CIRCLE ( 'NONE', #64353, 0.09999999999999939493 ) ;
#85159=CIRCLE ( 'NONE', #18574, 12.77500000000000391 ) ;
#85165=VERTEX_POINT ( 'NONE', #11535 ) ;
#85170=ORIENTED_EDGE ( 'NONE', *, *, #192729, .F. ) ;
#85180=CARTESIAN_POINT ( 'NONE',  ( -20.00857864376270001, 63.93636616954134411, -213.0474835168086827 ) ) ;
#85188=CARTESIAN_POINT ( 'NONE',  ( -23.15000000000000213, 86.22912497777053886, -209.4057091359527192 ) ) ;
#85198=DIRECTION ( 'NONE',  ( 0.000000000000000000, 0.2617529984165031243, 0.9651348961777157509 ) ) ;
#85210=ORIENTED_EDGE ( 'NONE', *, *, #168412, .T. ) ;
#85244=CARTESIAN_POINT ( 'NONE',  ( -18.59999996769639097, 78.14787437627062161, -231.3748811062230857 ) ) ;
#85262=DIRECTION ( 'NONE',  ( 1.000000000000000000, 0.000000000000000000, 0.000000000000000000 ) ) ;
#85322=CARTESIAN_POINT ( 'NONE',  ( 21.05000000000000071, 76.00000000001126921, -203.5231074845248997 ) ) ;
#85332=TOROIDAL_SURFACE ( 'NONE', #47925, 0.2000000000000000111, 0.1000000000000000056 ) ;
#85350=DIRECTION ( 'NONE',  ( -1.000000000000000000, 0.000000000000000000, 0.000000000000000000 ) ) ;
#85359=ORIENTED_EDGE ( 'NONE', *, *, #65866, .F. ) ;
#85363=ORIENTED_EDGE ( 'NONE', *, *, #15282, .T. ) ;
#85395=LINE ( 'NONE', #106261, #193615 ) ;
#85478=AXIS2_PLACEMENT_3D ( 'NONE', #11631, #12925, #209816 ) ;
#85483=DIRECTION ( 'NONE',  ( 0.7071067811865460184, 0.6824534298470606997, -0.1850873201761399356 ) ) ;
#85512=EDGE_CURVE ( 'NONE', #211510, #251815, #170496, .T. ) ;
#85530=VERTEX_POINT ( 'NONE', #252530 ) ;
#85544=CIRCLE ( 'NONE', #164702, 3.899999999999996803 ) ;
#85553=CARTESIAN_POINT ( 'NONE',  ( -23.15000000000000213, 67.23127455305841238, -235.8551265064783991 ) ) ;
#85561=ORIENTED_EDGE ( 'NONE', *, *, #95234, .F. ) ;
#85571=ADVANCED_FACE ( 'NONE', ( #174345 ), #113036, .T. ) ;
#85601=TOROIDAL_SURFACE ( 'NONE', #64788, 0.2000000000000000111, 0.1000000000000000056 ) ;
#85612=AXIS2_PLACEMENT_3D ( 'NONE', #36644, #135694, #176144 ) ;
#85626=ORIENTED_EDGE ( 'NONE', *, *, #213416, .F. ) ;
#85633=EDGE_CURVE ( 'NONE', #48041, #135481, #42484, .T. ) ;
#85653=TOROIDAL_SURFACE ( 'NONE', #52361, 0.2000000000000000111, 0.1000000000000000056 ) ;
#85674=DIRECTION ( 'NONE',  ( 0.000000000000000000, 0.2617529984165044565, 0.9651348961777151958 ) ) ;
#85685=VERTEX_POINT ( 'NONE', #140274 ) ;
#85701=ORIENTED_EDGE ( 'NONE', *, *, #230400, .F. ) ;
#85703=VECTOR ( 'NONE', #223738, 1000.000000000000000 ) ;
#85705=AXIS2_PLACEMENT_3D ( 'NONE', #52509, #149080, #89073 ) ;
#85744=CARTESIAN_POINT ( 'NONE',  ( 23.14999999999999858, 65.65271564877468791, -222.5736063831752176 ) ) ;
#85746=ORIENTED_EDGE ( 'NONE', *, *, #219950, .F. ) ;
#85761=CARTESIAN_POINT ( 'NONE',  ( -20.94999999999999929, 72.05339752741123505, -225.0867394276846483 ) ) ;
#85768=CYLINDRICAL_SURFACE ( 'NONE', #90621, 0.1000000000000124678 ) ;
#85774=DIRECTION ( 'NONE',  ( 0.000000000000000000, -0.2617529984165152257, -0.9651348961777124202 ) ) ;
#85784=ORIENTED_EDGE ( 'NONE', *, *, #209585, .T. ) ;
#85789=DIRECTION ( 'NONE',  ( 0.000000000000000000, -0.9229812358756199764, 0.3848449534832346086 ) ) ;
#85794=AXIS2_PLACEMENT_3D ( 'NONE', #199234, #244749, #220071 ) ;
#85803=CARTESIAN_POINT ( 'NONE',  ( 20.95262331984806181, 59.07243101476477420, -225.8083546741112571 ) ) ;
#85824=AXIS2_PLACEMENT_3D ( 'NONE', #2198, #162592, #161313 ) ;
#85847=ADVANCED_FACE ( 'NONE', ( #63316 ), #89299, .F. ) ;
#85853=CARTESIAN_POINT ( 'NONE',  ( 21.08804582317334209, 61.89529605692450076, -221.6118240886515309 ) ) ;
#85869=DIRECTION ( 'NONE',  ( 0.000000000000000000, 0.2617529984165039569, 0.9651348961777154178 ) ) ;
#85870=ORIENTED_EDGE ( 'NONE', *, *, #29459, .F. ) ;
#85920=AXIS2_PLACEMENT_3D ( 'NONE', #245258, #169612, #150023 ) ;
#85926=VERTEX_POINT ( 'NONE', #11062 ) ;
#85948=CARTESIAN_POINT ( 'NONE',  ( 23.14999999999999858, 68.28935379556426710, -213.7087130192904567 ) ) ;
#85961=ORIENTED_EDGE ( 'NONE', *, *, #194450, .T. ) ;
#85980=ORIENTED_EDGE ( 'NONE', *, *, #73458, .T. ) ;
#86012=FACE_OUTER_BOUND ( 'NONE', #249629, .T. ) ;
#86044=DIRECTION ( 'NONE',  ( 0.000000000000000000, 0.2617529984165083423, 0.9651348961777143076 ) ) ;
#86056=AXIS2_PLACEMENT_3D ( 'NONE', #138174, #61227, #255521 ) ;
#86079=ADVANCED_FACE ( 'NONE', ( #116584 ), #76158, .T. ) ;
#86098=FACE_OUTER_BOUND ( 'NONE', #102239, .T. ) ;
#86100=DIRECTION ( 'NONE',  ( 0.000000000000000000, -0.2617529984165152257, -0.9651348961777124202 ) ) ;
#86139=AXIS2_PLACEMENT_3D ( 'NONE', #156161, #37484, #212273 ) ;
#86164=DIRECTION ( 'NONE',  ( -3.265361837132813093E-16, -0.9651348961777157509, 0.2617529984165031243 ) ) ;
#86184=LINE ( 'NONE', #105745, #92799 ) ;
#86196=ORIENTED_EDGE ( 'NONE', *, *, #220936, .T. ) ;
#86199=DIRECTION ( 'NONE',  ( 1.000000000000000000, 0.000000000000000000, 0.000000000000000000 ) ) ;
#86207=DIRECTION ( 'NONE',  ( 1.000000000000000000, -0.000000000000000000, -0.000000000000000000 ) ) ;
#86221=ORIENTED_EDGE ( 'NONE', *, *, #27547, .F. ) ;
#86240=ADVANCED_FACE ( 'NONE', ( #43466 ), #46021, .F. ) ;
#86247=AXIS2_PLACEMENT_3D ( 'NONE', #122185, #222536, #161319 ) ;
#86288=AXIS2_PLACEMENT_3D ( 'NONE', #94995, #50706, #250222 ) ;
#86321=ORIENTED_EDGE ( 'NONE', *, *, #132678, .T. ) ;
#86329=CARTESIAN_POINT ( 'NONE',  ( -21.05000000000000071, 61.12590067186530973, -234.3012893943865720 ) ) ;
#86369=TOROIDAL_SURFACE ( 'NONE', #128106, 2.100000000000002309, 0.1000000000000000056 ) ;
#86392=CARTESIAN_POINT ( 'NONE',  ( -23.25000000000000000, 64.27847795353595473, -247.1247091181747066 ) ) ;
#86400=EDGE_CURVE ( 'NONE', #108241, #11008, #238690, .T. ) ;
#86433=EDGE_CURVE ( 'NONE', #42744, #212838, #34692, .T. ) ;
#86441=EDGE_CURVE ( 'NONE', #141218, #160294, #102777, .T. ) ;
#86453=EDGE_CURVE ( 'NONE', #193203, #140485, #255193, .T. ) ;
#86498=CIRCLE ( 'NONE', #19924, 0.09999999999999875655 ) ;
#86523=DIRECTION ( 'NONE',  ( 0.000000000000000000, 0.9651348961777157509, -0.2617529984165031243 ) ) ;
#86525=DIRECTION ( 'NONE',  ( 0.000000000000000000, -0.9651348961777161950, 0.2617529984165014589 ) ) ;
#86532=CARTESIAN_POINT ( 'NONE',  ( -18.58735405345341718, 87.01880836603646685, -199.4423219559112681 ) ) ;
#86536=DIRECTION ( 'NONE',  ( -0.000000000000000000, 0.2617529984165031243, 0.9651348961777157509 ) ) ;
#86539=CIRCLE ( 'NONE', #249090, 0.09999999999999939493 ) ;
#86565=CARTESIAN_POINT ( 'NONE',  ( -22.47071067811865319, 59.75442326890419764, -233.9300113800878762 ) ) ;
#86596=CIRCLE ( 'NONE', #65776, 0.09999999999999939493 ) ;
#86633=ORIENTED_EDGE ( 'NONE', *, *, #153604, .T. ) ;
#86652=AXIS2_PLACEMENT_3D ( 'NONE', #166972, #168263, #160849 ) ;
#86654=EDGE_CURVE ( 'NONE', #52, #189967, #130528, .T. ) ;
#86662=DIRECTION ( 'NONE',  ( 0.000000000000000000, -0.9651348961777157509, 0.2617529984165031243 ) ) ;
#86690=DIRECTION ( 'NONE',  ( -1.000000000000000000, -0.000000000000000000, -0.000000000000000000 ) ) ;
#86695=AXIS2_PLACEMENT_3D ( 'NONE', #160783, #98169, #1659 ) ;
#86701=CARTESIAN_POINT ( 'NONE',  ( 19.99999999999998934, 61.47936603916259202, -212.1738987416902376 ) ) ;
#86715=CARTESIAN_POINT ( 'NONE',  ( -23.15000000000000213, 66.45861426436469799, -222.8494355952551018 ) ) ;
#86722=CIRCLE ( 'NONE', #95134, 0.1000000000000105804 ) ;
#86748=ORIENTED_EDGE ( 'NONE', *, *, #114301, .T. ) ;
#86792=CARTESIAN_POINT ( 'NONE',  ( -21.05000000000000071, 78.47509609352879068, -238.9045489380306435 ) ) ;
#86834=DIRECTION ( 'NONE',  ( -1.000000000000000000, 3.151514657663852580E-16, -8.547182517843351137E-17 ) ) ;
#86836=CARTESIAN_POINT ( 'NONE',  ( 18.49999999999999645, 62.13039908340535078, -248.0610840288475174 ) ) ;
#86839=CARTESIAN_POINT ( 'NONE',  ( 21.00000000000000000, 61.02768354592784306, -221.4801322937404393 ) ) ;
#86841=DIRECTION ( 'NONE',  ( -1.000000000000000000, -0.000000000000000000, 0.000000000000000000 ) ) ;
#86845=DIRECTION ( 'NONE',  ( 0.000000000000000000, 0.2617529984165152257, 0.9651348961777124202 ) ) ;
#86850=CIRCLE ( 'NONE', #182578, 0.09999999999999123479 ) ;
#86870=DIRECTION ( 'NONE',  ( 1.000000000000000000, 0.000000000000000000, 0.000000000000000000 ) ) ;
#86925=AXIS2_PLACEMENT_3D ( 'NONE', #4114, #82339, #2820 ) ;
#86935=CARTESIAN_POINT ( 'NONE',  ( -21.05000000000000071, 68.11887992016828264, -227.8068560890360175 ) ) ;
#86939=CARTESIAN_POINT ( 'NONE',  ( -23.25000000000000000, 82.09643798151613225, -215.4278993322501208 ) ) ;
#86949=DIRECTION ( 'NONE',  ( -0.7071067811865460184, -0.6824534298470606997, 0.1850873201761399356 ) ) ;
#86965=LINE ( 'NONE', #107840, #117159 ) ;
#86984=CARTESIAN_POINT ( 'NONE',  ( 20.94999999999999574, 72.02722222756958104, -225.1832529173024398 ) ) ;
#87013=CIRCLE ( 'NONE', #116290, 0.4000000000000121791 ) ;
#87039=DIRECTION ( 'NONE',  ( 1.000000000000000000, -2.849773892568378313E-16, 7.728835255496647986E-17 ) ) ;
#87041=CIRCLE ( 'NONE', #232838, 0.1000000000000066530 ) ;
#87048=EDGE_LOOP ( 'NONE', ( #178829, #42341, #255200, #54043 ) ) ;
#87060=CARTESIAN_POINT ( 'NONE',  ( -21.05000000000000071, 70.56573376625485139, -228.3808404818380779 ) ) ;
#87077=ORIENTED_EDGE ( 'NONE', *, *, #176685, .T. ) ;
#87082=ORIENTED_EDGE ( 'NONE', *, *, #247800, .T. ) ;
#87098=VERTEX_POINT ( 'NONE', #13668 ) ;
#87105=CARTESIAN_POINT ( 'NONE',  ( -20.64999999999999858, 65.77012247227901298, -213.5448142138000378 ) ) ;
#87109=AXIS2_PLACEMENT_3D ( 'NONE', #117556, #251928, #112436 ) ;
#87134=CYLINDRICAL_SURFACE ( 'NONE', #132091, 0.09999999999999939493 ) ;
#87150=EDGE_CURVE ( 'NONE', #150222, #156295, #188993, .T. ) ;
#87176=DIRECTION ( 'NONE',  ( 0.000000000000000000, 0.2617529984165031243, 0.9651348961777157509 ) ) ;
#87179=VERTEX_POINT ( 'NONE', #11108 ) ;
#87201=EDGE_LOOP ( 'NONE', ( #30831, #155606, #229770, #85561 ) ) ;
#87203=CARTESIAN_POINT ( 'NONE',  ( -23.25000000000000000, 64.25313205997782973, -247.2214437328673853 ) ) ;
#87234=EDGE_CURVE ( 'NONE', #99302, #18158, #51570, .T. ) ;
#87296=LINE ( 'NONE', #243815, #134536 ) ;
#87331=ORIENTED_EDGE ( 'NONE', *, *, #5341, .F. ) ;
#87383=CIRCLE ( 'NONE', #125017, 0.1000000000000124678 ) ;
#87399=LINE ( 'NONE', #166991, #39475 ) ;
#87428=DIRECTION ( 'NONE',  ( 0.000000000000000000, -0.9118278131605103143, 0.4105728183244983232 ) ) ;
#87450=DIRECTION ( 'NONE',  ( 0.7071067811865475727, -0.6824534298470373850, 0.1850873201762208153 ) ) ;
#87459=TOROIDAL_SURFACE ( 'NONE', #233249, 0.6000000000000006439, 0.1000000000000000056 ) ;
#87462=DIRECTION ( 'NONE',  ( 1.000000000000000000, 0.000000000000000000, 0.000000000000000000 ) ) ;
#87481=DIRECTION ( 'NONE',  ( -0.000000000000000000, -0.9651348961777157509, 0.2617529984165031243 ) ) ;
#87502=DIRECTION ( 'NONE',  ( 1.000000000000000000, 0.000000000000000000, 0.000000000000000000 ) ) ;
#87528=ORIENTED_EDGE ( 'NONE', *, *, #6673, .T. ) ;
#87535=EDGE_LOOP ( 'NONE', ( #121710, #131009, #135672, #203163 ) ) ;
#87538=CARTESIAN_POINT ( 'NONE',  ( -21.05000000000000071, 65.55628185913181483, -241.9744003048582215 ) ) ;
#87549=ORIENTED_EDGE ( 'NONE', *, *, #122678, .T. ) ;
#87605=EDGE_CURVE ( 'NONE', #159875, #58200, #18479, .T. ) ;
#87616=ORIENTED_EDGE ( 'NONE', *, *, #197486, .T. ) ;
#87641=DIRECTION ( 'NONE',  ( 1.000000000000000000, 0.000000000000000000, 0.000000000000000000 ) ) ;
#87719=SURFACE_SIDE_STYLE ('',( #244226 ) ) ;
#87731=CARTESIAN_POINT ( 'NONE',  ( -20.85000000000000142, 67.49222854868494892, -195.4187676019683693 ) ) ;
#87748=CIRCLE ( 'NONE', #220847, 0.1000000000000106498 ) ;
#87752=CARTESIAN_POINT ( 'NONE',  ( -23.15000000000000213, 66.26558728512915764, -222.7970849955717938 ) ) ;
#87774=LINE ( 'NONE', #85188, #92085 ) ;
#87775=DIRECTION ( 'NONE',  ( -1.000000000000000000, -0.000000000000000000, 0.000000000000000000 ) ) ;
#87776=AXIS2_PLACEMENT_3D ( 'NONE', #83943, #162270, #222192 ) ;
#87800=CIRCLE ( 'NONE', #104551, 0.1999999999999945155 ) ;
#87817=CARTESIAN_POINT ( 'NONE',  ( -21.14999999999999858, 64.27847795353595473, -247.1247091181747066 ) ) ;
#87854=ORIENTED_EDGE ( 'NONE', *, *, #158165, .T. ) ;
#87858=CIRCLE ( 'NONE', #217037, 0.1000000000000124678 ) ;
#87863=DIRECTION ( 'NONE',  ( -1.000000000000000000, -7.049440681616513945E-16, 1.911869773728115701E-16 ) ) ;
#87868=CARTESIAN_POINT ( 'NONE',  ( 18.49999999999999289, 63.86149674585136893, -209.2793526595898470 ) ) ;
#87902=EDGE_LOOP ( 'NONE', ( #242904, #196965, #197941, #26820 ) ) ;
#87918=ORIENTED_EDGE ( 'NONE', *, *, #37636, .T. ) ;
#88001=DIRECTION ( 'NONE',  ( 1.000000000000000000, 0.000000000000000000, 0.000000000000000000 ) ) ;
#88028=VECTOR ( 'NONE', #84089, 1000.000000000000000 ) ;
#88077=DIRECTION ( 'NONE',  ( -1.000000000000000000, 0.000000000000000000, 0.000000000000000000 ) ) ;
#88084=EDGE_LOOP ( 'NONE', ( #101074, #91414, #120277, #128873 ) ) ;
#88099=EDGE_CURVE ( 'NONE', #23382, #78723, #127652, .T. ) ;
#88100=ORIENTED_EDGE ( 'NONE', *, *, #14600, .T. ) ;
#88105=DIRECTION ( 'NONE',  ( 0.000000000000000000, -0.2617529984165031243, -0.9651348961777157509 ) ) ;
#88123=ORIENTED_EDGE ( 'NONE', *, *, #248299, .F. ) ;
#88136=ORIENTED_EDGE ( 'NONE', *, *, #14765, .T. ) ;
#88140=ADVANCED_FACE ( 'NONE', ( #188497 ), #209338, .F. ) ;
#88146=DIRECTION ( 'NONE',  ( -0.000000000000000000, 0.9651348961777155289, -0.2617529984165036794 ) ) ;
#88154=DIRECTION ( 'NONE',  ( -0.000000000000000000, 0.9651348961777157509, -0.2617529984165031243 ) ) ;
#88173=CARTESIAN_POINT ( 'NONE',  ( 23.24999999999999289, 64.04577702392042227, -222.1950530992138226 ) ) ;
#88195=CARTESIAN_POINT ( 'NONE',  ( 18.48197441911338501, 86.98964386969565510, -199.3644769928878588 ) ) ;
#88212=ADVANCED_FACE ( 'NONE', ( #132377 ), #210629, .F. ) ;
#88214=DIRECTION ( 'NONE',  ( 0.000000000000000000, 0.9651348961777160840, -0.2617529984165015700 ) ) ;
#88218=DIRECTION ( 'NONE',  ( 0.000000000000000000, 0.2617529984165031243, 0.9651348961777157509 ) ) ;
#88222=ORIENTED_EDGE ( 'NONE', *, *, #143173, .F. ) ;
#88234=DIRECTION ( 'NONE',  ( 0.000000000000000000, 0.2617529984164506107, 0.9651348961777299618 ) ) ;
#88261=DIRECTION ( 'NONE',  ( 0.000000000000000000, 0.9616958981405249185, -0.2741185865637159602 ) ) ;
#88262=DIRECTION ( 'NONE',  ( 1.000000000000000000, 0.000000000000000000, 0.000000000000000000 ) ) ;
#88267=DIRECTION ( 'NONE',  ( 0.000000000000000000, -0.2617529984165152257, -0.9651348961777124202 ) ) ;
#88294=DIRECTION ( 'NONE',  ( 0.000000000000000000, -0.2617529984165365975, -0.9651348961777066471 ) ) ;
#88316=CARTESIAN_POINT ( 'NONE',  ( 18.59999999999996945, 67.49222854868494892, -195.4187676019683693 ) ) ;
#88321=ORIENTED_EDGE ( 'NONE', *, *, #41883, .F. ) ;
#88333=DIRECTION ( 'NONE',  ( 0.000000000000000000, 0.1290532225515364506, 0.9916376685811525427 ) ) ;
#88353=VERTEX_POINT ( 'NONE', #181779 ) ;
#88371=CIRCLE ( 'NONE', #234130, 11.70000000000000995 ) ;
#88384=DIRECTION ( 'NONE',  ( 0.000000000000000000, 0.2617529984165152257, 0.9651348961777124202 ) ) ;
#88394=CARTESIAN_POINT ( 'NONE',  ( 20.94999999999999574, 64.21185867012613357, -224.4479740254296303 ) ) ;
#88423=CARTESIAN_POINT ( 'NONE',  ( 21.06277459767443005, 61.86219876617301594, -221.7541226652555224 ) ) ;
#88430=CARTESIAN_POINT ( 'NONE',  ( 18.39999999999999858, 78.24072131640578220, -231.5548844243369047 ) ) ;
#88447=DIRECTION ( 'NONE',  ( -0.000000000000000000, 0.2617529984165031243, 0.9651348961777157509 ) ) ;
#88449=ORIENTED_EDGE ( 'NONE', *, *, #158933, .F. ) ;
#88452=EDGE_LOOP ( 'NONE', ( #2407, #21029, #118762, #46155 ) ) ;
#88469=CARTESIAN_POINT ( 'NONE',  ( -23.15000000000000213, 68.69389471299010097, -223.1641309873017462 ) ) ;
#88487=VERTEX_POINT ( 'NONE', #166098 ) ;
#88490=VERTEX_POINT ( 'NONE', #210337 ) ;
#88508=CIRCLE ( 'NONE', #184386, 0.1000000000000106498 ) ;
#88520=ORIENTED_EDGE ( 'NONE', *, *, #221203, .F. ) ;
#88539=ORIENTED_EDGE ( 'NONE', *, *, #31581, .F. ) ;
#88554=LINE ( 'NONE', #14200, #24652 ) ;
#88567=DIRECTION ( 'NONE',  ( 1.000000000000000000, 0.000000000000000000, 0.000000000000000000 ) ) ;
#88586=DIRECTION ( 'NONE',  ( 0.000000000000000000, -0.9651348961777157509, 0.2617529984165028467 ) ) ;
#88609=ORIENTED_EDGE ( 'NONE', *, *, #137613, .F. ) ;
#88618=CARTESIAN_POINT ( 'NONE',  ( -18.50000000000001066, 86.96699927712943179, -199.3055931863049466 ) ) ;
#88623=CARTESIAN_POINT ( 'NONE',  ( 18.49999999999999289, 63.83083047455526327, -209.3924252461221158 ) ) ;
#88631=VECTOR ( 'NONE', #182274, 1000.000000000000000 ) ;
#88632=EDGE_LOOP ( 'NONE', ( #208623, #195354 ) ) ;
#88680=ADVANCED_FACE ( 'NONE', ( #96762 ), #138461, .F. ) ;
#88701=VECTOR ( 'NONE', #225900, 1000.000000000000000 ) ;
#88721=AXIS2_PLACEMENT_3D ( 'NONE', #4533, #84030, #198893 ) ;
#88744=AXIS2_PLACEMENT_3D ( 'NONE', #166559, #209499, #244766 ) ;
#88754=EDGE_CURVE ( 'NONE', #61360, #188240, #18552, .T. ) ;
#88757=DIRECTION ( 'NONE',  ( 1.000000000000000000, 0.000000000000000000, 0.000000000000000000 ) ) ;
#88810=CIRCLE ( 'NONE', #255364, 1.900000000000000799 ) ;
#88819=CARTESIAN_POINT ( 'NONE',  ( 21.05000000000000071, 78.50726470275242264, -228.6618886302502176 ) ) ;
#88879=VERTEX_POINT ( 'NONE', #53369 ) ;
#88904=VERTEX_POINT ( 'NONE', #41531 ) ;
#88914=DIRECTION ( 'NONE',  ( 0.000000000000000000, -0.2700277750006208621, -0.9628525332200221776 ) ) ;
#88917=EDGE_CURVE ( 'NONE', #244346, #14172, #147167, .T. ) ;
#88939=( BOUNDED_SURFACE ( )  B_SPLINE_SURFACE ( 3, 2, ( 
 ( #228172, #89920, #88623 ),
 ( #168232, #49529, #66528 ),
 ( #48236, #245164, #207333 ),
 ( #189039, #129067, #146045 ),
 ( #204729, #29993, #169517 ),
 ( #247722, #224305, #186475 ) ),
 .UNSPECIFIED., .F., .F., .F. ) 
 B_SPLINE_SURFACE_WITH_KNOTS ( ( 4, 2, 4 ),
 ( 3, 3 ),
 ( 3.141592653589827755, 3.926990816987264932, 4.712388980384702108 ),
 ( 0.000000000000000000, 1.000000000000000000 ),
 .UNSPECIFIED. ) 
 GEOMETRIC_REPRESENTATION_ITEM ( )  RATIONAL_B_SPLINE_SURFACE ( (
 ( 1.000000000000000000, 0.9238795325112765244, 1.000000000000000000),
 ( 1.000000000000000000, 0.9240297172240848900, 1.000000000000000000),
 ( 1.000000000000000000, 0.9038128468042962993, 1.000000000000000000),
 ( 1.000000000000000000, 0.8282379607645715680, 1.000000000000000000),
 ( 1.000000000000000000, 0.7727932973494031632, 1.000000000000000000),
 ( 1.000000000000000000, 0.7071067811866299513, 1.000000000000000000) ) ) 
 REPRESENTATION_ITEM ( '' )  SURFACE ( )  );
#88947=DIRECTION ( 'NONE',  ( 0.000000000000000000, -0.2617529984165033463, -0.9651348961777156399 ) ) ;
#88988=CARTESIAN_POINT ( 'NONE',  ( 21.05000000000000071, 76.00000000001126921, -203.5231074845248997 ) ) ;
#88992=AXIS2_PLACEMENT_3D ( 'NONE', #210769, #174261, #111669 ) ;
#89007=AXIS2_PLACEMENT_3D ( 'NONE', #136150, #30694, #110190 ) ;
#89021=AXIS2_PLACEMENT_3D ( 'NONE', #104302, #204691, #189957 ) ;
#89037=DIRECTION ( 'NONE',  ( 0.000000000000000000, 0.9651348961777148627, -0.2617529984165062329 ) ) ;
#89051=ORIENTED_EDGE ( 'NONE', *, *, #219712, .F. ) ;
#89073=DIRECTION ( 'NONE',  ( 0.000000000000000000, -0.2617529984164856383, -0.9651348961777204138 ) ) ;
#89084=VECTOR ( 'NONE', #230459, 1000.000000000000227 ) ;
#89155=EDGE_LOOP ( 'NONE', ( #58799, #37891, #94782, #50545 ) ) ;
#89156=DIRECTION ( 'NONE',  ( 0.000000000000000000, -0.7049548389605068133, 0.7092521942342977503 ) ) ;
#89181=AXIS2_PLACEMENT_3D ( 'NONE', #165114, #88105, #49009 ) ;
#89205=ORIENTED_EDGE ( 'NONE', *, *, #199378, .F. ) ;
#89218=AXIS2_PLACEMENT_3D ( 'NONE', #15388, #12829, #72809 ) ;
#89221=EDGE_CURVE ( 'NONE', #132077, #46773, #155755, .T. ) ;
#89245=ORIENTED_EDGE ( 'NONE', *, *, #225238, .T. ) ;
#89251=FACE_OUTER_BOUND ( 'NONE', #177828, .T. ) ;
#89267=VERTEX_POINT ( 'NONE', #225417 ) ;
#89293=DIRECTION ( 'NONE',  ( -0.000000000000000000, -0.7049548389605067023, 0.7092521942342977503 ) ) ;
#89299=CYLINDRICAL_SURFACE ( 'NONE', #238506, 0.09999999999999939493 ) ;
#89360=CARTESIAN_POINT ( 'NONE',  ( 18.59999999999997655, 76.00000000001126921, -203.5231074845248997 ) ) ;
#89377=DIRECTION ( 'NONE',  ( 0.000000000000000000, 0.2617529984165031243, 0.9651348961777157509 ) ) ;
#89410=CYLINDRICAL_SURFACE ( 'NONE', #42035, 0.09999999999999543976 ) ;
#89440=CARTESIAN_POINT ( 'NONE',  ( 18.49999999999999289, 66.40155400966892785, -213.5088390336144073 ) ) ;
#89453=DIRECTION ( 'NONE',  ( 0.000000000000000000, -0.9651348961777157509, 0.2617529984165031243 ) ) ;
#89469=EDGE_CURVE ( 'NONE', #206042, #82519, #51633, .T. ) ;
#89481=AXIS2_PLACEMENT_3D ( 'NONE', #173536, #195635, #233477 ) ;
#89484=LINE ( 'NONE', #4801, #21153 ) ;
#89510=DIRECTION ( 'NONE',  ( -0.000000000000000000, 0.9916376685811522096, -0.1290532225515392817 ) ) ;
#89551=ADVANCED_FACE ( 'NONE', ( #25650 ), #165159, .T. ) ;
#89569=AXIS2_PLACEMENT_3D ( 'NONE', #197547, #18911, #98405 ) ;
#89574=CARTESIAN_POINT ( 'NONE',  ( 18.52928932188133970, 63.77791826721860957, -209.3173802208384018 ) ) ;
#89588=DIRECTION ( 'NONE',  ( 0.000000000000000000, -0.9651348961777157509, 0.2617529984165031243 ) ) ;
#89609=CIRCLE ( 'NONE', #235363, 0.1000000000000124678 ) ;
#89623=ORIENTED_EDGE ( 'NONE', *, *, #217922, .T. ) ;
#89635=CARTESIAN_POINT ( 'NONE',  ( -22.50000000000000000, 65.59531831295525706, -241.8872196075891168 ) ) ;
#89638=EDGE_LOOP ( 'NONE', ( #218165, #25512, #15897, #216555 ) ) ;
#89653=CARTESIAN_POINT ( 'NONE',  ( 21.14999999999999858, 70.41157348381892689, -224.1287375179191201 ) ) ;
#89655=CARTESIAN_POINT ( 'NONE',  ( -22.59999999999999787, 55.86495732666938352, -232.8769840133977880 ) ) ;
#89657=CARTESIAN_POINT ( 'NONE',  ( 20.94999999999999929, 82.48249193998721296, -215.5326005316167084 ) ) ;
#89665=ORIENTED_EDGE ( 'NONE', *, *, #145996, .F. ) ;
#89703=EDGE_CURVE ( 'NONE', #147060, #73870, #131157, .T. ) ;
#89710=ADVANCED_FACE ( 'NONE', ( #150730 ), #180863, .T. ) ;
#89791=AXIS2_PLACEMENT_3D ( 'NONE', #132532, #212082, #77663 ) ;
#89807=CARTESIAN_POINT ( 'NONE',  ( -22.39999999999999858, 67.20509925321675837, -235.9516399960961337 ) ) ;
#89815=ORIENTED_EDGE ( 'NONE', *, *, #142678, .F. ) ;
#89835=AXIS2_PLACEMENT_3D ( 'NONE', #238199, #205160, #126933 ) ;
#89861=ORIENTED_EDGE ( 'NONE', *, *, #138898, .F. ) ;
#89885=CARTESIAN_POINT ( 'NONE',  ( 20.75572585718487773, 60.88282358376731196, -225.3291528674897677 ) ) ;
#89894=ORIENTED_EDGE ( 'NONE', *, *, #245017, .F. ) ;
#89914=( GEOMETRIC_REPRESENTATION_CONTEXT ( 3 ) GLOBAL_UNCERTAINTY_ASSIGNED_CONTEXT ( ( #34688 ) ) GLOBAL_UNIT_ASSIGNED_CONTEXT ( ( #476, #22655, #159578 ) ) REPRESENTATION_CONTEXT ( 'NONE', 'WORKASPACE' ) );
#89920=CARTESIAN_POINT ( 'NONE',  ( 18.49999999999999289, 63.79085327820362039, -209.3815830819284827 ) ) ;
#89941=EDGE_LOOP ( 'NONE', ( #47183, #76330, #38918, #161671 ) ) ;
#89945=ORIENTED_EDGE ( 'NONE', *, *, #40273, .F. ) ;
#89985=EDGE_LOOP ( 'NONE', ( #132684, #149900, #52619, #98049 ) ) ;
#89992=DIRECTION ( 'NONE',  ( 0.000000000000000000, -0.2617529984165067880, -0.9651348961777146407 ) ) ;
#90003=DIRECTION ( 'NONE',  ( 0.000000000000000000, 0.2617529984165152257, 0.9651348961777124202 ) ) ;
#90020=CARTESIAN_POINT ( 'NONE',  ( -18.50000000000000000, 68.68284540823283635, -224.2482512540334767 ) ) ;
#90050=EDGE_LOOP ( 'NONE', ( #214258, #17163, #148030, #139161 ) ) ;
#90082=CARTESIAN_POINT ( 'NONE',  ( -21.45000000000000284, 65.32753222054176945, -213.4247798787853867 ) ) ;
#90085=ORIENTED_EDGE ( 'NONE', *, *, #40311, .F. ) ;
#90129=ADVANCED_FACE ( 'NONE', ( #116123 ), #96600, .T. ) ;
#90136=DIRECTION ( 'NONE',  ( 1.000000000000000000, 0.000000000000000000, 0.000000000000000000 ) ) ;
#90151=CARTESIAN_POINT ( 'NONE',  ( -21.55000000000000071, 63.46669608621377279, -222.0380013001639270 ) ) ;
#90187=CIRCLE ( 'NONE', #40171, 12.87500000000000178 ) ;
#90192=ORIENTED_EDGE ( 'NONE', *, *, #57024, .F. ) ;
#90211=B_SPLINE_CURVE_WITH_KNOTS ( 'NONE', 3,
 ( #165757, #5343, #144871, #125329, #201015, #245281, #4085, #240144, #204841, #160628 ),
 .UNSPECIFIED., .F., .F.,
 ( 4, 3, 3, 4 ),
 ( 0.000000000000000000, 0.0002000000000008511354, 0.001000000000082984205, 0.001967863649483301593 ),
 .UNSPECIFIED. ) ;
#90242=EDGE_CURVE ( 'NONE', #202597, #126077, #222306, .T. ) ;
#90287=ORIENTED_EDGE ( 'NONE', *, *, #156048, .T. ) ;
#90323=EDGE_LOOP ( 'NONE', ( #216326, #96155, #214902, #105739 ) ) ;
#90345=CARTESIAN_POINT ( 'NONE',  ( -23.15000000000000213, 82.09643798151613225, -215.4278993322501208 ) ) ;
#90355=AXIS2_PLACEMENT_3D ( 'NONE', #1784, #218257, #180445 ) ;
#90356=EDGE_CURVE ( 'NONE', #130340, #181022, #134830, .T. ) ;
#90383=VECTOR ( 'NONE', #77193, 1000.000000000000000 ) ;
#90389=ORIENTED_EDGE ( 'NONE', *, *, #193809, .T. ) ;
#90450=PRODUCT_DEFINITION_FORMATION_WITH_SPECIFIED_SOURCE ( 'ANY', '', #7676, .NOT_KNOWN. ) ;
#90469=VERTEX_POINT ( 'NONE', #33746 ) ;
#90482=DIRECTION ( 'NONE',  ( 1.734723475976817507E-14, 0.9651348961777157509, -0.2617529984165031243 ) ) ;
#90499=CARTESIAN_POINT ( 'NONE',  ( -23.25000000000000000, 67.49222854868494892, -195.4187676019683693 ) ) ;
#90505=VERTEX_POINT ( 'NONE', #93668 ) ;
#90506=CARTESIAN_POINT ( 'NONE',  ( 18.59999999999999076, 66.54223038922117439, -213.7542166125332415 ) ) ;
#90522=DIRECTION ( 'NONE',  ( 1.000000000000000000, -0.000000000000000000, -0.000000000000000000 ) ) ;
#90530=DIRECTION ( 'NONE',  ( 0.000000000000000000, 0.2617529984165033463, 0.9651348961777157509 ) ) ;
#90537=ORIENTED_EDGE ( 'NONE', *, *, #106016, .T. ) ;
#90538=CARTESIAN_POINT ( 'NONE',  ( -21.33487959338958362, 60.74020368437641082, -234.0946914941910677 ) ) ;
#90542=CARTESIAN_POINT ( 'NONE',  ( 23.14999999999999503, 52.91185528119409298, -244.1460391050142675 ) ) ;
#90569=EDGE_CURVE ( 'NONE', #43432, #104140, #55902, .T. ) ;
#90570=DIRECTION ( 'NONE',  ( -1.000000000000000000, -0.000000000000000000, 0.000000000000000000 ) ) ;
#90571=DIRECTION ( 'NONE',  ( 0.000000000000000000, 0.7092521942343974484, 0.7049548389604062271 ) ) ;
#90598=CARTESIAN_POINT ( 'NONE',  ( 21.09696443733127325, 60.08364808979766991, -221.2398740259893657 ) ) ;
#90621=AXIS2_PLACEMENT_3D ( 'NONE', #145767, #62402, #3698 ) ;
#90634=DIRECTION ( 'NONE',  ( 1.000000000000000000, 0.000000000000000000, 0.000000000000000000 ) ) ;
#90647=AXIS2_PLACEMENT_3D ( 'NONE', #246742, #25168, #143793 ) ;
#90675=EDGE_LOOP ( 'NONE', ( #133865, #59454, #172332 ) ) ;
#90696=DIRECTION ( 'NONE',  ( -0.7071067811865475727, 0.6824534298470373850, -0.1850873201762210096 ) ) ;
#90704=CARTESIAN_POINT ( 'NONE',  ( 20.85882249326303040, 67.49222854868494892, -195.4187676019683693 ) ) ;
#90707=FACE_OUTER_BOUND ( 'NONE', #225524, .T. ) ;
#90744=DIRECTION ( 'NONE',  ( 0.000000000000000000, 0.2617529984165027912, 0.9651348961777157509 ) ) ;
#90751=DIRECTION ( 'NONE',  ( 0.000000000000000000, 0.2617529984165031243, 0.9651348961777157509 ) ) ;
#90754=ORIENTED_EDGE ( 'NONE', *, *, #181861, .T. ) ;
#90756=CARTESIAN_POINT ( 'NONE',  ( -20.94999999999999929, 70.44746257310249860, -228.4383880063670347 ) ) ;
#90812=ORIENTED_EDGE ( 'NONE', *, *, #94872, .T. ) ;
#90819=DIRECTION ( 'NONE',  ( -1.000000000000000000, 3.151514657663852580E-16, -8.547182517843351137E-17 ) ) ;
#90831=VERTEX_POINT ( 'NONE', #145613 ) ;
#90836=VERTEX_POINT ( 'NONE', #56762 ) ;
#90844=EDGE_CURVE ( 'NONE', #9861, #77283, #218220, .T. ) ;
#90845=EDGE_LOOP ( 'NONE', ( #189053, #246978, #69316, #42058, #200021, #215131, #44409, #64583, #114618, #72623 ) ) ;
#90853=EDGE_LOOP ( 'NONE', ( #120376, #51958, #147983, #231023 ) ) ;
#90883=EDGE_CURVE ( 'NONE', #101793, #62395, #210076, .T. ) ;
#90933=EDGE_CURVE ( 'NONE', #140695, #35438, #60012, .T. ) ;
#90938=DIRECTION ( 'NONE',  ( 0.000000000000000000, -0.9651348961777157509, 0.2617529984165031243 ) ) ;
#90954=DIRECTION ( 'NONE',  ( 0.000000000000000000, 0.2617529984165152257, 0.9651348961777124202 ) ) ;
#90960=DIRECTION ( 'NONE',  ( 1.000000000000000000, 0.000000000000000000, 0.000000000000000000 ) ) ;
#90963=ORIENTED_EDGE ( 'NONE', *, *, #111371, .F. ) ;
#90967=CARTESIAN_POINT ( 'NONE',  ( -21.14999999999999858, 79.33069327855442054, -236.1318330389568985 ) ) ;
#91014=ORIENTED_EDGE ( 'NONE', *, *, #163624, .T. ) ;
#91108=CARTESIAN_POINT ( 'NONE',  ( -20.85000000000000142, 80.69087520990402140, -192.8618289658565743 ) ) ;
#91112=ORIENTED_EDGE ( 'NONE', *, *, #211141, .F. ) ;
#91126=AXIS2_PLACEMENT_3D ( 'NONE', #13144, #212629, #193068 ) ;
#91148=DIRECTION ( 'NONE',  ( 0.000000000000000000, 0.2617529984165503087, 0.9651348961777028723 ) ) ;
#91168=EDGE_CURVE ( 'NONE', #123166, #160843, #18702, .T. ) ;
#91170=ORIENTED_EDGE ( 'NONE', *, *, #197516, .F. ) ;
#91187=CARTESIAN_POINT ( 'NONE',  ( 20.84451136049846554, 58.94296221207902420, -225.8426244149431454 ) ) ;
#91188=DIRECTION ( 'NONE',  ( 1.000000000000000000, 0.000000000000000000, 0.000000000000000000 ) ) ;
#91192=CARTESIAN_POINT ( 'NONE',  ( -20.85000000000000142, 79.14291928130900544, -196.3819507745080557 ) ) ;
#91200=EDGE_CURVE ( 'NONE', #151453, #29169, #214339, .T. ) ;
#91226=AXIS2_PLACEMENT_3D ( 'NONE', #31317, #187802, #173412 ) ;
#91233=DIRECTION ( 'NONE',  ( 0.000000000000000000, -0.2617529984165032908, -0.9651348961777156399 ) ) ;
#91238=PLANE ( 'NONE',  #216678 ) ;
#91248=ORIENTED_EDGE ( 'NONE', *, *, #82285, .T. ) ;
#91301=EDGE_LOOP ( 'NONE', ( #52530, #183593, #137113, #65429 ) ) ;
#91343=AXIS2_PLACEMENT_3D ( 'NONE', #52383, #235837, #237136 ) ;
#91353=CARTESIAN_POINT ( 'NONE',  ( 21.14999999999999858, 52.91185528119409298, -244.1460391050142675 ) ) ;
#91410=CARTESIAN_POINT ( 'NONE',  ( -21.11927991906891222, 65.53459516797913409, -242.0764145625574315 ) ) ;
#91414=ORIENTED_EDGE ( 'NONE', *, *, #63698, .T. ) ;
#91416=ADVANCED_FACE ( 'NONE', ( #65482 ), #151133, .T. ) ;
#91431=EDGE_LOOP ( 'NONE', ( #81592, #65100, #182382, #130852 ) ) ;
#91453=ORIENTED_EDGE ( 'NONE', *, *, #180410, .T. ) ;
#91481=DIRECTION ( 'NONE',  ( 0.000000000000000000, 0.2617529984165031243, 0.9651348961777157509 ) ) ;
#91500=AXIS2_PLACEMENT_3D ( 'NONE', #239239, #41064, #100952 ) ;
#91513=ORIENTED_EDGE ( 'NONE', *, *, #220957, .T. ) ;
#91538=EDGE_LOOP ( 'NONE', ( #74492, #98581, #154153, #95692, #145860, #5253 ) ) ;
#91547=ORIENTED_EDGE ( 'NONE', *, *, #166193, .F. ) ;
#91550=VERTEX_POINT ( 'NONE', #213662 ) ;
#91580=EDGE_CURVE ( 'NONE', #74710, #166612, #252771, .T. ) ;
#91584=AXIS2_PLACEMENT_3D ( 'NONE', #234995, #56326, #103158 ) ;
#91626=AXIS2_PLACEMENT_3D ( 'NONE', #195573, #235950, #217657 ) ;
#91657=CARTESIAN_POINT ( 'NONE',  ( 18.59999999999999076, 52.81534179157633702, -244.1198638051726277 ) ) ;
#91669=EDGE_LOOP ( 'NONE', ( #235656, #125860, #232702, #239762 ) ) ;
#91673=CARTESIAN_POINT ( 'NONE',  ( -21.05000000000000426, 65.63239632895212594, -242.1325452132893759 ) ) ;
#91681=DIRECTION ( 'NONE',  ( 0.000000000000000000, 0.2617529984165152257, 0.9651348961777124202 ) ) ;
#91700=EDGE_CURVE ( 'NONE', #16660, #198941, #137953, .T. ) ;
#91709=ORIENTED_EDGE ( 'NONE', *, *, #211141, .T. ) ;
#91717=EDGE_CURVE ( 'NONE', #69974, #128036, #84356, .T. ) ;
#91730=ADVANCED_FACE ( 'NONE', ( #102663 ), #200513, .F. ) ;
#91732=CARTESIAN_POINT ( 'NONE',  ( 21.05000000000000071, 65.26666169030359299, -222.4689051838086300 ) ) ;
#91758=EDGE_CURVE ( 'NONE', #192701, #204834, #81807, .T. ) ;
#91777=DIRECTION ( 'NONE',  ( 0.000000000000000000, -0.7049548389604960441, 0.7092521942343085195 ) ) ;
#91798=LINE ( 'NONE', #90499, #103300 ) ;
#91803=EDGE_CURVE ( 'NONE', #158463, #58200, #210779, .T. ) ;
#91832=DIRECTION ( 'NONE',  ( -1.000000000000000000, 0.000000000000000000, 0.000000000000000000 ) ) ;
#91835=DIRECTION ( 'NONE',  ( -1.000000000000000000, 1.772924042024179943E-16, -4.808324575169860901E-17 ) ) ;
#91838=FACE_OUTER_BOUND ( 'NONE', #53189, .T. ) ;
#91849=ORIENTED_EDGE ( 'NONE', *, *, #149888, .F. ) ;
#91893=CARTESIAN_POINT ( 'NONE',  ( 21.13507111622890022, 60.09352091567126308, -221.2276406919921214 ) ) ;
#91899=ORIENTED_EDGE ( 'NONE', *, *, #249628, .F. ) ;
#91913=CYLINDRICAL_SURFACE ( 'NONE', #76124, 0.5000000000000014433 ) ;
#91914=CIRCLE ( 'NONE', #179425, 11.79999999999999716 ) ;
#91919=AXIS2_PLACEMENT_3D ( 'NONE', #100599, #58912, #181480 ) ;
#91959=ADVANCED_FACE ( 'NONE', ( #73874 ), #23189, .T. ) ;
#91993=DIRECTION ( 'NONE',  ( 0.000000000000000000, 0.9651348961777157509, -0.2617529984165031243 ) ) ;
#91996=CARTESIAN_POINT ( 'NONE',  ( -18.50000000000000000, 71.84303044094815505, -225.1053209871248271 ) ) ;
#92013=ADVANCED_FACE ( 'NONE', ( #175531 ), #106339, .T. ) ;
#92030=VERTEX_POINT ( 'NONE', #75152 ) ;
#92085=VECTOR ( 'NONE', #31710, 1000.000000000000000 ) ;
#92093=CARTESIAN_POINT ( 'NONE',  ( -18.59999999999999787, 70.29876110920605470, -198.0544810472949564 ) ) ;
#92124=AXIS2_PLACEMENT_3D ( 'NONE', #185946, #248487, #247189 ) ;
#92134=CARTESIAN_POINT ( 'NONE',  ( 18.50000324121758055, 67.49461024981972912, -195.5605382655040216 ) ) ;
#92139=ADVANCED_FACE ( 'NONE', ( #178092 ), #25432, .F. ) ;
#92162=DIRECTION ( 'NONE',  ( 0.000000000000000000, -0.9229812358756199764, 0.3848449534832346086 ) ) ;
#92226=DIRECTION ( 'NONE',  ( 1.000000000000000000, 0.000000000000000000, -0.000000000000000000 ) ) ;
#92231=CYLINDRICAL_SURFACE ( 'NONE', #169171, 0.1000000000000124678 ) ;
#92287=CARTESIAN_POINT ( 'NONE',  ( -21.05000000000000071, 57.78573798790818472, -226.2252221607603246 ) ) ;
#92294=AXIS2_PLACEMENT_3D ( 'NONE', #135388, #96261, #10658 ) ;
#92300=ORIENTED_EDGE ( 'NONE', *, *, #171082, .F. ) ;
#92306=DIRECTION ( 'NONE',  ( 0.000000000000000000, 0.2617529984165030688, 0.9651348961777157509 ) ) ;
#92310=ORIENTED_EDGE ( 'NONE', *, *, #170043, .T. ) ;
#92355=DIRECTION ( 'NONE',  ( 0.000000000000000000, -0.9916376685811618685, 0.1290532225514649800 ) ) ;
#92357=ADVANCED_FACE ( 'NONE', ( #57797 ), #254687, .F. ) ;
#92358=EDGE_CURVE ( 'NONE', #63643, #229783, #14989, .T. ) ;
#92396=CIRCLE ( 'NONE', #104841, 0.1000000000000106498 ) ;
#92411=CARTESIAN_POINT ( 'NONE',  ( 21.05000000000000071, 70.41157348381892689, -224.1287375179191201 ) ) ;
#92455=FACE_OUTER_BOUND ( 'NONE', #246143, .T. ) ;
#92513=DIRECTION ( 'NONE',  ( 0.000000000000000000, -0.9651348961777158619, 0.2617529984165032353 ) ) ;
#92534=ORIENTED_EDGE ( 'NONE', *, *, #40818, .F. ) ;
#92620=CARTESIAN_POINT ( 'NONE',  ( 20.95000000000000284, 62.99095723518624368, -207.1734234082435080 ) ) ;
#92621=CYLINDRICAL_SURFACE ( 'NONE', #79821, 0.09999999999998657185 ) ;
#92629=EDGE_CURVE ( 'NONE', #148934, #204227, #231844, .T. ) ;
#92643=CYLINDRICAL_SURFACE ( 'NONE', #215881, 0.09999999999999961697 ) ;
#92650=DIRECTION ( 'NONE',  ( -7.304098846218134667E-16, -0.9651348961777158619, 0.2617529984165031243 ) ) ;
#92667=AXIS2_PLACEMENT_3D ( 'NONE', #144148, #244544, #65922 ) ;
#92733=ORIENTED_EDGE ( 'NONE', *, *, #156511, .T. ) ;
#92738=CARTESIAN_POINT ( 'NONE',  ( 20.95545211741311320, 58.99965432765223028, -225.7624460179877417 ) ) ;
#92788=ORIENTED_EDGE ( 'NONE', *, *, #208856, .F. ) ;
#92790=ORIENTED_EDGE ( 'NONE', *, *, #138136, .F. ) ;
#92799=VECTOR ( 'NONE', #87481, 1000.000000000000000 ) ;
#92812=VERTEX_POINT ( 'NONE', #18165 ) ;
#92814=DIRECTION ( 'NONE',  ( 0.000000000000000000, -0.2617529984165032908, -0.9651348961777156399 ) ) ;
#92869=DIRECTION ( 'NONE',  ( 0.000000000000000000, 0.2617529984165033463, 0.9651348961777156399 ) ) ;
#92888=DIRECTION ( 'NONE',  ( 1.000000000000000000, -2.849773892568378313E-16, 7.728835255496647986E-17 ) ) ;
#92896=AXIS2_PLACEMENT_3D ( 'NONE', #221895, #244040, #100655 ) ;
#92908=ORIENTED_EDGE ( 'NONE', *, *, #118778, .T. ) ;
#92920=DIRECTION ( 'NONE',  ( 1.000000000000000000, 0.000000000000000000, 0.000000000000000000 ) ) ;
#92940=DIRECTION ( 'NONE',  ( 0.000000000000000000, 0.2617529984165152257, 0.9651348961777124202 ) ) ;
#92963=ORIENTED_EDGE ( 'NONE', *, *, #120412, .F. ) ;
#92971=ORIENTED_EDGE ( 'NONE', *, *, #170808, .T. ) ;
#92985=ORIENTED_EDGE ( 'NONE', *, *, #133294, .F. ) ;
#92992=DIRECTION ( 'NONE',  ( -1.000000000000000000, -0.000000000000000000, 0.000000000000000000 ) ) ;
#93031=VERTEX_POINT ( 'NONE', #212226 ) ;
#93034=VECTOR ( 'NONE', #15374, 1000.000000000000000 ) ;
#93051=LINE ( 'NONE', #172649, #224094 ) ;
#93053=DIRECTION ( 'NONE',  ( -2.915501640297154283E-16, -0.9651348961777159730, 0.2617529984165023471 ) ) ;
#93070=ORIENTED_EDGE ( 'NONE', *, *, #235378, .F. ) ;
#93075=CARTESIAN_POINT ( 'NONE',  ( -21.93340585971669654, 60.16248467656274102, -233.9380090624021591 ) ) ;
#93113=CARTESIAN_POINT ( 'NONE',  ( -18.50000000000000000, 57.82359945636609666, -226.0354702357591350 ) ) ;
#93120=ORIENTED_EDGE ( 'NONE', *, *, #246804, .T. ) ;
#93172=AXIS2_PLACEMENT_3D ( 'NONE', #198381, #22341, #8848 ) ;
#93190=DIRECTION ( 'NONE',  ( -1.000000000000000000, 2.849773892568378313E-16, -7.728835255496647986E-17 ) ) ;
#93215=ORIENTED_EDGE ( 'NONE', *, *, #232856, .F. ) ;
#93218=DIRECTION ( 'NONE',  ( 0.000000000000000000, -0.9651348961777157509, 0.2617529984165031243 ) ) ;
#93230=DIRECTION ( 'NONE',  ( 0.000000000000000000, 0.2617529984165152257, 0.9651348961777124202 ) ) ;
#93241=CARTESIAN_POINT ( 'NONE',  ( -18.50000000000001066, 78.21920613375266385, -231.3255402381754493 ) ) ;
#93245=VECTOR ( 'NONE', #57097, 1000.000000000000000 ) ;
#93261=AXIS2_PLACEMENT_3D ( 'NONE', #113428, #55992, #151289 ) ;
#93269=CARTESIAN_POINT ( 'NONE',  ( 19.75857864376268935, 62.39550153362034735, -208.7959266050682459 ) ) ;
#93275=ORIENTED_EDGE ( 'NONE', *, *, #98388, .T. ) ;
#93304=CARTESIAN_POINT ( 'NONE',  ( -18.50000000000000000, 78.52025535392039046, -230.5241873323956554 ) ) ;
#93315=CARTESIAN_POINT ( 'NONE',  ( -23.15000000000000213, 68.56901367119438362, -214.3038979092079046 ) ) ;
#93331=CIRCLE ( 'NONE', #239095, 0.09999999999999317768 ) ;
#93340=B_SPLINE_CURVE_WITH_KNOTS ( 'NONE', 3,
 ( #29760, #186238, #6292, #130096, #207084, #49279, #205786, #67563 ),
 .UNSPECIFIED., .F., .F.,
 ( 4, 2, 2, 4 ),
 ( 0.000000000000000000, 9.550056980124080818E-05, 0.0001910011396024816164, 0.0003820022792049778152 ),
 .UNSPECIFIED. ) ;
#93365=CARTESIAN_POINT ( 'NONE',  ( -20.54999999999999716, 63.56320957583155717, -222.0641766000055668 ) ) ;
#93371=DIRECTION ( 'NONE',  ( 0.000000000000000000, -0.2617529984165031243, -0.9651348961777157509 ) ) ;
#93394=DIRECTION ( 'NONE',  ( -0.000000000000000000, 0.9651348961777157509, -0.2617529984165031243 ) ) ;
#93399=ORIENTED_EDGE ( 'NONE', *, *, #78924, .F. ) ;
#93400=DIRECTION ( 'NONE',  ( 0.000000000000000000, -0.2617529984164506107, -0.9651348961777299618 ) ) ;
#93403=ORIENTED_EDGE ( 'NONE', *, *, #115364, .F. ) ;
#93414=CARTESIAN_POINT ( 'NONE',  ( 18.45139536634708932, 86.89352232322976022, -199.5971283272099015 ) ) ;
#93415=CARTESIAN_POINT ( 'NONE',  ( -21.44999999999999929, 65.67360898266123570, -213.5186389139583980 ) ) ;
#93418=ORIENTED_EDGE ( 'NONE', *, *, #7946, .T. ) ;
#93474=CIRCLE ( 'NONE', #64272, 4.299999999999945643 ) ;
#93495=ORIENTED_EDGE ( 'NONE', *, *, #230259, .T. ) ;
#93500=DIRECTION ( 'NONE',  ( 0.000000000000000000, 0.2617529984165030132, 0.9651348961777157509 ) ) ;
#93502=DIRECTION ( 'NONE',  ( -1.000000000000000000, -0.000000000000000000, 0.000000000000000000 ) ) ;
#93508=DIRECTION ( 'NONE',  ( 0.000000000000000000, 0.2617529984165026247, 0.9651348961777158619 ) ) ;
#93533=CARTESIAN_POINT ( 'NONE',  ( -23.15000000000000213, 66.23941198528750363, -222.8935984851895853 ) ) ;
#93560=EDGE_CURVE ( 'NONE', #11577, #166612, #23927, .T. ) ;
#93581=ORIENTED_EDGE ( 'NONE', *, *, #99034, .F. ) ;
#93589=DIRECTION ( 'NONE',  ( 0.000000000000000000, 0.2617529984165152257, 0.9651348961777124202 ) ) ;
#93610=EDGE_LOOP ( 'NONE', ( #158612, #249843, #109008, #145923, #157248 ) ) ;
#93618=AXIS2_PLACEMENT_3D ( 'NONE', #59409, #239376, #257587 ) ;
#93621=CARTESIAN_POINT ( 'NONE',  ( -20.94999999999999929, 60.99662849158838895, -205.1669373764474642 ) ) ;
#93656=ADVANCED_FACE ( 'NONE', ( #155802 ), #81333, .F. ) ;
#93668=CARTESIAN_POINT ( 'NONE',  ( 20.94999999999999929, 67.54115598404673904, -214.0823964242964053 ) ) ;
#93687=DIRECTION ( 'NONE',  ( 0.000000000000000000, 0.9651348961776677893, -0.2617529984166795387 ) ) ;
#93716=LINE ( 'NONE', #174603, #133407 ) ;
#93730=CARTESIAN_POINT ( 'NONE',  ( -23.15000000000000213, 78.50726470275243685, -228.6618886302502176 ) ) ;
#93746=ORIENTED_EDGE ( 'NONE', *, *, #162870, .T. ) ;
#93747=CARTESIAN_POINT ( 'NONE',  ( 20.22483756094572271, 60.19120353999515771, -225.5122212141894522 ) ) ;
#93752=ORIENTED_EDGE ( 'NONE', *, *, #71245, .T. ) ;
#93883=ADVANCED_FACE ( 'NONE', ( #10829 ), #78238, .T. ) ;
#93901=CARTESIAN_POINT ( 'NONE',  ( 23.14999999999999503, 57.93055674131822741, -245.5071546967800771 ) ) ;
#93922=DIRECTION ( 'NONE',  ( 0.000000000000000000, 0.2617529984164506107, 0.9651348961777299618 ) ) ;
#93926=AXIS2_PLACEMENT_3D ( 'NONE', #38289, #175265, #235203 ) ;
#93938=CARTESIAN_POINT ( 'NONE',  ( -18.47140463609785499, 87.08089277388562266, -199.6145310103756003 ) ) ;
#93966=DIRECTION ( 'NONE',  ( 0.7071067811865486830, -0.1850873201762207598, -0.6824534298470361637 ) ) ;
#93967=CARTESIAN_POINT ( 'NONE',  ( 21.13435531349745844, 65.53152359378273673, -242.1224433109954930 ) ) ;
#94031=DIRECTION ( 'NONE',  ( -0.000000000000000000, 0.9942466578594195692, -0.1071148137998398919 ) ) ;
#94070=AXIS2_PLACEMENT_3D ( 'NONE', #226919, #246480, #147385 ) ;
#94072=EDGE_LOOP ( 'NONE', ( #255170, #54357, #28903, #194833 ) ) ;
#94113=ADVANCED_FACE ( 'NONE', ( #203581 ), #103177, .T. ) ;
#94125=VERTEX_POINT ( 'NONE', #61511 ) ;
#94174=CIRCLE ( 'NONE', #148350, 0.1000000000000124678 ) ;
#94216=EDGE_LOOP ( 'NONE', ( #9497, #239364, #191847, #154519 ) ) ;
#94233=CARTESIAN_POINT ( 'NONE',  ( -21.05000000000000071, 65.49889199258218753, -241.8691648588935266 ) ) ;
#94242=VERTEX_POINT ( 'NONE', #148759 ) ;
#94261=ORIENTED_EDGE ( 'NONE', *, *, #142629, .F. ) ;
#94263=ADVANCED_FACE ( 'NONE', ( #226993 ), #186605, .T. ) ;
#94273=ORIENTED_EDGE ( 'NONE', *, *, #74453, .T. ) ;
#94314=EDGE_CURVE ( 'NONE', #137749, #20778, #36962, .T. ) ;
#94315=EDGE_CURVE ( 'NONE', #88353, #252254, #217675, .T. ) ;
#94348=EDGE_CURVE ( 'NONE', #230038, #195218, #136882, .T. ) ;
#94350=EDGE_LOOP ( 'NONE', ( #242849, #170073, #74272, #99444 ) ) ;
#94361=VERTEX_POINT ( 'NONE', #95191 ) ;
#94388=CARTESIAN_POINT ( 'NONE',  ( 23.14999999999999858, 75.47649400317826007, -205.4533772768803317 ) ) ;
#94428=DIRECTION ( 'NONE',  ( 0.000000000000000000, 0.2617529984165027912, 0.9651348961777157509 ) ) ;
#94465=EDGE_LOOP ( 'NONE', ( #121836, #211704, #212792, #119812 ) ) ;
#94499=SPHERICAL_SURFACE ( 'NONE', #46364, 0.1000000000000000056 ) ;
#94504=CARTESIAN_POINT ( 'NONE',  ( -23.15000000000000213, 61.47936603916259202, -212.1738987416902376 ) ) ;
#94517=CIRCLE ( 'NONE', #165262, 0.09999999999999939493 ) ;
#94521=EDGE_LOOP ( 'NONE', ( #14207, #147631, #198752, #180560 ) ) ;
#94536=AXIS2_PLACEMENT_3D ( 'NONE', #198046, #178524, #158961 ) ;
#94544=LINE ( 'NONE', #210654, #145240 ) ;
#94564=CIRCLE ( 'NONE', #244405, 0.1000000000000016154 ) ;
#94567=VECTOR ( 'NONE', #197122, 1000.000000000000000 ) ;
#94577=DIRECTION ( 'NONE',  ( 0.000000000000000000, 0.2617529984165031243, 0.9651348961777157509 ) ) ;
#94607=DIRECTION ( 'NONE',  ( -0.000000000000000000, 0.2617529984165031243, 0.9651348961777157509 ) ) ;
#94612=ADVANCED_FACE ( 'NONE', ( #214493 ), #157779, .T. ) ;
#94623=EDGE_CURVE ( 'NONE', #133438, #129974, #94544, .T. ) ;
#94626=ORIENTED_EDGE ( 'NONE', *, *, #83849, .F. ) ;
#94632=CARTESIAN_POINT ( 'NONE',  ( -18.59999999999999787, 80.78317333349157536, -192.9003134612048882 ) ) ;
#94679=ORIENTED_EDGE ( 'NONE', *, *, #131526, .F. ) ;
#94681=CARTESIAN_POINT ( 'NONE',  ( -20.00857864376270001, 63.96254146938299101, -212.9509700271909196 ) ) ;
#94699=CARTESIAN_POINT ( 'NONE',  ( 18.47688499308725341, 86.88896063274113146, -199.5328573411169941 ) ) ;
#94779=EDGE_LOOP ( 'NONE', ( #157616, #103823 ) ) ;
#94782=ORIENTED_EDGE ( 'NONE', *, *, #218, .T. ) ;
#94808=DIRECTION ( 'NONE',  ( 0.000000000000000000, 0.2617529984164915779, 0.9651348961777189706 ) ) ;
#94813=ORIENTED_EDGE ( 'NONE', *, *, #224870, .F. ) ;
#94846=ORIENTED_EDGE ( 'NONE', *, *, #215318, .T. ) ;
#94866=DIRECTION ( 'NONE',  ( 9.044546369203337730E-15, 0.8900778951570211817, 0.4558084472153261513 ) ) ;
#94872=EDGE_CURVE ( 'NONE', #133775, #193922, #68283, .T. ) ;
#94888=DIRECTION ( 'NONE',  ( 0.000000000000000000, -0.9651348961776677893, 0.2617529984166795387 ) ) ;
#94896=DIRECTION ( 'NONE',  ( 0.000000000000000000, -0.2617529984165152257, -0.9651348961777124202 ) ) ;
#94927=AXIS2_PLACEMENT_3D ( 'NONE', #176534, #218180, #42155 ) ;
#94952=VECTOR ( 'NONE', #64351, 1000.000000000000000 ) ;
#94958=EDGE_CURVE ( 'NONE', #216037, #92030, #240550, .T. ) ;
#94969=DIRECTION ( 'NONE',  ( 0.000000000000000000, 0.2617529984165035684, 0.9651348961777156399 ) ) ;
#94990=AXIS2_PLACEMENT_3D ( 'NONE', #120527, #235299, #215727 ) ;
#94995=CARTESIAN_POINT ( 'NONE',  ( -21.44999999999999929, 63.34400729675436281, -222.1083394899400503 ) ) ;
#95027=CARTESIAN_POINT ( 'NONE',  ( 20.53930447207968157, 60.77696664501686996, -225.3571726667190376 ) ) ;
#95042=DIRECTION ( 'NONE',  ( 0.000000000000000000, -0.2558827019434133376, 0.9667078373770113808 ) ) ;
#95057=CIRCLE ( 'NONE', #219962, 0.5999999999999872102 ) ;
#95058=CARTESIAN_POINT ( 'NONE',  ( -18.39999999999999858, 87.08727414655710675, -199.6327537731849873 ) ) ;
#95134=AXIS2_PLACEMENT_3D ( 'NONE', #52986, #193796, #210787 ) ;
#95159=CARTESIAN_POINT ( 'NONE',  ( 21.05000000000000071, 86.27712145182582049, -209.5223386573213702 ) ) ;
#95164=AXIS2_PLACEMENT_3D ( 'NONE', #241726, #123074, #71788 ) ;
#95191=CARTESIAN_POINT ( 'NONE',  ( 23.15000000000000213, 81.86853375790846599, -214.9828603846715964 ) ) ;
#95222=TOROIDAL_SURFACE ( 'NONE', #236862, 11.70000000000000107, 0.1000000000000000056 ) ;
#95234=EDGE_CURVE ( 'NONE', #206482, #94125, #120151, .T. ) ;
#95258=ADVANCED_FACE ( 'NONE', ( #143645 ), #122825, .T. ) ;
#95271=EDGE_LOOP ( 'NONE', ( #125046, #216839, #170551, #61665 ) ) ;
#95305=AXIS2_PLACEMENT_3D ( 'NONE', #16710, #14156, #214891 ) ;
#95329=DIRECTION ( 'NONE',  ( -1.000000000000000000, -0.000000000000000000, 0.000000000000000000 ) ) ;
#95350=VECTOR ( 'NONE', #152363, 1000.000000000000000 ) ;
#95359=ORIENTED_EDGE ( 'NONE', *, *, #140541, .T. ) ;
#95364=CIRCLE ( 'NONE', #141165, 0.1000000000000124678 ) ;
#95365=AXIS2_PLACEMENT_3D ( 'NONE', #91353, #151338, #127905 ) ;
#95393=VERTEX_POINT ( 'NONE', #159085 ) ;
#95445=CARTESIAN_POINT ( 'NONE',  ( -18.39999999999999858, 78.33723480602354527, -231.5810597241785729 ) ) ;
#95446=CARTESIAN_POINT ( 'NONE',  ( -20.94999999999999929, 57.84918772656043728, -226.1321410194968280 ) ) ;
#95452=ORIENTED_EDGE ( 'NONE', *, *, #142097, .T. ) ;
#95458=DIRECTION ( 'NONE',  ( 0.000000000000000000, -0.2617529984165033463, -0.9651348961777157509 ) ) ;
#95483=AXIS2_PLACEMENT_3D ( 'NONE', #207082, #144513, #27191 ) ;
#95518=EDGE_CURVE ( 'NONE', #185762, #28751, #195145, .T. ) ;
#95532=CARTESIAN_POINT ( 'NONE',  ( -23.15000000000000213, 86.52890073500824997, -209.5906233940697234 ) ) ;
#95541=DIRECTION ( 'NONE',  ( 0.000000000000000000, -0.9651348961777157509, 0.2617529984165031243 ) ) ;
#95543=DIRECTION ( 'NONE',  ( -0.000000000000000000, 0.9651348961777157509, -0.2617529984165031243 ) ) ;
#95567=AXIS2_PLACEMENT_3D ( 'NONE', #60952, #158808, #16718 ) ;
#95609=ORIENTED_EDGE ( 'NONE', *, *, #65694, .F. ) ;
#95617=DIRECTION ( 'NONE',  ( 0.000000000000000000, -0.2617529984165036239, -0.9651348961777156399 ) ) ;
#95647=CARTESIAN_POINT ( 'NONE',  ( 21.05000000000000071, 77.04701199367727327, -199.6625678998140359 ) ) ;
#95652=CARTESIAN_POINT ( 'NONE',  ( 23.24999999999999645, 67.23127455305841238, -235.8551265064783991 ) ) ;
#95692=ORIENTED_EDGE ( 'NONE', *, *, #19191, .T. ) ;
#95695=DIRECTION ( 'NONE',  ( 1.000000000000000000, 0.000000000000000000, -0.000000000000000000 ) ) ;
#95751=AXIS2_PLACEMENT_3D ( 'NONE', #80369, #63391, #142918 ) ;
#95752=DIRECTION ( 'NONE',  ( 0.000000000000000000, 0.2617529984165045120, 0.9651348961777153068 ) ) ;
#95778=EDGE_CURVE ( 'NONE', #191015, #54157, #82833, .T. ) ;
#95801=DIRECTION ( 'NONE',  ( -0.000000000000000000, 0.9916376685811522096, -0.1290532225515392817 ) ) ;
#95807=CARTESIAN_POINT ( 'NONE',  ( 21.05000000000000071, 70.41157348381892689, -224.1287375179191201 ) ) ;
#95831=FACE_OUTER_BOUND ( 'NONE', #78495, .T. ) ;
#95848=EDGE_CURVE ( 'NONE', #19933, #11153, #127642, .T. ) ;
#95854=LINE ( 'NONE', #175438, #136028 ) ;
#95908=DIRECTION ( 'NONE',  ( 1.000000000000000000, 0.000000000000000000, -0.000000000000000000 ) ) ;
#95917=CARTESIAN_POINT ( 'NONE',  ( -18.59999999999999787, 76.00000000001126921, -203.5231074845248997 ) ) ;
#95927=CARTESIAN_POINT ( 'NONE',  ( -18.50016250449483479, 67.49429988484524756, -195.5441618131978316 ) ) ;
#95973=CARTESIAN_POINT ( 'NONE',  ( 18.39999999999999858, 86.89640087696871262, -199.6396878666313341 ) ) ;
#95978=DIRECTION ( 'NONE',  ( 0.000000000000000000, -0.2617529984165045120, -0.9651348961777153068 ) ) ;
#96026=ORIENTED_EDGE ( 'NONE', *, *, #8183, .F. ) ;
#96041=EDGE_LOOP ( 'NONE', ( #67495, #113979, #71500, #23014 ) ) ;
#96071=DIRECTION ( 'NONE',  ( 0.000000000000000000, -0.8636236514130390951, 0.5041370733441546959 ) ) ;
#96076=TOROIDAL_SURFACE ( 'NONE', #154396, 0.2000000000000000111, 0.1000000000000000056 ) ;
#96108=VERTEX_POINT ( 'NONE', #131164 ) ;
#96128=ORIENTED_EDGE ( 'NONE', *, *, #131526, .T. ) ;
#96155=ORIENTED_EDGE ( 'NONE', *, *, #140851, .T. ) ;
#96165=ADVANCED_FACE ( 'NONE', ( #126023 ), #220616, .F. ) ;
#96188=EDGE_CURVE ( 'NONE', #198131, #158463, #66494, .T. ) ;
#96245=EDGE_CURVE ( 'NONE', #185020, #220166, #231566, .T. ) ;
#96251=DIRECTION ( 'NONE',  ( 0.000000000000000000, -0.2558827019433787542, 0.9667078373770204847 ) ) ;
#96261=DIRECTION ( 'NONE',  ( 0.000000000000000000, 0.9651348961777157509, -0.2617529984165031243 ) ) ;
#96263=DIRECTION ( 'NONE',  ( 0.000000000000000000, 0.2617529984164035373, 0.9651348961777428404 ) ) ;
#96266=FACE_OUTER_BOUND ( 'NONE', #75236, .T. ) ;
#96295=EDGE_CURVE ( 'NONE', #50451, #115380, #99774, .T. ) ;
#96296=DIRECTION ( 'NONE',  ( 1.000000000000000000, 0.000000000000000000, 0.000000000000000000 ) ) ;
#96328=CARTESIAN_POINT ( 'NONE',  ( 23.15000000000000213, 87.19425987394825484, -209.6674621343692024 ) ) ;
#96343=ORIENTED_EDGE ( 'NONE', *, *, #174601, .F. ) ;
#96362=LINE ( 'NONE', #135491, #14396 ) ;
#96390=CIRCLE ( 'NONE', #217186, 12.77499999999999325 ) ;
#96394=ORIENTED_EDGE ( 'NONE', *, *, #236152, .T. ) ;
#96412=CARTESIAN_POINT ( 'NONE',  ( -20.54999999999999716, 76.00000000001126921, -203.5231074845248997 ) ) ;
#96441=ORIENTED_EDGE ( 'NONE', *, *, #128198, .F. ) ;
#96448=CARTESIAN_POINT ( 'NONE',  ( -20.94999999999999929, 70.37092869010230345, -198.1237041667535550 ) ) ;
#96449=DIRECTION ( 'NONE',  ( 1.000000000000000000, 0.000000000000000000, 0.000000000000000000 ) ) ;
#96452=ORIENTED_EDGE ( 'NONE', *, *, #12018, .F. ) ;
#96490=EDGE_CURVE ( 'NONE', #4288, #210631, #108375, .T. ) ;
#96496=DIRECTION ( 'NONE',  ( 1.000000000000000000, 0.000000000000000000, 0.000000000000000000 ) ) ;
#96508=DIRECTION ( 'NONE',  ( -1.000000000000000000, -0.000000000000000000, -0.000000000000000000 ) ) ;
#96558=CARTESIAN_POINT ( 'NONE',  ( 21.05000000000024585, 60.89892960307708591, -225.3088725716038709 ) ) ;
#96561=DIRECTION ( 'NONE',  ( 0.000000000000000000, 0.2617529984165031243, 0.9651348961777157509 ) ) ;
#96567=VECTOR ( 'NONE', #57019, 1000.000000000000000 ) ;
#96576=DIRECTION ( 'NONE',  ( -1.000000000000000000, -0.000000000000000000, -0.000000000000000000 ) ) ;
#96579=( BOUNDED_CURVE ( )  B_SPLINE_CURVE ( 3, ( #17755, #196406, #253807, #235529 ),
 .UNSPECIFIED., .F., .F. ) 
 B_SPLINE_CURVE_WITH_KNOTS ( ( 4, 4 ),
 ( 4.712388980384696779, 6.231880751915386263 ),
 .UNSPECIFIED. ) 
 CURVE ( )  GEOMETRIC_REPRESENTATION_ITEM ( )  RATIONAL_B_SPLINE_CURVE ( ( 1.000000000000000000, 0.8166740347213244933, 0.8166740347213244933, 1.000000000000000000 ) ) 
 REPRESENTATION_ITEM ( '' )  );
#96591=ORIENTED_EDGE ( 'NONE', *, *, #149896, .F. ) ;
#96598=EDGE_CURVE ( 'NONE', #173665, #90836, #208158, .T. ) ;
#96600=( BOUNDED_SURFACE ( )  B_SPLINE_SURFACE ( 3, 2, ( 
 ( #75713, #19590, #57399 ),
 ( #93967, #117394, #196923 ),
 ( #133113, #18291, #157849 ),
 ( #237348, #177400, #256846 ),
 ( #174854, #114823, #138215 ),
 ( #76975, #135655, #173572 ) ),
 .UNSPECIFIED., .F., .F., .F. ) 
 B_SPLINE_SURFACE_WITH_KNOTS ( ( 4, 2, 4 ),
 ( 3, 3 ),
 ( 0.0001300404313046487020, 0.0003183318589266567809, 0.0005066232865486648869 ),
 ( 0.000000000000000000, 1.000000000000000000 ),
 .UNSPECIFIED. ) 
 GEOMETRIC_REPRESENTATION_ITEM ( )  RATIONAL_B_SPLINE_SURFACE ( (
 ( 1.000000000000000000, 0.7071067811865732189, 1.000000000000000000),
 ( 1.000000000000000000, 0.7625113560535831114, 1.000000000000000000),
 ( 1.000000000000000000, 0.8126073484694227300, 1.000000000000000000),
 ( 1.000000000000000000, 0.8923049332726431526, 1.000000000000000000),
 ( 1.000000000000000000, 0.9231914937774265972, 1.000000000000000000),
 ( 1.000000000000000000, 0.9238795325112875156, 1.000000000000000000) ) ) 
 REPRESENTATION_ITEM ( '' )  SURFACE ( )  );
#96607=CARTESIAN_POINT ( 'NONE',  ( -18.59999999999999787, 70.22889768795992893, -198.1282601183952750 ) ) ;
#96669=AXIS2_PLACEMENT_3D ( 'NONE', #47434, #63147, #3170 ) ;
#96672=FACE_OUTER_BOUND ( 'NONE', #87201, .T. ) ;
#96685=EDGE_CURVE ( 'NONE', #114917, #53100, #225542, .T. ) ;
#96686=CARTESIAN_POINT ( 'NONE',  ( -20.94999999999999929, 76.00000000001126921, -203.5231074845248997 ) ) ;
#96725=CIRCLE ( 'NONE', #113504, 2.000000000000000000 ) ;
#96728=VECTOR ( 'NONE', #198104, 1000.000000000000000 ) ;
#96730=CIRCLE ( 'NONE', #42590, 0.1999999999999945155 ) ;
#96741=ORIENTED_EDGE ( 'NONE', *, *, #181861, .F. ) ;
#96750=DIRECTION ( 'NONE',  ( 1.000000000000000000, -2.849773892568378313E-16, 7.728835255496647986E-17 ) ) ;
#96757=ADVANCED_FACE ( 'NONE', ( #234554 ), #57172, .F. ) ;
#96759=LINE ( 'NONE', #177650, #33533 ) ;
#96762=FACE_OUTER_BOUND ( 'NONE', #228000, .T. ) ;
#96789=ADVANCED_FACE ( 'NONE', ( #52048 ), #255344, .T. ) ;
#96843=AXIS2_PLACEMENT_3D ( 'NONE', #69025, #148551, #49441 ) ;
#96864=AXIS2_PLACEMENT_3D ( 'NONE', #73620, #132273, #12358 ) ;
#96882=DIRECTION ( 'NONE',  ( 0.000000000000000000, 0.2617529984165152257, 0.9651348961777124202 ) ) ;
#96894=VECTOR ( 'NONE', #95543, 1000.000000000000000 ) ;
#96921=EDGE_CURVE ( 'NONE', #124804, #178010, #212614, .T. ) ;
#96983=ADVANCED_FACE ( 'NONE', ( #28385 ), #229181, .T. ) ;
#96991=EDGE_CURVE ( 'NONE', #249371, #29748, #58450, .T. ) ;
#97003=FACE_OUTER_BOUND ( 'NONE', #89941, .T. ) ;
#97011=LINE ( 'NONE', #176612, #74499 ) ;
#97022=CARTESIAN_POINT ( 'NONE',  ( -22.50000000000000000, 55.89093952297024970, -232.7795287750844579 ) ) ;
#97051=DIRECTION ( 'NONE',  ( 0.000000000000000000, -0.2617529984165152257, -0.9651348961777124202 ) ) ;
#97053=AXIS2_PLACEMENT_3D ( 'NONE', #36102, #215987, #170521 ) ;
#97056=ORIENTED_EDGE ( 'NONE', *, *, #109345, .F. ) ;
#97067=DIRECTION ( 'NONE',  ( 0.000000000000000000, 0.9651348961777157509, -0.2617529984165031243 ) ) ;
#97073=TOROIDAL_SURFACE ( 'NONE', #109591, 4.149999999999999467, 0.1000000000000000056 ) ;
#97075=EDGE_CURVE ( 'NONE', #118789, #122630, #8598, .T. ) ;
#97089=CARTESIAN_POINT ( 'NONE',  ( 20.87600722750343252, 67.49230083716666684, -195.4236814984208763 ) ) ;
#97095=CARTESIAN_POINT ( 'NONE',  ( -18.40000000000000213, 78.24390740893980478, -231.6169762517609456 ) ) ;
#97112=EDGE_CURVE ( 'NONE', #42158, #149408, #141854, .T. ) ;
#97143=CARTESIAN_POINT ( 'NONE',  ( 22.48660254037843842, 55.97436536266719997, -232.8539608197349935 ) ) ;
#97183=CIRCLE ( 'NONE', #89218, 11.79999999999999361 ) ;
#97189=CARTESIAN_POINT ( 'NONE',  ( 18.59999999999999076, 66.34920340998563404, -213.7018660128499334 ) ) ;
#97200=DIRECTION ( 'NONE',  ( 1.000000000000000000, -3.151514657663852580E-16, 8.547182517843351137E-17 ) ) ;
#97220=FACE_OUTER_BOUND ( 'NONE', #116757, .T. ) ;
#97221=CARTESIAN_POINT ( 'NONE',  ( 18.58222699835054570, 67.49225400653517681, -195.4205142095401584 ) ) ;
#97234=ORIENTED_EDGE ( 'NONE', *, *, #64242, .F. ) ;
#97256=VECTOR ( 'NONE', #163706, 1000.000000000000114 ) ;
#97278=ORIENTED_EDGE ( 'NONE', *, *, #38315, .T. ) ;
#97299=EDGE_CURVE ( 'NONE', #92030, #223374, #204869, .T. ) ;
#97336=ORIENTED_EDGE ( 'NONE', *, *, #224165, .T. ) ;
#97349=CIRCLE ( 'NONE', #72467, 0.1000000000000124678 ) ;
#97372=SPHERICAL_SURFACE ( 'NONE', #100998, 0.1000000000000000056 ) ;
#97462=ORIENTED_EDGE ( 'NONE', *, *, #57496, .T. ) ;
#97486=FACE_OUTER_BOUND ( 'NONE', #118845, .T. ) ;
#97495=VERTEX_POINT ( 'NONE', #38020 ) ;
#97513=VERTEX_POINT ( 'NONE', #156690 ) ;
#97531=DIRECTION ( 'NONE',  ( 0.000000000000000000, 0.2617529984165024026, 0.9651348961777158619 ) ) ;
#97542=AXIS2_PLACEMENT_3D ( 'NONE', #190515, #245334, #187930 ) ;
#97561=CARTESIAN_POINT ( 'NONE',  ( 21.56666275994539816, 65.41016251146582761, -242.5699255415354685 ) ) ;
#97612=ADVANCED_FACE ( 'NONE', ( #183922 ), #84200, .T. ) ;
#97631=CARTESIAN_POINT ( 'NONE',  ( 20.94999999999999574, 59.10678033798691189, -225.7992625810339575 ) ) ;
#97633=DIRECTION ( 'NONE',  ( -1.000000000000000000, -0.000000000000000000, 0.000000000000000000 ) ) ;
#97661=CARTESIAN_POINT ( 'NONE',  ( -22.57320508075687826, 55.89093952297026391, -232.7795287750844579 ) ) ;
#97667=DIRECTION ( 'NONE',  ( -0.000000000000000000, 0.9651348961777161950, -0.2617529984165014589 ) ) ;
#97701=DIRECTION ( 'NONE',  ( 0.000000000000000000, -0.2617529984165031243, -0.9651348961777157509 ) ) ;
#97740=LINE ( 'NONE', #157798, #21589 ) ;
#97794=CARTESIAN_POINT ( 'NONE',  ( -18.59999999999999787, 59.16775194334852728, -221.0793150863668473 ) ) ;
#97807=EDGE_LOOP ( 'NONE', ( #242763, #71648, #182326, #156929 ) ) ;
#97813=ORIENTED_EDGE ( 'NONE', *, *, #215601, .F. ) ;
#97837=FACE_OUTER_BOUND ( 'NONE', #11988, .T. ) ;
#97852=DIRECTION ( 'NONE',  ( -1.000000000000000000, 0.000000000000000000, 0.000000000000000000 ) ) ;
#97872=CARTESIAN_POINT ( 'NONE',  ( 20.94999999999999574, 58.93913529358839298, -225.8436373810195334 ) ) ;
#97886=CARTESIAN_POINT ( 'NONE',  ( -21.59142135623730852, 65.21721683441403172, -213.2912489251323507 ) ) ;
#97892=EDGE_LOOP ( 'NONE', ( #104946, #13814, #112409, #199331 ) ) ;
#97920=EDGE_LOOP ( 'NONE', ( #985, #209782, #119870, #193271, #90287, #77995, #209130, #80561, #112324, #141862, #55441, #159899, #230828, #157688, #257707, #179094 ) ) ;
#97987=AXIS2_PLACEMENT_3D ( 'NONE', #28484, #128835, #46703 ) ;
#98002=DIRECTION ( 'NONE',  ( -1.000000000000000000, -0.000000000000000000, 0.000000000000000000 ) ) ;
#98010=DIRECTION ( 'NONE',  ( 1.000000000000000000, 0.000000000000000000, 0.000000000000000000 ) ) ;
#98036=CARTESIAN_POINT ( 'NONE',  ( 18.54286124688534798, 87.05290861654455625, -199.5360271546132367 ) ) ;
#98043=ORIENTED_EDGE ( 'NONE', *, *, #52920, .F. ) ;
#98049=ORIENTED_EDGE ( 'NONE', *, *, #191362, .F. ) ;
#98063=CIRCLE ( 'NONE', #48030, 0.5000000000000014433 ) ;
#98104=DIRECTION ( 'NONE',  ( 0.000000000000000000, 0.2617529984164955192, 0.9651348961777178603 ) ) ;
#98109=ORIENTED_EDGE ( 'NONE', *, *, #173253, .F. ) ;
#98132=ORIENTED_EDGE ( 'NONE', *, *, #54203, .F. ) ;
#98169=DIRECTION ( 'NONE',  ( -0.000000000000000000, -0.9651348961777157509, 0.2617529984165031243 ) ) ;
#98181=CARTESIAN_POINT ( 'NONE',  ( -21.05000000000000071, 60.91865828504416669, -234.1430899377568267 ) ) ;
#98203=DIRECTION ( 'NONE',  ( 1.000000000000000000, 0.000000000000000000, 0.000000000000000000 ) ) ;
#98209=DIRECTION ( 'NONE',  ( -0.000000000000000000, -0.9651348961777157509, 0.2617529984165031243 ) ) ;
#98232=CARTESIAN_POINT ( 'NONE',  ( -18.50000000000000000, 79.19526988099229925, -196.1889237952725296 ) ) ;
#98269=CARTESIAN_POINT ( 'NONE',  ( -22.45372860728439690, 64.16750481150683072, -247.0948467376672113 ) ) ;
#98312=AXIS2_PLACEMENT_3D ( 'NONE', #2410, #178532, #81924 ) ;
#98319=FACE_OUTER_BOUND ( 'NONE', #4275, .T. ) ;
#98322=CARTESIAN_POINT ( 'NONE',  ( 21.09610168723073187, 65.52914536258586509, -242.0028871142699245 ) ) ;
#98375=CARTESIAN_POINT ( 'NONE',  ( -18.54159361262911077, 78.20960248048282892, -231.5287758789899044 ) ) ;
#98376=EDGE_CURVE ( 'NONE', #195218, #44096, #201151, .T. ) ;
#98388=EDGE_CURVE ( 'NONE', #87098, #146093, #13100, .T. ) ;
#98393=CARTESIAN_POINT ( 'NONE',  ( -20.85000000000000142, 87.34033503009941057, -206.5987052159188124 ) ) ;
#98400=CARTESIAN_POINT ( 'NONE',  ( -20.54999999999999716, 67.41730047816177773, -218.5504914523898208 ) ) ;
#98405=DIRECTION ( 'NONE',  ( 0.000000000000000000, 0.2617529984164506107, 0.9651348961777299618 ) ) ;
#98443=CARTESIAN_POINT ( 'NONE',  ( -20.94999999999999929, 70.08587962373171365, -198.1273832143211848 ) ) ;
#98462=EDGE_CURVE ( 'NONE', #82116, #148169, #33796, .T. ) ;
#98475=LINE ( 'NONE', #677, #9616 ) ;
#98518=VECTOR ( 'NONE', #89293, 1000.000000000000114 ) ;
#98519=CARTESIAN_POINT ( 'NONE',  ( -23.15000000000000213, 86.30329675166747450, -209.4258251677035787 ) ) ;
#98554=AXIS2_PLACEMENT_3D ( 'NONE', #230520, #247508, #27211 ) ;
#98568=FACE_OUTER_BOUND ( 'NONE', #188005, .T. ) ;
#98574=EDGE_LOOP ( 'NONE', ( #26034, #164338, #96441, #104470 ) ) ;
#98579=DIRECTION ( 'NONE',  ( 1.000000000000000000, 0.000000000000000000, 0.000000000000000000 ) ) ;
#98581=ORIENTED_EDGE ( 'NONE', *, *, #50248, .T. ) ;
#98612=DIRECTION ( 'NONE',  ( -0.000000000000000000, 0.5041370733442164243, 0.8636236514130032349 ) ) ;
#98678=EDGE_CURVE ( 'NONE', #9680, #133293, #225252, .T. ) ;
#98708=AXIS2_PLACEMENT_3D ( 'NONE', #81421, #180562, #83969 ) ;
#98711=PLANE ( 'NONE',  #227491 ) ;
#98738=CYLINDRICAL_SURFACE ( 'NONE', #55705, 4.049999999999987388 ) ;
#98741=AXIS2_PLACEMENT_3D ( 'NONE', #226801, #208548, #29917 ) ;
#98746=EDGE_CURVE ( 'NONE', #96108, #12116, #194997, .T. ) ;
#98780=CARTESIAN_POINT ( 'NONE',  ( 23.15000000000000213, 78.50726470275242264, -228.6618886302502176 ) ) ;
#98793=DIRECTION ( 'NONE',  ( 1.000000000000000000, 0.000000000000000000, 0.000000000000000000 ) ) ;
#98838=CARTESIAN_POINT ( 'NONE',  ( 22.39999999999999503, 65.19201463318205469, -243.3742797652979277 ) ) ;
#98858=EDGE_LOOP ( 'NONE', ( #207349, #247140, #141242, #46917 ) ) ;
#98862=AXIS2_PLACEMENT_3D ( 'NONE', #48532, #105913, #128079 ) ;
#98887=ORIENTED_EDGE ( 'NONE', *, *, #9901, .T. ) ;
#98889=ORIENTED_EDGE ( 'NONE', *, *, #196269, .T. ) ;
#98890=CARTESIAN_POINT ( 'NONE',  ( 20.02499999999999858, 63.38346053167636995, -212.7939182281409956 ) ) ;
#98902=EDGE_LOOP ( 'NONE', ( #240332, #187215, #253677, #70856 ) ) ;
#98955=DIRECTION ( 'NONE',  ( 0.000000000000000000, 0.2617529984165031243, 0.9651348961777157509 ) ) ;
#98973=DIRECTION ( 'NONE',  ( 1.000000000000000000, -0.000000000000000000, -0.000000000000000000 ) ) ;
#99034=EDGE_CURVE ( 'NONE', #185637, #188542, #163132, .T. ) ;
#99093=ORIENTED_EDGE ( 'NONE', *, *, #188260, .T. ) ;
#99096=EDGE_CURVE ( 'NONE', #78772, #47754, #83949, .T. ) ;
#99124=CARTESIAN_POINT ( 'NONE',  ( 18.59999999999999787, 85.07617159379665850, -214.9471220678560428 ) ) ;
#99127=CARTESIAN_POINT ( 'NONE',  ( 20.95429402530552210, 60.89549333153017585, -225.3058276775725801 ) ) ;
#99142=VERTEX_POINT ( 'NONE', #238492 ) ;
#99154=FACE_OUTER_BOUND ( 'NONE', #74706, .T. ) ;
#99183=DIRECTION ( 'NONE',  ( 0.000000000000000000, 0.2617529984165152257, 0.9651348961777124202 ) ) ;
#99210=CARTESIAN_POINT ( 'NONE',  ( 23.25000000000000000, 78.00142589229885459, -228.9845759368473637 ) ) ;
#99222=DIRECTION ( 'NONE',  ( 0.000000000000000000, 0.2617529984165030132, 0.9651348961777157509 ) ) ;
#99297=CARTESIAN_POINT ( 'NONE',  ( 20.94999999999999574, 68.58368164137472434, -224.2353459317783120 ) ) ;
#99302=VERTEX_POINT ( 'NONE', #229212 ) ;
#99306=EDGE_CURVE ( 'NONE', #117062, #17708, #83584, .T. ) ;
#99310=AXIS2_PLACEMENT_3D ( 'NONE', #49594, #208689, #75602 ) ;
#99360=DIRECTION ( 'NONE',  ( 0.000000000000000000, 0.9651348961777379554, -0.2617529984164210233 ) ) ;
#99401=CARTESIAN_POINT ( 'NONE',  ( 20.04142135623731136, 62.34315093393703933, -208.9889535843037720 ) ) ;
#99433=CARTESIAN_POINT ( 'NONE',  ( 20.94999999999999574, 67.23127455305841238, -235.8551265064783991 ) ) ;
#99435=DIRECTION ( 'NONE',  ( 0.000000000000000000, 0.2617529984164856383, 0.9651348961777204138 ) ) ;
#99444=ORIENTED_EDGE ( 'NONE', *, *, #15526, .F. ) ;
#99453=DIRECTION ( 'NONE',  ( -1.000000000000000000, -0.000000000000000000, -0.000000000000000000 ) ) ;
#99487=AXIS2_PLACEMENT_3D ( 'NONE', #109155, #170486, #67473 ) ;
#99514=CYLINDRICAL_SURFACE ( 'NONE', #142979, 0.5000000000000014433 ) ;
#99531=AXIS2_PLACEMENT_3D ( 'NONE', #149400, #8583, #132374 ) ;
#99533=CIRCLE ( 'NONE', #253672, 1.900000000000000799 ) ;
#99565=CARTESIAN_POINT ( 'NONE',  ( -22.49917693094574389, 64.09964716284724773, -247.0764417527830119 ) ) ;
#99578=CYLINDRICAL_SURFACE ( 'NONE', #227051, 0.09999999999999543976 ) ;
#99597=EDGE_CURVE ( 'NONE', #182549, #222045, #125323, .T. ) ;
#99603=EDGE_LOOP ( 'NONE', ( #230066, #45913, #257589, #158951 ) ) ;
#99608=EDGE_CURVE ( 'NONE', #1095, #122095, #102485, .T. ) ;
#99645=ORIENTED_EDGE ( 'NONE', *, *, #185543, .T. ) ;
#99667=ORIENTED_EDGE ( 'NONE', *, *, #14282, .T. ) ;
#99670=CARTESIAN_POINT ( 'NONE',  ( 20.94788355080264353, 67.49401193140447219, -195.5283494629371432 ) ) ;
#99716=CARTESIAN_POINT ( 'NONE',  ( 20.94999999999999929, 62.98048128140160173, -207.0210305352945568 ) ) ;
#99735=EDGE_CURVE ( 'NONE', #72740, #148469, #183765, .T. ) ;
#99742=DIRECTION ( 'NONE',  ( 0.000000000000000000, 0.2617529984165027912, 0.9651348961777158619 ) ) ;
#99757=CARTESIAN_POINT ( 'NONE',  ( 21.05000000000000071, 68.03098227380377239, -227.7073825336181869 ) ) ;
#99774=CIRCLE ( 'NONE', #245565, 7.899999999999996803 ) ;
#99779=DIRECTION ( 'NONE',  ( 1.000000000000000000, 0.000000000000000000, 0.000000000000000000 ) ) ;
#99786=ORIENTED_EDGE ( 'NONE', *, *, #98746, .T. ) ;
#99790=ORIENTED_EDGE ( 'NONE', *, *, #10772, .F. ) ;
#99803=CARTESIAN_POINT ( 'NONE',  ( 18.55807992284871943, 67.49241595948059569, -195.4314365843280541 ) ) ;
#99829=AXIS2_PLACEMENT_3D ( 'NONE', #201278, #82582, #1781 ) ;
#99849=CARTESIAN_POINT ( 'NONE',  ( 21.05000000000000071, 79.23417978893664326, -236.1056577391152587 ) ) ;
#99850=CARTESIAN_POINT ( 'NONE',  ( -20.94999999999999929, 57.72708596674831938, -226.0092949359174952 ) ) ;
#99872=DIRECTION ( 'NONE',  ( 0.000000000000000000, -0.9651348961777157509, 0.2617529984165031243 ) ) ;
#99919=CIRCLE ( 'NONE', #91584, 1.900000000000000799 ) ;
#99930=ADVANCED_FACE ( 'NONE', ( #131065 ), #94499, .T. ) ;
#99937=ORIENTED_EDGE ( 'NONE', *, *, #238439, .F. ) ;
#99941=FACE_OUTER_BOUND ( 'NONE', #242944, .T. ) ;
#99951=LINE ( 'NONE', #81660, #36780 ) ;
#99992=DIRECTION ( 'NONE',  ( 0.000000000000000000, 0.9651348961777160840, -0.2617529984165018475 ) ) ;
#100055=DIRECTION ( 'NONE',  ( -0.000000000000000000, -0.2617529984165031243, -0.9651348961777157509 ) ) ;
#100077=CARTESIAN_POINT ( 'NONE',  ( 21.05000000000000071, 75.24091630460340241, -206.3219986834402846 ) ) ;
#100079=ORIENTED_EDGE ( 'NONE', *, *, #102915, .T. ) ;
#100085=EDGE_LOOP ( 'NONE', ( #131803, #251475, #49885, #129503 ) ) ;
#100090=ADVANCED_FACE ( 'NONE', ( #158377 ), #198740, .F. ) ;
#100095=DIRECTION ( 'NONE',  ( 1.000000000000000000, 0.000000000000000000, -0.000000000000000000 ) ) ;
#100117=FACE_OUTER_BOUND ( 'NONE', #253139, .T. ) ;
#100130=CARTESIAN_POINT ( 'NONE',  ( 21.14999999999999858, 65.51923798433685420, -242.1677427744926092 ) ) ;
#100131=FACE_OUTER_BOUND ( 'NONE', #76347, .T. ) ;
#100135=AXIS2_PLACEMENT_3D ( 'NONE', #65199, #45648, #245130 ) ;
#100154=ORIENTED_EDGE ( 'NONE', *, *, #98388, .F. ) ;
#100179=EDGE_LOOP ( 'NONE', ( #157770, #35390, #118538 ) ) ;
#100203=DIRECTION ( 'NONE',  ( 0.000000000000000000, 0.2617529984165031243, 0.9651348961777157509 ) ) ;
#100205=DIRECTION ( 'NONE',  ( -2.252264143451594314E-15, 0.3848449534832963370, 0.9229812358755945523 ) ) ;
#100242=CYLINDRICAL_SURFACE ( 'NONE', #215514, 0.1000000000000066530 ) ;
#100279=AXIS2_PLACEMENT_3D ( 'NONE', #217130, #118053, #197584 ) ;
#100317=DIRECTION ( 'NONE',  ( 1.000000000000000000, 0.000000000000000000, 0.000000000000000000 ) ) ;
#100331=CARTESIAN_POINT ( 'NONE',  ( 21.30000000000002558, 66.17117490947157421, -239.7639228359981303 ) ) ;
#100366=DIRECTION ( 'NONE',  ( 1.000000000000000000, 0.000000000000000000, 0.000000000000000000 ) ) ;
#100376=CARTESIAN_POINT ( 'NONE',  ( 18.59999999999999787, 72.02722222756958104, -225.1832529173024398 ) ) ;
#100379=ORIENTED_EDGE ( 'NONE', *, *, #20959, .F. ) ;
#100384=EDGE_LOOP ( 'NONE', ( #122308, #43968, #154791, #103756 ) ) ;
#100396=AXIS2_PLACEMENT_3D ( 'NONE', #33669, #146173, #93589 ) ;
#100404=EDGE_LOOP ( 'NONE', ( #245114, #247809, #257100, #213039 ) ) ;
#100412=ADVANCED_FACE ( 'NONE', ( #76922 ), #18245, .F. ) ;
#100431=CARTESIAN_POINT ( 'NONE',  ( 21.05000000000000071, 68.01971615331018484, -227.7939507667808527 ) ) ;
#100432=SPHERICAL_SURFACE ( 'NONE', #209861, 0.1000000000000000056 ) ;
#100435=ORIENTED_EDGE ( 'NONE', *, *, #69755, .T. ) ;
#100446=ORIENTED_EDGE ( 'NONE', *, *, #188020, .T. ) ;
#100463=VERTEX_POINT ( 'NONE', #136901 ) ;
#100487=ORIENTED_EDGE ( 'NONE', *, *, #255207, .F. ) ;
#100493=CARTESIAN_POINT ( 'NONE',  ( 21.13920837816993270, 61.96073055383985206, -221.7331827770995574 ) ) ;
#100530=CIRCLE ( 'NONE', #58843, 0.1000000000000088318 ) ;
#100535=ORIENTED_EDGE ( 'NONE', *, *, #52489, .T. ) ;
#100541=EDGE_CURVE ( 'NONE', #74935, #139316, #58630, .T. ) ;
#100544=DIRECTION ( 'NONE',  ( -0.000000000000000000, 0.9667078373770138233, 0.2558827019434041783 ) ) ;
#100545=DIRECTION ( 'NONE',  ( 0.000000000000000000, 0.2617529984165035684, 0.9651348961777156399 ) ) ;
#100567=EDGE_CURVE ( 'NONE', #148919, #109963, #83312, .T. ) ;
#100587=CARTESIAN_POINT ( 'NONE',  ( 21.46681500598292658, 65.43630044540458357, -242.4735498273664689 ) ) ;
#100590=DIRECTION ( 'NONE',  ( 0.000000000000000000, 0.2617529984165152257, 0.9651348961777124202 ) ) ;
#100599=CARTESIAN_POINT ( 'NONE',  ( 18.59999999999999787, 72.02722222756958104, -225.1832529173024398 ) ) ;
#100606=AXIS2_PLACEMENT_3D ( 'NONE', #133069, #172235, #213879 ) ;
#100613=FACE_OUTER_BOUND ( 'NONE', #119548, .T. ) ;
#100632=EDGE_LOOP ( 'NONE', ( #46559, #61412, #135993, #108006 ) ) ;
#100639=CYLINDRICAL_SURFACE ( 'NONE', #170097, 7.900000000000010125 ) ;
#100640=VECTOR ( 'NONE', #125981, 1000.000000000000114 ) ;
#100647=LINE ( 'NONE', #182811, #230394 ) ;
#100651=ORIENTED_EDGE ( 'NONE', *, *, #180549, .F. ) ;
#100655=DIRECTION ( 'NONE',  ( 0.000000000000000000, -0.2617529984165036239, -0.9651348961777156399 ) ) ;
#100661=AXIS2_PLACEMENT_3D ( 'NONE', #66608, #67884, #247806 ) ;
#100700=SPHERICAL_SURFACE ( 'NONE', #229492, 0.1000000000000000056 ) ;
#100707=CIRCLE ( 'NONE', #30048, 0.1999999999999987899 ) ;
#100710=AXIS2_PLACEMENT_3D ( 'NONE', #22491, #101971, #45878 ) ;
#100734=ORIENTED_EDGE ( 'NONE', *, *, #157850, .F. ) ;
#100740=CARTESIAN_POINT ( 'NONE',  ( 22.39999999999999858, 65.09550114356429162, -243.3481044654562879 ) ) ;
#100748=CARTESIAN_POINT ( 'NONE',  ( -21.52071067811865746, 65.25928687755708779, -213.4062711467677502 ) ) ;
#100754=DIRECTION ( 'NONE',  ( 0.000000000000000000, 0.2617529984164915779, 0.9651348961777189706 ) ) ;
#100767=DIRECTION ( 'NONE',  ( -0.000000000000000000, 0.2617529984165031243, 0.9651348961777157509 ) ) ;
#100781=ORIENTED_EDGE ( 'NONE', *, *, #117134, .T. ) ;
#100814=CYLINDRICAL_SURFACE ( 'NONE', #82048, 2.000000000000013323 ) ;
#100820=CARTESIAN_POINT ( 'NONE',  ( -23.15000000000000213, 52.91185528119410009, -244.1460391050142960 ) ) ;
#100821=CIRCLE ( 'NONE', #9292, 0.09999999999999939493 ) ;
#100842=DIRECTION ( 'NONE',  ( 0.000000000000000000, -0.2617529984164506107, -0.9651348961777299618 ) ) ;
#100871=EDGE_CURVE ( 'NONE', #81393, #74489, #234171, .T. ) ;
#100872=ADVANCED_FACE ( 'NONE', ( #82677 ), #67003, .T. ) ;
#100909=DIRECTION ( 'NONE',  ( 1.000000000000000000, -2.849773892568378313E-16, 7.728835255496647986E-17 ) ) ;
#100915=EDGE_CURVE ( 'NONE', #180985, #200249, #225960, .T. ) ;
#100931=ORIENTED_EDGE ( 'NONE', *, *, #35526, .F. ) ;
#100940=ORIENTED_EDGE ( 'NONE', *, *, #10747, .F. ) ;
#100942=CARTESIAN_POINT ( 'NONE',  ( 21.76363531954645936, 60.43693072858058457, -234.1150195010416724 ) ) ;
#100945=CARTESIAN_POINT ( 'NONE',  ( -23.25000000000000000, 70.22659352830977753, -197.9852579278363578 ) ) ;
#100952=DIRECTION ( 'NONE',  ( 0.000000000000000000, 0.2617529984165023471, 0.9651348961777159730 ) ) ;
#100975=CIRCLE ( 'NONE', #234288, 4.000000000000000000 ) ;
#100977=VERTEX_POINT ( 'NONE', #186985 ) ;
#100998=AXIS2_PLACEMENT_3D ( 'NONE', #76557, #137800, #59530 ) ;
#101029=ORIENTED_EDGE ( 'NONE', *, *, #229601, .T. ) ;
#101046=EDGE_CURVE ( 'NONE', #101652, #40848, #13616, .T. ) ;
#101074=ORIENTED_EDGE ( 'NONE', *, *, #185387, .T. ) ;
#101113=VERTEX_POINT ( 'NONE', #178992 ) ;
#101156=DIRECTION ( 'NONE',  ( 2.465190328815662439E-32, -0.2617529984165030132, -0.9651348961777158619 ) ) ;
#101163=EDGE_CURVE ( 'NONE', #216037, #186212, #9510, .T. ) ;
#101169=VECTOR ( 'NONE', #135722, 1000.000000000000000 ) ;
#101232=CARTESIAN_POINT ( 'NONE',  ( 18.50000000000000000, 78.21362219944487038, -231.2727646510690533 ) ) ;
#101262=CARTESIAN_POINT ( 'NONE',  ( 22.39999999999999858, 59.68594599439719417, -233.9123800762197902 ) ) ;
#101285=CARTESIAN_POINT ( 'NONE',  ( 23.14999999999999503, 61.54970422893870108, -212.2965875311496688 ) ) ;
#101286=ADVANCED_FACE ( 'NONE', ( #203644 ), #142946, .T. ) ;
#101293=CARTESIAN_POINT ( 'NONE',  ( -20.64999999999999858, 70.73902226565648732, -215.2805781460175467 ) ) ;
#101312=CIRCLE ( 'NONE', #213810, 0.09999999999999939493 ) ;
#101319=VERTEX_POINT ( 'NONE', #125399 ) ;
#101334=CARTESIAN_POINT ( 'NONE',  ( 20.85000000000000142, 80.78317333349157536, -192.9003134612049166 ) ) ;
#101338=DIRECTION ( 'NONE',  ( 2.952720810173289112E-16, 0.9651348961777157509, -0.2617529984165031243 ) ) ;
#101361=AXIS2_PLACEMENT_3D ( 'NONE', #250238, #233272, #190279 ) ;
#101384=CARTESIAN_POINT ( 'NONE',  ( 21.53699400377785622, 60.68021703623425367, -234.0784225921813686 ) ) ;
#101409=DIRECTION ( 'NONE',  ( 1.000000000000000000, 0.000000000000000000, 0.000000000000000000 ) ) ;
#101412=ORIENTED_EDGE ( 'NONE', *, *, #61908, .T. ) ;
#101417=VERTEX_POINT ( 'NONE', #210075 ) ;
#101479=EDGE_CURVE ( 'NONE', #46658, #132077, #133099, .T. ) ;
#101563=LINE ( 'NONE', #66331, #35695 ) ;
#101578=ORIENTED_EDGE ( 'NONE', *, *, #94623, .F. ) ;
#101588=DIRECTION ( 'NONE',  ( 1.000000000000000000, 0.000000000000000000, -0.000000000000000000 ) ) ;
#101608=EDGE_LOOP ( 'NONE', ( #55167, #242146, #220353, #226045 ) ) ;
#101641=AXIS2_PLACEMENT_3D ( 'NONE', #46195, #104850, #187028 ) ;
#101652=VERTEX_POINT ( 'NONE', #241198 ) ;
#101665=DIRECTION ( 'NONE',  ( 0.000000000000000000, 0.3994087351226822125, 0.9167729611565227366 ) ) ;
#101668=EDGE_CURVE ( 'NONE', #140695, #206043, #204604, .T. ) ;
#101693=ORIENTED_EDGE ( 'NONE', *, *, #169692, .F. ) ;
#101716=AXIS2_PLACEMENT_3D ( 'NONE', #93315, #216793, #98104 ) ;
#101746=CARTESIAN_POINT ( 'NONE',  ( 18.60000000000001563, 78.14847862149032665, -231.3763292744987723 ) ) ;
#101767=ORIENTED_EDGE ( 'NONE', *, *, #208725, .F. ) ;
#101777=DIRECTION ( 'NONE',  ( 0.000000000000000000, 0.2617529984165031243, 0.9651348961777157509 ) ) ;
#101793=VERTEX_POINT ( 'NONE', #151070 ) ;
#101795=CIRCLE ( 'NONE', #247583, 7.799999999999997158 ) ;
#101827=AXIS2_PLACEMENT_3D ( 'NONE', #14448, #178664, #194539 ) ;
#101834=ORIENTED_EDGE ( 'NONE', *, *, #197806, .F. ) ;
#101873=EDGE_CURVE ( 'NONE', #15176, #88490, #245028, .T. ) ;
#101903=CARTESIAN_POINT ( 'NONE',  ( -23.25000000000000000, 70.22659352830977753, -197.9852579278363578 ) ) ;
#101906=PLANE ( 'NONE',  #86925 ) ;
#101908=AXIS2_PLACEMENT_3D ( 'NONE', #246896, #49991, #70874 ) ;
#101918=CARTESIAN_POINT ( 'NONE',  ( -18.59999999999999787, 68.11887992016828264, -227.8068560890360175 ) ) ;
#101928=LINE ( 'NONE', #61553, #181067 ) ;
#101946=DIRECTION ( 'NONE',  ( -1.000000000000000000, 0.000000000000000000, 0.000000000000000000 ) ) ;
#101949=CARTESIAN_POINT ( 'NONE',  ( -20.99551997958407057, 62.86709121503487552, -207.0570825002662332 ) ) ;
#101959=CARTESIAN_POINT ( 'NONE',  ( 19.97071067811865674, 62.37141908057010653, -208.9966201521277753 ) ) ;
#101971=DIRECTION ( 'NONE',  ( 1.000000000000000000, 0.000000000000000000, 0.000000000000000000 ) ) ;
#101972=CARTESIAN_POINT ( 'NONE',  ( 21.12400247839529399, 60.09006653341421611, -221.2258423852895817 ) ) ;
#101973=CARTESIAN_POINT ( 'NONE',  ( -21.40925344232282512, 60.77900513643817249, -234.2077395100402839 ) ) ;
#101985=AXIS2_PLACEMENT_3D ( 'NONE', #48977, #89377, #88077 ) ;
#102000=CARTESIAN_POINT ( 'NONE',  ( 23.14999999999999503, 62.82351852614503684, -207.2177435922979214 ) ) ;
#102022=CIRCLE ( 'NONE', #64459, 0.1000000000000124678 ) ;
#102026=EDGE_CURVE ( 'NONE', #15176, #12050, #1670, .T. ) ;
#102044=CARTESIAN_POINT ( 'NONE',  ( -23.15000000000000213, 66.36210077474692071, -222.8232602954134336 ) ) ;
#102047=ORIENTED_EDGE ( 'NONE', *, *, #12277, .T. ) ;
#102147=DIRECTION ( 'NONE',  ( 1.000000000000000000, -0.000000000000000000, -0.000000000000000000 ) ) ;
#102169=EDGE_CURVE ( 'NONE', #232695, #235134, #139212, .T. ) ;
#102173=ORIENTED_EDGE ( 'NONE', *, *, #161292, .F. ) ;
#102210=CARTESIAN_POINT ( 'NONE',  ( -21.14999999999999858, 67.23127455305841238, -235.8551265064783991 ) ) ;
#102239=EDGE_LOOP ( 'NONE', ( #146978, #142063, #126150 ) ) ;
#102251=TOROIDAL_SURFACE ( 'NONE', #248036, 0.2000000000000000111, 0.1000000000000000056 ) ;
#102256=ORIENTED_EDGE ( 'NONE', *, *, #39419, .F. ) ;
#102375=VERTEX_POINT ( 'NONE', #37241 ) ;
#102395=EDGE_CURVE ( 'NONE', #166406, #133646, #249682, .T. ) ;
#102402=CARTESIAN_POINT ( 'NONE',  ( -23.25000000000000000, 80.78317333349157536, -192.9003134612049166 ) ) ;
#102416=AXIS2_PLACEMENT_3D ( 'NONE', #213036, #55216, #194789 ) ;
#102440=ORIENTED_EDGE ( 'NONE', *, *, #53978, .F. ) ;
#102485=LINE ( 'NONE', #161223, #104440 ) ;
#102490=CARTESIAN_POINT ( 'NONE',  ( -21.07928932188134041, 61.09751618602744827, -234.2940654522722639 ) ) ;
#102501=DIRECTION ( 'NONE',  ( 0.000000000000000000, 0.2617529984165152257, 0.9651348961777124202 ) ) ;
#102532=DIRECTION ( 'NONE',  ( 1.000000000000000000, 0.000000000000000000, 0.000000000000000000 ) ) ;
#102534=CARTESIAN_POINT ( 'NONE',  ( -20.64999999999999858, 78.50726470275243685, -228.6618886302502176 ) ) ;
#102557=ADVANCED_FACE ( 'NONE', ( #167162 ), #151435, .F. ) ;
#102563=AXIS2_PLACEMENT_3D ( 'NONE', #224944, #183273, #144117 ) ;
#102566=SPHERICAL_SURFACE ( 'NONE', #23547, 0.1000000000000000056 ) ;
#102577=CARTESIAN_POINT ( 'NONE',  ( 20.94999999999999574, 79.23417978893664326, -236.1056577391152587 ) ) ;
#102663=FACE_OUTER_BOUND ( 'NONE', #248797, .T. ) ;
#102752=CYLINDRICAL_SURFACE ( 'NONE', #40699, 0.1000000000000106498 ) ;
#102766=CARTESIAN_POINT ( 'NONE',  ( -20.64999999999999858, 63.56320957583155717, -222.0641766000055668 ) ) ;
#102777=LINE ( 'NONE', #1113, #134431 ) ;
#102780=ORIENTED_EDGE ( 'NONE', *, *, #242099, .F. ) ;
#102791=EDGE_CURVE ( 'NONE', #52077, #208014, #14741, .T. ) ;
#102810=CARTESIAN_POINT ( 'NONE',  ( -18.59999999999999787, 70.17424292862648372, -198.1782849070719124 ) ) ;
#102814=CARTESIAN_POINT ( 'NONE',  ( 21.05000000000000071, 59.06404522663466139, -225.9140184048775950 ) ) ;
#102857=ORIENTED_EDGE ( 'NONE', *, *, #127930, .F. ) ;
#102860=VECTOR ( 'NONE', #40716, 1000.000000000000000 ) ;
#102915=EDGE_CURVE ( 'NONE', #70163, #4833, #243666, .T. ) ;
#102936=AXIS2_PLACEMENT_3D ( 'NONE', #112640, #236116, #150490 ) ;
#102938=CIRCLE ( 'NONE', #244422, 0.09999999999999543976 ) ;
#102950=DIRECTION ( 'NONE',  ( 0.000000000000000000, 0.2617529984165152257, 0.9651348961777124202 ) ) ;
#103053=CARTESIAN_POINT ( 'NONE',  ( -18.44204374631830490, 86.89455847109682907, -199.6122366425948655 ) ) ;
#103056=DIRECTION ( 'NONE',  ( -1.000000000000000000, -0.000000000000000000, 0.000000000000000000 ) ) ;
#103135=DIRECTION ( 'NONE',  ( 0.000000000000000000, -0.2617529984165152257, -0.9651348961777124202 ) ) ;
#103137=ORIENTED_EDGE ( 'NONE', *, *, #197969, .T. ) ;
#103158=DIRECTION ( 'NONE',  ( 0.000000000000000000, 0.2617529984165039569, 0.9651348961777155289 ) ) ;
#103159=LINE ( 'NONE', #143588, #134776 ) ;
#103168=VECTOR ( 'NONE', #67580, 1000.000000000000000 ) ;
#103177=CYLINDRICAL_SURFACE ( 'NONE', #16103, 0.1000000000000124678 ) ;
#103187=ORIENTED_EDGE ( 'NONE', *, *, #225224, .F. ) ;
#103193=FACE_OUTER_BOUND ( 'NONE', #132608, .T. ) ;
#103272=ADVANCED_FACE ( 'NONE', ( #24455 ), #173169, .T. ) ;
#103295=ADVANCED_FACE ( 'NONE', ( #238334, #40169 ), #21868, .F. ) ;
#103300=VECTOR ( 'NONE', #154381, 1000.000000000000000 ) ;
#103314=CARTESIAN_POINT ( 'NONE',  ( 18.59999999999999432, 86.96699927712941758, -199.3055931863049182 ) ) ;
#103341=EDGE_CURVE ( 'NONE', #204834, #176771, #64827, .T. ) ;
#103365=ORIENTED_EDGE ( 'NONE', *, *, #114051, .F. ) ;
#103382=CYLINDRICAL_SURFACE ( 'NONE', #139815, 0.09999999999999543976 ) ;
#103393=ORIENTED_EDGE ( 'NONE', *, *, #8795, .F. ) ;
#103409=FACE_OUTER_BOUND ( 'NONE', #209541, .T. ) ;
#103418=DIRECTION ( 'NONE',  ( -1.000000000000000000, 0.000000000000000000, 0.000000000000000000 ) ) ;
#103422=ORIENTED_EDGE ( 'NONE', *, *, #175378, .T. ) ;
#103429=CIRCLE ( 'NONE', #224257, 0.1000000000000124678 ) ;
#103441=EDGE_LOOP ( 'NONE', ( #123057, #193489, #154318, #156988 ) ) ;
#103465=ORIENTED_EDGE ( 'NONE', *, *, #170737, .T. ) ;
#103491=FACE_OUTER_BOUND ( 'NONE', #7561, .T. ) ;
#103519=ADVANCED_FACE ( 'NONE', ( #127381 ), #191233, .F. ) ;
#103532=EDGE_CURVE ( 'NONE', #216635, #110447, #167820, .T. ) ;
#103533=AXIS2_PLACEMENT_3D ( 'NONE', #60150, #22350, #158032 ) ;
#103535=DIRECTION ( 'NONE',  ( 0.000000000000000000, 0.2617529984165032908, 0.9651348961777156399 ) ) ;
#103545=CARTESIAN_POINT ( 'NONE',  ( 20.85000000000000142, 62.98048128140160173, -207.0210305352945568 ) ) ;
#103550=ORIENTED_EDGE ( 'NONE', *, *, #159485, .F. ) ;
#103577=AXIS2_PLACEMENT_3D ( 'NONE', #102210, #25300, #185644 ) ;
#103589=AXIS2_PLACEMENT_3D ( 'NONE', #244167, #184195, #143788 ) ;
#103605=DIRECTION ( 'NONE',  ( -3.265361837132813093E-16, -0.9651348961777158619, 0.2617529984165024026 ) ) ;
#103623=ADVANCED_FACE ( 'NONE', ( #33456 ), #17684, .T. ) ;
#103650=VERTEX_POINT ( 'NONE', #20281 ) ;
#103669=DIRECTION ( 'NONE',  ( 0.000000000000000000, 0.2617529984165036239, 0.9651348961777156399 ) ) ;
#103670=ORIENTED_EDGE ( 'NONE', *, *, #225396, .T. ) ;
#103672=AXIS2_PLACEMENT_3D ( 'NONE', #159703, #181826, #220932 ) ;
#103677=CARTESIAN_POINT ( 'NONE',  ( -18.59999999999999787, 80.82423061532404063, -192.8091306798888525 ) ) ;
#103680=ORIENTED_EDGE ( 'NONE', *, *, #230400, .T. ) ;
#103686=VERTEX_POINT ( 'NONE', #81485 ) ;
#103708=CARTESIAN_POINT ( 'NONE',  ( 18.49999999999999289, 70.22659352830977753, -197.9852579278363578 ) ) ;
#103742=ADVANCED_FACE ( 'NONE', ( #39856 ), #144044, .T. ) ;
#103756=ORIENTED_EDGE ( 'NONE', *, *, #46370, .F. ) ;
#103792=EDGE_CURVE ( 'NONE', #151240, #94361, #243455, .T. ) ;
#103794=CARTESIAN_POINT ( 'NONE',  ( -23.25000000000000000, 80.78317333349157536, -192.9003134612049166 ) ) ;
#103810=CYLINDRICAL_SURFACE ( 'NONE', #24141, 0.1000000000000124678 ) ;
#103823=ORIENTED_EDGE ( 'NONE', *, *, #192496, .T. ) ;
#103829=CARTESIAN_POINT ( 'NONE',  ( 18.47073956224749480, 78.23349094678856375, -231.4735393943770134 ) ) ;
#103910=CARTESIAN_POINT ( 'NONE',  ( 18.46932045258648714, 87.08041872038211295, -199.6132627942399438 ) ) ;
#103915=CARTESIAN_POINT ( 'NONE',  ( -20.94999999999999929, 79.26035508877831148, -236.0091442494974956 ) ) ;
#103944=DIRECTION ( 'NONE',  ( 0.000000000000000000, 0.2617529984165031243, 0.9651348961777157509 ) ) ;
#103996=AXIS2_PLACEMENT_3D ( 'NONE', #88819, #168441, #54834 ) ;
#103998=DIRECTION ( 'NONE',  ( 1.000000000000000000, 0.000000000000000000, 0.000000000000000000 ) ) ;
#104012=CARTESIAN_POINT ( 'NONE',  ( -21.05000000000000071, 72.02722222756958104, -225.1832529173024398 ) ) ;
#104029=EDGE_CURVE ( 'NONE', #71652, #23382, #67454, .T. ) ;
#104066=DIRECTION ( 'NONE',  ( -1.000000000000000000, -0.000000000000000000, 0.000000000000000000 ) ) ;
#104089=ORIENTED_EDGE ( 'NONE', *, *, #213108, .F. ) ;
#104107=CARTESIAN_POINT ( 'NONE',  ( -20.85000000000000142, 80.78317333349157536, -192.9003134612048882 ) ) ;
#104140=VERTEX_POINT ( 'NONE', #12646 ) ;
#104149=FACE_OUTER_BOUND ( 'NONE', #240498, .T. ) ;
#104206=DIRECTION ( 'NONE',  ( 3.265361837132813093E-16, 0.9651348961777157509, -0.2617529984165031243 ) ) ;
#104207=CARTESIAN_POINT ( 'NONE',  ( -18.59999999999999787, 61.47936603916259912, -212.1738987416902376 ) ) ;
#104217=AXIS2_PLACEMENT_3D ( 'NONE', #165883, #182883, #4207 ) ;
#104269=ADVANCED_FACE ( 'NONE', ( #21620 ), #120737, .F. ) ;
#104286=ORIENTED_EDGE ( 'NONE', *, *, #118265, .F. ) ;
#104292=DIRECTION ( 'NONE',  ( 0.000000000000000000, -0.9651348961777157509, 0.2617529984165031243 ) ) ;
#104295=ORIENTED_EDGE ( 'NONE', *, *, #249562, .T. ) ;
#104302=CARTESIAN_POINT ( 'NONE',  ( 23.24999999999999645, 76.00000000001126921, -203.5231074845248997 ) ) ;
#104305=EDGE_LOOP ( 'NONE', ( #195030, #100781, #68822, #213224 ) ) ;
#104323=DIRECTION ( 'NONE',  ( 0.000000000000000000, -0.2617529984161274248, -0.9651348961778176694 ) ) ;
#104328=DIRECTION ( 'NONE',  ( -1.836970198721029934E-16, -0.9651348961777157509, 0.2617529984165031243 ) ) ;
#104332=CARTESIAN_POINT ( 'NONE',  ( -18.43459694179560060, 86.89521445562479585, -199.6219428230616870 ) ) ;
#104335=DIRECTION ( 'NONE',  ( 1.000000000000000000, 0.000000000000000000, 0.000000000000000000 ) ) ;
#104338=CARTESIAN_POINT ( 'NONE',  ( 18.59999999999999076, 68.48451787451661232, -224.2224406095231757 ) ) ;
#104341=AXIS2_PLACEMENT_3D ( 'NONE', #228954, #66020, #145547 ) ;
#104366=EDGE_LOOP ( 'NONE', ( #92310, #250951, #91513, #190110 ) ) ;
#104423=DIRECTION ( 'NONE',  ( 0.000000000000000000, -0.2617529984165152257, -0.9651348961777124202 ) ) ;
#104431=FACE_OUTER_BOUND ( 'NONE', #60147, .T. ) ;
#104440=VECTOR ( 'NONE', #21711, 1000.000000000000114 ) ;
#104447=CARTESIAN_POINT ( 'NONE',  ( -18.50000000000000000, 55.91711482281190371, -232.6830152854666949 ) ) ;
#104458=LINE ( 'NONE', #5355, #155043 ) ;
#104470=ORIENTED_EDGE ( 'NONE', *, *, #115605, .F. ) ;
#104484=CARTESIAN_POINT ( 'NONE',  ( -23.15000000000000213, 52.81534179157633702, -244.1198638051726277 ) ) ;
#104492=EDGE_LOOP ( 'NONE', ( #146330, #253532, #39772, #172835 ) ) ;
#104528=DIRECTION ( 'NONE',  ( -0.000000000000000000, -0.2617529984165031243, -0.9651348961777157509 ) ) ;
#104547=CARTESIAN_POINT ( 'NONE',  ( -23.15000000000000213, 62.99095723518624368, -207.1734234082435080 ) ) ;
#104551=AXIS2_PLACEMENT_3D ( 'NONE', #255609, #40510, #220400 ) ;
#104573=DIRECTION ( 'NONE',  ( 0.000000000000000000, 0.2617529984165014589, 0.9651348961777161950 ) ) ;
#104602=EDGE_CURVE ( 'NONE', #55100, #248447, #14724, .T. ) ;
#104610=CARTESIAN_POINT ( 'NONE',  ( 18.59999999999999076, 62.96704557978079464, -212.5773704035085814 ) ) ;
#104660=ORIENTED_EDGE ( 'NONE', *, *, #156696, .F. ) ;
#104665=CARTESIAN_POINT ( 'NONE',  ( 18.59999999999999787, 67.23127455305841238, -235.8551265064783991 ) ) ;
#104734=AXIS2_PLACEMENT_3D ( 'NONE', #116482, #99453, #180303 ) ;
#104804=DIRECTION ( 'NONE',  ( 1.000000000000000000, 0.000000000000000000, 0.000000000000000000 ) ) ;
#104808=EDGE_CURVE ( 'NONE', #118480, #100463, #223150, .T. ) ;
#104809=CARTESIAN_POINT ( 'NONE',  ( -20.64999999999999858, 65.86663596189677605, -213.5709895136416776 ) ) ;
#104811=ORIENTED_EDGE ( 'NONE', *, *, #189146, .F. ) ;
#104826=VERTEX_POINT ( 'NONE', #64288 ) ;
#104841=AXIS2_PLACEMENT_3D ( 'NONE', #45899, #162018, #125445 ) ;
#104847=ORIENTED_EDGE ( 'NONE', *, *, #118778, .F. ) ;
#104850=DIRECTION ( 'NONE',  ( 1.000000000000000000, 0.000000000000000000, -0.000000000000000000 ) ) ;
#104854=AXIS2_PLACEMENT_3D ( 'NONE', #193698, #94577, #15064 ) ;
#104856=EDGE_LOOP ( 'NONE', ( #196196, #217841, #226557, #56253 ) ) ;
#104872=DIRECTION ( 'NONE',  ( 1.000000000000000000, 0.000000000000000000, 0.000000000000000000 ) ) ;
#104917=VECTOR ( 'NONE', #68349, 1000.000000000000000 ) ;
#104932=CARTESIAN_POINT ( 'NONE',  ( -23.15000000000000213, 59.16775194334852728, -221.0793150863668473 ) ) ;
#104946=ORIENTED_EDGE ( 'NONE', *, *, #50279, .F. ) ;
#105009=CIRCLE ( 'NONE', #250808, 11.75000000000000533 ) ;
#105017=CARTESIAN_POINT ( 'NONE',  ( -23.15000000000000213, 61.57587952878036219, -212.2000740415318774 ) ) ;
#105020=ORIENTED_EDGE ( 'NONE', *, *, #213390, .T. ) ;
#105037=EDGE_CURVE ( 'NONE', #7533, #159923, #54964, .T. ) ;
#105045=CARTESIAN_POINT ( 'NONE',  ( -20.64999999999999858, 82.57900542960499024, -215.5587758314583482 ) ) ;
#105091=CIRCLE ( 'NONE', #250859, 0.1999999999999945155 ) ;
#105096=CARTESIAN_POINT ( 'NONE',  ( 18.51565452909312626, 78.14133456817783951, -231.3592074214313072 ) ) ;
#105116=CARTESIAN_POINT ( 'NONE',  ( 18.39999999999999858, 87.08727414655710675, -199.6327537731849873 ) ) ;
#105130=FACE_OUTER_BOUND ( 'NONE', #126262, .T. ) ;
#105188=CARTESIAN_POINT ( 'NONE',  ( -18.55807992284872299, 67.49241595948059569, -195.4314365843280541 ) ) ;
#105206=LINE ( 'NONE', #145652, #108192 ) ;
#105207=EDGE_LOOP ( 'NONE', ( #212217, #837, #50240, #44080 ) ) ;
#105222=EDGE_LOOP ( 'NONE', ( #64017, #202022, #129069, #70668 ) ) ;
#105275=DIRECTION ( 'NONE',  ( 0.000000000000000000, 0.2617529984165152257, 0.9651348961777124202 ) ) ;
#105324=CARTESIAN_POINT ( 'NONE',  ( -23.25000000000000000, 68.18350826420393673, -222.4110246041809091 ) ) ;
#105342=ORIENTED_EDGE ( 'NONE', *, *, #202051, .T. ) ;
#105346=SPHERICAL_SURFACE ( 'NONE', #137775, 0.1000000000000000056 ) ;
#105350=AXIS2_PLACEMENT_3D ( 'NONE', #254861, #91993, #232819 ) ;
#105358=CIRCLE ( 'NONE', #59571, 0.1000000000000124678 ) ;
#105365=CARTESIAN_POINT ( 'NONE',  ( 21.05000000000000071, 58.88775506787933267, -225.6504858384382999 ) ) ;
#105397=CARTESIAN_POINT ( 'NONE',  ( 18.59999999999999432, 68.68284540823283635, -224.2482512540334767 ) ) ;
#105417=CARTESIAN_POINT ( 'NONE',  ( 22.60000000000000142, 67.23127455305841238, -235.8551265064783991 ) ) ;
#105424=DIRECTION ( 'NONE',  ( -1.000000000000000000, 2.849773892568378313E-16, -7.728835255496647986E-17 ) ) ;
#105492=DIRECTION ( 'NONE',  ( -0.000000000000000000, -0.2617529984165031243, -0.9651348961777157509 ) ) ;
#105560=EDGE_LOOP ( 'NONE', ( #25264, #49733, #141464, #184084 ) ) ;
#105583=EDGE_CURVE ( 'NONE', #221732, #207854, #94517, .T. ) ;
#105590=ORIENTED_EDGE ( 'NONE', *, *, #12381, .T. ) ;
#105598=ADVANCED_FACE ( 'NONE', ( #209264, #51447 ), #52750, .T. ) ;
#105609=CARTESIAN_POINT ( 'NONE',  ( -18.31331870001021400, 87.00168188095352662, -199.3901562392411506 ) ) ;
#105620=ADVANCED_FACE ( 'NONE', ( #74927 ), #30658, .T. ) ;
#105635=CARTESIAN_POINT ( 'NONE',  ( -22.60000000000094289, 64.05844819680055480, -247.1686437718134925 ) ) ;
#105669=LINE ( 'NONE', #125268, #148780 ) ;
#105670=DIRECTION ( 'NONE',  ( 0.000000000000000000, -0.9651348961777157509, 0.2617529984165031243 ) ) ;
#105679=ORIENTED_EDGE ( 'NONE', *, *, #120220, .T. ) ;
#105733=DIRECTION ( 'NONE',  ( 0.000000000000000000, 0.9651348961777157509, -0.2617529984165031243 ) ) ;
#105739=ORIENTED_EDGE ( 'NONE', *, *, #133247, .F. ) ;
#105742=EDGE_CURVE ( 'NONE', #120691, #61360, #173440, .T. ) ;
#105745=CARTESIAN_POINT ( 'NONE',  ( 21.14999999999999858, 81.77808381374873647, -227.1078217596952697 ) ) ;
#105751=CIRCLE ( 'NONE', #114143, 0.09999999999999112377 ) ;
#105812=AXIS2_PLACEMENT_3D ( 'NONE', #7689, #208468, #209733 ) ;
#105814=CARTESIAN_POINT ( 'NONE',  ( -20.94999999999999929, 86.27712145182582049, -209.5223386573213702 ) ) ;
#105817=ORIENTED_EDGE ( 'NONE', *, *, #97075, .F. ) ;
#105867=ORIENTED_EDGE ( 'NONE', *, *, #22013, .T. ) ;
#105913=DIRECTION ( 'NONE',  ( 1.000000000000000000, 0.000000000000000000, 0.000000000000000000 ) ) ;
#105917=CIRCLE ( 'NONE', #89181, 0.9750000000000036415 ) ;
#105920=AXIS2_PLACEMENT_3D ( 'NONE', #74432, #195648, #230920 ) ;
#105936=DIRECTION ( 'NONE',  ( 0.000000000000000000, 0.7216758089626587047, -0.6922311945860948335 ) ) ;
#105963=DIRECTION ( 'NONE',  ( 0.000000000000000000, 0.2617529984165152257, 0.9651348961777124202 ) ) ;
#106013=FACE_OUTER_BOUND ( 'NONE', #157720, .T. ) ;
#106015=DIRECTION ( 'NONE',  ( 0.000000000000000000, 0.2617529984165032908, 0.9651348961777156399 ) ) ;
#106016=EDGE_CURVE ( 'NONE', #57461, #88904, #149017, .T. ) ;
#106050=ADVANCED_FACE ( 'NONE', ( #228547 ), #2939, .T. ) ;
#106083=DIRECTION ( 'NONE',  ( -1.000000000000000000, 2.849773892568378313E-16, -7.728835255496647986E-17 ) ) ;
#106091=CYLINDRICAL_SURFACE ( 'NONE', #76032, 0.1000000000000124678 ) ;
#106126=EDGE_LOOP ( 'NONE', ( #236975, #35518, #100940, #95609 ) ) ;
#106132=DIRECTION ( 'NONE',  ( 0.000000000000000000, -0.9651348961777157509, 0.2617529984165031243 ) ) ;
#106134=CARTESIAN_POINT ( 'NONE',  ( 21.04999999999999361, 61.12590067187060328, -234.3012893943877373 ) ) ;
#106139=EDGE_CURVE ( 'NONE', #14440, #99302, #165654, .T. ) ;
#106140=DIRECTION ( 'NONE',  ( 1.000000000000000000, 0.000000000000000000, 0.000000000000000000 ) ) ;
#106177=FACE_OUTER_BOUND ( 'NONE', #247819, .T. ) ;
#106185=ORIENTED_EDGE ( 'NONE', *, *, #161934, .F. ) ;
#106231=EDGE_CURVE ( 'NONE', #176771, #185866, #186490, .T. ) ;
#106240=CARTESIAN_POINT ( 'NONE',  ( 21.14999999999999858, 63.99342642423710714, -222.3880800784493772 ) ) ;
#106261=CARTESIAN_POINT ( 'NONE',  ( -18.59999999999999787, 52.81534179157634412, -244.1198638051726277 ) ) ;
#106267=AXIS2_PLACEMENT_3D ( 'NONE', #120104, #40572, #114937 ) ;
#106284=ORIENTED_EDGE ( 'NONE', *, *, #91717, .T. ) ;
#106302=DIRECTION ( 'NONE',  ( -1.000000000000000000, -0.000000000000000000, -0.000000000000000000 ) ) ;
#106339=TOROIDAL_SURFACE ( 'NONE', #89791, 0.2000000000000000111, 0.1000000000000000056 ) ;
#106368=ORIENTED_EDGE ( 'NONE', *, *, #33504, .T. ) ;
#106383=EDGE_CURVE ( 'NONE', #55100, #234093, #69786, .T. ) ;
#106396=CARTESIAN_POINT ( 'NONE',  ( 18.41789779300689744, 78.24072138699057177, -231.5548841640768671 ) ) ;
#106397=DIRECTION ( 'NONE',  ( 0.000000000000000000, 0.2617529984165152257, 0.9651348961777124202 ) ) ;
#106435=DIRECTION ( 'NONE',  ( 0.000000000000000000, -0.9651348961777157509, 0.2617529984165031243 ) ) ;
#106437=DIRECTION ( 'NONE',  ( -1.000000000000000000, -0.000000000000000000, -0.000000000000000000 ) ) ;
#106447=ADVANCED_FACE ( 'NONE', ( #195550 ), #100242, .F. ) ;
#106490=DIRECTION ( 'NONE',  ( 0.000000000000000000, 0.2617529984165034018, 0.9651348961777157509 ) ) ;
#106491=EDGE_CURVE ( 'NONE', #186373, #142984, #119864, .T. ) ;
#106493=DIRECTION ( 'NONE',  ( -0.000000000000000000, -0.2617529984165031243, -0.9651348961777157509 ) ) ;
#106534=VECTOR ( 'NONE', #35111, 1000.000000000000000 ) ;
#106537=ADVANCED_FACE ( 'NONE', ( #3736 ), #159868, .F. ) ;
#106569=CARTESIAN_POINT ( 'NONE',  ( -21.53699400384572016, 65.45457063877245218, -242.4061840233274836 ) ) ;
#106571=VECTOR ( 'NONE', #233061, 999.9999999999998863 ) ;
#106573=CIRCLE ( 'NONE', #85705, 0.1999999999999945155 ) ;
#106584=FACE_OUTER_BOUND ( 'NONE', #240020, .T. ) ;
#106638=CARTESIAN_POINT ( 'NONE',  ( 18.59999999999999076, 63.58402440245809828, -209.2218768284338637 ) ) ;
#106657=ADVANCED_FACE ( 'NONE', ( #29758 ), #110534, .T. ) ;
#106660=CARTESIAN_POINT ( 'NONE',  ( -1.739115166359751801E-14, 59.19392724319018839, -220.9828015967491126 ) ) ;
#106751=ADVANCED_FACE ( 'NONE', ( #79091 ), #233083, .T. ) ;
#106783=EDGE_CURVE ( 'NONE', #952, #241619, #197773, .T. ) ;
#106807=FACE_OUTER_BOUND ( 'NONE', #65241, .T. ) ;
#106813=EDGE_LOOP ( 'NONE', ( #57053, #147334, #19752 ) ) ;
#106817=LINE ( 'NONE', #245059, #147423 ) ;
#106821=DIRECTION ( 'NONE',  ( -1.000000000000000000, -0.000000000000000000, -0.000000000000000000 ) ) ;
#106822=EDGE_CURVE ( 'NONE', #160294, #77989, #139048, .T. ) ;
#106847=CARTESIAN_POINT ( 'NONE',  ( 21.11101077988997332, 61.02755128856028932, -234.1884601127081567 ) ) ;
#106855=CIRCLE ( 'NONE', #6902, 0.1000000000000105804 ) ;
#106912=DIRECTION ( 'NONE',  ( 0.000000000000000000, -0.9651348961777157509, 0.2617529984165031243 ) ) ;
#106915=ORIENTED_EDGE ( 'NONE', *, *, #214869, .F. ) ;
#106921=ORIENTED_EDGE ( 'NONE', *, *, #150107, .T. ) ;
#106940=CARTESIAN_POINT ( 'NONE',  ( 18.59999999999999787, 68.49522935589659767, -224.1230159437372436 ) ) ;
#106941=DIRECTION ( 'NONE',  ( 0.000000000000000000, -0.2617529984164955192, -0.9651348961777178603 ) ) ;
#106981=EDGE_LOOP ( 'NONE', ( #92908, #180888, #31831, #85870 ) ) ;
#107002=CARTESIAN_POINT ( 'NONE',  ( -18.59999999999999787, 68.20313450767837082, -227.8297066677462794 ) ) ;
#107017=CIRCLE ( 'NONE', #165282, 0.4999999999999990008 ) ;
#107021=AXIS2_PLACEMENT_3D ( 'NONE', #151550, #56248, #92814 ) ;
#107031=CARTESIAN_POINT ( 'NONE',  ( -20.85000000000000142, 70.22659352830977753, -197.9852579278363578 ) ) ;
#107039=ORIENTED_EDGE ( 'NONE', *, *, #193069, .T. ) ;
#107067=DIRECTION ( 'NONE',  ( 0.000000000000000000, 0.2617529984165174461, 0.9651348961777118651 ) ) ;
#107114=CARTESIAN_POINT ( 'NONE',  ( -21.07954763557684430, 65.51098451068844497, -241.9465028898075047 ) ) ;
#107122=DIRECTION ( 'NONE',  ( 0.000000000000000000, -0.2617529984165031243, -0.9651348961777157509 ) ) ;
#107134=DIRECTION ( 'NONE',  ( 0.000000000000000000, -0.9651348961777379554, 0.2617529984164210233 ) ) ;
#107163=DIRECTION ( 'NONE',  ( 0.000000000000000000, 0.2617529984165152257, 0.9651348961777124202 ) ) ;
#107178=VECTOR ( 'NONE', #253222, 1000.000000000000114 ) ;
#107196=CIRCLE ( 'NONE', #215540, 0.1000000000000124678 ) ;
#107209=ORIENTED_EDGE ( 'NONE', *, *, #108141, .F. ) ;
#107232=( BOUNDED_CURVE ( )  B_SPLINE_CURVE ( 3, ( #95446, #18488, #116316, #214120 ),
 .UNSPECIFIED., .F., .F. ) 
 B_SPLINE_CURVE_WITH_KNOTS ( ( 4, 4 ),
 ( 3.141592653589793116, 4.712388980384689674 ),
 .UNSPECIFIED. ) 
 CURVE ( )  GEOMETRIC_REPRESENTATION_ITEM ( )  RATIONAL_B_SPLINE_CURVE ( ( 1.000000000000000000, 0.8047378541243649375, 0.8047378541243649375, 1.000000000000000000 ) ) 
 REPRESENTATION_ITEM ( '' )  );
#107238=CARTESIAN_POINT ( 'NONE',  ( 21.05000000000000071, 86.43238724539048690, -209.5644480942280836 ) ) ;
#107265=ORIENTED_EDGE ( 'NONE', *, *, #59342, .F. ) ;
#107278=DIRECTION ( 'NONE',  ( 1.000000000000000000, 0.000000000000000000, 0.000000000000000000 ) ) ;
#107283=AXIS2_PLACEMENT_3D ( 'NONE', #149505, #54217, #69965 ) ;
#107297=( LENGTH_UNIT ( ) NAMED_UNIT ( * ) SI_UNIT ( .MILLI., .METRE. ) );
#107303=CARTESIAN_POINT ( 'NONE',  ( 20.94999999999999929, 67.44464249442897597, -214.0562211244547655 ) ) ;
#107373=CARTESIAN_POINT ( 'NONE',  ( 23.24999999999999645, 65.65271564877468791, -222.5736063831752176 ) ) ;
#107383=ORIENTED_EDGE ( 'NONE', *, *, #162133, .T. ) ;
#107450=ORIENTED_EDGE ( 'NONE', *, *, #53978, .T. ) ;
#107462=EDGE_LOOP ( 'NONE', ( #119080, #50333, #3273, #192331 ) ) ;
#107520=ADVANCED_FACE ( 'NONE', ( #23316 ), #166738, .T. ) ;
#107551=ORIENTED_EDGE ( 'NONE', *, *, #201471, .F. ) ;
#107563=ADVANCED_FACE ( 'NONE', ( #6270 ), #198066, .T. ) ;
#107589=ORIENTED_EDGE ( 'NONE', *, *, #113538, .T. ) ;
#107615=ADVANCED_FACE ( 'NONE', ( #242325 ), #105346, .T. ) ;
#107629=ORIENTED_EDGE ( 'NONE', *, *, #48847, .F. ) ;
#107667=CYLINDRICAL_SURFACE ( 'NONE', #101985, 0.09999999999999939493 ) ;
#107711=CARTESIAN_POINT ( 'NONE',  ( -23.15000000000000213, 77.02083669383561926, -199.7590813894317989 ) ) ;
#107735=EDGE_CURVE ( 'NONE', #50639, #168, #110520, .T. ) ;
#107740=DIRECTION ( 'NONE',  ( 0.000000000000000000, -0.9667078373770160438, -0.2558827019433957961 ) ) ;
#107742=DIRECTION ( 'NONE',  ( 1.000000000000000000, 0.000000000000000000, 0.000000000000000000 ) ) ;
#107755=CARTESIAN_POINT ( 'NONE',  ( -23.25000000000000000, 66.30975017506362690, -223.0162872746489882 ) ) ;
#107839=ORIENTED_EDGE ( 'NONE', *, *, #108229, .T. ) ;
#107840=CARTESIAN_POINT ( 'NONE',  ( -22.39999999999999858, 65.59531831295525706, -241.8872196075891168 ) ) ;
#107851=CARTESIAN_POINT ( 'NONE',  ( 20.85000000000000142, 80.78317333349157536, -192.9003134612048882 ) ) ;
#107870=AXIS2_PLACEMENT_3D ( 'NONE', #180865, #79168, #196558 ) ;
#107874=EDGE_CURVE ( 'NONE', #222414, #206042, #810, .T. ) ;
#107925=DIRECTION ( 'NONE',  ( 0.7071067811865474617, -0.6824534298470372740, 0.1850873201762209819 ) ) ;
#107928=FACE_OUTER_BOUND ( 'NONE', #76725, .T. ) ;
#107947=VERTEX_POINT ( 'NONE', #146739 ) ;
#107957=DIRECTION ( 'NONE',  ( 0.000000000000000000, -0.9651348961777379554, 0.2617529984164210233 ) ) ;
#107980=FACE_OUTER_BOUND ( 'NONE', #169409, .T. ) ;
#107987=FACE_BOUND ( 'NONE', #75116, .T. ) ;
#107999=CARTESIAN_POINT ( 'NONE',  ( 23.15000000000000213, 86.27712145182582049, -209.5223386573213702 ) ) ;
#108006=ORIENTED_EDGE ( 'NONE', *, *, #126979, .F. ) ;
#108018=VECTOR ( 'NONE', #171205, 1000.000000000000000 ) ;
#108037=EDGE_CURVE ( 'NONE', #181022, #77841, #181716, .T. ) ;
#108042=CARTESIAN_POINT ( 'NONE',  ( 20.94999999999999929, 82.57900542960499024, -215.5587758314583766 ) ) ;
#108098=CARTESIAN_POINT ( 'NONE',  ( 23.14999999999999858, 67.63082410804655353, -211.8415745842588649 ) ) ;
#108141=EDGE_CURVE ( 'NONE', #248135, #93031, #56778, .T. ) ;
#108181=CARTESIAN_POINT ( 'NONE',  ( -18.59999999999999787, 57.84918772656043018, -226.1321410194968280 ) ) ;
#108192=VECTOR ( 'NONE', #103944, 1000.000000000000000 ) ;
#108195=ORIENTED_EDGE ( 'NONE', *, *, #216381, .T. ) ;
#108198=AXIS2_PLACEMENT_3D ( 'NONE', #204828, #87450, #246532 ) ;
#108216=ADVANCED_FACE ( 'NONE', ( #115341 ), #215712, .F. ) ;
#108223=DIRECTION ( 'NONE',  ( -1.000000000000000000, 0.000000000000000000, 0.000000000000000000 ) ) ;
#108229=EDGE_CURVE ( 'NONE', #191700, #40380, #36174, .T. ) ;
#108235=ADVANCED_FACE ( 'NONE', ( #175350 ), #15330, .T. ) ;
#108241=VERTEX_POINT ( 'NONE', #145164 ) ;
#108276=CARTESIAN_POINT ( 'NONE',  ( 21.14999999999999858, 65.61575147395463148, -242.1939180743342774 ) ) ;
#108321=DIRECTION ( 'NONE',  ( -1.000000000000000000, 7.049440681616512959E-16, -1.911869773728117674E-16 ) ) ;
#108332=CIRCLE ( 'NONE', #150039, 0.09999999999999939493 ) ;
#108353=DIRECTION ( 'NONE',  ( 0.000000000000000000, 0.2617529984165033463, 0.9651348961777157509 ) ) ;
#108360=DIRECTION ( 'NONE',  ( 0.000000000000000000, 0.9651348961777157509, -0.2617529984165031243 ) ) ;
#108375=CIRCLE ( 'NONE', #25004, 0.5000000000000051070 ) ;
#108395=ORIENTED_EDGE ( 'NONE', *, *, #225096, .T. ) ;
#108429=CARTESIAN_POINT ( 'NONE',  ( -22.24259225415828212, 59.97461308214577969, -233.9897012460487247 ) ) ;
#108431=FACE_OUTER_BOUND ( 'NONE', #116160, .T. ) ;
#108440=DIRECTION ( 'NONE',  ( -1.000000000000000000, 0.000000000000000000, 0.000000000000000000 ) ) ;
#108445=DIRECTION ( 'NONE',  ( 0.000000000000000000, 0.2617529984165032908, 0.9651348961777156399 ) ) ;
#108493=CARTESIAN_POINT ( 'NONE',  ( -21.07954640115303135, 61.10538041441509449, -234.2621228157806001 ) ) ;
#108512=CIRCLE ( 'NONE', #37813, 1.900000000000000799 ) ;
#108539=ORIENTED_EDGE ( 'NONE', *, *, #172828, .T. ) ;
#108556=CIRCLE ( 'NONE', #254282, 0.1000000000000124678 ) ;
#108570=DIRECTION ( 'NONE',  ( -1.000000000000000000, 1.772924042024179943E-16, -4.808324575169860901E-17 ) ) ;
#108573=DIRECTION ( 'NONE',  ( 0.000000000000000000, 0.2617529984165035128, 0.9651348961777155289 ) ) ;
#108661=DIRECTION ( 'NONE',  ( -0.000000000000000000, 0.2617529984165031243, 0.9651348961777157509 ) ) ;
#108682=EDGE_LOOP ( 'NONE', ( #13678, #233125, #102780, #121100 ) ) ;
#108685=DIRECTION ( 'NONE',  ( -1.000000000000000000, -0.000000000000000000, -0.000000000000000000 ) ) ;
#108690=SPHERICAL_SURFACE ( 'NONE', #209119, 0.1000000000000000056 ) ;
#108695=DIRECTION ( 'NONE',  ( 0.000000000000000000, 0.9673461469267252699, -0.2534589355813257061 ) ) ;
#108755=AXIS2_PLACEMENT_3D ( 'NONE', #772, #99872, #221123 ) ;
#108768=DIRECTION ( 'NONE',  ( 0.000000000000000000, 0.2617529984165152257, 0.9651348961777124202 ) ) ;
#108791=DIRECTION ( 'NONE',  ( -0.000000000000000000, -0.2617529984165031243, -0.9651348961777157509 ) ) ;
#108795=AXIS2_PLACEMENT_3D ( 'NONE', #180862, #3483, #23087 ) ;
#108800=ORIENTED_EDGE ( 'NONE', *, *, #226547, .F. ) ;
#108805=ORIENTED_EDGE ( 'NONE', *, *, #95778, .F. ) ;
#108848=DIRECTION ( 'NONE',  ( 0.000000000000000000, 0.2617529984165022361, 0.9651348961777160840 ) ) ;
#108853=ORIENTED_EDGE ( 'NONE', *, *, #65061, .T. ) ;
#108867=CARTESIAN_POINT ( 'NONE',  ( 21.05000000000000071, 60.99662849158838895, -205.1669373764474642 ) ) ;
#108932=LINE ( 'NONE', #188473, #134323 ) ;
#108938=PLANE ( 'NONE',  #39956 ) ;
#108956=CARTESIAN_POINT ( 'NONE',  ( 23.14999999999999858, 76.00000000001126921, -203.5231074845248997 ) ) ;
#108976=CARTESIAN_POINT ( 'NONE',  ( 20.04142135623731136, 62.37381720523315209, -208.8758809977715032 ) ) ;
#108992=LINE ( 'NONE', #9900, #22574 ) ;
#109008=ORIENTED_EDGE ( 'NONE', *, *, #178113, .F. ) ;
#109022=DIRECTION ( 'NONE',  ( 2.840903330521632269E-16, 0.7106264324241464703, -0.7035695228903323661 ) ) ;
#109042=DIRECTION ( 'NONE',  ( 1.000000000000000000, -2.849773892568378313E-16, 7.728835255496647986E-17 ) ) ;
#109069=DIRECTION ( 'NONE',  ( 0.000000000000000000, 0.2617529984165059553, 0.9651348961777148627 ) ) ;
#109074=FACE_OUTER_BOUND ( 'NONE', #167614, .T. ) ;
#109085=DIRECTION ( 'NONE',  ( -1.000000000000000000, -0.000000000000000000, 0.000000000000000000 ) ) ;
#109088=ORIENTED_EDGE ( 'NONE', *, *, #159619, .T. ) ;
#109093=ORIENTED_EDGE ( 'NONE', *, *, #9935, .T. ) ;
#109116=ADVANCED_FACE ( 'NONE', ( #29473 ), #86369, .T. ) ;
#109138=AXIS2_PLACEMENT_3D ( 'NONE', #42306, #160982, #181815 ) ;
#109152=DIRECTION ( 'NONE',  ( 0.000000000000000000, 0.2617529984165031243, 0.9651348961777157509 ) ) ;
#109155=CARTESIAN_POINT ( 'NONE',  ( -23.25000000000000000, 67.23127455305841238, -235.8551265064783991 ) ) ;
#109162=ADVANCED_FACE ( 'NONE', ( #174125 ), #198824, .T. ) ;
#109183=ORIENTED_EDGE ( 'NONE', *, *, #62009, .F. ) ;
#109212=CIRCLE ( 'NONE', #196699, 0.09999999999999642508 ) ;
#109282=ADVANCED_FACE ( 'NONE', ( #158402 ), #175394, .F. ) ;
#109319=CARTESIAN_POINT ( 'NONE',  ( 18.59999999999999076, 63.62814136979439184, -224.4990371885399441 ) ) ;
#109345=EDGE_CURVE ( 'NONE', #30986, #25213, #199009, .T. ) ;
#109352=EDGE_CURVE ( 'NONE', #153125, #253128, #76248, .T. ) ;
#109374=ORIENTED_EDGE ( 'NONE', *, *, #76677, .F. ) ;
#109395=ORIENTED_EDGE ( 'NONE', *, *, #36449, .F. ) ;
#109401=EDGE_CURVE ( 'NONE', #189304, #77283, #186565, .T. ) ;
#109446=CARTESIAN_POINT ( 'NONE',  ( 20.19326291201597812, 59.46099628735877474, -225.7055034009678991 ) ) ;
#109464=CARTESIAN_POINT ( 'NONE',  ( 22.39999999999999503, 59.71212129423884818, -233.8158665866020272 ) ) ;
#109475=LINE ( 'NONE', #80604, #134314 ) ;
#109504=DIRECTION ( 'NONE',  ( -1.000000000000000000, -0.000000000000000000, 0.000000000000000000 ) ) ;
#109507=CARTESIAN_POINT ( 'NONE',  ( -23.15000000000000213, 66.14499960962992020, -239.8604363256158933 ) ) ;
#109518=ADVANCED_FACE ( 'NONE', ( #31732 ), #151676, .T. ) ;
#109529=ORIENTED_EDGE ( 'NONE', *, *, #194905, .T. ) ;
#109591=AXIS2_PLACEMENT_3D ( 'NONE', #220636, #42014, #4142 ) ;
#109650=ORIENTED_EDGE ( 'NONE', *, *, #101479, .T. ) ;
#109695=DIRECTION ( 'NONE',  ( 0.000000000000000000, 0.2617529984165029577, 0.9651348961777157509 ) ) ;
#109709=EDGE_CURVE ( 'NONE', #231654, #51680, #154258, .T. ) ;
#109731=CYLINDRICAL_SURFACE ( 'NONE', #241314, 0.09999999999999939493 ) ;
#109745=CIRCLE ( 'NONE', #55549, 0.1000000000000132172 ) ;
#109801=ORIENTED_EDGE ( 'NONE', *, *, #9935, .F. ) ;
#109843=CIRCLE ( 'NONE', #134955, 0.5999999999999872102 ) ;
#109866=CARTESIAN_POINT ( 'NONE',  ( -18.59999999999999787, 78.12133356376091342, -231.3112718935514636 ) ) ;
#109868=ORIENTED_EDGE ( 'NONE', *, *, #163624, .F. ) ;
#109920=AXIS2_PLACEMENT_3D ( 'NONE', #45183, #128580, #188547 ) ;
#109922=ADVANCED_FACE ( 'NONE', ( #65375, #22424 ), #101906, .T. ) ;
#109926=CARTESIAN_POINT ( 'NONE',  ( 21.05000000000000071, 67.23127455305841238, -235.8551265064783991 ) ) ;
#109935=DIRECTION ( 'NONE',  ( 1.000000000000000000, 0.000000000000000000, 0.000000000000000000 ) ) ;
#109963=VERTEX_POINT ( 'NONE', #212605 ) ;
#109997=ORIENTED_EDGE ( 'NONE', *, *, #133355, .T. ) ;
#110026=DIRECTION ( 'NONE',  ( 1.734723475976817507E-14, 0.2617529984165031243, 0.9651348961777157509 ) ) ;
#110058=CIRCLE ( 'NONE', #184881, 0.09999999999999939493 ) ;
#110066=CIRCLE ( 'NONE', #139081, 0.09999999999999939493 ) ;
#110105=DIRECTION ( 'NONE',  ( 1.000000000000000000, -7.049440681616513945E-16, 1.911869773728117674E-16 ) ) ;
#110118=ORIENTED_EDGE ( 'NONE', *, *, #50279, .T. ) ;
#110183=DIRECTION ( 'NONE',  ( 0.000000000000000000, -0.2617529984164856383, -0.9651348961777204138 ) ) ;
#110190=DIRECTION ( 'NONE',  ( 0.000000000000000000, -0.2617529984165152257, -0.9651348961777124202 ) ) ;
#110207=AXIS2_PLACEMENT_3D ( 'NONE', #51792, #131345, #210886 ) ;
#110243=EDGE_CURVE ( 'NONE', #78723, #74229, #24692, .T. ) ;
#110252=DIRECTION ( 'NONE',  ( 0.000000000000000000, 0.2617529984165036239, 0.9651348961777156399 ) ) ;
#110283=CIRCLE ( 'NONE', #243560, 0.09999999999999939493 ) ;
#110316=DIRECTION ( 'NONE',  ( -1.000000000000000000, -0.000000000000000000, -0.000000000000000000 ) ) ;
#110330=CYLINDRICAL_SURFACE ( 'NONE', #10803, 0.09999999999999939493 ) ;
#110336=AXIS2_PLACEMENT_3D ( 'NONE', #62718, #1443, #44451 ) ;
#110349=DIRECTION ( 'NONE',  ( 1.000000000000000000, -0.000000000000000000, 0.000000000000000000 ) ) ;
#110355=LINE ( 'NONE', #129911, #187209 ) ;
#110368=ADVANCED_FACE ( 'NONE', ( #129845 ), #41056, .F. ) ;
#110369=VERTEX_POINT ( 'NONE', #201381 ) ;
#110405=CARTESIAN_POINT ( 'NONE',  ( -18.50000000000000000, 61.63293978347611812, -221.5406706031726003 ) ) ;
#110419=ADVANCED_FACE ( 'NONE', ( #218357 ), #3751, .F. ) ;
#110447=VERTEX_POINT ( 'NONE', #180550 ) ;
#110463=VERTEX_POINT ( 'NONE', #121861 ) ;
#110469=EDGE_CURVE ( 'NONE', #85685, #165864, #257445, .T. ) ;
#110512=DIRECTION ( 'NONE',  ( 0.000000000000000000, -0.9651348961777157509, 0.2617529984165031243 ) ) ;
#110514=FACE_OUTER_BOUND ( 'NONE', #15293, .T. ) ;
#110520=B_SPLINE_CURVE_WITH_KNOTS ( 'NONE', 3,
 ( #132662, #192638, #173117, #29739, #252588, #171821 ),
 .UNSPECIFIED., .F., .F.,
 ( 4, 2, 4 ),
 ( 0.000000000000000000, 0.0001497467027049069303, 0.0002994934054098138607 ),
 .UNSPECIFIED. ) ;
#110534=SPHERICAL_SURFACE ( 'NONE', #36677, 0.1000000000000000056 ) ;
#110541=ORIENTED_EDGE ( 'NONE', *, *, #68486, .F. ) ;
#110583=CARTESIAN_POINT ( 'NONE',  ( 21.07928932188134397, 65.47931918658503037, -241.9371126717015841 ) ) ;
#110584=ORIENTED_EDGE ( 'NONE', *, *, #125044, .F. ) ;
#110595=CARTESIAN_POINT ( 'NONE',  ( 18.49999999999998934, 63.62814136979439184, -224.4990371885399441 ) ) ;
#110603=CIRCLE ( 'NONE', #256269, 0.1000000000000027117 ) ;
#110607=AXIS2_PLACEMENT_3D ( 'NONE', #29053, #147677, #148977 ) ;
#110678=VERTEX_POINT ( 'NONE', #207383 ) ;
#110681=CARTESIAN_POINT ( 'NONE',  ( 20.94560253601876809, 62.83003337064300808, -207.1937220765705376 ) ) ;
#110685=CARTESIAN_POINT ( 'NONE',  ( -18.59999999999999787, 79.11538813396778380, -196.3722783875038544 ) ) ;
#110697=TOROIDAL_SURFACE ( 'NONE', #206378, 0.2000000000000000111, 0.1000000000000000056 ) ;
#110726=FACE_OUTER_BOUND ( 'NONE', #163371, .T. ) ;
#110740=CARTESIAN_POINT ( 'NONE',  ( 20.11144452913859837, 59.70930804554667759, -225.6397765276010716 ) ) ;
#110805=EDGE_LOOP ( 'NONE', ( #134847, #62108, #68168, #124317 ) ) ;
#110808=CARTESIAN_POINT ( 'NONE',  ( -20.85000000000000142, 80.78317333349157536, -192.9003134612048882 ) ) ;
#110823=ADVANCED_FACE ( 'NONE', ( #86098 ), #189091, .T. ) ;
#110858=SPHERICAL_SURFACE ( 'NONE', #197491, 0.1000000000000000056 ) ;
#110885=LINE ( 'NONE', #176022, #40556 ) ;
#110886=CIRCLE ( 'NONE', #131733, 0.09999999999999543976 ) ;
#110890=ADVANCED_FACE ( 'NONE', ( #195535 ), #153868, .F. ) ;
#110895=CARTESIAN_POINT ( 'NONE',  ( -20.05000000000000426, 63.83985267992358104, -213.0213082169670145 ) ) ;
#110902=CARTESIAN_POINT ( 'NONE',  ( -20.94999999999999929, 55.11435547888748232, -226.8560373590520101 ) ) ;
#110910=VERTEX_POINT ( 'NONE', #149987 ) ;
#110970=CYLINDRICAL_SURFACE ( 'NONE', #238931, 0.1000000000000048767 ) ;
#110984=ORIENTED_EDGE ( 'NONE', *, *, #120153, .F. ) ;
#110994=CARTESIAN_POINT ( 'NONE',  ( -22.47071067811865319, 59.75442326890419764, -233.9300113800878762 ) ) ;
#111041=AXIS2_PLACEMENT_3D ( 'NONE', #44243, #162921, #45516 ) ;
#111052=LINE ( 'NONE', #233583, #237368 ) ;
#111071=CARTESIAN_POINT ( 'NONE',  ( 23.24999999999999289, 55.98745301258800566, -232.8057040749261262 ) ) ;
#111076=AXIS2_PLACEMENT_3D ( 'NONE', #25587, #206783, #47688 ) ;
#111117=VECTOR ( 'NONE', #23424, 1000.000000000000000 ) ;
#111127=DIRECTION ( 'NONE',  ( -7.304098846218134667E-16, 0.9651348961777158619, -0.2617529984165031243 ) ) ;
#111173=ADVANCED_FACE ( 'NONE', ( #181412 ), #247779, .F. ) ;
#111225=CARTESIAN_POINT ( 'NONE',  ( 20.85000000000000142, 76.00000000001126921, -203.5231074845248997 ) ) ;
#111242=EDGE_CURVE ( 'NONE', #257696, #256658, #186534, .T. ) ;
#111271=VERTEX_POINT ( 'NONE', #208677 ) ;
#111278=EDGE_CURVE ( 'NONE', #230992, #134353, #228600, .T. ) ;
#111285=CARTESIAN_POINT ( 'NONE',  ( -18.59999999999999787, 63.74333919030581086, -212.9951329171253747 ) ) ;
#111371=EDGE_CURVE ( 'NONE', #15317, #213246, #145180, .T. ) ;
#111398=DIRECTION ( 'NONE',  ( 1.000000000000000000, 0.000000000000000000, 0.000000000000000000 ) ) ;
#111419=ORIENTED_EDGE ( 'NONE', *, *, #221705, .T. ) ;
#111474=CARTESIAN_POINT ( 'NONE',  ( 18.59999999999999076, 62.39550153362034735, -208.7959266050682459 ) ) ;
#111479=FACE_OUTER_BOUND ( 'NONE', #116650, .T. ) ;
#111532=CARTESIAN_POINT ( 'NONE',  ( -18.46856557590793457, 78.23413713284891458, -231.4806561747373053 ) ) ;
#111548=CARTESIAN_POINT ( 'NONE',  ( -21.65000000000000213, 65.32753222054176945, -213.4247798787853867 ) ) ;
#111583=DIRECTION ( 'NONE',  ( -2.952720810173289112E-16, -0.9651348961777159730, 0.2617529984165024026 ) ) ;
#111596=ORIENTED_EDGE ( 'NONE', *, *, #80169, .F. ) ;
#111617=LINE ( 'NONE', #51600, #21034 ) ;
#111621=LINE ( 'NONE', #33402, #147321 ) ;
#111638=DIRECTION ( 'NONE',  ( 1.296989514748957725E-15, 0.9151430362303984989, -0.4031292884906871321 ) ) ;
#111650=TOROIDAL_SURFACE ( 'NONE', #15832, 12.97499999999999787, 0.1000000000000000056 ) ;
#111669=DIRECTION ( 'NONE',  ( 1.000000000000000000, 0.000000000000000000, 0.000000000000000000 ) ) ;
#111671=CARTESIAN_POINT ( 'NONE',  ( -20.85000000000000142, 76.30149234032609229, -203.6488173052385946 ) ) ;
#111683=CIRCLE ( 'NONE', #144987, 12.87500000000000178 ) ;
#111721=CARTESIAN_POINT ( 'NONE',  ( 18.59999999999999076, 63.58402440245809828, -209.2218768284338637 ) ) ;
#111751=SPHERICAL_SURFACE ( 'NONE', #136278, 0.1000000000000000056 ) ;
#111767=ADVANCED_FACE ( 'NONE', ( #256066 ), #196154, .F. ) ;
#111773=LINE ( 'NONE', #229158, #15554 ) ;
#111801=TOROIDAL_SURFACE ( 'NONE', #207668, 2.100000000000002309, 0.1000000000000000056 ) ;
#111807=DIRECTION ( 'NONE',  ( 1.000000000000000000, 0.000000000000000000, 0.000000000000000000 ) ) ;
#111820=DIRECTION ( 'NONE',  ( 0.000000000000000000, 0.2617529984165180013, 0.9651348961777117541 ) ) ;
#111824=PLANE ( 'NONE',  #44442 ) ;
#111828=ORIENTED_EDGE ( 'NONE', *, *, #222090, .T. ) ;
#111843=ORIENTED_EDGE ( 'NONE', *, *, #213764, .F. ) ;
#111849=DIRECTION ( 'NONE',  ( 0.000000000000000000, 0.9651348961777157509, -0.2617529984165031243 ) ) ;
#111869=AXIS2_PLACEMENT_3D ( 'NONE', #212100, #178112, #55534 ) ;
#111894=DIRECTION ( 'NONE',  ( 1.000000000000000000, 0.000000000000000000, 0.000000000000000000 ) ) ;
#111965=AXIS2_PLACEMENT_3D ( 'NONE', #255248, #76660, #177080 ) ;
#111971=FACE_OUTER_BOUND ( 'NONE', #248916, .T. ) ;
#111993=TOROIDAL_SURFACE ( 'NONE', #103577, 6.258578643762700899, 0.1000000000000000056 ) ;
#112013=DIRECTION ( 'NONE',  ( 1.000000000000000000, 0.000000000000000000, 0.000000000000000000 ) ) ;
#112025=DIRECTION ( 'NONE',  ( -0.000000000000000000, -0.2617529984165031243, -0.9651348961777157509 ) ) ;
#112039=CARTESIAN_POINT ( 'NONE',  ( 21.05000000000000071, 79.13126459505528487, -235.8705213229730191 ) ) ;
#112072=CYLINDRICAL_SURFACE ( 'NONE', #161669, 0.09999999999999543976 ) ;
#112080=ORIENTED_EDGE ( 'NONE', *, *, #206924, .F. ) ;
#112101=ORIENTED_EDGE ( 'NONE', *, *, #163982, .F. ) ;
#112106=EDGE_LOOP ( 'NONE', ( #183649, #253325, #57554, #162465 ) ) ;
#112112=ADVANCED_FACE ( 'NONE', ( #217962 ), #170754, .F. ) ;
#112136=ORIENTED_EDGE ( 'NONE', *, *, #36196, .F. ) ;
#112143=CARTESIAN_POINT ( 'NONE',  ( 23.14999999999999503, 52.81534179157632991, -244.1198638051726277 ) ) ;
#112146=EDGE_CURVE ( 'NONE', #46658, #47300, #141455, .T. ) ;
#112149=EDGE_CURVE ( 'NONE', #118789, #35199, #99919, .T. ) ;
#112179=CARTESIAN_POINT ( 'NONE',  ( -22.39999999999999503, 59.68594599439717285, -233.9123800762197902 ) ) ;
#112197=B_SPLINE_CURVE_WITH_KNOTS ( 'NONE', 3,
 ( #230141, #252258, #231445, #235265, #155772, #56600, #131038 ),
 .UNSPECIFIED., .F., .F.,
 ( 4, 3, 4 ),
 ( 0.000000000000000000, 1.860045280647521529E-05, 5.251155757304300621E-05 ),
 .UNSPECIFIED. ) ;
#112206=EDGE_CURVE ( 'NONE', #72701, #223936, #29081, .T. ) ;
#112210=DIRECTION ( 'NONE',  ( 0.000000000000000000, 0.2617529984164915779, 0.9651348961777187485 ) ) ;
#112268=CARTESIAN_POINT ( 'NONE',  ( -21.08198257630413508, 65.50254075141489807, -241.9517825296665023 ) ) ;
#112273=AXIS2_PLACEMENT_3D ( 'NONE', #199690, #25849, #138379 ) ;
#112276=CARTESIAN_POINT ( 'NONE',  ( 18.59999999999999432, 70.47363787294415260, -228.3418745167492432 ) ) ;
#112311=CARTESIAN_POINT ( 'NONE',  ( 20.85000000000000142, 70.15623657602074559, -198.0563205710787713 ) ) ;
#112314=EDGE_CURVE ( 'NONE', #81173, #26209, #24970, .T. ) ;
#112321=VERTEX_POINT ( 'NONE', #165743 ) ;
#112324=ORIENTED_EDGE ( 'NONE', *, *, #152117, .F. ) ;
#112331=CARTESIAN_POINT ( 'NONE',  ( 20.95052659398289308, 59.09967180796918029, -225.8008737851698982 ) ) ;
#112336=EDGE_CURVE ( 'NONE', #242990, #181475, #48336, .T. ) ;
#112345=ORIENTED_EDGE ( 'NONE', *, *, #133374, .T. ) ;
#112360=ORIENTED_EDGE ( 'NONE', *, *, #132845, .F. ) ;
#112375=EDGE_LOOP ( 'NONE', ( #215840, #29823, #40217, #206699 ) ) ;
#112409=ORIENTED_EDGE ( 'NONE', *, *, #244413, .T. ) ;
#112436=DIRECTION ( 'NONE',  ( 0.000000000000000000, 0.9651348961777379554, -0.2617529984164210233 ) ) ;
#112444=CIRCLE ( 'NONE', #149870, 0.6000000000000005329 ) ;
#112446=TOROIDAL_SURFACE ( 'NONE', #79082, 11.65000000000000036, 0.1000000000000000056 ) ;
#112502=ORIENTED_EDGE ( 'NONE', *, *, #168728, .F. ) ;
#112545=ORIENTED_EDGE ( 'NONE', *, *, #218961, .T. ) ;
#112610=CIRCLE ( 'NONE', #62720, 11.75000000000000533 ) ;
#112632=CARTESIAN_POINT ( 'NONE',  ( -21.05000000000000071, 72.91131461869652242, -214.9116992594219369 ) ) ;
#112640=CARTESIAN_POINT ( 'NONE',  ( -23.15000000000000213, 62.92003201576280702, -207.2439188921395612 ) ) ;
#112670=EDGE_LOOP ( 'NONE', ( #56507, #30684, #69518, #64872 ) ) ;
#112687=CARTESIAN_POINT ( 'NONE',  ( 18.49999999999999645, 72.02722222756958104, -225.1832529173024398 ) ) ;
#112696=ORIENTED_EDGE ( 'NONE', *, *, #11743, .F. ) ;
#112703=CARTESIAN_POINT ( 'NONE',  ( 20.94999999999999929, 74.92681270650359693, -207.4801605588535551 ) ) ;
#112741=DIRECTION ( 'NONE',  ( 0.000000000000000000, -0.2617529984165031243, -0.9651348961777157509 ) ) ;
#112750=EDGE_LOOP ( 'NONE', ( #174976, #156747, #187369, #27264, #155370 ) ) ;
#112808=CARTESIAN_POINT ( 'NONE',  ( -22.14074124539699540, 65.20130011066974873, -242.9616211335017226 ) ) ;
#112816=DIRECTION ( 'NONE',  ( 0.000000000000000000, 0.9651348961777149738, -0.2617529984165058998 ) ) ;
#112818=CARTESIAN_POINT ( 'NONE',  ( -18.45068461519105796, 78.23730666619897534, -231.5159245159509567 ) ) ;
#112848=EDGE_CURVE ( 'NONE', #90469, #180736, #79461, .T. ) ;
#112858=AXIS2_PLACEMENT_3D ( 'NONE', #202851, #106302, #84136 ) ;
#112911=CARTESIAN_POINT ( 'NONE',  ( 21.05000000000000426, 61.18186820035567308, -234.2493224657541759 ) ) ;
#112926=CARTESIAN_POINT ( 'NONE',  ( -21.05000000000000071, 67.99035824846625076, -233.0562353075630142 ) ) ;
#112957=ORIENTED_EDGE ( 'NONE', *, *, #220097, .F. ) ;
#112969=DIRECTION ( 'NONE',  ( 1.000000000000000000, 0.000000000000000000, 0.000000000000000000 ) ) ;
#112977=CARTESIAN_POINT ( 'NONE',  ( 22.48660254037844197, 55.97436536266718576, -232.8539608197349935 ) ) ;
#112978=DIRECTION ( 'NONE',  ( 1.000000000000000000, 0.000000000000000000, 0.000000000000000000 ) ) ;
#113004=LINE ( 'NONE', #232970, #115596 ) ;
#113018=ORIENTED_EDGE ( 'NONE', *, *, #112206, .F. ) ;
#113036=CYLINDRICAL_SURFACE ( 'NONE', #63324, 12.87500000000000178 ) ;
#113079=VERTEX_POINT ( 'NONE', #6010 ) ;
#113098=ORIENTED_EDGE ( 'NONE', *, *, #102915, .F. ) ;
#113125=VECTOR ( 'NONE', #146172, 1000.000000000000000 ) ;
#113126=ORIENTED_EDGE ( 'NONE', *, *, #165243, .T. ) ;
#113141=EDGE_CURVE ( 'NONE', #74710, #57461, #158796, .T. ) ;
#113143=CARTESIAN_POINT ( 'NONE',  ( -21.03571358706064487, 57.67743169815677362, -226.1923800109734088 ) ) ;
#113282=CYLINDRICAL_SURFACE ( 'NONE', #37545, 0.1000000000000124678 ) ;
#113291=CYLINDRICAL_SURFACE ( 'NONE', #101361, 0.5000000000000014433 ) ;
#113297=AXIS2_PLACEMENT_3D ( 'NONE', #249278, #91481, #191892 ) ;
#113311=DIRECTION ( 'NONE',  ( 0.000000000000000000, -0.9651348961777379554, 0.2617529984164210233 ) ) ;
#113313=CARTESIAN_POINT ( 'NONE',  ( 21.05000000000000071, 76.00000000001126921, -203.5231074845248997 ) ) ;
#113332=CARTESIAN_POINT ( 'NONE',  ( 21.33487959338958362, 60.74020368437640371, -234.0946914941910393 ) ) ;
#113364=VECTOR ( 'NONE', #167991, 1000.000000000000000 ) ;
#113378=ADVANCED_FACE ( 'NONE', ( #10546 ), #92621, .F. ) ;
#113409=AXIS2_PLACEMENT_3D ( 'NONE', #216094, #72783, #252650 ) ;
#113410=LINE ( 'NONE', #174719, #27544 ) ;
#113422=DIRECTION ( 'NONE',  ( 1.000000000000000000, 0.000000000000000000, 0.000000000000000000 ) ) ;
#113428=CARTESIAN_POINT ( 'NONE',  ( -21.05000000000000071, 70.53171716061257257, -228.4612385850772682 ) ) ;
#113468=DIRECTION ( 'NONE',  ( 0.000000000000000000, 0.2617529984165152257, 0.9651348961777124202 ) ) ;
#113480=DIRECTION ( 'NONE',  ( 1.000000000000000000, 0.000000000000000000, 0.000000000000000000 ) ) ;
#113488=AXIS2_PLACEMENT_3D ( 'NONE', #43993, #205622, #148228 ) ;
#113492=EDGE_CURVE ( 'NONE', #62, #85530, #233802, .T. ) ;
#113504=AXIS2_PLACEMENT_3D ( 'NONE', #36454, #194243, #230797 ) ;
#113538=EDGE_CURVE ( 'NONE', #7014, #65920, #97740, .T. ) ;
#113550=DIRECTION ( 'NONE',  ( 1.000000000000000000, -7.049440681616512959E-16, 1.911869773728117674E-16 ) ) ;
#113571=EDGE_CURVE ( 'NONE', #138609, #234093, #213110, .T. ) ;
#113600=CARTESIAN_POINT ( 'NONE',  ( 20.95462737510932882, 59.02401302535630379, -225.7858342150956616 ) ) ;
#113607=FACE_OUTER_BOUND ( 'NONE', #4513, .T. ) ;
#113623=AXIS2_PLACEMENT_3D ( 'NONE', #223893, #221321, #84344 ) ;
#113641=ORIENTED_EDGE ( 'NONE', *, *, #21633, .F. ) ;
#113694=CARTESIAN_POINT ( 'NONE',  ( -20.64999999999999858, 63.56320957583155717, -222.0641766000055668 ) ) ;
#113737=CARTESIAN_POINT ( 'NONE',  ( -18.59999999999999787, 67.23127455305841238, -235.8551265064783991 ) ) ;
#113753=EDGE_CURVE ( 'NONE', #207794, #170116, #163250, .T. ) ;
#113777=LINE ( 'NONE', #91657, #6511 ) ;
#113796=EDGE_CURVE ( 'NONE', #115375, #255725, #100821, .T. ) ;
#113798=AXIS2_PLACEMENT_3D ( 'NONE', #185450, #179365, #65488 ) ;
#113811=VERTEX_POINT ( 'NONE', #67628 ) ;
#113837=CARTESIAN_POINT ( 'NONE',  ( -23.15000000000000213, 78.00142589229885459, -228.9845759368473637 ) ) ;
#113842=ORIENTED_EDGE ( 'NONE', *, *, #175926, .F. ) ;
#113883=AXIS2_PLACEMENT_3D ( 'NONE', #190939, #72262, #230040 ) ;
#113890=EDGE_CURVE ( 'NONE', #250378, #40334, #36233, .T. ) ;
#113959=CARTESIAN_POINT ( 'NONE',  ( -23.25000000000000000, 86.27712145182582049, -209.5223386573213702 ) ) ;
#113979=ORIENTED_EDGE ( 'NONE', *, *, #22050, .T. ) ;
#114004=FACE_OUTER_BOUND ( 'NONE', #90675, .T. ) ;
#114010=CIRCLE ( 'NONE', #218234, 0.1000000000000018374 ) ;
#114013=TOROIDAL_SURFACE ( 'NONE', #176419, 0.4000000000000005773, 0.1000000000000000056 ) ;
#114029=CARTESIAN_POINT ( 'NONE',  ( -18.50000000000000000, 68.48451787451661232, -224.2224406095231757 ) ) ;
#114045=CIRCLE ( 'NONE', #184783, 11.74999999999999822 ) ;
#114051=EDGE_CURVE ( 'NONE', #163468, #149860, #88371, .T. ) ;
#114100=CARTESIAN_POINT ( 'NONE',  ( -18.59999999999999787, 80.78317333349157536, -192.9003134612049166 ) ) ;
#114104=TOROIDAL_SURFACE ( 'NONE', #51729, 0.2000000000000000111, 0.1000000000000000056 ) ;
#114114=DIRECTION ( 'NONE',  ( 1.040834085586001836E-13, -0.4105728183244014562, -0.9118278131605539460 ) ) ;
#114124=EDGE_CURVE ( 'NONE', #251232, #249371, #239547, .T. ) ;
#114142=CYLINDRICAL_SURFACE ( 'NONE', #104854, 0.09999999999999939493 ) ;
#114143=AXIS2_PLACEMENT_3D ( 'NONE', #191843, #234788, #138231 ) ;
#114181=CARTESIAN_POINT ( 'NONE',  ( 22.49999999999999645, 55.86495732666937641, -232.8769840133978164 ) ) ;
#114182=CARTESIAN_POINT ( 'NONE',  ( -18.50000000000000000, 61.38756220455727686, -221.6813469827248184 ) ) ;
#114226=AXIS2_PLACEMENT_3D ( 'NONE', #73734, #151994, #226680 ) ;
#114231=ORIENTED_EDGE ( 'NONE', *, *, #231550, .T. ) ;
#114239=AXIS2_PLACEMENT_3D ( 'NONE', #167229, #87641, #190634 ) ;
#114243=EDGE_CURVE ( 'NONE', #64537, #242736, #171826, .T. ) ;
#114250=ORIENTED_EDGE ( 'NONE', *, *, #94348, .F. ) ;
#114265=CARTESIAN_POINT ( 'NONE',  ( 22.39999999999999503, 64.18196446391819165, -247.0985338183330668 ) ) ;
#114268=DIRECTION ( 'NONE',  ( 0.000000000000000000, 0.8636236514130390951, -0.5041370733441546959 ) ) ;
#114301=EDGE_CURVE ( 'NONE', #231796, #112321, #128581, .T. ) ;
#114314=AXIS2_PLACEMENT_3D ( 'NONE', #229179, #93502, #132641 ) ;
#114326=EDGE_LOOP ( 'NONE', ( #136715, #153231, #225316, #174251 ) ) ;
#114340=ORIENTED_EDGE ( 'NONE', *, *, #100541, .T. ) ;
#114369=EDGE_CURVE ( 'NONE', #148648, #72740, #17598, .T. ) ;
#114377=VERTEX_POINT ( 'NONE', #176708 ) ;
#114410=CARTESIAN_POINT ( 'NONE',  ( 22.59999999999999076, 55.87393739788256397, -232.8427108587849261 ) ) ;
#114415=ORIENTED_EDGE ( 'NONE', *, *, #202946, .T. ) ;
#114439=DIRECTION ( 'NONE',  ( 0.000000000000000000, 0.2617529984165152257, 0.9651348961777124202 ) ) ;
#114473=LINE ( 'NONE', #148475, #202975 ) ;
#114543=AXIS2_PLACEMENT_3D ( 'NONE', #157562, #54559, #94969 ) ;
#114551=DIRECTION ( 'NONE',  ( 0.000000000000000000, 0.9651348961777161950, -0.2617529984165014589 ) ) ;
#114555=CARTESIAN_POINT ( 'NONE',  ( -18.59999999999999787, 79.24821784679178904, -196.3217825494968736 ) ) ;
#114558=EDGE_LOOP ( 'NONE', ( #78660, #107589, #107265, #253831 ) ) ;
#114561=CARTESIAN_POINT ( 'NONE',  ( 23.24999999999999645, 73.97321671803808840, -202.9734261878502366 ) ) ;
#114571=CARTESIAN_POINT ( 'NONE',  ( 23.14999999999998437, 68.29137419664525055, -231.9463301769586394 ) ) ;
#114585=CARTESIAN_POINT ( 'NONE',  ( 20.94999999999999574, 72.02722222756958104, -225.1832529173024398 ) ) ;
#114586=ORIENTED_EDGE ( 'NONE', *, *, #96490, .F. ) ;
#114599=ORIENTED_EDGE ( 'NONE', *, *, #134920, .F. ) ;
#114600=CARTESIAN_POINT ( 'NONE',  ( 18.59999999999999076, 68.48451787451661232, -224.2224406095231757 ) ) ;
#114612=ORIENTED_EDGE ( 'NONE', *, *, #176470, .F. ) ;
#114618=ORIENTED_EDGE ( 'NONE', *, *, #145239, .T. ) ;
#114649=LINE ( 'NONE', #174678, #45050 ) ;
#114718=DIRECTION ( 'NONE',  ( -0.000000000000000000, -0.9651348961777157509, 0.2617529984165031243 ) ) ;
#114725=EDGE_CURVE ( 'NONE', #50639, #12116, #1261, .T. ) ;
#114737=DIRECTION ( 'NONE',  ( 1.000000000000000000, 0.000000000000000000, 0.000000000000000000 ) ) ;
#114758=LINE ( 'NONE', #110902, #177736 ) ;
#114765=DIRECTION ( 'NONE',  ( 0.000000000000000000, 0.2617529984165152257, 0.9651348961777124202 ) ) ;
#114801=CARTESIAN_POINT ( 'NONE',  ( -20.54999999999999716, 65.86663596189677605, -213.5709895136416776 ) ) ;
#114810=FACE_OUTER_BOUND ( 'NONE', #62318, .T. ) ;
#114818=CARTESIAN_POINT ( 'NONE',  ( 18.59999999999998721, 48.66983769917126779, -228.4584249288054423 ) ) ;
#114823=CARTESIAN_POINT ( 'NONE',  ( 21.05000000000000071, 65.53249566929501668, -241.9221741022459469 ) ) ;
#114828=EDGE_CURVE ( 'NONE', #90505, #162955, #87296, .T. ) ;
#114832=ORIENTED_EDGE ( 'NONE', *, *, #21633, .T. ) ;
#114883=CARTESIAN_POINT ( 'NONE',  ( -23.25000000000000000, 80.69087520990402140, -192.8618289658565743 ) ) ;
#114893=AXIS2_PLACEMENT_3D ( 'NONE', #181581, #78600, #99435 ) ;
#114917=VERTEX_POINT ( 'NONE', #229403 ) ;
#114929=EDGE_LOOP ( 'NONE', ( #38533, #86321, #140175, #160892 ) ) ;
#114937=DIRECTION ( 'NONE',  ( 0.000000000000000000, -0.2617529984165152257, -0.9651348961777124202 ) ) ;
#114986=FACE_OUTER_BOUND ( 'NONE', #161084, .T. ) ;
#114987=CYLINDRICAL_SURFACE ( 'NONE', #87109, 0.09999999999999543976 ) ;
#115019=ADVANCED_FACE ( 'NONE', ( #110726 ), #113291, .F. ) ;
#115082=AXIS2_PLACEMENT_3D ( 'NONE', #12421, #90634, #30706 ) ;
#115147=ORIENTED_EDGE ( 'NONE', *, *, #178859, .F. ) ;
#115159=LINE ( 'NONE', #73494, #63445 ) ;
#115235=ORIENTED_EDGE ( 'NONE', *, *, #160011, .F. ) ;
#115245=CIRCLE ( 'NONE', #23704, 0.3999999999999926392 ) ;
#115260=AXIS2_PLACEMENT_3D ( 'NONE', #517, #239151, #60490 ) ;
#115268=ORIENTED_EDGE ( 'NONE', *, *, #240821, .F. ) ;
#115308=CARTESIAN_POINT ( 'NONE',  ( 21.05193202509564543, 60.06742710682065933, -221.2999661778954419 ) ) ;
#115318=DIRECTION ( 'NONE',  ( 1.000000000000000000, 0.000000000000000000, 0.000000000000000000 ) ) ;
#115332=ADVANCED_FACE ( 'NONE', ( #60374 ), #64239, .T. ) ;
#115334=EDGE_CURVE ( 'NONE', #124124, #209902, #118168, .T. ) ;
#115340=DIRECTION ( 'NONE',  ( 0.000000000000000000, 0.2617529984165031243, 0.9651348961777158619 ) ) ;
#115341=FACE_OUTER_BOUND ( 'NONE', #16702, .T. ) ;
#115364=EDGE_CURVE ( 'NONE', #229929, #217493, #105091, .T. ) ;
#115375=VERTEX_POINT ( 'NONE', #142478 ) ;
#115378=DIRECTION ( 'NONE',  ( 0.000000000000000000, 0.1290532225515392817, 0.9916376685811522096 ) ) ;
#115380=VERTEX_POINT ( 'NONE', #22559 ) ;
#115412=CARTESIAN_POINT ( 'NONE',  ( -18.48550754432065801, 78.20977376872917830, -231.5291668078544376 ) ) ;
#115415=EDGE_LOOP ( 'NONE', ( #105867, #173108, #8897, #49452 ) ) ;
#115416=VERTEX_POINT ( 'NONE', #100748 ) ;
#115423=VECTOR ( 'NONE', #46886, 1000.000000000000000 ) ;
#115459=DIRECTION ( 'NONE',  ( -0.000000000000000000, -0.3850724248243104775, 0.9228863568391969530 ) ) ;
#115465=CARTESIAN_POINT ( 'NONE',  ( 23.14999999999999503, 63.99342642423710714, -222.3880800784493772 ) ) ;
#115483=DIRECTION ( 'NONE',  ( 1.000000000000000000, 0.000000000000000000, 0.000000000000000000 ) ) ;
#115485=B_SPLINE_CURVE_WITH_KNOTS ( 'NONE', 3,
 ( #98838, #20645, #97561, #100130 ),
 .UNSPECIFIED., .F., .F.,
 ( 4, 4 ),
 ( 0.000000000000000000, 0.001767853679387116229 ),
 .UNSPECIFIED. ) ;
#115549=DIRECTION ( 'NONE',  ( 1.000000000000000000, 0.000000000000000000, 0.000000000000000000 ) ) ;
#115567=CARTESIAN_POINT ( 'NONE',  ( -20.54999999999999716, 70.22209180797715078, -215.6584443947398313 ) ) ;
#115569=ORIENTED_EDGE ( 'NONE', *, *, #83471, .F. ) ;
#115577=EDGE_LOOP ( 'NONE', ( #92971, #118193 ) ) ;
#115596=VECTOR ( 'NONE', #133843, 1000.000000000000000 ) ;
#115605=EDGE_CURVE ( 'NONE', #44096, #242024, #189332, .T. ) ;
#115621=ORIENTED_EDGE ( 'NONE', *, *, #177512, .F. ) ;
#115669=CIRCLE ( 'NONE', #149008, 0.1000000000000088318 ) ;
#115681=CARTESIAN_POINT ( 'NONE',  ( -23.25000000000000000, 64.27847795353595473, -247.1247091181747066 ) ) ;
#115700=ADVANCED_FACE ( 'NONE', ( #173671 ), #74559, .F. ) ;
#115749=TOROIDAL_SURFACE ( 'NONE', #99531, 11.65000000000000036, 0.1000000000000000056 ) ;
#115800=LINE ( 'NONE', #12874, #36975 ) ;
#115824=DIRECTION ( 'NONE',  ( -0.000000000000000000, 0.3896596508880146303, 0.9209589331071341700 ) ) ;
#115851=EDGE_CURVE ( 'NONE', #52077, #77989, #226090, .T. ) ;
#115878=VECTOR ( 'NONE', #46833, 1000.000000000000114 ) ;
#115911=CIRCLE ( 'NONE', #240813, 0.09999999999999939493 ) ;
#115939=ORIENTED_EDGE ( 'NONE', *, *, #37378, .T. ) ;
#115953=CARTESIAN_POINT ( 'NONE',  ( -18.59999999999999787, 70.53171716061257257, -228.4612385850772682 ) ) ;
#115981=DIRECTION ( 'NONE',  ( -0.000000000000000000, 0.3896596508880098009, 0.9209589331071360574 ) ) ;
#116005=CARTESIAN_POINT ( 'NONE',  ( -20.94999999999999929, 64.23744694032046709, -224.5446448091673233 ) ) ;
#116068=CARTESIAN_POINT ( 'NONE',  ( -20.54999999999999716, 66.26558728512915764, -222.7970849955717938 ) ) ;
#116103=ADVANCED_FACE ( 'NONE', ( #19369 ), #42777, .F. ) ;
#116117=VERTEX_POINT ( 'NONE', #138004 ) ;
#116121=DIRECTION ( 'NONE',  ( 1.000000000000000000, 0.000000000000000000, 0.000000000000000000 ) ) ;
#116123=FACE_OUTER_BOUND ( 'NONE', #176970, .T. ) ;
#116141=EDGE_LOOP ( 'NONE', ( #102440, #134046, #164625, #134978 ) ) ;
#116160=EDGE_LOOP ( 'NONE', ( #107839, #55080, #174456, #145208 ) ) ;
#116196=CYLINDRICAL_SURFACE ( 'NONE', #247437, 12.87500000000000178 ) ;
#116210=CARTESIAN_POINT ( 'NONE',  ( -20.64999999999999858, 82.09643798151613225, -215.4278993322501208 ) ) ;
#116216=AXIS2_PLACEMENT_3D ( 'NONE', #67658, #168093, #248873 ) ;
#116237=DIRECTION ( 'NONE',  ( 0.000000000000000000, 0.2617529984164506107, 0.9651348961777299618 ) ) ;
#116240=CARTESIAN_POINT ( 'NONE',  ( 23.14999999999999858, 67.92720994251783395, -214.1870976236629929 ) ) ;
#116241=VERTEX_POINT ( 'NONE', #206987 ) ;
#116287=FACE_OUTER_BOUND ( 'NONE', #110805, .T. ) ;
#116290=AXIS2_PLACEMENT_3D ( 'NONE', #21947, #183582, #164021 ) ;
#116316=CARTESIAN_POINT ( 'NONE',  ( -21.05000000000000071, 57.81354981234518675, -226.1844220500876474 ) ) ;
#116321=ORIENTED_EDGE ( 'NONE', *, *, #191408, .T. ) ;
#116328=FACE_OUTER_BOUND ( 'NONE', #94216, .T. ) ;
#116331=LINE ( 'NONE', #17233, #72510 ) ;
#116364=DIRECTION ( 'NONE',  ( 0.000000000000000000, -0.2617529984165031243, -0.9651348961777157509 ) ) ;
#116454=TOROIDAL_SURFACE ( 'NONE', #153915, 0.4000000000000005773, 0.1000000000000000056 ) ;
#116477=ORIENTED_EDGE ( 'NONE', *, *, #46479, .T. ) ;
#116482=CARTESIAN_POINT ( 'NONE',  ( -23.25000000000000000, 76.00000000001126921, -203.5231074845248997 ) ) ;
#116500=ADVANCED_FACE ( 'NONE', ( #37351 ), #21631, .T. ) ;
#116507=AXIS2_PLACEMENT_3D ( 'NONE', #105814, #143677, #66723 ) ;
#116584=FACE_OUTER_BOUND ( 'NONE', #131793, .T. ) ;
#116590=ORIENTED_EDGE ( 'NONE', *, *, #222090, .F. ) ;
#116592=CARTESIAN_POINT ( 'NONE',  ( -22.39999999999999858, 64.18196446391819165, -247.0985338183330668 ) ) ;
#116610=DIRECTION ( 'NONE',  ( 1.000000000000000000, 0.000000000000000000, 0.000000000000000000 ) ) ;
#116624=ORIENTED_EDGE ( 'NONE', *, *, #78991, .F. ) ;
#116630=FACE_OUTER_BOUND ( 'NONE', #122263, .T. ) ;
#116650=EDGE_LOOP ( 'NONE', ( #221875, #77327, #81620, #42823 ) ) ;
#116660=CIRCLE ( 'NONE', #150013, 0.09999999999999543976 ) ;
#116662=CARTESIAN_POINT ( 'NONE',  ( 20.94999999999999929, 76.00000000001126921, -203.5231074845248997 ) ) ;
#116672=FACE_BOUND ( 'NONE', #233338, .T. ) ;
#116690=CARTESIAN_POINT ( 'NONE',  ( -18.59999999999999787, 64.65966496992309942, -200.4475097531309586 ) ) ;
#116692=VECTOR ( 'NONE', #205908, 1000.000000000000114 ) ;
#116727=EDGE_CURVE ( 'NONE', #130829, #12569, #187138, .T. ) ;
#116750=CARTESIAN_POINT ( 'NONE',  ( 22.50014994443972682, 55.86946353937215548, -232.8597856945308422 ) ) ;
#116752=CIRCLE ( 'NONE', #62602, 0.1000000000000040579 ) ;
#116757=EDGE_LOOP ( 'NONE', ( #255990, #44412, #141771, #119085 ) ) ;
#116790=DIRECTION ( 'NONE',  ( 0.000000000000000000, 0.2617529984165180013, 0.9651348961777117541 ) ) ;
#116808=CIRCLE ( 'NONE', #241710, 0.09999999999999789613 ) ;
#116897=DIRECTION ( 'NONE',  ( 1.000000000000000000, -3.151514657663852580E-16, 8.547182517843351137E-17 ) ) ;
#116911=CARTESIAN_POINT ( 'NONE',  ( 22.57320508075687115, 55.89093952297024970, -232.7795287750844579 ) ) ;
#116962=CARTESIAN_POINT ( 'NONE',  ( 18.59999999999999076, 63.62814136979439184, -224.4990371885399441 ) ) ;
#116965=VERTEX_POINT ( 'NONE', #216932 ) ;
#116972=DIRECTION ( 'NONE',  ( -1.000000000000000000, -0.000000000000000000, 0.000000000000000000 ) ) ;
#117062=VERTEX_POINT ( 'NONE', #242598 ) ;
#117063=CIRCLE ( 'NONE', #212745, 0.1000000000000106498 ) ;
#117067=VECTOR ( 'NONE', #192570, 1000.000000000000000 ) ;
#117085=CARTESIAN_POINT ( 'NONE',  ( -21.05000000000000071, 57.76315019072730905, -226.2583585926041110 ) ) ;
#117098=DIRECTION ( 'NONE',  ( -1.000000000000000000, 0.000000000000000000, 0.000000000000000000 ) ) ;
#117123=AXIS2_PLACEMENT_3D ( 'NONE', #149378, #228894, #85483 ) ;
#117132=DIRECTION ( 'NONE',  ( 0.000000000000000000, -0.2617529984165031243, -0.9651348961777157509 ) ) ;
#117134=EDGE_CURVE ( 'NONE', #191649, #129114, #130802, .T. ) ;
#117159=VECTOR ( 'NONE', #166564, 1000.000000000000000 ) ;
#117167=DIRECTION ( 'NONE',  ( 1.000000000000000000, 0.000000000000000000, -0.000000000000000000 ) ) ;
#117171=ORIENTED_EDGE ( 'NONE', *, *, #239374, .F. ) ;
#117175=CIRCLE ( 'NONE', #150496, 3.999999999999996447 ) ;
#117177=ORIENTED_EDGE ( 'NONE', *, *, #237101, .F. ) ;
#117181=ADVANCED_FACE ( 'NONE', ( #166965 ), #151692, .F. ) ;
#117229=DIRECTION ( 'NONE',  ( -1.000000000000000000, 0.000000000000000000, 0.000000000000000000 ) ) ;
#117259=CARTESIAN_POINT ( 'NONE',  ( -22.50000000000000000, 55.96597777900654336, -232.8853806925634444 ) ) ;
#117270=AXIS2_PLACEMENT_3D ( 'NONE', #60170, #154501, #43197 ) ;
#117306=FACE_OUTER_BOUND ( 'NONE', #105222, .T. ) ;
#117341=DIRECTION ( 'NONE',  ( 1.000000000000000000, 0.000000000000000000, -0.000000000000000000 ) ) ;
#117394=CARTESIAN_POINT ( 'NONE',  ( 21.04999999999940741, 65.54469922025401729, -242.1294324713720698 ) ) ;
#117425=EDGE_LOOP ( 'NONE', ( #153166, #158289, #213704, #136561 ) ) ;
#117437=CARTESIAN_POINT ( 'NONE',  ( 20.95263205890701030, 60.86783962820125993, -225.3331190451696955 ) ) ;
#117452=DIRECTION ( 'NONE',  ( 0.000000000000000000, -0.2617529984165152257, -0.9651348961777124202 ) ) ;
#117462=CARTESIAN_POINT ( 'NONE',  ( 21.05000000000000071, 86.58125133469154378, -209.3975964148341973 ) ) ;
#117473=B_SPLINE_CURVE_WITH_KNOTS ( 'NONE', 3,
 ( #194923, #18825, #138735, #237878, #98322, #177922, #78781, #243004 ),
 .UNSPECIFIED., .F., .F.,
 ( 4, 2, 2, 4 ),
 ( 0.000000000000000000, 0.0001306511400390957911, 0.0001959767100586836666, 0.0002613022800782715421 ),
 .UNSPECIFIED. ) ;
#117484=DIRECTION ( 'NONE',  ( -1.000000000000000000, -0.000000000000000000, 0.000000000000000000 ) ) ;
#117502=CARTESIAN_POINT ( 'NONE',  ( -23.15000000000000213, 52.91185528119410009, -244.1460391050142960 ) ) ;
#117529=EDGE_LOOP ( 'NONE', ( #244089, #19156, #137636, #7383, #113098 ) ) ;
#117537=ORIENTED_EDGE ( 'NONE', *, *, #240009, .F. ) ;
#117556=CARTESIAN_POINT ( 'NONE',  ( 23.24999999999999289, 59.16775194334852017, -221.0793150863668473 ) ) ;
#117590=DIRECTION ( 'NONE',  ( -1.000000000000000000, -0.000000000000000000, -0.000000000000000000 ) ) ;
#117594=CYLINDRICAL_SURFACE ( 'NONE', #62650, 12.87500000000000178 ) ;
#117636=CARTESIAN_POINT ( 'NONE',  ( 18.39999999999999858, 87.08727414655710675, -199.6327537731849873 ) ) ;
#117686=EDGE_LOOP ( 'NONE', ( #145553, #58487, #211458, #83200 ) ) ;
#117690=CARTESIAN_POINT ( 'NONE',  ( 23.14999999999999858, 76.00000000001126921, -203.5231074845248997 ) ) ;
#117703=ORIENTED_EDGE ( 'NONE', *, *, #220718, .T. ) ;
#117741=EDGE_CURVE ( 'NONE', #177774, #94125, #159907, .T. ) ;
#117743=EDGE_LOOP ( 'NONE', ( #62347, #237548, #159751, #3386, #191916 ) ) ;
#117769=EDGE_CURVE ( 'NONE', #51680, #231796, #204252, .T. ) ;
#117770=CARTESIAN_POINT ( 'NONE',  ( -23.25000000000000000, 68.62136427087769164, -214.1108709299723500 ) ) ;
#117771=AXIS2_PLACEMENT_3D ( 'NONE', #176640, #175366, #179214 ) ;
#117788=DIRECTION ( 'NONE',  ( 1.000000000000000000, 0.000000000000000000, 0.000000000000000000 ) ) ;
#117813=CARTESIAN_POINT ( 'NONE',  ( 21.05000000000000071, 86.48473784507378070, -209.3714211149925575 ) ) ;
#117815=DIRECTION ( 'NONE',  ( -1.000000000000000000, -0.000000000000000000, -0.000000000000000000 ) ) ;
#117858=( BOUNDED_CURVE ( )  B_SPLINE_CURVE ( 3, ( #232572, #49070, #13505, #226403 ),
 .UNSPECIFIED., .F., .F. ) 
 B_SPLINE_CURVE_WITH_KNOTS ( ( 4, 4 ),
 ( 3.192897208853993085, 4.712388980384696779 ),
 .UNSPECIFIED. ) 
 CURVE ( )  GEOMETRIC_REPRESENTATION_ITEM ( )  RATIONAL_B_SPLINE_CURVE ( ( 1.000000000000000000, 0.8166740347213210516, 0.8166740347213210516, 1.000000000000000000 ) ) 
 REPRESENTATION_ITEM ( '' )  );
#117902=DIRECTION ( 'NONE',  ( 0.000000000000000000, -0.9651348961777155289, 0.2617529984165036794 ) ) ;
#117912=CARTESIAN_POINT ( 'NONE',  ( 21.05000000000000071, 67.92720994251783395, -214.1870976236629929 ) ) ;
#117913=FACE_OUTER_BOUND ( 'NONE', #61827, .T. ) ;
#117926=( BOUNDED_SURFACE ( )  B_SPLINE_SURFACE ( 3, 2, ( 
 ( #132213, #33154, #172674 ),
 ( #93075, #252147, #188335 ),
 ( #73557, #50097, #232624 ),
 ( #168820, #14858, #253431 ) ),
 .UNSPECIFIED., .F., .F., .F. ) 
 B_SPLINE_SURFACE_WITH_KNOTS ( ( 4, 4 ),
 ( 3, 3 ),
 ( 0.04058434257139457990, 0.04256401539001584966 ),
 ( 0.000000000000000000, 1.000000000000000000 ),
 .UNSPECIFIED. ) 
 GEOMETRIC_REPRESENTATION_ITEM ( )  RATIONAL_B_SPLINE_SURFACE ( (
 ( 1.000000000000000000, 0.7103081912008947230, 1.000000000000000000),
 ( 1.000000000000000000, 0.7104998333553655954, 1.000000000000000000),
 ( 1.000000000000000000, 0.7107238315756251312, 1.000000000000000000),
 ( 1.000000000000000000, 0.7110073749539724819, 1.000000000000000000) ) ) 
 REPRESENTATION_ITEM ( '' )  SURFACE ( )  );
#117962=AXIS2_PLACEMENT_3D ( 'NONE', #203128, #61044, #119769 ) ;
#117983=DIRECTION ( 'NONE',  ( 0.000000000000000000, 0.2617529984164955192, 0.9651348961777177493 ) ) ;
#118053=DIRECTION ( 'NONE',  ( 0.000000000000000000, -0.9651348961777157509, 0.2617529984165031243 ) ) ;
#118068=DIRECTION ( 'NONE',  ( 0.000000000000000000, 0.2617529984165024026, 0.9651348961777158619 ) ) ;
#118126=DIRECTION ( 'NONE',  ( 0.000000000000000000, -0.2617529984165031243, -0.9651348961777158619 ) ) ;
#118128=DIRECTION ( 'NONE',  ( 0.7071067811865460184, 0.6824534298470606997, -0.1850873201761399356 ) ) ;
#118137=LINE ( 'NONE', #197662, #62562 ) ;
#118142=EDGE_LOOP ( 'NONE', ( #85961, #130247, #239592, #115621 ) ) ;
#118156=ADVANCED_FACE ( 'NONE', ( #188010 ), #109731, .T. ) ;
#118160=CARTESIAN_POINT ( 'NONE',  ( 23.14999999999999858, 74.95298800634525094, -207.3836470692357636 ) ) ;
#118168=CIRCLE ( 'NONE', #238404, 2.000000000000013323 ) ;
#118175=DIRECTION ( 'NONE',  ( 1.000000000000000000, 0.000000000000000000, 0.000000000000000000 ) ) ;
#118193=ORIENTED_EDGE ( 'NONE', *, *, #12018, .T. ) ;
#118228=ORIENTED_EDGE ( 'NONE', *, *, #30815, .T. ) ;
#118256=AXIS2_PLACEMENT_3D ( 'NONE', #219558, #140012, #40967 ) ;
#118265=EDGE_CURVE ( 'NONE', #6907, #43706, #195353, .T. ) ;
#118316=DIRECTION ( 'NONE',  ( 0.000000000000000000, 0.2617529984165306578, 0.9651348961777082014 ) ) ;
#118337=VECTOR ( 'NONE', #142647, 1000.000000000000000 ) ;
#118338=DIRECTION ( 'NONE',  ( 0.000000000000000000, 0.2617529984165033463, 0.9651348961777157509 ) ) ;
#118360=( BOUNDED_SURFACE ( )  B_SPLINE_SURFACE ( 3, 2, ( 
 ( #220658, #185375, #66717 ),
 ( #107114, #186674, #142391 ),
 ( #8036, #87538, #181545 ),
 ( #221904, #65421, #241501 ),
 ( #143672, #184087, #167129 ),
 ( #43306, #122849, #5421 ) ),
 .UNSPECIFIED., .F., .F., .F. ) 
 B_SPLINE_SURFACE_WITH_KNOTS ( ( 4, 2, 4 ),
 ( 3, 3 ),
 ( 0.0001792624049599680035, 0.0003686986002124869027, 0.0005581347954650057747 ),
 ( 0.000000000000000000, 1.000000000000000000 ),
 .UNSPECIFIED. ) 
 GEOMETRIC_REPRESENTATION_ITEM ( )  RATIONAL_B_SPLINE_SURFACE ( (
 ( 1.000000000000000000, 0.9238795325112821866, 1.000000000000000000),
 ( 1.000000000000000000, 0.9229318695238644121, 1.000000000000000000),
 ( 1.000000000000000000, 0.8926288119230598728, 1.000000000000000000),
 ( 1.000000000000000000, 0.8123777807271286289, 1.000000000000000000),
 ( 1.000000000000000000, 0.7629087100931351006, 1.000000000000000000),
 ( 1.000000000000000000, 0.7071067811865610064, 1.000000000000000000) ) ) 
 REPRESENTATION_ITEM ( '' )  SURFACE ( )  );
#118430=AXIS2_PLACEMENT_3D ( 'NONE', #209933, #170845, #191670 ) ;
#118480=VERTEX_POINT ( 'NONE', #31950 ) ;
#118538=ORIENTED_EDGE ( 'NONE', *, *, #186594, .F. ) ;
#118545=LINE ( 'NONE', #135496, #190243 ) ;
#118565=ORIENTED_EDGE ( 'NONE', *, *, #227647, .F. ) ;
#118610=CIRCLE ( 'NONE', #201775, 11.64999999999998970 ) ;
#118621=DIRECTION ( 'NONE',  ( 1.836970198721029934E-16, 0.9651348961777157509, -0.2617529984165031243 ) ) ;
#118627=DIRECTION ( 'NONE',  ( -1.000000000000000000, -0.000000000000000000, 0.000000000000000000 ) ) ;
#118680=CIRCLE ( 'NONE', #81214, 0.09999999999999543976 ) ;
#118681=CARTESIAN_POINT ( 'NONE',  ( -23.25000000000000000, 67.23127455305841238, -235.8551265064783991 ) ) ;
#118687=AXIS2_PLACEMENT_3D ( 'NONE', #2955, #119075, #77353 ) ;
#118694=DIRECTION ( 'NONE',  ( 1.000000000000000000, 0.000000000000000000, 0.000000000000000000 ) ) ;
#118705=DIRECTION ( 'NONE',  ( -1.000000000000000000, 3.151514657663852580E-16, -8.547182517843351137E-17 ) ) ;
#118736=CARTESIAN_POINT ( 'NONE',  ( 20.95392731769792150, 60.88864066144310527, -225.3048589129162167 ) ) ;
#118762=ORIENTED_EDGE ( 'NONE', *, *, #48774, .F. ) ;
#118778=EDGE_CURVE ( 'NONE', #69945, #250282, #62610, .T. ) ;
#118783=MECHANICAL_DESIGN_GEOMETRIC_PRESENTATION_REPRESENTATION('',(#1851),#77068);
#118789=VERTEX_POINT ( 'NONE', #141297 ) ;
#118792=ORIENTED_EDGE ( 'NONE', *, *, #110243, .F. ) ;
#118798=CYLINDRICAL_SURFACE ( 'NONE', #197059, 4.049999999999987388 ) ;
#118805=ORIENTED_EDGE ( 'NONE', *, *, #15282, .F. ) ;
#118823=ORIENTED_EDGE ( 'NONE', *, *, #194952, .F. ) ;
#118845=EDGE_LOOP ( 'NONE', ( #47962, #240942, #72836, #101693 ) ) ;
#118874=CARTESIAN_POINT ( 'NONE',  ( 20.84999999999998721, 64.65966496992309942, -200.4475097531309586 ) ) ;
#118892=EDGE_LOOP ( 'NONE', ( #240626, #148401, #177534, #60621 ) ) ;
#118904=DIRECTION ( 'NONE',  ( 1.000000000000000000, 0.000000000000000000, 0.000000000000000000 ) ) ;
#118922=CARTESIAN_POINT ( 'NONE',  ( 22.39999999999999503, 65.19201463318205469, -243.3742797652979277 ) ) ;
#118960=LINE ( 'NONE', #101918, #44120 ) ;
#118963=CARTESIAN_POINT ( 'NONE',  ( -20.95000000000000284, 62.92003201576282123, -207.2439188921395896 ) ) ;
#118975=DIRECTION ( 'NONE',  ( 0.000000000000000000, 0.9651348961777160840, -0.2617529984165015700 ) ) ;
#118986=CARTESIAN_POINT ( 'NONE',  ( -20.64999999999999858, 76.49733069700262433, -201.6893511817872309 ) ) ;
#119075=DIRECTION ( 'NONE',  ( 0.000000000000000000, 0.9651348961777157509, -0.2617529984165031243 ) ) ;
#119080=ORIENTED_EDGE ( 'NONE', *, *, #190639, .T. ) ;
#119082=EDGE_LOOP ( 'NONE', ( #201570, #32898, #179941, #50049 ) ) ;
#119085=ORIENTED_EDGE ( 'NONE', *, *, #114725, .T. ) ;
#119112=EDGE_CURVE ( 'NONE', #204366, #952, #204240, .T. ) ;
#119160=SPHERICAL_SURFACE ( 'NONE', #186517, 0.1000000000000000056 ) ;
#119248=DIRECTION ( 'NONE',  ( 1.000000000000000000, 0.000000000000000000, 0.000000000000000000 ) ) ;
#119285=CARTESIAN_POINT ( 'NONE',  ( -18.43599941264924169, 78.24390722508243812, -231.6169757740163107 ) ) ;
#119291=DIRECTION ( 'NONE',  ( 0.000000000000000000, 0.2617529984165152257, 0.9651348961777124202 ) ) ;
#119367=ADVANCED_FACE ( 'NONE', ( #62447 ), #242353, .T. ) ;
#119441=DIRECTION ( 'NONE',  ( 0.000000000000000000, 0.2617529984165031243, 0.9651348961777157509 ) ) ;
#119442=CARTESIAN_POINT ( 'NONE',  ( -21.05000000000000071, 67.46931694187804851, -235.9558427390807083 ) ) ;
#119490=DIRECTION ( 'NONE',  ( 1.000000000000000000, 0.000000000000000000, 0.000000000000000000 ) ) ;
#119548=EDGE_LOOP ( 'NONE', ( #33454, #198641, #74609, #5053 ) ) ;
#119553=ORIENTED_EDGE ( 'NONE', *, *, #174641, .T. ) ;
#119555=CYLINDRICAL_SURFACE ( 'NONE', #79699, 0.1000000000000124678 ) ;
#119557=CARTESIAN_POINT ( 'NONE',  ( 20.94999999999999929, 65.17014820068582992, -222.4427298839669618 ) ) ;
#119561=CIRCLE ( 'NONE', #236243, 0.09999999999999939493 ) ;
#119566=CARTESIAN_POINT ( 'NONE',  ( -18.50000000000000711, 57.82359945636609666, -226.0354702357591350 ) ) ;
#119653=AXIS2_PLACEMENT_3D ( 'NONE', #190460, #250400, #211285 ) ;
#119686=FACE_OUTER_BOUND ( 'NONE', #105207, .T. ) ;
#119709=CARTESIAN_POINT ( 'NONE',  ( -21.14999999999999858, 55.98745301258801987, -232.8057040749261262 ) ) ;
#119725=DIRECTION ( 'NONE',  ( 0.000000000000000000, -0.2617529984165031243, -0.9651348961777157509 ) ) ;
#119763=EDGE_CURVE ( 'NONE', #23903, #191649, #62136, .T. ) ;
#119764=ORIENTED_EDGE ( 'NONE', *, *, #15494, .F. ) ;
#119765=AXIS2_PLACEMENT_3D ( 'NONE', #256027, #197386, #18754 ) ;
#119769=DIRECTION ( 'NONE',  ( -6.938893903907222067E-15, -0.9651348961777157509, 0.2617529984165031243 ) ) ;
#119771=EDGE_CURVE ( 'NONE', #12116, #137789, #77826, .T. ) ;
#119812=ORIENTED_EDGE ( 'NONE', *, *, #91580, .F. ) ;
#119825=CIRCLE ( 'NONE', #74049, 0.3999999999999926392 ) ;
#119837=EDGE_CURVE ( 'NONE', #72929, #222045, #100530, .T. ) ;
#119844=CARTESIAN_POINT ( 'NONE',  ( -22.49544290803695290, 55.87396915977456047, -232.8425975917331243 ) ) ;
#119857=ADVANCED_FACE ( 'NONE', ( #158696 ), #222452, .F. ) ;
#119864=LINE ( 'NONE', #198086, #140885 ) ;
#119870=ORIENTED_EDGE ( 'NONE', *, *, #195161, .F. ) ;
#119887=FACE_OUTER_BOUND ( 'NONE', #132522, .T. ) ;
#119890=ADVANCED_FACE ( 'NONE', ( #99941 ), #119555, .T. ) ;
#119913=LINE ( 'NONE', #199438, #161854 ) ;
#119914=CARTESIAN_POINT ( 'NONE',  ( 22.60000000000000142, 64.05844819680034163, -247.1686437718134073 ) ) ;
#119941=SHAPE_DEFINITION_REPRESENTATION ( #153648, #241717 ) ;
#119972=EDGE_CURVE ( 'NONE', #77258, #144320, #44837, .T. ) ;
#119973=EDGE_LOOP ( 'NONE', ( #208927, #243696, #104089, #232179 ) ) ;
#119998=DIRECTION ( 'NONE',  ( -1.000000000000000000, -0.000000000000000000, -0.000000000000000000 ) ) ;
#120007=ORIENTED_EDGE ( 'NONE', *, *, #167048, .T. ) ;
#120022=AXIS2_PLACEMENT_3D ( 'NONE', #168689, #108661, #109935 ) ;
#120053=ORIENTED_EDGE ( 'NONE', *, *, #163278, .F. ) ;
#120055=FACE_OUTER_BOUND ( 'NONE', #7162, .T. ) ;
#120075=CIRCLE ( 'NONE', #20086, 12.87500000000000178 ) ;
#120078=FACE_OUTER_BOUND ( 'NONE', #20701, .T. ) ;
#120103=ORIENTED_EDGE ( 'NONE', *, *, #217690, .T. ) ;
#120104=CARTESIAN_POINT ( 'NONE',  ( -21.05000000000000071, 86.27712145182582049, -209.5223386573213702 ) ) ;
#120114=DIRECTION ( 'NONE',  ( 0.000000000000000000, -0.9651348961777157509, 0.2617529984165031243 ) ) ;
#120132=ORIENTED_EDGE ( 'NONE', *, *, #168383, .T. ) ;
#120135=CARTESIAN_POINT ( 'NONE',  ( -23.15000000000000213, 76.00000000001126921, -203.5231074845248997 ) ) ;
#120151=CIRCLE ( 'NONE', #36757, 0.1000000000000106498 ) ;
#120153=EDGE_CURVE ( 'NONE', #178237, #212838, #90211, .T. ) ;
#120167=CYLINDRICAL_SURFACE ( 'NONE', #239858, 0.1000000000000124678 ) ;
#120176=ADVANCED_FACE ( 'NONE', ( #124052 ), #122776, .T. ) ;
#120179=ORIENTED_EDGE ( 'NONE', *, *, #15160, .T. ) ;
#120194=DIRECTION ( 'NONE',  ( -0.000000000000000000, -0.2617529984165031243, -0.9651348961777157509 ) ) ;
#120203=SPHERICAL_SURFACE ( 'NONE', #66747, 0.1000000000000000056 ) ;
#120215=CARTESIAN_POINT ( 'NONE',  ( -21.45000000000000284, 65.32753222054176945, -213.4247798787853867 ) ) ;
#120220=EDGE_CURVE ( 'NONE', #148469, #115416, #70522, .T. ) ;
#120259=CARTESIAN_POINT ( 'NONE',  ( -23.25000000000000000, 70.60814576644823148, -215.7631455941064189 ) ) ;
#120277=ORIENTED_EDGE ( 'NONE', *, *, #83027, .F. ) ;
#120287=FACE_OUTER_BOUND ( 'NONE', #240459, .T. ) ;
#120309=EDGE_CURVE ( 'NONE', #179646, #72929, #250399, .T. ) ;
#120324=ORIENTED_EDGE ( 'NONE', *, *, #52031, .T. ) ;
#120351=AXIS2_PLACEMENT_3D ( 'NONE', #196853, #256782, #35263 ) ;
#120374=DIRECTION ( 'NONE',  ( 1.000000000000000000, 0.000000000000000000, 0.000000000000000000 ) ) ;
#120376=ORIENTED_EDGE ( 'NONE', *, *, #134920, .T. ) ;
#120384=AXIS2_PLACEMENT_3D ( 'NONE', #176272, #53723, #74617 ) ;
#120399=EDGE_LOOP ( 'NONE', ( #207274, #120007, #85701, #101767, #45257, #209298 ) ) ;
#120412=EDGE_CURVE ( 'NONE', #207794, #8721, #100707, .T. ) ;
#120423=EDGE_LOOP ( 'NONE', ( #229210, #9511, #64808, #243541 ) ) ;
#120438=ORIENTED_EDGE ( 'NONE', *, *, #241465, .F. ) ;
#120450=ORIENTED_EDGE ( 'NONE', *, *, #6187, .T. ) ;
#120471=AXIS2_PLACEMENT_3D ( 'NONE', #77463, #157046, #95752 ) ;
#120489=CARTESIAN_POINT ( 'NONE',  ( -20.94788355080264353, 67.49401193140447219, -195.5283494629371432 ) ) ;
#120493=TOROIDAL_SURFACE ( 'NONE', #66315, 0.2000000000000000111, 0.1000000000000000056 ) ;
#120514=DIRECTION ( 'NONE',  ( 0.000000000000000000, -0.2617529984164955192, -0.9651348961777178603 ) ) ;
#120527=CARTESIAN_POINT ( 'NONE',  ( 20.94999999999999929, 60.99662849158838895, -205.1669373764474642 ) ) ;
#120537=ORIENTED_EDGE ( 'NONE', *, *, #38698, .F. ) ;
#120555=DIRECTION ( 'NONE',  ( 1.000000000000000000, -2.824170522722115425E-14, 2.841386468225606068E-14 ) ) ;
#120572=CARTESIAN_POINT ( 'NONE',  ( 20.91682497891423154, 67.49276774653023381, -195.4544018784149841 ) ) ;
#120589=CARTESIAN_POINT ( 'NONE',  ( 21.05000000000000071, 63.43511439055885148, -224.4466865888566360 ) ) ;
#120609=TOROIDAL_SURFACE ( 'NONE', #170713, 12.77499999999999858, 0.1000000000000000056 ) ;
#120613=CARTESIAN_POINT ( 'NONE',  ( -23.25000000000000000, 64.65966496992309942, -200.4475097531309586 ) ) ;
#120671=CARTESIAN_POINT ( 'NONE',  ( 22.47071067811865319, 65.11488425470513164, -243.2801022963548405 ) ) ;
#120676=ORIENTED_EDGE ( 'NONE', *, *, #219485, .T. ) ;
#120691=VERTEX_POINT ( 'NONE', #68920 ) ;
#120737=CYLINDRICAL_SURFACE ( 'NONE', #93618, 0.09999999999999868716 ) ;
#120738=ORIENTED_EDGE ( 'NONE', *, *, #222631, .F. ) ;
#120753=EDGE_CURVE ( 'NONE', #252932, #26421, #71906, .T. ) ;
#120772=DIRECTION ( 'NONE',  ( 1.000000000000000000, 0.000000000000000000, 0.000000000000000000 ) ) ;
#120795=DIRECTION ( 'NONE',  ( 1.000000000000000000, 0.000000000000000000, 0.000000000000000000 ) ) ;
#120797=DIRECTION ( 'NONE',  ( 0.000000000000000000, -0.2617529984165031243, -0.9651348961777157509 ) ) ;
#120802=CARTESIAN_POINT ( 'NONE',  ( 23.14999999999999147, 63.22596473392088967, -234.7688515630498785 ) ) ;
#120818=EDGE_CURVE ( 'NONE', #201773, #70810, #25933, .T. ) ;
#120854=CARTESIAN_POINT ( 'NONE',  ( 23.24999999999997513, 62.82351852614503684, -207.2177435922979214 ) ) ;
#120869=ORIENTED_EDGE ( 'NONE', *, *, #94315, .T. ) ;
#120892=DIRECTION ( 'NONE',  ( 0.000000000000000000, 0.2617529984165152257, 0.9651348961777124202 ) ) ;
#120904=EDGE_CURVE ( 'NONE', #126428, #178010, #80465, .T. ) ;
#120917=ORIENTED_EDGE ( 'NONE', *, *, #186509, .T. ) ;
#120928=CARTESIAN_POINT ( 'NONE',  ( 23.14999999999999858, 67.92720994251783395, -214.1870976236629929 ) ) ;
#120995=CARTESIAN_POINT ( 'NONE',  ( -20.94999999999999929, 68.49522935589659767, -224.1230159437372436 ) ) ;
#121036=EDGE_CURVE ( 'NONE', #104140, #137094, #159396, .T. ) ;
#121049=DIRECTION ( 'NONE',  ( 0.000000000000000000, 0.2617529984165039569, 0.9651348961777155289 ) ) ;
#121064=VERTEX_POINT ( 'NONE', #29498 ) ;
#121071=AXIS2_PLACEMENT_3D ( 'NONE', #176265, #254456, #36765 ) ;
#121100=ORIENTED_EDGE ( 'NONE', *, *, #249136, .F. ) ;
#121127=ORIENTED_EDGE ( 'NONE', *, *, #243642, .T. ) ;
#121161=EDGE_LOOP ( 'NONE', ( #186429, #58049, #238443, #112696 ) ) ;
#121186=DIRECTION ( 'NONE',  ( 0.000000000000000000, -0.2617529984165031243, -0.9651348961777157509 ) ) ;
#121202=CARTESIAN_POINT ( 'NONE',  ( 22.39999999999999503, 64.25313205997782973, -247.2214437328673853 ) ) ;
#121216=EDGE_CURVE ( 'NONE', #143771, #8746, #46922, .T. ) ;
#121257=EDGE_CURVE ( 'NONE', #114377, #115375, #246843, .T. ) ;
#121297=DIRECTION ( 'NONE',  ( 7.304098846218134667E-16, -0.9651348961777158619, 0.2617529984165031243 ) ) ;
#121322=EDGE_CURVE ( 'NONE', #152104, #76073, #209432, .T. ) ;
#121332=CARTESIAN_POINT ( 'NONE',  ( -2.995603634470891112E-16, 66.37537870982728805, -213.6053525232321704 ) ) ;
#121343=EDGE_CURVE ( 'NONE', #32310, #208014, #125684, .T. ) ;
#121366=AXIS2_PLACEMENT_3D ( 'NONE', #135579, #176035, #215135 ) ;
#121380=VERTEX_POINT ( 'NONE', #166139 ) ;
#121389=ORIENTED_EDGE ( 'NONE', *, *, #26719, .T. ) ;
#121395=AXIS2_PLACEMENT_3D ( 'NONE', #189180, #108360, #31420 ) ;
#121417=ORIENTED_EDGE ( 'NONE', *, *, #23159, .F. ) ;
#121452=ORIENTED_EDGE ( 'NONE', *, *, #5902, .F. ) ;
#121487=CARTESIAN_POINT ( 'NONE',  ( 20.94999999999999929, 74.95298800634525094, -207.3836470692357636 ) ) ;
#121489=LINE ( 'NONE', #200998, #228819 ) ;
#121496=ORIENTED_EDGE ( 'NONE', *, *, #210388, .F. ) ;
#121521=DIRECTION ( 'NONE',  ( -7.304098846218134667E-16, 0.9651348961777158619, -0.2617529984165031243 ) ) ;
#121566=DIRECTION ( 'NONE',  ( 0.7071067811865474617, -0.6824534298470372740, 0.1850873201762208153 ) ) ;
#121578=VECTOR ( 'NONE', #94607, 1000.000000000000000 ) ;
#121582=CIRCLE ( 'NONE', #9114, 0.1000000000000124678 ) ;
#121592=CARTESIAN_POINT ( 'NONE',  ( 19.81427058490550053, 62.44792297811893178, -208.9137562170004117 ) ) ;
#121645=ORIENTED_EDGE ( 'NONE', *, *, #80618, .T. ) ;
#121666=CARTESIAN_POINT ( 'NONE',  ( -21.05000000000000071, 68.22930980752001062, -227.7331931781284879 ) ) ;
#121668=EDGE_CURVE ( 'NONE', #256377, #145620, #9701, .T. ) ;
#121674=ORIENTED_EDGE ( 'NONE', *, *, #228823, .T. ) ;
#121693=AXIS2_PLACEMENT_3D ( 'NONE', #154856, #12776, #51853 ) ;
#121710=ORIENTED_EDGE ( 'NONE', *, *, #100915, .T. ) ;
#121752=PRODUCT_DEFINITION ( 'UNKNOWN', '', #90450, #84306 ) ;
#121759=CARTESIAN_POINT ( 'NONE',  ( -18.59999999999999787, 59.16775194334852728, -221.0793150863668473 ) ) ;
#121764=CARTESIAN_POINT ( 'NONE',  ( -20.90851465518105812, 67.49261718274587452, -195.4446851895584416 ) ) ;
#121777=EDGE_CURVE ( 'NONE', #178174, #15176, #202707, .T. ) ;
#121787=VERTEX_POINT ( 'NONE', #67062 ) ;
#121806=DIRECTION ( 'NONE',  ( -1.000000000000000000, -0.000000000000000000, -0.000000000000000000 ) ) ;
#121807=ORIENTED_EDGE ( 'NONE', *, *, #51760, .T. ) ;
#121829=CIRCLE ( 'NONE', #9378, 0.09999999999999939493 ) ;
#121836=ORIENTED_EDGE ( 'NONE', *, *, #48546, .T. ) ;
#121861=CARTESIAN_POINT ( 'NONE',  ( -20.54999999999999716, 70.71284696581484752, -215.3770916356353382 ) ) ;
#121865=EDGE_CURVE ( 'NONE', #40848, #76927, #65769, .T. ) ;
#121886=FACE_OUTER_BOUND ( 'NONE', #54560, .T. ) ;
#121893=CIRCLE ( 'NONE', #146976, 12.97499999999998899 ) ;
#121898=AXIS2_PLACEMENT_3D ( 'NONE', #164387, #243904, #66571 ) ;
#121909=CARTESIAN_POINT ( 'NONE',  ( -21.05000000000000071, 70.56573376625485139, -228.3808404818380779 ) ) ;
#121928=CARTESIAN_POINT ( 'NONE',  ( -21.05000000000000071, 70.53171716061257257, -228.4612385850772682 ) ) ;
#121947=CARTESIAN_POINT ( 'NONE',  ( -18.39999999999999858, 86.89640087696872683, -199.6396878666313341 ) ) ;
#121962=CARTESIAN_POINT ( 'NONE',  ( 18.49999999999999645, 64.18627039993180006, -224.3513032416919089 ) ) ;
#121996=AXIS2_PLACEMENT_3D ( 'NONE', #97189, #37287, #157244 ) ;
#122020=AXIS2_PLACEMENT_3D ( 'NONE', #121759, #82572, #100842 ) ;
#122042=VECTOR ( 'NONE', #138894, 1000.000000000000114 ) ;
#122063=ORIENTED_EDGE ( 'NONE', *, *, #213114, .T. ) ;
#122077=AXIS2_PLACEMENT_3D ( 'NONE', #134617, #255825, #194650 ) ;
#122095=VERTEX_POINT ( 'NONE', #4197 ) ;
#122099=LINE ( 'NONE', #105045, #85703 ) ;
#122110=DIRECTION ( 'NONE',  ( 0.000000000000000000, 0.9167729611565434977, -0.3994087351226345284 ) ) ;
#122125=CARTESIAN_POINT ( 'NONE',  ( 20.94999999999999929, 64.08993991385487732, -222.4142553782910454 ) ) ;
#122138=DIRECTION ( 'NONE',  ( 7.304098846218134667E-16, 0.9651348961777158619, -0.2617529984165031243 ) ) ;
#122155=CIRCLE ( 'NONE', #134593, 0.1999999999999945155 ) ;
#122166=CARTESIAN_POINT ( 'NONE',  ( 23.24999999999999645, 76.00000000001126921, -203.5231074845248997 ) ) ;
#122185=CARTESIAN_POINT ( 'NONE',  ( -23.15000000000000213, 76.00000000001126921, -203.5231074845248997 ) ) ;
#122250=CARTESIAN_POINT ( 'NONE',  ( -21.05000000000000071, 63.65372963998873246, -224.5957079722776655 ) ) ;
#122254=DIRECTION ( 'NONE',  ( 0.000000000000000000, 0.2617529984165071766, 0.9651348961777145297 ) ) ;
#122263=EDGE_LOOP ( 'NONE', ( #65978, #142496, #214332, #190402 ) ) ;
#122275=CIRCLE ( 'NONE', #55586, 0.1000000000000106498 ) ;
#122308=ORIENTED_EDGE ( 'NONE', *, *, #234032, .F. ) ;
#122322=CARTESIAN_POINT ( 'NONE',  ( 20.94999999999999574, 68.49765435822607174, -224.1215006111142714 ) ) ;
#122330=CIRCLE ( 'NONE', #193081, 0.5000000000000014433 ) ;
#122332=CARTESIAN_POINT ( 'NONE',  ( -20.64999999999999858, 76.00000000001126921, -203.5231074845248997 ) ) ;
#122364=ORIENTED_EDGE ( 'NONE', *, *, #9939, .T. ) ;
#122365=CYLINDRICAL_SURFACE ( 'NONE', #161613, 0.09999999999999230338 ) ;
#122387=ORIENTED_EDGE ( 'NONE', *, *, #52250, .T. ) ;
#122447=DIRECTION ( 'NONE',  ( 0.000000000000000000, 0.2617529984165036239, 0.9651348961777156399 ) ) ;
#122455=ADVANCED_FACE ( 'NONE', ( #155307 ), #151487, .F. ) ;
#122477=CARTESIAN_POINT ( 'NONE',  ( 18.49999999999999645, 72.10920423909969657, -225.0008277277438822 ) ) ;
#122493=EDGE_LOOP ( 'NONE', ( #27933, #56293, #215995, #193608 ) ) ;
#122525=EDGE_LOOP ( 'NONE', ( #184174, #176700, #61643, #162364 ) ) ;
#122549=B_SPLINE_CURVE_WITH_KNOTS ( 'NONE', 3,
 ( #84186, #202911, #243312, #205469 ),
 .UNSPECIFIED., .F., .F.,
 ( 4, 4 ),
 ( 0.000000000000000000, 0.0002118541922231950789 ),
 .UNSPECIFIED. ) ;
#122557=ORIENTED_EDGE ( 'NONE', *, *, #162400, .F. ) ;
#122596=CARTESIAN_POINT ( 'NONE',  ( 23.14999999999999503, 61.57587952878035509, -212.2000740415318774 ) ) ;
#122609=EDGE_CURVE ( 'NONE', #159875, #7826, #219082, .T. ) ;
#122615=CARTESIAN_POINT ( 'NONE',  ( -18.59999999999999787, 57.82359945636609666, -226.0354702357591350 ) ) ;
#122630=VERTEX_POINT ( 'NONE', #131548 ) ;
#122641=VECTOR ( 'NONE', #227851, 1000.000000000000000 ) ;
#122674=ORIENTED_EDGE ( 'NONE', *, *, #96598, .T. ) ;
#122678=EDGE_CURVE ( 'NONE', #75171, #96108, #207256, .T. ) ;
#122684=CARTESIAN_POINT ( 'NONE',  ( 21.05281448260627641, 61.94770618465719991, -221.8088539820179506 ) ) ;
#122695=ORIENTED_EDGE ( 'NONE', *, *, #202284, .F. ) ;
#122699=AXIS2_PLACEMENT_3D ( 'NONE', #232258, #52288, #108440 ) ;
#122702=EDGE_CURVE ( 'NONE', #230038, #251252, #168157, .T. ) ;
#122716=CARTESIAN_POINT ( 'NONE',  ( 23.24999999999999289, 66.34920340998563404, -213.7018660128499334 ) ) ;
#122763=DIRECTION ( 'NONE',  ( 1.000000000000000000, 0.000000000000000000, 0.000000000000000000 ) ) ;
#122772=EDGE_CURVE ( 'NONE', #194221, #189304, #255288, .T. ) ;
#122776=CYLINDRICAL_SURFACE ( 'NONE', #196410, 0.09999999999999939493 ) ;
#122792=VERTEX_POINT ( 'NONE', #252764 ) ;
#122825=CYLINDRICAL_SURFACE ( 'NONE', #61658, 3.999999999999996447 ) ;
#122849=CARTESIAN_POINT ( 'NONE',  ( -21.05000000000000782, 65.51923798433685420, -242.1677427744925808 ) ) ;
#122854=CARTESIAN_POINT ( 'NONE',  ( 20.04142135391667168, 62.35689476345314119, -208.9382773759953409 ) ) ;
#122857=DIRECTION ( 'NONE',  ( 0.000000000000000000, 0.1290532225515364506, 0.9916376685811525427 ) ) ;
#122872=FACE_OUTER_BOUND ( 'NONE', #46977, .T. ) ;
#122917=CARTESIAN_POINT ( 'NONE',  ( 21.14999999999999858, 78.47509609352879068, -238.9045489380306435 ) ) ;
#122925=AXIS2_PLACEMENT_3D ( 'NONE', #101334, #23166, #162660 ) ;
#122935=FACE_OUTER_BOUND ( 'NONE', #33699, .T. ) ;
#122947=ORIENTED_EDGE ( 'NONE', *, *, #205642, .T. ) ;
#122955=CIRCLE ( 'NONE', #10531, 0.1000000000000088318 ) ;
#122974=ORIENTED_EDGE ( 'NONE', *, *, #215929, .F. ) ;
#122986=VECTOR ( 'NONE', #72677, 1000.000000000000000 ) ;
#123026=CARTESIAN_POINT ( 'NONE',  ( 21.05000000000000071, 65.49889199258218753, -241.8691648588935266 ) ) ;
#123051=EDGE_CURVE ( 'NONE', #70381, #177774, #176489, .T. ) ;
#123052=VECTOR ( 'NONE', #148223, 1000.000000000000000 ) ;
#123057=ORIENTED_EDGE ( 'NONE', *, *, #84595, .T. ) ;
#123070=EDGE_LOOP ( 'NONE', ( #142337, #196325, #102256, #226280 ) ) ;
#123074=DIRECTION ( 'NONE',  ( -1.000000000000000000, -0.000000000000000000, 0.000000000000000000 ) ) ;
#123082=CARTESIAN_POINT ( 'NONE',  ( -18.50000000000000000, 59.16775194334852728, -221.0793150863668473 ) ) ;
#123100=FACE_OUTER_BOUND ( 'NONE', #95271, .T. ) ;
#123128=CARTESIAN_POINT ( 'NONE',  ( -23.15000000000000213, 76.00000000001126921, -203.5231074845248997 ) ) ;
#123132=CIRCLE ( 'NONE', #131490, 0.1000000000000124678 ) ;
#123140=DIRECTION ( 'NONE',  ( -1.000000000000000000, -0.000000000000000000, 0.000000000000000000 ) ) ;
#123153=VERTEX_POINT ( 'NONE', #117770 ) ;
#123166=VERTEX_POINT ( 'NONE', #215577 ) ;
#123199=DIRECTION ( 'NONE',  ( 0.000000000000000000, -0.2617529984165052337, -0.9651348961777151958 ) ) ;
#123232=ORIENTED_EDGE ( 'NONE', *, *, #208856, .T. ) ;
#123245=ORIENTED_EDGE ( 'NONE', *, *, #21696, .F. ) ;
#123249=( BOUNDED_SURFACE ( )  B_SPLINE_SURFACE ( 3, 2, ( 
 ( #197045, #237477, #240049 ),
 ( #198341, #61401, #185203 ),
 ( #66545, #224324, #125233 ),
 ( #26141, #206050, #105635 ) ),
 .UNSPECIFIED., .F., .F., .F. ) 
 B_SPLINE_SURFACE_WITH_KNOTS ( ( 4, 4 ),
 ( 3, 3 ),
 ( -1.341700188450811737E-18, 0.0003124336117481280473 ),
 ( 0.000000000000000000, 1.000000000000000000 ),
 .UNSPECIFIED. ) 
 GEOMETRIC_REPRESENTATION_ITEM ( )  RATIONAL_B_SPLINE_SURFACE ( (
 ( 1.000000000000000000, 0.7040654476016059427, 1.000000000000000000),
 ( 1.000000000000000000, 0.7039193538780386117, 1.000000000000000000),
 ( 1.000000000000000000, 0.7089171279146311289, 1.000000000000000000),
 ( 1.000000000000000000, 0.7071067811865457964, 1.000000000000000000) ) ) 
 REPRESENTATION_ITEM ( '' )  SURFACE ( )  );
#123277=LINE ( 'NONE', #67153, #88028 ) ;
#123287=FACE_BOUND ( 'NONE', #179687, .T. ) ;
#123309=AXIS2_PLACEMENT_3D ( 'NONE', #225303, #187511, #71414 ) ;
#123361=ORIENTED_EDGE ( 'NONE', *, *, #11399, .F. ) ;
#123374=ORIENTED_EDGE ( 'NONE', *, *, #53564, .T. ) ;
#123391=CARTESIAN_POINT ( 'NONE',  ( -18.59999999999999787, 72.02722222756958104, -225.1832529173024398 ) ) ;
#123421=CARTESIAN_POINT ( 'NONE',  ( 18.46082813848008897, 78.23583199935188759, -231.4993683512706752 ) ) ;
#123430=CYLINDRICAL_SURFACE ( 'NONE', #235625, 0.1000000000000124678 ) ;
#123431=CARTESIAN_POINT ( 'NONE',  ( 23.14999999999999503, 61.57587952878035509, -212.2000740415318774 ) ) ;
#123434=AXIS2_PLACEMENT_3D ( 'NONE', #75015, #235331, #256120 ) ;
#123438=ORIENTED_EDGE ( 'NONE', *, *, #42364, .F. ) ;
#123443=VECTOR ( 'NONE', #113550, 1000.000000000000000 ) ;
#123450=CARTESIAN_POINT ( 'NONE',  ( 21.05000000000000071, 65.17014820068582992, -222.4427298839669618 ) ) ;
#123455=DIRECTION ( 'NONE',  ( 1.000000000000000000, 0.000000000000000000, 0.000000000000000000 ) ) ;
#123507=DIRECTION ( 'NONE',  ( -3.265361837132813093E-16, -0.9651348961777146407, 0.2617529984165072321 ) ) ;
#123508=CARTESIAN_POINT ( 'NONE',  ( 18.43630871534871574, 87.08575402747911198, -199.6284159481674010 ) ) ;
#123556=EDGE_LOOP ( 'NONE', ( #102857, #159773, #114415, #249608, #73237, #64466, #8846, #20302, #54652, #115939, #218832, #171024 ) ) ;
#123570=EDGE_CURVE ( 'NONE', #184831, #54640, #174937, .T. ) ;
#123572=CARTESIAN_POINT ( 'NONE',  ( 22.47071067811865319, 59.75442326890422606, -233.9300113800879046 ) ) ;
#123581=DIRECTION ( 'NONE',  ( 0.000000000000000000, -0.9651348961777157509, 0.2617529984165027912 ) ) ;
#123621=EDGE_LOOP ( 'NONE', ( #220813, #79238, #36089, #199616 ) ) ;
#123652=CARTESIAN_POINT ( 'NONE',  ( 18.59999999999999432, 62.13039908340535078, -248.0610840288475174 ) ) ;
#123665=DIRECTION ( 'NONE',  ( -1.000000000000000000, 0.000000000000000000, 0.000000000000000000 ) ) ;
#123676=DIRECTION ( 'NONE',  ( 1.000000000000000000, 0.000000000000000000, -0.000000000000000000 ) ) ;
#123760=CARTESIAN_POINT ( 'NONE',  ( 23.14999999999999503, 59.16775194334852017, -221.0793150863668473 ) ) ;
#123796=DIRECTION ( 'NONE',  ( 0.000000000000000000, -0.9609271840673806464, 0.2768012769485257429 ) ) ;
#123814=VERTEX_POINT ( 'NONE', #247688 ) ;
#123820=CARTESIAN_POINT ( 'NONE',  ( 20.94999999999999929, 78.50726470275242264, -228.6618886302502176 ) ) ;
#123828=CARTESIAN_POINT ( 'NONE',  ( -20.94999999999999929, 86.52890073500824997, -209.5906233940697234 ) ) ;
#123850=ORIENTED_EDGE ( 'NONE', *, *, #244045, .T. ) ;
#123852=DIRECTION ( 'NONE',  ( 0.000000000000000000, 0.2617529984164955192, 0.9651348961777177493 ) ) ;
#123891=AXIS2_PLACEMENT_3D ( 'NONE', #214853, #77901, #75377 ) ;
#123894=EDGE_CURVE ( 'NONE', #26209, #227798, #173340, .T. ) ;
#123906=ORIENTED_EDGE ( 'NONE', *, *, #31082, .T. ) ;
#123923=EDGE_LOOP ( 'NONE', ( #202467, #183842, #138248 ) ) ;
#123925=CARTESIAN_POINT ( 'NONE',  ( -18.50000000000000000, 70.22659352830977753, -197.9852579278363578 ) ) ;
#123993=DIRECTION ( 'NONE',  ( 0.000000000000000000, -0.9691069652679039637, 0.2466408114429434750 ) ) ;
#124012=ORIENTED_EDGE ( 'NONE', *, *, #255549, .F. ) ;
#124013=CARTESIAN_POINT ( 'NONE',  ( -21.55000000000000071, 65.89281126173843006, -213.4744760240239145 ) ) ;
#124052=FACE_OUTER_BOUND ( 'NONE', #206788, .T. ) ;
#124095=CARTESIAN_POINT ( 'NONE',  ( -21.45000000000000284, 62.99793053463489656, -222.0144804547670390 ) ) ;
#124124=VERTEX_POINT ( 'NONE', #208264 ) ;
#124154=CARTESIAN_POINT ( 'NONE',  ( 21.14999999999999858, 64.14229051353817113, -222.2212283990554624 ) ) ;
#124185=CARTESIAN_POINT ( 'NONE',  ( -21.05000000000000071, 79.03091752131670944, -235.9469187808398942 ) ) ;
#124187=ORIENTED_EDGE ( 'NONE', *, *, #148172, .T. ) ;
#124188=VECTOR ( 'NONE', #162685, 1000.000000000000000 ) ;
#124195=CARTESIAN_POINT ( 'NONE',  ( -21.64999999999999858, 65.79629777212066699, -213.4483007241822747 ) ) ;
#124198=LINE ( 'NONE', #203722, #18224 ) ;
#124217=AXIS2_PLACEMENT_3D ( 'NONE', #186532, #223071, #86100 ) ;
#124221=EDGE_LOOP ( 'NONE', ( #186513, #96128, #75033, #41497, #52567, #118823 ) ) ;
#124222=CARTESIAN_POINT ( 'NONE',  ( -21.13435531349827201, 60.96395774854146765, -234.1553755472027945 ) ) ;
#124228=ORIENTED_EDGE ( 'NONE', *, *, #37698, .T. ) ;
#124261=DIRECTION ( 'NONE',  ( 1.000000000000000000, 0.000000000000000000, 0.000000000000000000 ) ) ;
#124277=CIRCLE ( 'NONE', #186636, 0.1000000000000124678 ) ;
#124284=EDGE_CURVE ( 'NONE', #148169, #42365, #72822, .T. ) ;
#124292=CARTESIAN_POINT ( 'NONE',  ( 20.94999999999999929, 58.88775506787933978, -225.6504858384382999 ) ) ;
#124296=DIRECTION ( 'NONE',  ( 0.000000000000000000, 0.4558084472153119959, -0.8900778951570285091 ) ) ;
#124317=ORIENTED_EDGE ( 'NONE', *, *, #195618, .F. ) ;
#124321=ORIENTED_EDGE ( 'NONE', *, *, #209770, .F. ) ;
#124394=CARTESIAN_POINT ( 'NONE',  ( 23.14999999999999858, 79.76402609510435582, -204.5439441783492498 ) ) ;
#124428=CARTESIAN_POINT ( 'NONE',  ( -20.64999999999999858, 67.23127455305841238, -235.8551265064783991 ) ) ;
#124433=EDGE_CURVE ( 'NONE', #210786, #174802, #126953, .T. ) ;
#124489=ORIENTED_EDGE ( 'NONE', *, *, #96295, .T. ) ;
#124519=CARTESIAN_POINT ( 'NONE',  ( -18.47690164073606311, 86.88895830507721030, -199.5328223242795787 ) ) ;
#124539=EDGE_CURVE ( 'NONE', #88490, #116117, #10625, .T. ) ;
#124546=CIRCLE ( 'NONE', #70417, 0.09999999999999939493 ) ;
#124588=ORIENTED_EDGE ( 'NONE', *, *, #219712, .T. ) ;
#124609=AXIS2_PLACEMENT_3D ( 'NONE', #4809, #126052, #123507 ) ;
#124663=PRESENTATION_STYLE_ASSIGNMENT (( #167654 ) ) ;
#124714=ORIENTED_EDGE ( 'NONE', *, *, #150107, .F. ) ;
#124765=ORIENTED_EDGE ( 'NONE', *, *, #214154, .F. ) ;
#124774=EDGE_CURVE ( 'NONE', #136435, #221590, #202153, .T. ) ;
#124791=FACE_OUTER_BOUND ( 'NONE', #79914, .T. ) ;
#124804=VERTEX_POINT ( 'NONE', #125218 ) ;
#124873=ADVANCED_FACE ( 'NONE', ( #224308 ), #204732, .F. ) ;
#124874=ORIENTED_EDGE ( 'NONE', *, *, #37636, .F. ) ;
#124876=CARTESIAN_POINT ( 'NONE',  ( -20.94999999999999929, 76.00000000001126921, -203.5231074845248997 ) ) ;
#124878=FACE_OUTER_BOUND ( 'NONE', #176989, .T. ) ;
#124934=DIRECTION ( 'NONE',  ( 0.000000000000000000, 0.2617529984165071766, 0.9651348961777145297 ) ) ;
#124943=DIRECTION ( 'NONE',  ( 0.000000000000000000, 0.2617529984165032908, 0.9651348961777156399 ) ) ;
#124954=DIRECTION ( 'NONE',  ( 0.000000000000000000, 0.2617529984165152257, 0.9651348961777124202 ) ) ;
#124955=FACE_OUTER_BOUND ( 'NONE', #230078, .T. ) ;
#124970=AXIS2_PLACEMENT_3D ( 'NONE', #22657, #1767, #222082 ) ;
#125006=ADVANCED_FACE ( 'NONE', ( #72978 ), #232037, .F. ) ;
#125013=DIRECTION ( 'NONE',  ( -0.000000000000000000, -0.1290532225515364506, -0.9916376685811525427 ) ) ;
#125017=AXIS2_PLACEMENT_3D ( 'NONE', #183021, #102147, #200007 ) ;
#125038=CARTESIAN_POINT ( 'NONE',  ( -23.25000000000000000, 66.23941198528750363, -222.8935984851895853 ) ) ;
#125041=DIRECTION ( 'NONE',  ( 0.000000000000000000, 0.2617529984165030132, 0.9651348961777158619 ) ) ;
#125044=EDGE_CURVE ( 'NONE', #252329, #198528, #134476, .T. ) ;
#125046=ORIENTED_EDGE ( 'NONE', *, *, #199981, .F. ) ;
#125079=CIRCLE ( 'NONE', #254227, 0.5000000000000014433 ) ;
#125098=AXIS2_PLACEMENT_3D ( 'NONE', #25270, #40995, #60505 ) ;
#125180=EDGE_LOOP ( 'NONE', ( #190580, #196727, #203591, #137048, #192215, #107383, #129949 ) ) ;
#125182=VERTEX_POINT ( 'NONE', #114182 ) ;
#125196=ORIENTED_EDGE ( 'NONE', *, *, #237142, .T. ) ;
#125218=CARTESIAN_POINT ( 'NONE',  ( 21.87500000000000355, 61.05385884576948996, -221.3836188041226762 ) ) ;
#125232=ORIENTED_EDGE ( 'NONE', *, *, #127527, .T. ) ;
#125233=CARTESIAN_POINT ( 'NONE',  ( -22.59999970745345976, 64.16457265427982293, -247.1984059110171188 ) ) ;
#125251=AXIS2_PLACEMENT_3D ( 'NONE', #4519, #219715, #103605 ) ;
#125267=ADVANCED_FACE ( 'NONE', ( #253680 ), #110330, .T. ) ;
#125268=CARTESIAN_POINT ( 'NONE',  ( -21.05000000000000071, 79.26035508877831148, -236.0091442494974956 ) ) ;
#125279=AXIS2_PLACEMENT_3D ( 'NONE', #210940, #250065, #191407 ) ;
#125282=ORIENTED_EDGE ( 'NONE', *, *, #44807, .F. ) ;
#125291=EDGE_CURVE ( 'NONE', #94242, #7533, #118960, .T. ) ;
#125323=CIRCLE ( 'NONE', #167047, 0.09999999999999868716 ) ;
#125327=VECTOR ( 'NONE', #194545, 1000.000000000000000 ) ;
#125329=CARTESIAN_POINT ( 'NONE',  ( 21.22070241538126467, 65.44227650827568254, -242.0736050779767936 ) ) ;
#125391=DIRECTION ( 'NONE',  ( 0.000000000000000000, 0.2617529984165034573, 0.9651348961777156399 ) ) ;
#125399=CARTESIAN_POINT ( 'NONE',  ( -20.85000000000000142, 87.34033503009941057, -206.5987052159188124 ) ) ;
#125408=AXIS2_PLACEMENT_3D ( 'NONE', #27909, #125686, #205209 ) ;
#125439=EDGE_CURVE ( 'NONE', #255695, #177651, #94174, .T. ) ;
#125445=DIRECTION ( 'NONE',  ( 0.000000000000000000, 0.2617529984164506107, 0.9651348961777299618 ) ) ;
#125449=ADVANCED_FACE ( 'NONE', ( #43266 ), #206187, .T. ) ;
#125492=CARTESIAN_POINT ( 'NONE',  ( -21.11825140030087766, 61.00870122228366910, -234.1749742158648360 ) ) ;
#125496=EDGE_LOOP ( 'NONE', ( #230687, #40793, #243920, #113126 ) ) ;
#125524=ORIENTED_EDGE ( 'NONE', *, *, #76817, .F. ) ;
#125536=ORIENTED_EDGE ( 'NONE', *, *, #205891, .T. ) ;
#125550=ORIENTED_EDGE ( 'NONE', *, *, #106231, .F. ) ;
#125568=DIRECTION ( 'NONE',  ( 0.000000000000000000, 0.2617529984165180013, 0.9651348961777117541 ) ) ;
#125569=VERTEX_POINT ( 'NONE', #32729 ) ;
#125587=CIRCLE ( 'NONE', #121366, 0.1000000000000124678 ) ;
#125595=ORIENTED_EDGE ( 'NONE', *, *, #1133, .F. ) ;
#125610=CIRCLE ( 'NONE', #142178, 12.87500000000000178 ) ;
#125613=CARTESIAN_POINT ( 'NONE',  ( 18.39999999999999858, 87.01908966642815813, -199.5693496768551825 ) ) ;
#125643=CYLINDRICAL_SURFACE ( 'NONE', #35594, 0.1000000000000124678 ) ;
#125648=TOROIDAL_SURFACE ( 'NONE', #200679, 11.70000000000000639, 0.1000000000000000056 ) ;
#125651=DIRECTION ( 'NONE',  ( 1.000000000000000000, 0.000000000000000000, -0.000000000000000000 ) ) ;
#125683=VERTEX_POINT ( 'NONE', #160367 ) ;
#125684=LINE ( 'NONE', #207827, #242752 ) ;
#125686=DIRECTION ( 'NONE',  ( -1.000000000000000000, -0.000000000000000000, 0.000000000000000000 ) ) ;
#125693=EDGE_CURVE ( 'NONE', #150591, #191015, #200747, .T. ) ;
#125694=ORIENTED_EDGE ( 'NONE', *, *, #209710, .T. ) ;
#125714=CARTESIAN_POINT ( 'NONE',  ( 21.05000000000000071, 60.94483358488582070, -234.0465764481390636 ) ) ;
#125737=DIRECTION ( 'NONE',  ( -0.000000000000000000, -0.3848449534832868446, -0.9229812358755982160 ) ) ;
#125772=ORIENTED_EDGE ( 'NONE', *, *, #18641, .T. ) ;
#125776=DIRECTION ( 'NONE',  ( 1.000000000000000000, -2.849773892568378313E-16, 7.728835255496647986E-17 ) ) ;
#125848=CARTESIAN_POINT ( 'NONE',  ( 20.94999999999999929, 70.08587962373171365, -198.1273832143211848 ) ) ;
#125860=ORIENTED_EDGE ( 'NONE', *, *, #105742, .T. ) ;
#125871=DIRECTION ( 'NONE',  ( 0.000000000000000000, -0.9628525332200033038, 0.2700277750006890298 ) ) ;
#125877=ORIENTED_EDGE ( 'NONE', *, *, #114828, .F. ) ;
#125886=DIRECTION ( 'NONE',  ( 1.000000000000000000, -2.849773892568378313E-16, 7.728835255496647986E-17 ) ) ;
#125899=DIRECTION ( 'NONE',  ( 0.000000000000000000, 0.2617529984165152257, 0.9651348961777124202 ) ) ;
#125907=ORIENTED_EDGE ( 'NONE', *, *, #101163, .F. ) ;
#125946=VECTOR ( 'NONE', #62189, 1000.000000000000114 ) ;
#125975=EDGE_CURVE ( 'NONE', #8746, #141218, #95854, .T. ) ;
#125976=CARTESIAN_POINT ( 'NONE',  ( 18.49999999999999645, 79.19526988099229925, -196.1889237952725296 ) ) ;
#125978=AXIS2_PLACEMENT_3D ( 'NONE', #255074, #179468, #235557 ) ;
#125981=DIRECTION ( 'NONE',  ( 0.000000000000000000, -0.9651348961777155289, 0.2617529984165036794 ) ) ;
#126023=FACE_OUTER_BOUND ( 'NONE', #90853, .T. ) ;
#126024=AXIS2_PLACEMENT_3D ( 'NONE', #227361, #248220, #13464 ) ;
#126034=ORIENTED_EDGE ( 'NONE', *, *, #193809, .F. ) ;
#126052=DIRECTION ( 'NONE',  ( 1.000000000000000000, -3.151514657663852580E-16, 8.547182517843351137E-17 ) ) ;
#126053=CARTESIAN_POINT ( 'NONE',  ( 18.59999996954842771, 86.99283344320274125, -199.3727709741243075 ) ) ;
#126075=EDGE_CURVE ( 'NONE', #207794, #101319, #3173, .T. ) ;
#126077=VERTEX_POINT ( 'NONE', #140116 ) ;
#126089=CARTESIAN_POINT ( 'NONE',  ( 23.14999999999999503, 61.57587952878035509, -212.2000740415318774 ) ) ;
#126096=DIRECTION ( 'NONE',  ( -0.000000000000000000, -0.7049548389605067023, 0.7092521942342977503 ) ) ;
#126103=CARTESIAN_POINT ( 'NONE',  ( 19.75857864376268935, 62.46583972339646351, -208.9186153945276487 ) ) ;
#126118=ORIENTED_EDGE ( 'NONE', *, *, #251635, .F. ) ;
#126128=ORIENTED_EDGE ( 'NONE', *, *, #120818, .F. ) ;
#126150=ORIENTED_EDGE ( 'NONE', *, *, #243428, .F. ) ;
#126190=ORIENTED_EDGE ( 'NONE', *, *, #223347, .T. ) ;
#126252=FACE_OUTER_BOUND ( 'NONE', #168614, .T. ) ;
#126254=AXIS2_PLACEMENT_3D ( 'NONE', #189661, #11022, #249645 ) ;
#126262=EDGE_LOOP ( 'NONE', ( #116477, #2295, #236878, #88321 ) ) ;
#126263=DIRECTION ( 'NONE',  ( -1.000000000000000000, -0.000000000000000000, -0.000000000000000000 ) ) ;
#126273=DIRECTION ( 'NONE',  ( -2.557131231893036492E-16, -0.7049548389605068133, 0.7092521942342976393 ) ) ;
#126288=CARTESIAN_POINT ( 'NONE',  ( 21.09546886439546398, 61.86536912340749694, -221.7206923045749249 ) ) ;
#126296=DIRECTION ( 'NONE',  ( 1.000000000000000000, 0.000000000000000000, 0.000000000000000000 ) ) ;
#126361=ADVANCED_FACE ( 'NONE', ( #142396 ), #26577, .T. ) ;
#126424=AXIS2_PLACEMENT_3D ( 'NONE', #18348, #178749, #135714 ) ;
#126428=VERTEX_POINT ( 'NONE', #126694 ) ;
#126485=CARTESIAN_POINT ( 'NONE',  ( -18.58744394320964943, 87.01875307878489707, -199.4421687346215037 ) ) ;
#126486=EDGE_LOOP ( 'NONE', ( #176701, #122695, #14342, #16195 ) ) ;
#126509=CIRCLE ( 'NONE', #151673, 0.1000000000000124678 ) ;
#126511=EDGE_LOOP ( 'NONE', ( #80678, #107450, #104847 ) ) ;
#126532=ORIENTED_EDGE ( 'NONE', *, *, #13491, .T. ) ;
#126541=DIRECTION ( 'NONE',  ( 0.000000000000000000, 0.2534589355812664757, 0.9673461469267405910 ) ) ;
#126590=DIRECTION ( 'NONE',  ( 1.000000000000000000, 0.000000000000000000, 0.000000000000000000 ) ) ;
#126594=CARTESIAN_POINT ( 'NONE',  ( -20.64999999999999858, 68.76258920191057200, -222.5680764032308048 ) ) ;
#126606=EDGE_CURVE ( 'NONE', #228033, #236044, #194725, .T. ) ;
#126633=DIRECTION ( 'NONE',  ( -7.304098846218135653E-16, 0.9651348961777157509, -0.2617529984165031243 ) ) ;
#126674=AXIS2_PLACEMENT_3D ( 'NONE', #177085, #77940, #58360 ) ;
#126694=CARTESIAN_POINT ( 'NONE',  ( 20.95512820512820440, 61.84489010471549619, -221.8053782964821039 ) ) ;
#126696=LINE ( 'NONE', #48430, #128382 ) ;
#126735=DIRECTION ( 'NONE',  ( 0.000000000000000000, -0.9651348961777161950, 0.2617529984165014589 ) ) ;
#126747=DIRECTION ( 'NONE',  ( 0.000000000000000000, 0.2617529984164856383, 0.9651348961777204138 ) ) ;
#126756=ORIENTED_EDGE ( 'NONE', *, *, #249182, .T. ) ;
#126838=CARTESIAN_POINT ( 'NONE',  ( -22.39999999999999858, 55.96127771274636586, -232.9022175645438892 ) ) ;
#126869=ORIENTED_EDGE ( 'NONE', *, *, #236653, .T. ) ;
#126885=VECTOR ( 'NONE', #137230, 1000.000000000000000 ) ;
#126904=ORIENTED_EDGE ( 'NONE', *, *, #179694, .T. ) ;
#126921=DIRECTION ( 'NONE',  ( -1.000000000000000000, 1.772924042024179204E-16, -4.808324575169892332E-17 ) ) ;
#126933=DIRECTION ( 'NONE',  ( 0.000000000000000000, -0.2617529984165034018, -0.9651348961777157509 ) ) ;
#126936=ORIENTED_EDGE ( 'NONE', *, *, #143257, .T. ) ;
#126937=CARTESIAN_POINT ( 'NONE',  ( 21.14999999999999858, 64.18196446391819165, -247.0985338183330668 ) ) ;
#126953=CIRCLE ( 'NONE', #177051, 0.09999999999998951394 ) ;
#126966=ADVANCED_FACE ( 'NONE', ( #111971 ), #212358, .T. ) ;
#126969=DIRECTION ( 'NONE',  ( -0.000000000000000000, 0.8900778951570254005, 0.4558084472153182132 ) ) ;
#126978=CARTESIAN_POINT ( 'NONE',  ( -18.49999999999997868, 78.12133356376092763, -231.3112718935514920 ) ) ;
#126979=EDGE_CURVE ( 'NONE', #11153, #116241, #31035, .T. ) ;
#126991=AXIS2_PLACEMENT_3D ( 'NONE', #21831, #257811, #220024 ) ;
#127013=CARTESIAN_POINT ( 'NONE',  ( 21.14999999999999858, 56.01362831242965967, -232.7091905853083347 ) ) ;
#127034=ADVANCED_FACE ( 'NONE', ( #231920 ), #10306, .F. ) ;
#127035=AXIS2_PLACEMENT_3D ( 'NONE', #199244, #165235, #163962 ) ;
#127098=CARTESIAN_POINT ( 'NONE',  ( 21.05000000000000071, 65.61575147395463148, -242.1939180743342774 ) ) ;
#127103=ADVANCED_FACE ( 'NONE', ( #79218 ), #199196, .T. ) ;
#127106=CARTESIAN_POINT ( 'NONE',  ( -20.54999999999999716, 68.63171270270233038, -223.0506438513196770 ) ) ;
#127108=DIRECTION ( 'NONE',  ( 0.000000000000000000, 0.2617529984165031243, 0.9651348961777156399 ) ) ;
#127136=CIRCLE ( 'NONE', #193779, 0.09999999999999939493 ) ;
#127140=ADVANCED_FACE ( 'NONE', ( #144318 ), #208010, .T. ) ;
#127184=AXIS2_PLACEMENT_3D ( 'NONE', #245481, #182943, #186795 ) ;
#127233=FACE_OUTER_BOUND ( 'NONE', #225609, .T. ) ;
#127244=ORIENTED_EDGE ( 'NONE', *, *, #68268, .F. ) ;
#127358=CARTESIAN_POINT ( 'NONE',  ( 18.50000000000000000, 86.87893363400692692, -199.4025658100844680 ) ) ;
#127381=FACE_OUTER_BOUND ( 'NONE', #183433, .T. ) ;
#127461=CIRCLE ( 'NONE', #15055, 0.1000000000000016015 ) ;
#127515=EDGE_LOOP ( 'NONE', ( #60071, #13420, #38255, #149168 ) ) ;
#127524=EDGE_LOOP ( 'NONE', ( #131869, #101834, #183663, #150233 ) ) ;
#127527=EDGE_CURVE ( 'NONE', #249371, #66847, #169749, .T. ) ;
#127570=FACE_OUTER_BOUND ( 'NONE', #245638, .T. ) ;
#127596=DIRECTION ( 'NONE',  ( 0.000000000000000000, 0.2617529984164915779, 0.9651348961777187485 ) ) ;
#127602=DIRECTION ( 'NONE',  ( -1.000000000000000000, -0.000000000000000000, 0.000000000000000000 ) ) ;
#127642=LINE ( 'NONE', #87203, #95350 ) ;
#127652=CIRCLE ( 'NONE', #111076, 0.1000000000000066530 ) ;
#127663=DIRECTION ( 'NONE',  ( -0.000000000000000000, -0.2617529984165031243, -0.9651348961777157509 ) ) ;
#127666=DIRECTION ( 'NONE',  ( 0.000000000000000000, -0.2617529984164506107, -0.9651348961777299618 ) ) ;
#127779=DIRECTION ( 'NONE',  ( -1.000000000000000000, -0.000000000000000000, 0.000000000000000000 ) ) ;
#127780=CARTESIAN_POINT ( 'NONE',  ( 23.14999999999999503, 62.92003201576280702, -207.2439188921395612 ) ) ;
#127787=CARTESIAN_POINT ( 'NONE',  ( -23.15000000000000213, 82.09643798151613225, -215.4278993322501208 ) ) ;
#127808=ORIENTED_EDGE ( 'NONE', *, *, #89703, .F. ) ;
#127822=ORIENTED_EDGE ( 'NONE', *, *, #66796, .F. ) ;
#127829=EDGE_LOOP ( 'NONE', ( #75819, #217827, #140312 ) ) ;
#127852=ORIENTED_EDGE ( 'NONE', *, *, #66796, .T. ) ;
#127856=ADVANCED_FACE ( 'NONE', ( #166873 ), #129002, .F. ) ;
#127876=TOROIDAL_SURFACE ( 'NONE', #86139, 12.97499999999999609, 0.1000000000000000056 ) ;
#127901=AXIS2_PLACEMENT_3D ( 'NONE', #71822, #131775, #210050 ) ;
#127905=DIRECTION ( 'NONE',  ( 1.000000000000000000, 0.000000000000000000, 0.000000000000000000 ) ) ;
#127930=EDGE_CURVE ( 'NONE', #114917, #15410, #198735, .T. ) ;
#127969=DIRECTION ( 'NONE',  ( 0.000000000000000000, -0.9651348961777157509, 0.2617529984165031243 ) ) ;
#127971=CARTESIAN_POINT ( 'NONE',  ( -20.94999999999999929, 62.98048128140160173, -207.0210305352945852 ) ) ;
#127978=TOROIDAL_SURFACE ( 'NONE', #48849, 0.2000000000000000111, 0.1000000000000000056 ) ;
#128036=VERTEX_POINT ( 'NONE', #119709 ) ;
#128048=VERTEX_POINT ( 'NONE', #161408 ) ;
#128050=ORIENTED_EDGE ( 'NONE', *, *, #164073, .T. ) ;
#128067=ORIENTED_EDGE ( 'NONE', *, *, #94623, .T. ) ;
#128079=DIRECTION ( 'NONE',  ( 0.000000000000000000, 0.2617529984165045120, 0.9651348961777153068 ) ) ;
#128095=DIRECTION ( 'NONE',  ( -1.000000000000000000, 0.000000000000000000, 0.000000000000000000 ) ) ;
#128106=AXIS2_PLACEMENT_3D ( 'NONE', #108956, #222473, #43870 ) ;
#128120=EDGE_CURVE ( 'NONE', #70810, #29169, #215655, .T. ) ;
#128126=EDGE_CURVE ( 'NONE', #145620, #154671, #53183, .T. ) ;
#128168=CARTESIAN_POINT ( 'NONE',  ( -18.43569575749026868, 78.24390740893983320, -231.6169762517609456 ) ) ;
#128198=EDGE_CURVE ( 'NONE', #242024, #255081, #136551, .T. ) ;
#128208=FACE_OUTER_BOUND ( 'NONE', #17249, .T. ) ;
#128238=CIRCLE ( 'NONE', #161577, 11.79999999999999361 ) ;
#128256=DIRECTION ( 'NONE',  ( 0.000000000000000000, -0.9651348961777161950, 0.2617529984165014589 ) ) ;
#128260=CARTESIAN_POINT ( 'NONE',  ( -21.05000000000000071, 68.48451787451661232, -224.2224406095231757 ) ) ;
#128268=ORIENTED_EDGE ( 'NONE', *, *, #226798, .T. ) ;
#128300=PLANE ( 'NONE',  #157030 ) ;
#128303=CARTESIAN_POINT ( 'NONE',  ( 21.05000000000000071, 60.96493190257000805, -234.1404541814610241 ) ) ;
#128336=ORIENTED_EDGE ( 'NONE', *, *, #13632, .T. ) ;
#128382=VECTOR ( 'NONE', #107122, 1000.000000000000000 ) ;
#128400=AXIS2_PLACEMENT_3D ( 'NONE', #116962, #196484, #17843 ) ;
#128409=DIRECTION ( 'NONE',  ( -2.812466655313719426E-14, -0.3896596508880124654, -0.9209589331071350582 ) ) ;
#128466=CARTESIAN_POINT ( 'NONE',  ( 23.14999999999999858, 76.00000000001126921, -203.5231074845248997 ) ) ;
#128476=CARTESIAN_POINT ( 'NONE',  ( -20.85000000000000142, 64.65966496992309942, -200.4475097531309586 ) ) ;
#128496=CIRCLE ( 'NONE', #41035, 0.09999999999999939493 ) ;
#128509=( NAMED_UNIT ( * ) SI_UNIT ( $, .STERADIAN. ) SOLID_ANGLE_UNIT ( ) );
#128518=ORIENTED_EDGE ( 'NONE', *, *, #172480, .T. ) ;
#128521=DIRECTION ( 'NONE',  ( 1.000000000000000000, 0.000000000000000000, 0.000000000000000000 ) ) ;
#128525=LINE ( 'NONE', #192350, #253863 ) ;
#128533=ORIENTED_EDGE ( 'NONE', *, *, #177512, .T. ) ;
#128580=DIRECTION ( 'NONE',  ( -1.000000000000000000, -0.000000000000000000, -0.000000000000000000 ) ) ;
#128581=LINE ( 'NONE', #165144, #5163 ) ;
#128582=EDGE_CURVE ( 'NONE', #59315, #248135, #115911, .T. ) ;
#128621=ORIENTED_EDGE ( 'NONE', *, *, #56374, .T. ) ;
#128624=CIRCLE ( 'NONE', #232876, 0.09999999999999875655 ) ;
#128656=CARTESIAN_POINT ( 'NONE',  ( -23.25000000000000000, 75.39949836213489220, -250.2448839681187849 ) ) ;
#128662=CIRCLE ( 'NONE', #253525, 0.09999999999999939493 ) ;
#128703=VERTEX_POINT ( 'NONE', #94388 ) ;
#128722=ORIENTED_EDGE ( 'NONE', *, *, #149145, .T. ) ;
#128734=AXIS2_PLACEMENT_3D ( 'NONE', #76614, #216119, #94888 ) ;
#128779=ORIENTED_EDGE ( 'NONE', *, *, #92358, .T. ) ;
#128802=CARTESIAN_POINT ( 'NONE',  ( 18.49999999999998934, 48.66983769917126779, -228.4584249288054423 ) ) ;
#128808=ADVANCED_FACE ( 'NONE', ( #232650 ), #194812, .F. ) ;
#128827=CARTESIAN_POINT ( 'NONE',  ( -22.57320508075687115, 55.98745301258801987, -232.8057040749260977 ) ) ;
#128835=DIRECTION ( 'NONE',  ( 1.000000000000000000, 0.000000000000000000, 0.000000000000000000 ) ) ;
#128873=ORIENTED_EDGE ( 'NONE', *, *, #137025, .T. ) ;
#128905=VERTEX_POINT ( 'NONE', #197341 ) ;
#128913=EDGE_CURVE ( 'NONE', #148934, #194645, #211772, .T. ) ;
#128922=AXIS2_PLACEMENT_3D ( 'NONE', #5733, #85262, #244358 ) ;
#128933=EDGE_CURVE ( 'NONE', #204719, #49363, #45347, .T. ) ;
#128942=ORIENTED_EDGE ( 'NONE', *, *, #43470, .F. ) ;
#128944=ADVANCED_FACE ( 'NONE', ( #10715 ), #245483, .T. ) ;
#128967=VERTEX_POINT ( 'NONE', #64266 ) ;
#128971=CARTESIAN_POINT ( 'NONE',  ( 22.39999999999999503, 65.49880482333749399, -241.8610443077474486 ) ) ;
#128975=CARTESIAN_POINT ( 'NONE',  ( -18.50000000000000000, 56.01362831242967388, -232.7091905853083347 ) ) ;
#128985=AXIS2_PLACEMENT_3D ( 'NONE', #245335, #184064, #5398 ) ;
#128990=FACE_OUTER_BOUND ( 'NONE', #145777, .T. ) ;
#129002=PLANE ( 'NONE',  #98741 ) ;
#129009=DIRECTION ( 'NONE',  ( 0.000000000000000000, 0.2617529984165152257, 0.9651348961777124202 ) ) ;
#129067=CARTESIAN_POINT ( 'NONE',  ( 18.49999999999964473, 63.70204416476671128, -209.2375263527553102 ) ) ;
#129069=ORIENTED_EDGE ( 'NONE', *, *, #108229, .F. ) ;
#129081=LINE ( 'NONE', #233336, #198685 ) ;
#129086=EDGE_CURVE ( 'NONE', #171727, #178174, #24726, .T. ) ;
#129091=FACE_OUTER_BOUND ( 'NONE', #161220, .T. ) ;
#129094=CARTESIAN_POINT ( 'NONE',  ( 20.99142135623731065, 62.99095723518624368, -207.1734234082434796 ) ) ;
#129097=ORIENTED_EDGE ( 'NONE', *, *, #193658, .F. ) ;
#129104=CIRCLE ( 'NONE', #74956, 0.1000000000000018374 ) ;
#129114=VERTEX_POINT ( 'NONE', #40245 ) ;
#129132=CARTESIAN_POINT ( 'NONE',  ( -23.15000000000000213, 78.37638820354418101, -229.1444560783390898 ) ) ;
#129147=CIRCLE ( 'NONE', #233218, 11.64999999999998970 ) ;
#129161=DIRECTION ( 'NONE',  ( 0.000000000000000000, 0.9916376685811618685, -0.1290532225514649800 ) ) ;
#129166=DIRECTION ( 'NONE',  ( 0.000000000000000000, 0.3896596508880098009, 0.9209589331071361684 ) ) ;
#129199=DIRECTION ( 'NONE',  ( 1.000000000000000000, 0.000000000000000000, 0.000000000000000000 ) ) ;
#129233=EDGE_CURVE ( 'NONE', #143687, #40333, #23250, .T. ) ;
#129244=AXIS2_PLACEMENT_3D ( 'NONE', #137715, #136417, #118175 ) ;
#129249=ORIENTED_EDGE ( 'NONE', *, *, #210181, .F. ) ;
#129252=ADVANCED_FACE ( 'NONE', ( #66198 ), #62354, .F. ) ;
#129287=EDGE_CURVE ( 'NONE', #253128, #110463, #87013, .T. ) ;
#129291=CIRCLE ( 'NONE', #166740, 0.09999999999999543976 ) ;
#129292=DIRECTION ( 'NONE',  ( 0.000000000000000000, 0.2617529984164915779, 0.9651348961777187485 ) ) ;
#129300=ADVANCED_FACE ( 'NONE', ( #205693 ), #251233, .T. ) ;
#129311=CARTESIAN_POINT ( 'NONE',  ( 20.95017935633852346, 59.10443188204394716, -225.7998842055091302 ) ) ;
#129319=CARTESIAN_POINT ( 'NONE',  ( 20.85000000000000142, 80.82423061532404063, -192.8091306798888525 ) ) ;
#129384=ORIENTED_EDGE ( 'NONE', *, *, #127527, .F. ) ;
#129404=EDGE_LOOP ( 'NONE', ( #189900, #97234, #192648, #22929 ) ) ;
#129414=CIRCLE ( 'NONE', #8620, 0.1000000000000124678 ) ;
#129426=ORIENTED_EDGE ( 'NONE', *, *, #21072, .F. ) ;
#129431=EDGE_CURVE ( 'NONE', #248822, #110463, #199689, .T. ) ;
#129488=ORIENTED_EDGE ( 'NONE', *, *, #21294, .T. ) ;
#129491=DIRECTION ( 'NONE',  ( 0.000000000000000000, 0.9651348961777158619, -0.2617529984165031243 ) ) ;
#129497=VERTEX_POINT ( 'NONE', #118160 ) ;
#129503=ORIENTED_EDGE ( 'NONE', *, *, #251062, .T. ) ;
#129603=CARTESIAN_POINT ( 'NONE',  ( 18.59999999999999787, 64.21185867012613357, -224.4479740254296303 ) ) ;
#129652=AXIS2_PLACEMENT_3D ( 'NONE', #214839, #15382, #174495 ) ;
#129654=EDGE_LOOP ( 'NONE', ( #27173, #146027, #23428, #147863 ) ) ;
#129655=EDGE_CURVE ( 'NONE', #79096, #65394, #166374, .T. ) ;
#129668=CARTESIAN_POINT ( 'NONE',  ( -20.94999999999999929, 67.23127455305841238, -235.8551265064783991 ) ) ;
#129721=DIRECTION ( 'NONE',  ( 1.000000000000000000, 0.000000000000000000, 0.000000000000000000 ) ) ;
#129738=ORIENTED_EDGE ( 'NONE', *, *, #2408, .F. ) ;
#129741=CARTESIAN_POINT ( 'NONE',  ( 21.05563370358598263, 60.06990615304147241, -221.2897009653380564 ) ) ;
#129755=DIRECTION ( 'NONE',  ( -1.000000000000000000, -0.000000000000000000, -0.000000000000000000 ) ) ;
#129771=DIRECTION ( 'NONE',  ( 0.000000000000000000, 0.2617529984165180013, 0.9651348961777117541 ) ) ;
#129811=ORIENTED_EDGE ( 'NONE', *, *, #226731, .F. ) ;
#129845=FACE_OUTER_BOUND ( 'NONE', #120399, .T. ) ;
#129855=CARTESIAN_POINT ( 'NONE',  ( -21.14999999999999858, 64.18196446391819165, -247.0985338183330668 ) ) ;
#129893=CIRCLE ( 'NONE', #79993, 0.1000000000000124678 ) ;
#129900=VERTEX_POINT ( 'NONE', #74906 ) ;
#129908=DIRECTION ( 'NONE',  ( 0.000000000000000000, 0.9229812358756199764, -0.3848449534832346086 ) ) ;
#129911=CARTESIAN_POINT ( 'NONE',  ( -23.25000000000000000, 87.08727414655710675, -199.6327537731849873 ) ) ;
#129915=EDGE_LOOP ( 'NONE', ( #241489, #103670, #108805, #138579 ) ) ;
#129934=ORIENTED_EDGE ( 'NONE', *, *, #82573, .T. ) ;
#129949=ORIENTED_EDGE ( 'NONE', *, *, #250870, .T. ) ;
#129974=VERTEX_POINT ( 'NONE', #37066 ) ;
#129992=ADVANCED_FACE ( 'NONE', ( #153173 ), #111801, .T. ) ;
#129993=CIRCLE ( 'NONE', #96669, 0.5000000000000014433 ) ;
#130041=CARTESIAN_POINT ( 'NONE',  ( -20.94999999999999929, 68.03098227380377239, -227.7073825336181869 ) ) ;
#130068=CYLINDRICAL_SURFACE ( 'NONE', #181588, 12.87500000000000178 ) ;
#130074=AXIS2_PLACEMENT_3D ( 'NONE', #158629, #98579, #238123 ) ;
#130096=CARTESIAN_POINT ( 'NONE',  ( -21.05000000000000071, 61.14816101960737882, -234.1879056010411659 ) ) ;
#130099=VERTEX_POINT ( 'NONE', #79980 ) ;
#130109=CARTESIAN_POINT ( 'NONE',  ( 22.59080734064468388, 55.88289069467541026, -232.8092063914162111 ) ) ;
#130118=ORIENTED_EDGE ( 'NONE', *, *, #107735, .T. ) ;
#130135=ORIENTED_EDGE ( 'NONE', *, *, #133374, .F. ) ;
#130152=DIRECTION ( 'NONE',  ( -1.000000000000000000, -0.000000000000000000, 0.000000000000000000 ) ) ;
#130172=AXIS2_PLACEMENT_3D ( 'NONE', #177116, #59675, #96251 ) ;
#130206=DIRECTION ( 'NONE',  ( 1.000000000000000000, -3.151514657663852580E-16, 8.547182517843351137E-17 ) ) ;
#130234=CARTESIAN_POINT ( 'NONE',  ( 20.95512820512820440, 60.15812638745688901, -221.3479132702343009 ) ) ;
#130241=VECTOR ( 'NONE', #11020, 1000.000000000000000 ) ;
#130247=ORIENTED_EDGE ( 'NONE', *, *, #103341, .F. ) ;
#130270=CIRCLE ( 'NONE', #176099, 0.09999999999999868716 ) ;
#130285=EDGE_CURVE ( 'NONE', #152520, #217417, #41272, .T. ) ;
#130299=CARTESIAN_POINT ( 'NONE',  ( 20.50589344625456789, 59.09583819986320918, -225.8021589099539597 ) ) ;
#130318=ADVANCED_FACE ( 'NONE', ( #116287 ), #195835, .F. ) ;
#130328=ORIENTED_EDGE ( 'NONE', *, *, #229537, .T. ) ;
#130334=CARTESIAN_POINT ( 'NONE',  ( 18.46858270002952906, 78.23413370411033441, -231.4806182615872103 ) ) ;
#130340=VERTEX_POINT ( 'NONE', #251924 ) ;
#130406=DIRECTION ( 'NONE',  ( 0.000000000000000000, -0.2617529984165031243, -0.9651348961777157509 ) ) ;
#130410=ORIENTED_EDGE ( 'NONE', *, *, #47586, .F. ) ;
#130509=ORIENTED_EDGE ( 'NONE', *, *, #3243, .F. ) ;
#130518=CARTESIAN_POINT ( 'NONE',  ( -21.08134388332232589, 65.49997743402062156, -241.9491019618814391 ) ) ;
#130528=CIRCLE ( 'NONE', #159763, 11.70000000000000817 ) ;
#130582=CARTESIAN_POINT ( 'NONE',  ( 20.95520789717937404, 59.00725844674948917, -225.7706358438024949 ) ) ;
#130585=CARTESIAN_POINT ( 'NONE',  ( 23.15000000000000213, 81.75190851390706825, -227.2043352493130612 ) ) ;
#130608=ORIENTED_EDGE ( 'NONE', *, *, #215929, .T. ) ;
#130642=VECTOR ( 'NONE', #202824, 1000.000000000000000 ) ;
#130707=CARTESIAN_POINT ( 'NONE',  ( 20.94999999999999929, 67.42187159639590277, -195.4898302452107544 ) ) ;
#130727=ORIENTED_EDGE ( 'NONE', *, *, #215303, .T. ) ;
#130777=CARTESIAN_POINT ( 'NONE',  ( 21.14999999999999858, 59.16775194334852017, -221.0793150863668473 ) ) ;
#130781=AXIS2_PLACEMENT_3D ( 'NONE', #140443, #182161, #141731 ) ;
#130792=CARTESIAN_POINT ( 'NONE',  ( 20.85000000000000142, 80.69087520990402140, -192.8618289658565743 ) ) ;
#130802=CIRCLE ( 'NONE', #55756, 0.1000000000000124678 ) ;
#130805=AXIS2_PLACEMENT_3D ( 'NONE', #29013, #227160, #205011 ) ;
#130829=VERTEX_POINT ( 'NONE', #136803 ) ;
#130845=ORIENTED_EDGE ( 'NONE', *, *, #20959, .T. ) ;
#130852=ORIENTED_EDGE ( 'NONE', *, *, #13706, .F. ) ;
#130865=CARTESIAN_POINT ( 'NONE',  ( -20.64999999999999858, 66.23941198528750363, -222.8935984851895853 ) ) ;
#130870=DIRECTION ( 'NONE',  ( 1.000000000000000000, 0.000000000000000000, 0.000000000000000000 ) ) ;
#130910=ADVANCED_FACE ( 'NONE', ( #31965 ), #48925, .T. ) ;
#130920=EDGE_CURVE ( 'NONE', #206475, #77283, #154085, .T. ) ;
#130951=VECTOR ( 'NONE', #214319, 1000.000000000000000 ) ;
#130995=ADVANCED_FACE ( 'NONE', ( #153205 ), #172780, .F. ) ;
#131009=ORIENTED_EDGE ( 'NONE', *, *, #234430, .F. ) ;
#131022=AXIS2_PLACEMENT_3D ( 'NONE', #149223, #125776, #226133 ) ;
#131032=DIRECTION ( 'NONE',  ( -1.000000000000000000, 0.000000000000000000, 0.000000000000000000 ) ) ;
#131038=CARTESIAN_POINT ( 'NONE',  ( -22.50000000000000000, 55.96169194136206215, -232.9023299069559130 ) ) ;
#131050=DIRECTION ( 'NONE',  ( 0.000000000000000000, 0.1290532225515392817, 0.9916376685811522096 ) ) ;
#131055=CARTESIAN_POINT ( 'NONE',  ( 20.94999999999999929, 82.09643798151613225, -215.4278993322501208 ) ) ;
#131056=ADVANCED_FACE ( 'NONE', ( #232726 ), #134859, .T. ) ;
#131065=FACE_OUTER_BOUND ( 'NONE', #106813, .T. ) ;
#131087=CARTESIAN_POINT ( 'NONE',  ( -20.94999999999999929, 76.00000000001126921, -203.5231074845248997 ) ) ;
#131109=ORIENTED_EDGE ( 'NONE', *, *, #32969, .F. ) ;
#131149=EDGE_CURVE ( 'NONE', #19956, #695, #87383, .T. ) ;
#131154=LINE ( 'NONE', #32085, #207288 ) ;
#131157=LINE ( 'NONE', #138519, #255820 ) ;
#131164=CARTESIAN_POINT ( 'NONE',  ( 21.05000000000000071, 60.06173988932783203, -221.3217724115915814 ) ) ;
#131174=EDGE_CURVE ( 'NONE', #215885, #206475, #249891, .T. ) ;
#131194=FACE_OUTER_BOUND ( 'NONE', #201214, .T. ) ;
#131203=ORIENTED_EDGE ( 'NONE', *, *, #76413, .F. ) ;
#131214=CARTESIAN_POINT ( 'NONE',  ( -18.56579813702275672, 67.49234744263520724, -195.4268335588911327 ) ) ;
#131229=AXIS2_PLACEMENT_3D ( 'NONE', #47678, #25582, #245910 ) ;
#131231=CYLINDRICAL_SURFACE ( 'NONE', #26206, 0.09999999999999935330 ) ;
#131260=CARTESIAN_POINT ( 'NONE',  ( 18.53317502108576420, 67.49276774653023381, -195.4544018784149841 ) ) ;
#131264=CARTESIAN_POINT ( 'NONE',  ( -20.94999999999999574, 62.98661795304985844, -207.1103002134591122 ) ) ;
#131265=CARTESIAN_POINT ( 'NONE',  ( 18.41416235934319090, 86.89640087696875526, -199.6396878666313626 ) ) ;
#131267=EDGE_LOOP ( 'NONE', ( #4707, #77070, #151515, #56093 ) ) ;
#131321=AXIS2_PLACEMENT_3D ( 'NONE', #248781, #209644, #225331 ) ;
#131345=DIRECTION ( 'NONE',  ( 1.000000000000000000, 0.000000000000000000, 0.000000000000000000 ) ) ;
#131446=LINE ( 'NONE', #194011, #93034 ) ;
#131466=ADVANCED_FACE ( 'NONE', ( #116328 ), #117594, .T. ) ;
#131490=AXIS2_PLACEMENT_3D ( 'NONE', #68409, #90522, #12309 ) ;
#131524=DIRECTION ( 'NONE',  ( 1.000000000000000000, 0.000000000000000000, 0.000000000000000000 ) ) ;
#131525=ADVANCED_FACE ( 'NONE', ( #56318 ), #120203, .F. ) ;
#131526=EDGE_CURVE ( 'NONE', #143126, #213407, #158348, .T. ) ;
#131548=CARTESIAN_POINT ( 'NONE',  ( 21.05000000000000071, 75.47649400317826007, -205.4533772768803317 ) ) ;
#131590=CARTESIAN_POINT ( 'NONE',  ( 20.74625933824081869, 60.89740640166220231, -225.2731031595071443 ) ) ;
#131594=CARTESIAN_POINT ( 'NONE',  ( -21.55000000000000071, 65.67360898266123570, -213.5186389139583980 ) ) ;
#131605=ORIENTED_EDGE ( 'NONE', *, *, #251693, .F. ) ;
#131606=EDGE_LOOP ( 'NONE', ( #28689, #91547, #112502, #100651 ) ) ;
#131620=ORIENTED_EDGE ( 'NONE', *, *, #91700, .F. ) ;
#131630=( BOUNDED_SURFACE ( )  B_SPLINE_SURFACE ( 3, 2, ( 
 ( #23855, #98181, #69388 ),
 ( #124222, #145043, #185468 ),
 ( #125492, #186765, #168518 ),
 ( #224581, #10685, #189326 ),
 ( #108493, #27717, #208879 ),
 ( #203747, #86329, #148922 ) ),
 .UNSPECIFIED., .F., .F., .F. ) 
 B_SPLINE_SURFACE_WITH_KNOTS ( ( 4, 2, 4 ),
 ( 3, 3 ),
 ( 0.0001300404313046778129, 0.0003183318589266858375, 0.0005066232865486938351 ),
 ( 0.000000000000000000, 1.000000000000000000 ),
 .UNSPECIFIED. ) 
 GEOMETRIC_REPRESENTATION_ITEM ( )  RATIONAL_B_SPLINE_SURFACE ( (
 ( 1.000000000000000000, 0.7071067811865352493, 1.000000000000000000),
 ( 1.000000000000000000, 0.7625113560543027580, 1.000000000000000000),
 ( 1.000000000000000000, 0.8126073484685780723, 1.000000000000000000),
 ( 1.000000000000000000, 0.8923049332735644157, 1.000000000000000000),
 ( 1.000000000000000000, 0.9231914937767029539, 1.000000000000000000),
 ( 1.000000000000000000, 0.9238795325112919565, 1.000000000000000000) ) ) 
 REPRESENTATION_ITEM ( '' )  SURFACE ( )  );
#131631=ORIENTED_EDGE ( 'NONE', *, *, #34645, .F. ) ;
#131634=CIRCLE ( 'NONE', #177468, 0.1000000000000124678 ) ;
#131669=EDGE_CURVE ( 'NONE', #92812, #62695, #166732, .T. ) ;
#131681=AXIS2_PLACEMENT_3D ( 'NONE', #160134, #35071, #97531 ) ;
#131708=DIRECTION ( 'NONE',  ( -3.265361837132813093E-16, -0.9651348961777157509, 0.2617529984165031243 ) ) ;
#131733=AXIS2_PLACEMENT_3D ( 'NONE', #257358, #115340, #237861 ) ;
#131735=AXIS2_PLACEMENT_3D ( 'NONE', #7747, #106821, #67710 ) ;
#131745=DIRECTION ( 'NONE',  ( 1.000000000000000000, 0.000000000000000000, 0.000000000000000000 ) ) ;
#131769=EDGE_LOOP ( 'NONE', ( #197332, #16297, #63498, #246484, #174679, #257854 ) ) ;
#131770=ORIENTED_EDGE ( 'NONE', *, *, #52499, .T. ) ;
#131775=DIRECTION ( 'NONE',  ( 1.000000000000000000, 0.000000000000000000, -0.000000000000000000 ) ) ;
#131790=DIRECTION ( 'NONE',  ( 0.000000000000000000, 0.2617529984165031243, 0.9651348961777157509 ) ) ;
#131793=EDGE_LOOP ( 'NONE', ( #103422, #190319, #83782, #6225 ) ) ;
#131803=ORIENTED_EDGE ( 'NONE', *, *, #129233, .F. ) ;
#131822=ORIENTED_EDGE ( 'NONE', *, *, #173086, .F. ) ;
#131829=ORIENTED_EDGE ( 'NONE', *, *, #220936, .F. ) ;
#131839=CARTESIAN_POINT ( 'NONE',  ( -23.25000000000000000, 66.45861426436469799, -222.8494355952551018 ) ) ;
#131841=ORIENTED_EDGE ( 'NONE', *, *, #90883, .T. ) ;
#131842=DIRECTION ( 'NONE',  ( 1.000000000000000000, 0.000000000000000000, 0.000000000000000000 ) ) ;
#131844=AXIS2_PLACEMENT_3D ( 'NONE', #215963, #37364, #257611 ) ;
#131858=CIRCLE ( 'NONE', #23570, 0.1000000000000124678 ) ;
#131867=DIRECTION ( 'NONE',  ( 0.000000000000000000, -0.1290532225515392262, -0.9916376685811520986 ) ) ;
#131868=ADVANCED_FACE ( 'NONE', ( #119887 ), #162862, .F. ) ;
#131869=ORIENTED_EDGE ( 'NONE', *, *, #165761, .F. ) ;
#131893=CARTESIAN_POINT ( 'NONE',  ( -22.39999999999999858, 65.19201463318205469, -243.3742797652979561 ) ) ;
#131933=DIRECTION ( 'NONE',  ( 0.000000000000000000, 0.2617529984165032908, 0.9651348961777156399 ) ) ;
#131944=ORIENTED_EDGE ( 'NONE', *, *, #13473, .F. ) ;
#131994=ADVANCED_FACE ( 'NONE', ( #177302 ), #141922, .T. ) ;
#132069=AXIS2_PLACEMENT_3D ( 'NONE', #28242, #107740, #81725 ) ;
#132077=VERTEX_POINT ( 'NONE', #149721 ) ;
#132087=CARTESIAN_POINT ( 'NONE',  ( 21.05000000000000071, 86.52890073500824997, -209.5906233940697234 ) ) ;
#132091=AXIS2_PLACEMENT_3D ( 'NONE', #166722, #247510, #246231 ) ;
#132111=DIRECTION ( 'NONE',  ( 1.000000000000000000, 0.000000000000000000, 0.000000000000000000 ) ) ;
#132168=PLANE ( 'NONE',  #343 ) ;
#132203=ORIENTED_EDGE ( 'NONE', *, *, #256353, .T. ) ;
#132209=VECTOR ( 'NONE', #118627, 1000.000000000000000 ) ;
#132213=CARTESIAN_POINT ( 'NONE',  ( -22.40000000000000568, 59.71212129423881976, -233.8158665866019987 ) ) ;
#132216=ORIENTED_EDGE ( 'NONE', *, *, #143468, .T. ) ;
#132245=AXIS2_PLACEMENT_3D ( 'NONE', #154610, #214541, #55438 ) ;
#132248=CARTESIAN_POINT ( 'NONE',  ( -18.50000000000000000, 73.32445833535280144, -249.6821150215233160 ) ) ;
#132273=DIRECTION ( 'NONE',  ( -1.000000000000000000, 3.151514657663852580E-16, -8.547182517843351137E-17 ) ) ;
#132286=DIRECTION ( 'NONE',  ( 1.000000000000000000, 0.000000000000000000, 0.000000000000000000 ) ) ;
#132317=CARTESIAN_POINT ( 'NONE',  ( 23.14999999999999858, 65.65271564877468791, -222.5736063831752176 ) ) ;
#132374=DIRECTION ( 'NONE',  ( 0.000000000000000000, 0.2617529984165035128, 0.9651348961777155289 ) ) ;
#132377=FACE_OUTER_BOUND ( 'NONE', #94521, .T. ) ;
#132381=ADVANCED_FACE ( 'NONE', ( #11011 ), #71011, .F. ) ;
#132384=ORIENTED_EDGE ( 'NONE', *, *, #72617, .F. ) ;
#132385=CARTESIAN_POINT ( 'NONE',  ( 22.50046968637449751, 64.11207000662210476, -247.1836817737965077 ) ) ;
#132405=LINE ( 'NONE', #251048, #209924 ) ;
#132437=VECTOR ( 'NONE', #151417, 1000.000000000000000 ) ;
#132449=DIRECTION ( 'NONE',  ( 2.342056488767301376E-15, 0.3896596508880124654, 0.9209589331071350582 ) ) ;
#132454=AXIS2_PLACEMENT_3D ( 'NONE', #120259, #22423, #23719 ) ;
#132457=CIRCLE ( 'NONE', #44974, 0.09999999999999939493 ) ;
#132467=CARTESIAN_POINT ( 'NONE',  ( -18.59999999999999787, 78.21362219944482774, -231.2727646510690533 ) ) ;
#132475=EDGE_CURVE ( 'NONE', #19956, #73870, #9023, .T. ) ;
#132486=DIRECTION ( 'NONE',  ( 0.000000000000000000, -0.9651348961777379554, 0.2617529984164210233 ) ) ;
#132493=VERTEX_POINT ( 'NONE', #160745 ) ;
#132522=EDGE_LOOP ( 'NONE', ( #22647, #100379, #63893 ) ) ;
#132532=CARTESIAN_POINT ( 'NONE',  ( -18.59999999999999787, 79.19526988099229925, -196.1889237952725296 ) ) ;
#132558=CARTESIAN_POINT ( 'NONE',  ( -21.05000000000000071, 62.99095723518624368, -207.1734234082435080 ) ) ;
#132568=CIRCLE ( 'NONE', #244987, 0.09999999999999123479 ) ;
#132608=EDGE_LOOP ( 'NONE', ( #124714, #162466, #139171, #237070 ) ) ;
#132641=DIRECTION ( 'NONE',  ( 0.000000000000000000, -0.2617529984164915779, -0.9651348961777189706 ) ) ;
#132644=ORIENTED_EDGE ( 'NONE', *, *, #6170, .F. ) ;
#132662=CARTESIAN_POINT ( 'NONE',  ( 21.13461538461538325, 60.21941965847794620, -221.1573116214326831 ) ) ;
#132678=EDGE_CURVE ( 'NONE', #75171, #137789, #92396, .T. ) ;
#132684=ORIENTED_EDGE ( 'NONE', *, *, #33724, .T. ) ;
#132696=AXIS2_PLACEMENT_3D ( 'NONE', #216603, #120114, #142202 ) ;
#132764=FACE_OUTER_BOUND ( 'NONE', #59528, .T. ) ;
#132778=CIRCLE ( 'NONE', #95164, 7.900000000000010125 ) ;
#132783=CARTESIAN_POINT ( 'NONE',  ( -20.00857864376270001, 61.53642629385834795, -221.5144953033309321 ) ) ;
#132804=ORIENTED_EDGE ( 'NONE', *, *, #69969, .T. ) ;
#132809=DIRECTION ( 'NONE',  ( -2.952720810173289112E-16, -0.9651348961777159730, 0.2617529984165024026 ) ) ;
#132811=AXIS2_PLACEMENT_3D ( 'NONE', #78900, #95908, #60629 ) ;
#132844=FACE_OUTER_BOUND ( 'NONE', #107462, .T. ) ;
#132845=EDGE_CURVE ( 'NONE', #128703, #30986, #615, .T. ) ;
#132849=CARTESIAN_POINT ( 'NONE',  ( 23.14999999999999147, 67.23127455305841238, -235.8551265064783991 ) ) ;
#132853=ADVANCED_FACE ( 'NONE', ( #10631 ), #213020, .F. ) ;
#132855=AXIS2_PLACEMENT_3D ( 'NONE', #201980, #23370, #178592 ) ;
#132874=LINE ( 'NONE', #214958, #44712 ) ;
#132885=ORIENTED_EDGE ( 'NONE', *, *, #254879, .F. ) ;
#132892=CARTESIAN_POINT ( 'NONE',  ( -22.59999999999999787, 67.23127455305841238, -235.8551265064783991 ) ) ;
#132916=DIRECTION ( 'NONE',  ( 1.000000000000000000, -7.049440681616512959E-16, 1.911869773728117674E-16 ) ) ;
#132930=ORIENTED_EDGE ( 'NONE', *, *, #29459, .T. ) ;
#132940=AXIS2_PLACEMENT_3D ( 'NONE', #100945, #593, #119291 ) ;
#133063=ORIENTED_EDGE ( 'NONE', *, *, #75342, .F. ) ;
#133069=CARTESIAN_POINT ( 'NONE',  ( -20.64999999999999858, 76.00000000001126921, -203.5231074845248997 ) ) ;
#133073=DIRECTION ( 'NONE',  ( 0.000000000000000000, -0.7035695228903320331, -0.7106264324241468033 ) ) ;
#133084=CIRCLE ( 'NONE', #103996, 0.5000000000000014433 ) ;
#133099=LINE ( 'NONE', #212644, #22194 ) ;
#133113=CARTESIAN_POINT ( 'NONE',  ( 21.11825140030089898, 65.53721733114183223, -242.0739286986531908 ) ) ;
#133127=DIRECTION ( 'NONE',  ( -1.000000000000000000, -0.000000000000000000, -0.000000000000000000 ) ) ;
#133156=ORIENTED_EDGE ( 'NONE', *, *, #254265, .T. ) ;
#133163=ORIENTED_EDGE ( 'NONE', *, *, #96245, .F. ) ;
#133167=CARTESIAN_POINT ( 'NONE',  ( 20.95512820512820440, 58.98414156600839675, -225.6766266970810477 ) ) ;
#133192=AXIS2_PLACEMENT_3D ( 'NONE', #254784, #193588, #116610 ) ;
#133217=AXIS2_PLACEMENT_3D ( 'NONE', #40026, #41306, #19140 ) ;
#133247=EDGE_CURVE ( 'NONE', #126077, #26209, #200741, .T. ) ;
#133252=AXIS2_PLACEMENT_3D ( 'NONE', #211033, #14137, #92355 ) ;
#133258=ORIENTED_EDGE ( 'NONE', *, *, #219234, .F. ) ;
#133290=CARTESIAN_POINT ( 'NONE',  ( -20.54999999999999716, 68.56901367119438362, -214.3038979092079046 ) ) ;
#133293=VERTEX_POINT ( 'NONE', #168152 ) ;
#133294=EDGE_CURVE ( 'NONE', #176136, #113811, #221557, .T. ) ;
#133305=ADVANCED_FACE ( 'NONE', ( #199227 ), #174580, .F. ) ;
#133355=EDGE_CURVE ( 'NONE', #71652, #74229, #30253, .T. ) ;
#133374=EDGE_CURVE ( 'NONE', #4584, #15317, #36313, .T. ) ;
#133407=VECTOR ( 'NONE', #35070, 1000.000000000000000 ) ;
#133438=VERTEX_POINT ( 'NONE', #46539 ) ;
#133447=VERTEX_POINT ( 'NONE', #205616 ) ;
#133448=LINE ( 'NONE', #212984, #12847 ) ;
#133458=AXIS2_PLACEMENT_3D ( 'NONE', #77627, #142442, #162035 ) ;
#133464=EDGE_CURVE ( 'NONE', #6279, #20693, #242606, .T. ) ;
#133506=DIRECTION ( 'NONE',  ( 0.000000000000000000, -0.9667078373770160438, -0.2558827019433957961 ) ) ;
#133587=CARTESIAN_POINT ( 'NONE',  ( 21.05933563467872105, 60.07238536843232168, -221.2794350522829632 ) ) ;
#133621=DIRECTION ( 'NONE',  ( 1.000000000000000000, 0.000000000000000000, 0.000000000000000000 ) ) ;
#133638=CARTESIAN_POINT ( 'NONE',  ( 21.05000000000000071, 86.48473784507378070, -209.3714211149925575 ) ) ;
#133646=VERTEX_POINT ( 'NONE', #253729 ) ;
#133648=CARTESIAN_POINT ( 'NONE',  ( -21.30740335185485890, 65.41956451911318027, -242.1572894605589283 ) ) ;
#133674=DIRECTION ( 'NONE',  ( 0.000000000000000000, 0.9651348961777157509, -0.2617529984165031243 ) ) ;
#133730=CARTESIAN_POINT ( 'NONE',  ( 18.39999999999999858, 73.22794484573502416, -249.6559397216816478 ) ) ;
#133743=ADVANCED_FACE ( 'NONE', ( #136331 ), #196996, .T. ) ;
#133746=CARTESIAN_POINT ( 'NONE',  ( 21.05000000000000071, 61.16604239671103471, -234.3115055913011417 ) ) ;
#133761=DIRECTION ( 'NONE',  ( 0.000000000000000000, 0.9333616406058473647, 0.3589373870824282275 ) ) ;
#133771=EDGE_CURVE ( 'NONE', #206711, #12050, #138698, .T. ) ;
#133775=VERTEX_POINT ( 'NONE', #34726 ) ;
#133782=CARTESIAN_POINT ( 'NONE',  ( 23.24999999999997513, 62.92003201576280702, -207.2439188921395612 ) ) ;
#133792=DIRECTION ( 'NONE',  ( 0.000000000000000000, 0.2617529984164856383, 0.9651348961777204138 ) ) ;
#133822=ADVANCED_FACE ( 'NONE', ( #28988 ), #155356, .F. ) ;
#133823=CARTESIAN_POINT ( 'NONE',  ( 22.41477678272288188, 64.18116553293013737, -247.0983321412288660 ) ) ;
#133835=CARTESIAN_POINT ( 'NONE',  ( -20.54999999999999716, 76.00000000001126921, -203.5231074845248997 ) ) ;
#133843=DIRECTION ( 'NONE',  ( 1.000000000000000000, 0.000000000000000000, 0.000000000000000000 ) ) ;
#133865=ORIENTED_EDGE ( 'NONE', *, *, #186595, .F. ) ;
#133876=DIRECTION ( 'NONE',  ( 1.000000000000000000, 0.000000000000000000, 0.000000000000000000 ) ) ;
#133894=EDGE_LOOP ( 'NONE', ( #61034, #13500, #193601 ) ) ;
#133916=LINE ( 'NONE', #128802, #89084 ) ;
#133924=EDGE_CURVE ( 'NONE', #151423, #145620, #25126, .T. ) ;
#133939=LINE ( 'NONE', #34885, #138240 ) ;
#133945=DIRECTION ( 'NONE',  ( 0.000000000000000000, 0.2617529984165152257, 0.9651348961777124202 ) ) ;
#133992=CARTESIAN_POINT ( 'NONE',  ( -21.05000000000000071, 86.48473784507379492, -209.3714211149925575 ) ) ;
#133993=CARTESIAN_POINT ( 'NONE',  ( 21.05000000000000071, 86.30329675166747450, -209.4258251677035787 ) ) ;
#134046=ORIENTED_EDGE ( 'NONE', *, *, #251909, .F. ) ;
#134084=CARTESIAN_POINT ( 'NONE',  ( 21.14999999999998082, 78.57160958314655375, -238.9307242378722833 ) ) ;
#134089=CYLINDRICAL_SURFACE ( 'NONE', #114543, 11.75000000000000178 ) ;
#134135=DIRECTION ( 'NONE',  ( 1.000000000000000000, 0.000000000000000000, 0.000000000000000000 ) ) ;
#134136=CARTESIAN_POINT ( 'NONE',  ( -21.59142135623730852, 62.86143984866549062, -221.9774629907318229 ) ) ;
#134215=CARTESIAN_POINT ( 'NONE',  ( -23.25000000000000000, 77.02083669383561926, -199.7590813894317989 ) ) ;
#134247=DIRECTION ( 'NONE',  ( 0.000000000000000000, -0.9667078373770113808, -0.2558827019434133376 ) ) ;
#134268=EDGE_CURVE ( 'NONE', #7048, #49647, #26082, .T. ) ;
#134272=AXIS2_PLACEMENT_3D ( 'NONE', #217474, #114551, #74175 ) ;
#134295=DIRECTION ( 'NONE',  ( 0.000000000000000000, -0.2617529984165152257, -0.9651348961777124202 ) ) ;
#134304=CYLINDRICAL_SURFACE ( 'NONE', #28784, 0.1000000000000124678 ) ;
#134314=VECTOR ( 'NONE', #195476, 1000.000000000000114 ) ;
#134321=ORIENTED_EDGE ( 'NONE', *, *, #5341, .T. ) ;
#134323=VECTOR ( 'NONE', #168963, 1000.000000000000114 ) ;
#134326=CARTESIAN_POINT ( 'NONE',  ( -20.64999999999999858, 65.86663596189677605, -213.5709895136416776 ) ) ;
#134343=FACE_OUTER_BOUND ( 'NONE', #16303, .T. ) ;
#134353=VERTEX_POINT ( 'NONE', #211125 ) ;
#134382=AXIS2_PLACEMENT_3D ( 'NONE', #187927, #131790, #10576 ) ;
#134430=ORIENTED_EDGE ( 'NONE', *, *, #233129, .T. ) ;
#134431=VECTOR ( 'NONE', #42838, 1000.000000000000000 ) ;
#134449=VECTOR ( 'NONE', #10119, 1000.000000000000000 ) ;
#134458=EDGE_CURVE ( 'NONE', #79058, #133293, #155161, .T. ) ;
#134464=DIRECTION ( 'NONE',  ( -1.000000000000000000, -0.000000000000000000, -0.000000000000000000 ) ) ;
#134476=B_SPLINE_CURVE_WITH_KNOTS ( 'NONE', 3,
 ( #148644, #70415, #149934, #228175, #130334, #229455, #170815, #71681, #151207, #187322 ),
 .UNSPECIFIED., .F., .F.,
 ( 4, 2, 2, 2, 4 ),
 ( 0.000000000000000000, 0.0001584437871625818894, 0.0002376656807438358356, 0.0002772766275344235335, 0.0003168875743250112315 ),
 .UNSPECIFIED. ) ;
#134505=TOROIDAL_SURFACE ( 'NONE', #138583, 0.2000000000000000111, 0.1000000000000000056 ) ;
#134513=ORIENTED_EDGE ( 'NONE', *, *, #62653, .F. ) ;
#134522=CARTESIAN_POINT ( 'NONE',  ( -23.25000000000000000, 80.82423061532404063, -192.8091306798888525 ) ) ;
#134536=VECTOR ( 'NONE', #228121, 1000.000000000000000 ) ;
#134591=CARTESIAN_POINT ( 'NONE',  ( 22.00356870068118553, 65.33245486358892151, -242.8564489551373811 ) ) ;
#134593=AXIS2_PLACEMENT_3D ( 'NONE', #232912, #178066, #155944 ) ;
#134597=AXIS2_PLACEMENT_3D ( 'NONE', #55878, #172046, #254093 ) ;
#134614=ORIENTED_EDGE ( 'NONE', *, *, #6187, .F. ) ;
#134617=CARTESIAN_POINT ( 'NONE',  ( -22.50000000000000000, 67.23127455305841238, -235.8551265064783991 ) ) ;
#134619=FACE_OUTER_BOUND ( 'NONE', #185140, .T. ) ;
#134630=DIRECTION ( 'NONE',  ( 0.000000000000000000, -0.9651348961777157509, 0.2617529984165031243 ) ) ;
#134642=DIRECTION ( 'NONE',  ( -1.000000000000000000, 0.000000000000000000, 0.000000000000000000 ) ) ;
#134656=AXIS2_PLACEMENT_3D ( 'NONE', #54734, #114718, #90003 ) ;
#134662=DIRECTION ( 'NONE',  ( 0.000000000000000000, 0.9651348961777148627, -0.2617529984165062329 ) ) ;
#134666=FACE_OUTER_BOUND ( 'NONE', #35949, .T. ) ;
#134693=ORIENTED_EDGE ( 'NONE', *, *, #204088, .T. ) ;
#134701=CARTESIAN_POINT ( 'NONE',  ( 23.15000000000000213, 86.52890073500824997, -209.5906233940697234 ) ) ;
#134714=EDGE_CURVE ( 'NONE', #177651, #116965, #246099, .T. ) ;
#134745=LINE ( 'NONE', #53944, #137388 ) ;
#134751=EDGE_CURVE ( 'NONE', #146536, #157096, #7469, .T. ) ;
#134764=CARTESIAN_POINT ( 'NONE',  ( 20.94999999999999929, 64.23744694032048130, -224.5446448091673233 ) ) ;
#134776=VECTOR ( 'NONE', #21105, 1000.000000000000114 ) ;
#134790=AXIS2_PLACEMENT_3D ( 'NONE', #178482, #256644, #257932 ) ;
#134797=ORIENTED_EDGE ( 'NONE', *, *, #238324, .T. ) ;
#134830=CIRCLE ( 'NONE', #226410, 0.1000000000000124678 ) ;
#134847=ORIENTED_EDGE ( 'NONE', *, *, #58815, .T. ) ;
#134859=SPHERICAL_SURFACE ( 'NONE', #133192, 0.1000000000000000056 ) ;
#134907=ORIENTED_EDGE ( 'NONE', *, *, #114828, .T. ) ;
#134920=EDGE_CURVE ( 'NONE', #224282, #118480, #159412, .T. ) ;
#134940=DIRECTION ( 'NONE',  ( 0.000000000000000000, -0.2617529984165031243, -0.9651348961777157509 ) ) ;
#134947=DIRECTION ( 'NONE',  ( 1.000000000000000000, 0.000000000000000000, -0.000000000000000000 ) ) ;
#134952=AXIS2_PLACEMENT_3D ( 'NONE', #125976, #86834, #243355 ) ;
#134953=EDGE_CURVE ( 'NONE', #101113, #72258, #213551, .T. ) ;
#134955=AXIS2_PLACEMENT_3D ( 'NONE', #86939, #182233, #122254 ) ;
#134966=ADVANCED_FACE ( 'NONE', ( #55546 ), #158563, .F. ) ;
#134978=ORIENTED_EDGE ( 'NONE', *, *, #75895, .F. ) ;
#134983=VERTEX_POINT ( 'NONE', #236775 ) ;
#134992=DIRECTION ( 'NONE',  ( -1.000000000000000000, 2.849773892568378313E-16, -7.728835255496647986E-17 ) ) ;
#135054=ADVANCED_FACE ( 'NONE', ( #24180 ), #84079, .T. ) ;
#135091=CARTESIAN_POINT ( 'NONE',  ( 22.49806830649814060, 64.10711748978857827, -247.0785650319148203 ) ) ;
#135104=FACE_OUTER_BOUND ( 'NONE', #141948, .T. ) ;
#135109=DIRECTION ( 'NONE',  ( 0.000000000000000000, -0.9121259477928120862, 0.4099100576505341209 ) ) ;
#135135=VECTOR ( 'NONE', #174586, 1000.000000000000114 ) ;
#135138=CARTESIAN_POINT ( 'NONE',  ( 20.04142135623730070, 61.57587952878035509, -212.2000740415318774 ) ) ;
#135140=DIRECTION ( 'NONE',  ( 5.421010862427554711E-16, 0.9651348961777166391, -0.2617529984164999601 ) ) ;
#135160=DIRECTION ( 'NONE',  ( 0.000000000000000000, 0.000000000000000000, 1.000000000000000000 ) ) ;
#135164=VERTEX_POINT ( 'NONE', #231368 ) ;
#135185=ADVANCED_FACE ( 'NONE', ( #52701 ), #30608, .T. ) ;
#135211=ADVANCED_FACE ( 'NONE', ( #57828 ), #216912, .T. ) ;
#135245=EDGE_CURVE ( 'NONE', #2377, #160646, #80424, .T. ) ;
#135251=DIRECTION ( 'NONE',  ( -1.000000000000000000, 3.151514657663852580E-16, -8.547182517843351137E-17 ) ) ;
#135253=CARTESIAN_POINT ( 'NONE',  ( -21.14999999893415250, 57.68250670178610306, -226.1736674723211706 ) ) ;
#135318=AXIS2_PLACEMENT_3D ( 'NONE', #57504, #215313, #116237 ) ;
#135348=CIRCLE ( 'NONE', #2063, 0.1000000000000018374 ) ;
#135380=ADVANCED_FACE ( 'NONE', ( #223327 ), #99514, .F. ) ;
#135388=CARTESIAN_POINT ( 'NONE',  ( -23.15000000000000213, 68.62136427087769164, -214.1108709299723500 ) ) ;
#135398=DIRECTION ( 'NONE',  ( 0.000000000000000000, 0.001293682058376932620, 0.9999991631930158498 ) ) ;
#135400=ORIENTED_EDGE ( 'NONE', *, *, #114243, .F. ) ;
#135481=VERTEX_POINT ( 'NONE', #8159 ) ;
#135491=CARTESIAN_POINT ( 'NONE',  ( 18.57071067811864040, 62.96913842657221494, -212.6815504609503762 ) ) ;
#135496=CARTESIAN_POINT ( 'NONE',  ( -18.50000000000000000, 52.91185528119410719, -244.1460391050142960 ) ) ;
#135552=CARTESIAN_POINT ( 'NONE',  ( 19.97071067811864609, 62.37141908057012074, -208.9966201521278037 ) ) ;
#135579=CARTESIAN_POINT ( 'NONE',  ( 20.85000000000000142, 78.04167338765999773, -195.9950552943387265 ) ) ;
#135606=EDGE_CURVE ( 'NONE', #68619, #107947, #68180, .T. ) ;
#135626=EDGE_LOOP ( 'NONE', ( #250566, #171141, #217254, #13235, #130135 ) ) ;
#135631=DIRECTION ( 'NONE',  ( 0.000000000000000000, -0.7035695228903320331, -0.7106264324241468033 ) ) ;
#135648=ORIENTED_EDGE ( 'NONE', *, *, #125291, .T. ) ;
#135651=FACE_OUTER_BOUND ( 'NONE', #238653, .T. ) ;
#135655=CARTESIAN_POINT ( 'NONE',  ( 21.05000000000000426, 65.48742650828103251, -241.9089677661080771 ) ) ;
#135664=ORIENTED_EDGE ( 'NONE', *, *, #228823, .F. ) ;
#135672=ORIENTED_EDGE ( 'NONE', *, *, #217706, .F. ) ;
#135674=CYLINDRICAL_SURFACE ( 'NONE', #143913, 11.79999999999999361 ) ;
#135675=ORIENTED_EDGE ( 'NONE', *, *, #153904, .T. ) ;
#135686=CIRCLE ( 'NONE', #239758, 0.09999999999999395484 ) ;
#135694=DIRECTION ( 'NONE',  ( -1.000000000000000000, -0.000000000000000000, -0.000000000000000000 ) ) ;
#135697=CARTESIAN_POINT ( 'NONE',  ( -18.50000000000000000, 78.21362219944489880, -231.2727646510690533 ) ) ;
#135714=DIRECTION ( 'NONE',  ( 1.000000000000000000, 0.000000000000000000, 0.000000000000000000 ) ) ;
#135722=DIRECTION ( 'NONE',  ( -0.000000000000000000, -0.2617529984165031243, -0.9651348961777157509 ) ) ;
#135731=AXIS2_PLACEMENT_3D ( 'NONE', #248689, #171749, #70076 ) ;
#135853=CARTESIAN_POINT ( 'NONE',  ( -20.85000000000000142, 79.19526988099229925, -196.1889237952725296 ) ) ;
#135877=EDGE_LOOP ( 'NONE', ( #115235, #90963, #51167, #22906, #28053 ) ) ;
#135885=LINE ( 'NONE', #53805, #225892 ) ;
#135895=AXIS2_PLACEMENT_3D ( 'NONE', #175312, #254765, #50177 ) ;
#135904=DIRECTION ( 'NONE',  ( 0.000000000000000000, -0.2617529984165031243, -0.9651348961777157509 ) ) ;
#135933=CARTESIAN_POINT ( 'NONE',  ( -21.14999999999999858, 65.61575147395463148, -242.1939180743342774 ) ) ;
#135986=DIRECTION ( 'NONE',  ( 2.694716079187273439E-16, 0.9651348961777159730, -0.2617529984165023471 ) ) ;
#135989=EDGE_CURVE ( 'NONE', #213407, #140695, #39356, .T. ) ;
#135993=ORIENTED_EDGE ( 'NONE', *, *, #148583, .F. ) ;
#136016=EDGE_LOOP ( 'NONE', ( #72871, #136388, #125772, #176058 ) ) ;
#136028=VECTOR ( 'NONE', #76294, 1000.000000000000000 ) ;
#136096=CARTESIAN_POINT ( 'NONE',  ( 20.85000000000000142, 80.80934863333322937, -192.8037999715871535 ) ) ;
#136114=CARTESIAN_POINT ( 'NONE',  ( 23.15000000000000213, 86.27712145182582049, -209.5223386573213702 ) ) ;
#136134=CARTESIAN_POINT ( 'NONE',  ( -20.94403535211772294, 67.49374512151688066, -195.5131169347613991 ) ) ;
#136140=CARTESIAN_POINT ( 'NONE',  ( -21.05000000000000071, 72.02722222756958104, -225.1832529173024398 ) ) ;
#136150=CARTESIAN_POINT ( 'NONE',  ( 20.94999999999999929, 70.42128727326085880, -228.5349014959848262 ) ) ;
#136189=EDGE_CURVE ( 'NONE', #43432, #148962, #18283, .T. ) ;
#136205=AXIS2_PLACEMENT_3D ( 'NONE', #195074, #93371, #76364 ) ;
#136240=EDGE_CURVE ( 'NONE', #52077, #140929, #246322, .T. ) ;
#136248=TOROIDAL_SURFACE ( 'NONE', #7089, 11.70000000000000107, 0.1000000000000000056 ) ;
#136249=EDGE_CURVE ( 'NONE', #209902, #124124, #39547, .T. ) ;
#136274=CIRCLE ( 'NONE', #190499, 0.1999999999999945155 ) ;
#136278=AXIS2_PLACEMENT_3D ( 'NONE', #135138, #231710, #210851 ) ;
#136295=VERTEX_POINT ( 'NONE', #168115 ) ;
#136321=CYLINDRICAL_SURFACE ( 'NONE', #26398, 0.09999999999999543976 ) ;
#136331=FACE_OUTER_BOUND ( 'NONE', #168175, .T. ) ;
#136350=DIRECTION ( 'NONE',  ( 1.000000000000000000, 0.000000000000000000, 0.000000000000000000 ) ) ;
#136353=ORIENTED_EDGE ( 'NONE', *, *, #20997, .F. ) ;
#136364=CARTESIAN_POINT ( 'NONE',  ( 18.50000000000000000, 86.87843438503968230, -199.3967801207316484 ) ) ;
#136368=CARTESIAN_POINT ( 'NONE',  ( 23.25000000000000000, 78.50726470275242264, -228.6618886302502176 ) ) ;
#136371=AXIS2_PLACEMENT_3D ( 'NONE', #129668, #111398, #90530 ) ;
#136373=DIRECTION ( 'NONE',  ( 0.000000000000000000, -0.9651348961777379554, 0.2617529984164210233 ) ) ;
#136388=ORIENTED_EDGE ( 'NONE', *, *, #101668, .T. ) ;
#136403=DIRECTION ( 'NONE',  ( 1.000000000000000000, 0.000000000000000000, 0.000000000000000000 ) ) ;
#136406=CARTESIAN_POINT ( 'NONE',  ( -18.50000000000000000, 72.10920423909969657, -225.0008277277438822 ) ) ;
#136417=DIRECTION ( 'NONE',  ( 0.000000000000000000, -0.2617529984165031243, -0.9651348961777157509 ) ) ;
#136426=DIRECTION ( 'NONE',  ( 1.000000000000000000, 7.049440681616512959E-16, -1.911869773728117674E-16 ) ) ;
#136435=VERTEX_POINT ( 'NONE', #74132 ) ;
#136464=VECTOR ( 'NONE', #128256, 1000.000000000000000 ) ;
#136539=EDGE_CURVE ( 'NONE', #193203, #248447, #56050, .T. ) ;
#136540=CARTESIAN_POINT ( 'NONE',  ( 21.07928932188134397, 61.09751618602743406, -234.2940654522722639 ) ) ;
#136551=CIRCLE ( 'NONE', #40755, 0.09999999999999961697 ) ;
#136561=ORIENTED_EDGE ( 'NONE', *, *, #38212, .F. ) ;
#136566=CARTESIAN_POINT ( 'NONE',  ( 21.05000000000000426, 58.86930248204848937, -225.7185241593660692 ) ) ;
#136577=CIRCLE ( 'NONE', #40946, 0.1999999999999945155 ) ;
#136597=CIRCLE ( 'NONE', #169983, 0.09999999999999935330 ) ;
#136653=CARTESIAN_POINT ( 'NONE',  ( -23.25000000000000000, 62.92003201576280702, -207.2439188921395896 ) ) ;
#136661=CARTESIAN_POINT ( 'NONE',  ( -20.94999999999999929, 79.13126459505528487, -235.8705213229730191 ) ) ;
#136687=CARTESIAN_POINT ( 'NONE',  ( -21.14999999999999858, 60.91865828504416669, -234.1430899377568551 ) ) ;
#136701=LINE ( 'NONE', #196677, #45268 ) ;
#136715=ORIENTED_EDGE ( 'NONE', *, *, #89469, .T. ) ;
#136744=ORIENTED_EDGE ( 'NONE', *, *, #90883, .F. ) ;
#136746=EDGE_LOOP ( 'NONE', ( #33875, #81097, #232030, #62567 ) ) ;
#136786=AXIS2_PLACEMENT_3D ( 'NONE', #176826, #253759, #19006 ) ;
#136802=DIRECTION ( 'NONE',  ( 1.000000000000000000, 0.000000000000000000, 0.000000000000000000 ) ) ;
#136803=CARTESIAN_POINT ( 'NONE',  ( 18.52928932188133970, 62.89880023679608456, -212.5588616714909733 ) ) ;
#136851=TOROIDAL_SURFACE ( 'NONE', #36943, 0.4000000000000012990, 0.1000000000000000056 ) ;
#136880=DIRECTION ( 'NONE',  ( 0.000000000000000000, -0.9651348961777157509, 0.2617529984165031243 ) ) ;
#136882=LINE ( 'NONE', #254241, #211903 ) ;
#136901=CARTESIAN_POINT ( 'NONE',  ( -20.00857864376270001, 61.41373750439892376, -221.5848334931070553 ) ) ;
#136914=EDGE_CURVE ( 'NONE', #50451, #122095, #56234, .T. ) ;
#136923=ORIENTED_EDGE ( 'NONE', *, *, #108141, .T. ) ;
#136988=CARTESIAN_POINT ( 'NONE',  ( 21.05000000000390159, 60.86818597347610904, -225.3357246298605219 ) ) ;
#136994=CARTESIAN_POINT ( 'NONE',  ( -23.15000000000000213, 76.00000000001126921, -203.5231074845248997 ) ) ;
#137025=EDGE_CURVE ( 'NONE', #197069, #12386, #64799, .T. ) ;
#137048=ORIENTED_EDGE ( 'NONE', *, *, #96921, .T. ) ;
#137064=DIRECTION ( 'NONE',  ( 0.000000000000000000, 0.2617529984165024026, 0.9651348961777158619 ) ) ;
#137090=VERTEX_POINT ( 'NONE', #147572 ) ;
#137094=VERTEX_POINT ( 'NONE', #10636 ) ;
#137113=ORIENTED_EDGE ( 'NONE', *, *, #48774, .T. ) ;
#137161=EDGE_CURVE ( 'NONE', #107947, #143687, #43959, .T. ) ;
#137193=DIRECTION ( 'NONE',  ( 0.000000000000000000, 0.2617529984165030132, 0.9651348961777158619 ) ) ;
#137195=CARTESIAN_POINT ( 'NONE',  ( 18.43709777086140278, 87.08727414655709254, -199.6327537731849873 ) ) ;
#137201=ORIENTED_EDGE ( 'NONE', *, *, #103532, .T. ) ;
#137225=ORIENTED_EDGE ( 'NONE', *, *, #21415, .T. ) ;
#137230=DIRECTION ( 'NONE',  ( 0.000000000000000000, -0.2617529984165031243, -0.9651348961777157509 ) ) ;
#137231=CARTESIAN_POINT ( 'NONE',  ( -20.94999999999999929, 79.38304387823771435, -235.9388060597213723 ) ) ;
#137236=CARTESIAN_POINT ( 'NONE',  ( -20.94999999999999929, 86.32947205150912851, -209.3293116780858156 ) ) ;
#137243=AXIS2_PLACEMENT_3D ( 'NONE', #77879, #157470, #118316 ) ;
#137283=AXIS2_PLACEMENT_3D ( 'NONE', #73103, #254246, #33984 ) ;
#137286=DIRECTION ( 'NONE',  ( -1.000000000000000000, 7.049440681616512959E-16, -1.911869773728117674E-16 ) ) ;
#137313=ORIENTED_EDGE ( 'NONE', *, *, #44147, .F. ) ;
#137339=DIRECTION ( 'NONE',  ( 0.000000000000000000, 0.2558827019434435912, -0.9667078373770033872 ) ) ;
#137357=FACE_OUTER_BOUND ( 'NONE', #191776, .T. ) ;
#137360=CARTESIAN_POINT ( 'NONE',  ( 20.85000000000000142, 80.78317333349157536, -192.9003134612049166 ) ) ;
#137363=CARTESIAN_POINT ( 'NONE',  ( 21.05000000000000071, 86.27712145182582049, -209.5223386573213702 ) ) ;
#137388=VECTOR ( 'NONE', #187377, 1000.000000000000000 ) ;
#137410=DIRECTION ( 'NONE',  ( 0.000000000000000000, 0.2617529984164506107, 0.9651348961777299618 ) ) ;
#137458=EDGE_LOOP ( 'NONE', ( #216262, #85626, #59336, #236726 ) ) ;
#137465=ORIENTED_EDGE ( 'NONE', *, *, #48807, .F. ) ;
#137475=CYLINDRICAL_SURFACE ( 'NONE', #78641, 7.900000000000010125 ) ;
#137558=EDGE_LOOP ( 'NONE', ( #8839, #193483, #158915, #240355 ) ) ;
#137596=CARTESIAN_POINT ( 'NONE',  ( -20.85000000000000142, 76.00000000001126921, -203.5231074845248997 ) ) ;
#137597=FACE_OUTER_BOUND ( 'NONE', #100179, .T. ) ;
#137611=CARTESIAN_POINT ( 'NONE',  ( -23.25000000000000000, 68.76204065042992397, -214.3562485088912126 ) ) ;
#137613=EDGE_CURVE ( 'NONE', #188240, #151423, #153737, .T. ) ;
#137620=CIRCLE ( 'NONE', #75134, 0.5000000000000014433 ) ;
#137623=DIRECTION ( 'NONE',  ( 1.000000000000000000, 0.000000000000000000, 0.000000000000000000 ) ) ;
#137626=ORIENTED_EDGE ( 'NONE', *, *, #226731, .T. ) ;
#137627=DIRECTION ( 'NONE',  ( 1.000000000000000000, 0.000000000000000000, 0.000000000000000000 ) ) ;
#137636=ORIENTED_EDGE ( 'NONE', *, *, #208106, .F. ) ;
#137674=AXIS2_PLACEMENT_3D ( 'NONE', #180472, #53144, #16610 ) ;
#137710=AXIS2_PLACEMENT_3D ( 'NONE', #251360, #135251, #213512 ) ;
#137715=CARTESIAN_POINT ( 'NONE',  ( 20.94999999999999929, 61.94127660284455317, -221.8315191551248517 ) ) ;
#137722=ADVANCED_FACE ( 'NONE', ( #242188 ), #25718, .T. ) ;
#137749=VERTEX_POINT ( 'NONE', #47824 ) ;
#137775=AXIS2_PLACEMENT_3D ( 'NONE', #203201, #46681, #24595 ) ;
#137789=VERTEX_POINT ( 'NONE', #184784 ) ;
#137794=ORIENTED_EDGE ( 'NONE', *, *, #90356, .F. ) ;
#137800=DIRECTION ( 'NONE',  ( 0.000000000000000000, -0.9651348961777157509, 0.2617529984165031243 ) ) ;
#137802=ORIENTED_EDGE ( 'NONE', *, *, #15526, .T. ) ;
#137806=CARTESIAN_POINT ( 'NONE',  ( -21.05000000000000071, 76.00000000001126921, -203.5231074845248997 ) ) ;
#137814=CIRCLE ( 'NONE', #171200, 0.1000000000000066530 ) ;
#137921=ORIENTED_EDGE ( 'NONE', *, *, #171813, .F. ) ;
#137928=CARTESIAN_POINT ( 'NONE',  ( 23.14999999999999503, 52.91185528119409298, -244.1460391050142675 ) ) ;
#137933=CIRCLE ( 'NONE', #225221, 0.09999999999999543976 ) ;
#137953=LINE ( 'NONE', #19309, #73094 ) ;
#137969=DIRECTION ( 'NONE',  ( 1.000000000000000000, 0.000000000000000000, 0.000000000000000000 ) ) ;
#137975=ORIENTED_EDGE ( 'NONE', *, *, #234430, .T. ) ;
#137978=CARTESIAN_POINT ( 'NONE',  ( 21.53752568617683849, 60.65518257771599764, -234.1741829020553780 ) ) ;
#137984=ADVANCED_FACE ( 'NONE', ( #51670 ), #131231, .T. ) ;
#138004=CARTESIAN_POINT ( 'NONE',  ( -21.05000000000000071, 72.02722222756959525, -225.1832529173024398 ) ) ;
#138022=ORIENTED_EDGE ( 'NONE', *, *, #52221, .F. ) ;
#138028=ORIENTED_EDGE ( 'NONE', *, *, #158333, .F. ) ;
#138038=CIRCLE ( 'NONE', #175498, 0.09999999999999939493 ) ;
#138045=ORIENTED_EDGE ( 'NONE', *, *, #170737, .F. ) ;
#138066=CIRCLE ( 'NONE', #25659, 0.09999999999999939493 ) ;
#138116=CARTESIAN_POINT ( 'NONE',  ( -22.39999999999999858, 65.09550114356427741, -243.3481044654562879 ) ) ;
#138131=EDGE_CURVE ( 'NONE', #175678, #164109, #18979, .T. ) ;
#138136=EDGE_CURVE ( 'NONE', #74229, #234918, #98475, .T. ) ;
#138174=CARTESIAN_POINT ( 'NONE',  ( -22.47071067811865319, 67.23127455305841238, -235.8551265064783991 ) ) ;
#138198=EDGE_LOOP ( 'NONE', ( #194697, #8519, #161351, #229351, #209754, #249075, #155481, #126532, #80083, #162417 ) ) ;
#138201=EDGE_CURVE ( 'NONE', #204625, #206475, #175661, .T. ) ;
#138215=CARTESIAN_POINT ( 'NONE',  ( 21.05000000000000071, 65.56210617110382088, -241.8873743484695353 ) ) ;
#138222=ORIENTED_EDGE ( 'NONE', *, *, #25154, .F. ) ;
#138231=DIRECTION ( 'NONE',  ( 0.000000000000000000, -0.2617529984167792922, -0.9651348961776409219 ) ) ;
#138235=ORIENTED_EDGE ( 'NONE', *, *, #199378, .T. ) ;
#138240=VECTOR ( 'NONE', #53126, 999.9999999999998863 ) ;
#138248=ORIENTED_EDGE ( 'NONE', *, *, #227989, .F. ) ;
#138296=CARTESIAN_POINT ( 'NONE',  ( 23.24999999999999289, 55.91711482281188950, -232.6830152854666949 ) ) ;
#138300=ADVANCED_FACE ( 'NONE', ( #193485 ), #117926, .F. ) ;
#138344=ORIENTED_EDGE ( 'NONE', *, *, #216275, .T. ) ;
#138350=EDGE_CURVE ( 'NONE', #212838, #61516, #109745, .T. ) ;
#138379=DIRECTION ( 'NONE',  ( 2.940209281316622002E-16, 0.9651348961777150848, -0.2617529984165055112 ) ) ;
#138392=ORIENTED_EDGE ( 'NONE', *, *, #202058, .F. ) ;
#138393=AXIS2_PLACEMENT_3D ( 'NONE', #46417, #25596, #185940 ) ;
#138398=CIRCLE ( 'NONE', #844, 0.5000000000000051070 ) ;
#138413=ORIENTED_EDGE ( 'NONE', *, *, #63548, .F. ) ;
#138423=CIRCLE ( 'NONE', #121898, 11.70000000000000817 ) ;
#138425=DIRECTION ( 'NONE',  ( 0.000000000000000000, 0.2617529984165031243, 0.9651348961777157509 ) ) ;
#138432=VERTEX_POINT ( 'NONE', #237732 ) ;
#138445=CARTESIAN_POINT ( 'NONE',  ( 20.94999999999999929, 64.11611521369653133, -222.3177418886732539 ) ) ;
#138461=PLANE ( 'NONE',  #252708 ) ;
#138471=EDGE_CURVE ( 'NONE', #132077, #257696, #82474, .T. ) ;
#138486=CARTESIAN_POINT ( 'NONE',  ( 20.04142135623730070, 52.81534179157633702, -244.1198638051726277 ) ) ;
#138519=CARTESIAN_POINT ( 'NONE',  ( -23.25000000000000000, 86.52890073500824997, -209.5906233940697234 ) ) ;
#138579=ORIENTED_EDGE ( 'NONE', *, *, #125693, .F. ) ;
#138583=AXIS2_PLACEMENT_3D ( 'NONE', #85180, #163477, #243001 ) ;
#138588=AXIS2_PLACEMENT_3D ( 'NONE', #106240, #206651, #127108 ) ;
#138604=ORIENTED_EDGE ( 'NONE', *, *, #131669, .F. ) ;
#138609=VERTEX_POINT ( 'NONE', #192860 ) ;
#138654=ORIENTED_EDGE ( 'NONE', *, *, #21294, .F. ) ;
#138661=CARTESIAN_POINT ( 'NONE',  ( -20.54999999999999716, 66.36210077474692071, -222.8232602954134336 ) ) ;
#138698=CIRCLE ( 'NONE', #38800, 0.1999999999999945155 ) ;
#138722=ADVANCED_FACE ( 'NONE', ( #100131 ), #34971, .F. ) ;
#138735=CARTESIAN_POINT ( 'NONE',  ( 21.12230431290518951, 65.53595890941556945, -242.0861857336640526 ) ) ;
#138747=CIRCLE ( 'NONE', #192780, 0.1999999999999945155 ) ;
#138753=DIRECTION ( 'NONE',  ( 0.000000000000000000, 0.2617529984165026247, 0.9651348961777158619 ) ) ;
#138759=DIRECTION ( 'NONE',  ( -0.000000000000000000, 0.2617529984165031243, 0.9651348961777157509 ) ) ;
#138774=FACE_OUTER_BOUND ( 'NONE', #180268, .T. ) ;
#138802=ORIENTED_EDGE ( 'NONE', *, *, #78791, .F. ) ;
#138825=EDGE_LOOP ( 'NONE', ( #9822, #211003, #221966, #178744 ) ) ;
#138829=VERTEX_POINT ( 'NONE', #2326 ) ;
#138852=ORIENTED_EDGE ( 'NONE', *, *, #1025, .F. ) ;
#138866=AXIS2_PLACEMENT_3D ( 'NONE', #76125, #193527, #35749 ) ;
#138879=LINE ( 'NONE', #60649, #232315 ) ;
#138894=DIRECTION ( 'NONE',  ( 0.000000000000000000, -0.9651348961777155289, 0.2617529984165036794 ) ) ;
#138898=EDGE_CURVE ( 'NONE', #159529, #198941, #126509, .T. ) ;
#138912=EDGE_CURVE ( 'NONE', #216037, #124124, #183557, .T. ) ;
#138939=CARTESIAN_POINT ( 'NONE',  ( -20.54999999999999716, 76.00000000001126921, -203.5231074845248997 ) ) ;
#138961=AXIS2_PLACEMENT_3D ( 'NONE', #23865, #25141, #100754 ) ;
#138978=CIRCLE ( 'NONE', #68107, 0.1000000000000090677 ) ;
#138981=DIRECTION ( 'NONE',  ( -0.000000000000000000, -0.2617529984165030132, -0.9651348961777157509 ) ) ;
#138997=CARTESIAN_POINT ( 'NONE',  ( 23.14999999999999503, 52.81534179157632991, -244.1198638051726277 ) ) ;
#139048=LINE ( 'NONE', #218603, #7604 ) ;
#139081=AXIS2_PLACEMENT_3D ( 'NONE', #195320, #38792, #16672 ) ;
#139094=ORIENTED_EDGE ( 'NONE', *, *, #206547, .T. ) ;
#139120=LINE ( 'NONE', #140427, #25615 ) ;
#139148=EDGE_CURVE ( 'NONE', #235804, #130099, #55928, .T. ) ;
#139161=ORIENTED_EDGE ( 'NONE', *, *, #145100, .F. ) ;
#139171=ORIENTED_EDGE ( 'NONE', *, *, #91580, .T. ) ;
#139180=ADVANCED_FACE ( 'NONE', ( #215927 ), #62023, .T. ) ;
#139187=LINE ( 'NONE', #174550, #30336 ) ;
#139190=ORIENTED_EDGE ( 'NONE', *, *, #206597, .T. ) ;
#139212=CIRCLE ( 'NONE', #185035, 0.2000000000000042577 ) ;
#139224=CARTESIAN_POINT ( 'NONE',  ( 20.94999999999999929, 77.07318729351892728, -199.5660544101962728 ) ) ;
#139229=DIRECTION ( 'NONE',  ( 0.000000000000000000, 0.2617529984165031243, 0.9651348961777157509 ) ) ;
#139259=ORIENTED_EDGE ( 'NONE', *, *, #99096, .F. ) ;
#139316=VERTEX_POINT ( 'NONE', #144093 ) ;
#139317=CIRCLE ( 'NONE', #147723, 0.09999999999999939493 ) ;
#139337=TOROIDAL_SURFACE ( 'NONE', #172731, 0.6000000000000009770, 0.1000000000000000056 ) ;
#139350=DIRECTION ( 'NONE',  ( 1.000000000000000000, 0.000000000000000000, 0.000000000000000000 ) ) ;
#139386=DIRECTION ( 'NONE',  ( 1.000000000000000000, 0.000000000000000000, 0.000000000000000000 ) ) ;
#139470=DIRECTION ( 'NONE',  ( 0.000000000000000000, -0.2617529984165013479, -0.9651348961777163060 ) ) ;
#139526=DIRECTION ( 'NONE',  ( -1.000000000000000000, 0.000000000000000000, 0.000000000000000000 ) ) ;
#139563=CARTESIAN_POINT ( 'NONE',  ( 21.14999999999999858, 60.12405517993034465, -221.1314479434109614 ) ) ;
#139580=ADVANCED_FACE ( 'NONE', ( #194828 ), #16188, .F. ) ;
#139603=CIRCLE ( 'NONE', #222825, 11.79999999999999361 ) ;
#139609=CARTESIAN_POINT ( 'NONE',  ( 18.49999999999999645, 68.48451787451661232, -224.2224406095231757 ) ) ;
#139629=DIRECTION ( 'NONE',  ( 1.000000000000000000, 0.000000000000000000, 0.000000000000000000 ) ) ;
#139670=VECTOR ( 'NONE', #62285, 1000.000000000000114 ) ;
#139675=CIRCLE ( 'NONE', #247846, 0.1000000000000124678 ) ;
#139694=DIRECTION ( 'NONE',  ( -0.000000000000000000, -0.2617529984165030132, -0.9651348961777157509 ) ) ;
#139744=ADVANCED_FACE ( 'NONE', ( #229637 ), #110970, .T. ) ;
#139748=DIRECTION ( 'NONE',  ( 0.000000000000000000, 0.2617529984165152257, 0.9651348961777124202 ) ) ;
#139756=EDGE_CURVE ( 'NONE', #148962, #215885, #159819, .T. ) ;
#139758=ORIENTED_EDGE ( 'NONE', *, *, #36684, .T. ) ;
#139785=DIRECTION ( 'NONE',  ( 1.000000000000000000, 0.000000000000000000, 0.000000000000000000 ) ) ;
#139794=EDGE_LOOP ( 'NONE', ( #21328, #120917, #39912, #242268 ) ) ;
#139798=ORIENTED_EDGE ( 'NONE', *, *, #227017, .F. ) ;
#139799=DIRECTION ( 'NONE',  ( 0.000000000000000000, 0.2617529984165152257, 0.9651348961777124202 ) ) ;
#139815=AXIS2_PLACEMENT_3D ( 'NONE', #142518, #85091, #43440 ) ;
#139833=CARTESIAN_POINT ( 'NONE',  ( 21.09793522318404158, 60.08423627381927901, -221.2353571599898032 ) ) ;
#139906=ORIENTED_EDGE ( 'NONE', *, *, #91803, .T. ) ;
#139925=ORIENTED_EDGE ( 'NONE', *, *, #256277, .F. ) ;
#139943=CARTESIAN_POINT ( 'NONE',  ( -21.14999999999999858, 57.66663670110953888, -226.2321832927624712 ) ) ;
#139978=CIRCLE ( 'NONE', #56580, 11.64999999999998970 ) ;
#140012=DIRECTION ( 'NONE',  ( 0.000000000000000000, 0.2617529984165031243, 0.9651348961777158619 ) ) ;
#140020=CARTESIAN_POINT ( 'NONE',  ( -20.85000000000000142, 70.22659352830977753, -197.9852579278363578 ) ) ;
#140039=DIRECTION ( 'NONE',  ( 0.000000000000000000, 0.2617529984165036239, 0.9651348961777156399 ) ) ;
#140053=CARTESIAN_POINT ( 'NONE',  ( -20.85000000000000142, 64.75617845954087670, -200.4736850529726269 ) ) ;
#140062=CARTESIAN_POINT ( 'NONE',  ( -21.05000000000000071, 68.59681812508419796, -224.1344059333694361 ) ) ;
#140072=AXIS2_PLACEMENT_3D ( 'NONE', #55332, #133621, #194906 ) ;
#140075=VECTOR ( 'NONE', #203208, 1000.000000000000000 ) ;
#140116=CARTESIAN_POINT ( 'NONE',  ( -20.54999999999999716, 68.71679287596359131, -222.9654461259447658 ) ) ;
#140121=ORIENTED_EDGE ( 'NONE', *, *, #217922, .F. ) ;
#140159=DIRECTION ( 'NONE',  ( 0.000000000000000000, 0.2617529984165152257, 0.9651348961777124202 ) ) ;
#140175=ORIENTED_EDGE ( 'NONE', *, *, #119771, .F. ) ;
#140188=ADVANCED_FACE ( 'NONE', ( #39211, #198249, #156605 ), #177445, .F. ) ;
#140232=ORIENTED_EDGE ( 'NONE', *, *, #213416, .T. ) ;
#140251=CARTESIAN_POINT ( 'NONE',  ( 23.14999999999999858, 62.99095723518624368, -207.1734234082435080 ) ) ;
#140271=TOROIDAL_SURFACE ( 'NONE', #27912, 4.099999999999999645, 0.1000000000000000056 ) ;
#140274=CARTESIAN_POINT ( 'NONE',  ( 20.94999999999999574, 68.20313450767837082, -227.8297066677462794 ) ) ;
#140283=DIRECTION ( 'NONE',  ( -3.265361837132813586E-16, -0.9651348961777156399, 0.2617529984165041235 ) ) ;
#140288=EDGE_CURVE ( 'NONE', #28102, #85530, #202115, .T. ) ;
#140300=DIRECTION ( 'NONE',  ( 0.000000000000000000, 0.2617529984165031243, 0.9651348961777157509 ) ) ;
#140312=ORIENTED_EDGE ( 'NONE', *, *, #8809, .F. ) ;
#140313=CARTESIAN_POINT ( 'NONE',  ( 23.14999999999999503, 64.23880400315596262, -222.2474036988971307 ) ) ;
#140369=CARTESIAN_POINT ( 'NONE',  ( -22.39999999999999858, 67.13476106344063510, -235.8289512066367024 ) ) ;
#140373=AXIS2_PLACEMENT_3D ( 'NONE', #122716, #83530, #62724 ) ;
#140377=CYLINDRICAL_SURFACE ( 'NONE', #57381, 0.09999999999999543976 ) ;
#140395=ORIENTED_EDGE ( 'NONE', *, *, #134714, .T. ) ;
#140404=CIRCLE ( 'NONE', #185821, 4.100000000000008527 ) ;
#140427=CARTESIAN_POINT ( 'NONE',  ( 20.94999999999999929, 65.71172719659838890, -223.0701118083454446 ) ) ;
#140428=EDGE_CURVE ( 'NONE', #123153, #208014, #64143, .T. ) ;
#140431=CIRCLE ( 'NONE', #48859, 0.09999999999999939493 ) ;
#140443=CARTESIAN_POINT ( 'NONE',  ( 21.14999999999999858, 64.04577702392042227, -222.1950530992138226 ) ) ;
#140453=CIRCLE ( 'NONE', #252891, 7.900000000000010125 ) ;
#140485=VERTEX_POINT ( 'NONE', #256240 ) ;
#140488=DIRECTION ( 'NONE',  ( 0.000000000000000000, 0.2617529984165152257, 0.9651348961777124202 ) ) ;
#140523=CARTESIAN_POINT ( 'NONE',  ( -21.14999999999999858, 55.89093952297024970, -232.7795287750844579 ) ) ;
#140541=EDGE_CURVE ( 'NONE', #207046, #22691, #189402, .T. ) ;
#140606=ORIENTED_EDGE ( 'NONE', *, *, #3754, .T. ) ;
#140624=EDGE_LOOP ( 'NONE', ( #147878, #255976, #206843, #57529 ) ) ;
#140645=DIRECTION ( 'NONE',  ( 0.000000000000000000, -0.2617529984165152257, -0.9651348961777124202 ) ) ;
#140655=CARTESIAN_POINT ( 'NONE',  ( 20.94999999999999929, 67.63082410804655353, -211.8415745842588649 ) ) ;
#140664=EDGE_CURVE ( 'NONE', #35438, #252099, #231331, .T. ) ;
#140681=ORIENTED_EDGE ( 'NONE', *, *, #203497, .T. ) ;
#140693=B_SPLINE_CURVE_WITH_KNOTS ( 'NONE', 3,
 ( #119914, #237268, #18216, #217668, #160321, #121202 ),
 .UNSPECIFIED., .F., .F.,
 ( 4, 2, 4 ),
 ( 0.000000000000000000, 0.0001569047307838622170, 0.0003138094615677244339 ),
 .UNSPECIFIED. ) ;
#140695=VERTEX_POINT ( 'NONE', #173960 ) ;
#140715=EDGE_LOOP ( 'NONE', ( #24112, #77364, #23312 ) ) ;
#140728=FACE_OUTER_BOUND ( 'NONE', #1994, .T. ) ;
#140739=CARTESIAN_POINT ( 'NONE',  ( -20.54999999999999716, 63.44052078637213299, -222.1345147897817185 ) ) ;
#140753=AXIS2_PLACEMENT_3D ( 'NONE', #132317, #93190, #171488 ) ;
#140830=CARTESIAN_POINT ( 'NONE',  ( 18.49999999999998934, 62.46583972339646351, -208.9186153945276487 ) ) ;
#140851=EDGE_CURVE ( 'NONE', #202597, #193142, #35498, .T. ) ;
#140885=VECTOR ( 'NONE', #98955, 1000.000000000000000 ) ;
#140886=AXIS2_PLACEMENT_3D ( 'NONE', #139609, #83479, #180057 ) ;
#140900=CARTESIAN_POINT ( 'NONE',  ( -21.37071067811865532, 64.97802595716100882, -213.3299907329700318 ) ) ;
#140914=ORIENTED_EDGE ( 'NONE', *, *, #119837, .T. ) ;
#140922=DIRECTION ( 'NONE',  ( 1.000000000000000000, 0.000000000000000000, 0.000000000000000000 ) ) ;
#140929=VERTEX_POINT ( 'NONE', #102044 ) ;
#140954=CLOSED_SHELL ( 'NONE', ( #125449, #195887, #224364, #179453, #217914, #3780, #82190, #214282, #147364, #164489, #55296, #80285, #192190, #11386, #109116, #112112, #55731, #34189, #129992, #172528, #158152, #2127, #57027, #130995, #23904, #26664, #205120, #23977, #203352, #216162, #44886, #66738, #92013, #246714, #213720, #15336, #14733, #108235, #216665, #33651, #2916, #43220, #46735, #159439, #59904, #255043, #84469, #80099, #131466, #115019, #21465, #167643, #64455, #198271, #216557, #13238, #135054, #203696, #210196, #130910, #146478, #48798, #105598, #173593, #241793, #92357, #96757, #86240, #173142, #88140, #140188, #110890, #78041, #220797, #157730, #26179, #65802, #127856, #55418, #251874, #77847, #252541, #80793, #129300, #15269, #71675, #182297, #84076, #250274, #226979, #74123, #109282, #485, #103519, #4215, #209993, #28841, #162540, #23910, #32361, #238068, #2601, #207828, #88212, #108216, #242232, #25850, #212695, #93656, #191602, #67016, #103295, #111767, #213608, #254236, #5204, #182743, #6677, #135380, #247742, #44997, #85571, #6816, #209083, #139180, #19696, #153637, #132381, #29627, #67541, #235192, #111173, #5039, #67667, #115700, #925, #187834, #125006, #95258, #238748, #134966, #257198, #124873, #6591, #116103, #88680, #109922, #17638, #77262, #12356, #69187, #218282, #195782, #36242, #206253, #220446, #169822, #18014, #52807, #100090, #210479, #102557, #233188, #55222, #219080, #245715, #6272, #128808, #177238, #75997, #44277, #75965, #219391, #143011, #86079, #39132, #221676, #89710, #168552, #138722, #54481, #103623, #13030, #184987, #146808, #9652, #146259, #4864, #232180, #8789, #51490, #61463, #55492, #135185, #618, #214780, #191950, #28173, #96165, #12677, #131056, #5203, #117181, #189214, #159718, #110823, #109162, #243922, #126361, #27337, #105620, #19345, #171879, #158191, #44427, #235770, #146479, #100872, #151215, #226386, #216484, #150525, #113378, #175097, #143702, #235647, #214855, #144146, #182397, #99930, #147426, #106537, #59966, #75881, #41287, #8613, #210840, #107563, #17546, #103742, #109518, #81140, #161281, #53232, #46649, #10974, #208317, #32904, #35382, #4957, #15457, #76145, #51380, #14161, #58103, #56211, #110368, #101286, #219732, #135211, #186476, #128944, #33121, #115332, #69793, #247384, #47361, #122455, #107615, #231095, #29535, #96789, #54451, #252012, #237488, #153316, #120176, #255351, #79973, #118156, #54335, #221164, #125267, #103272, #198837, #137984, #204793, #54303, #157202, #246871, #60915, #133743, #55600, #198194, #79327, #167738, #119367, #76120, #19130, #127140, #34031, #161903, #226025, #67273, #58470, #119890, #188843, #178520, #221389, #77704, #106751, #216356, #106447, #40655, #211784, #137722, #106050, #139744, #204738, #85847, #176520, #44785, #14813, #67893, #116500, #173103, #216789, #55816, #91730, #148586, #165483, #23873, #173719, #61358, #160116, #126966, #94113, #224567, #41861, #150467, #242719, #43411, #213621, #133822, #153230, #249595, #200831, #35712, #17095, #92139, #240367, #160884, #171505, #74410, #27622, #210003, #146026, #129252, #84677, #197331, #49113, #239892, #72739, #187373, #139580, #225041, #231518, #3788, #130318, #209848, #91959, #82894, #213970, #65325, #104269, #145327, #235975, #60555, #28420, #44874, #222208, #29186, #54596, #209868, #159490, #133305, #221236, #228454, #73071, #154794, #225050, #96983, #164941, #161836, #16978, #94612, #51708, #40929, #9690, #178437, #55162, #253686, #72328, #219083, #52870, #178316, #66323, #132853, #18519, #110419, #52080, #246129, #218036, #197030, #228631, #89551, #229350, #170417, #180378, #221228, #33957, #93883, #171078, #79442, #15784, #127103, #197111, #37317, #230179, #131994, #42624, #60363, #156580, #174902, #148574, #127034, #138300, #169436, #208006, #119857, #97612, #91416, #206640, #20868, #100412, #188012, #214280, #207494, #131868, #16567, #248637, #236217, #106657, #3904, #149966, #256254, #107520, #225129, #32626, #235346, #67354, #174270, #8176, #29663, #131525, #181555, #90129, #248136, #153018, #215638, #8466, #181920, #13427, #56369, #254616, #196596, #94263, #237900 ) ) ;
#140956=CARTESIAN_POINT ( 'NONE',  ( 21.05000000000000071, 68.48451787451661232, -224.2224406095231757 ) ) ;
#140967=CIRCLE ( 'NONE', #203315, 0.3999999999999926392 ) ;
#140981=CARTESIAN_POINT ( 'NONE',  ( 22.39999999999999503, 59.71212129423884818, -233.8158665866020272 ) ) ;
#140984=AXIS2_PLACEMENT_3D ( 'NONE', #227509, #122857, #163270 ) ;
#141013=CARTESIAN_POINT ( 'NONE',  ( 21.05000000000000071, 67.23127455305841238, -235.8551265064783991 ) ) ;
#141014=DIRECTION ( 'NONE',  ( -0.000000000000000000, -0.9667078373770160438, -0.2558827019433959071 ) ) ;
#141043=AXIS2_PLACEMENT_3D ( 'NONE', #137363, #216903, #257271 ) ;
#141045=AXIS2_PLACEMENT_3D ( 'NONE', #49418, #5117, #9006 ) ;
#141103=DIRECTION ( 'NONE',  ( 0.000000000000000000, 0.2617529984165033463, 0.9651348961777157509 ) ) ;
#141116=ORIENTED_EDGE ( 'NONE', *, *, #48847, .T. ) ;
#141119=AXIS2_PLACEMENT_3D ( 'NONE', #59923, #37844, #139470 ) ;
#141131=CARTESIAN_POINT ( 'NONE',  ( 19.97071067695804203, 62.37829099644529407, -208.9712820482884581 ) ) ;
#141138=ORIENTED_EDGE ( 'NONE', *, *, #44073, .T. ) ;
#141142=CARTESIAN_POINT ( 'NONE',  ( 20.95512820512820440, 60.15812638745688901, -221.3479132702343009 ) ) ;
#141164=CARTESIAN_POINT ( 'NONE',  ( -23.25000000000000000, 76.00000000001126921, -203.5231074845248997 ) ) ;
#141165=AXIS2_PLACEMENT_3D ( 'NONE', #37821, #213864, #114765 ) ;
#141189=EDGE_LOOP ( 'NONE', ( #226596, #9005, #199142, #3222 ) ) ;
#141218=VERTEX_POINT ( 'NONE', #87 ) ;
#141220=ORIENTED_EDGE ( 'NONE', *, *, #17032, .F. ) ;
#141224=DIRECTION ( 'NONE',  ( -1.000000000000000000, -0.000000000000000000, 0.000000000000000000 ) ) ;
#141238=LINE ( 'NONE', #67792, #174161 ) ;
#141242=ORIENTED_EDGE ( 'NONE', *, *, #192842, .F. ) ;
#141261=AXIS2_PLACEMENT_3D ( 'NONE', #140053, #85198, #160942 ) ;
#141293=CARTESIAN_POINT ( 'NONE',  ( -22.44366136229477249, 64.17290991523515231, -247.0962312331226940 ) ) ;
#141296=FILL_AREA_STYLE ('',( #61754 ) ) ;
#141297=CARTESIAN_POINT ( 'NONE',  ( 20.94999999999999929, 75.50266930301991408, -205.3568637872625686 ) ) ;
#141298=CARTESIAN_POINT ( 'NONE',  ( 21.05000000000000426, 65.52973064315669660, -241.8780481312162749 ) ) ;
#141316=DIRECTION ( 'NONE',  ( 0.000000000000000000, 0.9916376685811618685, -0.1290532225514649800 ) ) ;
#141319=CYLINDRICAL_SURFACE ( 'NONE', #16090, 11.79999999999999361 ) ;
#141377=DIRECTION ( 'NONE',  ( 2.952720810173289112E-16, 0.9651348961777146407, -0.2617529984165072321 ) ) ;
#141392=AXIS2_PLACEMENT_3D ( 'NONE', #27102, #186145, #7500 ) ;
#141426=DIRECTION ( 'NONE',  ( 0.000000000000000000, 0.2617529984164915779, 0.9651348961777187485 ) ) ;
#141446=CARTESIAN_POINT ( 'NONE',  ( -20.94999999999999929, 57.84918772656043728, -226.1321410194968280 ) ) ;
#141455=CIRCLE ( 'NONE', #187279, 0.09999999999999543976 ) ;
#141464=ORIENTED_EDGE ( 'NONE', *, *, #218672, .F. ) ;
#141483=DIRECTION ( 'NONE',  ( -1.000000000000000000, 2.849773892568378313E-16, -7.728835255496647986E-17 ) ) ;
#141487=DIRECTION ( 'NONE',  ( -1.000000000000000000, -0.000000000000000000, 0.000000000000000000 ) ) ;
#141491=EDGE_LOOP ( 'NONE', ( #231760, #35475, #6602, #63993 ) ) ;
#141509=ORIENTED_EDGE ( 'NONE', *, *, #38315, .F. ) ;
#141522=CARTESIAN_POINT ( 'NONE',  ( -18.59999999999999787, 67.23127455305841238, -235.8551265064783991 ) ) ;
#141562=TOROIDAL_SURFACE ( 'NONE', #233184, 11.65000000000000036, 0.1000000000000000056 ) ;
#141578=DIRECTION ( 'NONE',  ( 0.000000000000000000, 0.2617529984165180013, 0.9651348961777117541 ) ) ;
#141657=FACE_OUTER_BOUND ( 'NONE', #129915, .T. ) ;
#141660=DIRECTION ( 'NONE',  ( -1.000000000000000000, 0.000000000000000000, 0.000000000000000000 ) ) ;
#141695=TOROIDAL_SURFACE ( 'NONE', #54204, 11.90000000000000213, 0.1000000000000000056 ) ;
#141704=EDGE_LOOP ( 'NONE', ( #197568, #174377, #155381, #165716 ) ) ;
#141706=LINE ( 'NONE', #60883, #125946 ) ;
#141710=EDGE_CURVE ( 'NONE', #165270, #204719, #80577, .T. ) ;
#141712=CARTESIAN_POINT ( 'NONE',  ( 21.14999999999999858, 60.09787988008869775, -221.2279614330287245 ) ) ;
#141719=LINE ( 'NONE', #896, #253606 ) ;
#141722=FACE_OUTER_BOUND ( 'NONE', #235600, .T. ) ;
#141731=DIRECTION ( 'NONE',  ( 0.000000000000000000, 0.2617529984165152257, 0.9651348961777124202 ) ) ;
#141738=CARTESIAN_POINT ( 'NONE',  ( 23.14999999999999858, 77.93026979236670115, -204.0466134813579231 ) ) ;
#141745=CARTESIAN_POINT ( 'NONE',  ( 23.14999999999999858, 77.04701199367727327, -199.6625678998140359 ) ) ;
#141758=CARTESIAN_POINT ( 'NONE',  ( 20.94999999999999574, 79.28653038861995128, -235.9126307598797325 ) ) ;
#141759=EDGE_CURVE ( 'NONE', #222651, #172976, #173249, .T. ) ;
#141767=DIRECTION ( 'NONE',  ( 0.000000000000000000, -0.9209589331071864615, 0.3896596508878908960 ) ) ;
#141771=ORIENTED_EDGE ( 'NONE', *, *, #207671, .F. ) ;
#141815=ORIENTED_EDGE ( 'NONE', *, *, #154989, .F. ) ;
#141822=DIRECTION ( 'NONE',  ( -1.000000000000000000, -0.000000000000000000, -0.000000000000000000 ) ) ;
#141849=CARTESIAN_POINT ( 'NONE',  ( -20.85000000000000142, 80.78317333349157536, -192.9003134612049166 ) ) ;
#141850=AXIS2_PLACEMENT_3D ( 'NONE', #157935, #117484, #57480 ) ;
#141854=CIRCLE ( 'NONE', #158467, 0.1000000000000124678 ) ;
#141862=ORIENTED_EDGE ( 'NONE', *, *, #161303, .T. ) ;
#141864=AXIS2_PLACEMENT_3D ( 'NONE', #128827, #50532, #11452 ) ;
#141865=CARTESIAN_POINT ( 'NONE',  ( 21.00000000000000000, 61.05385884576949707, -221.3836188041226762 ) ) ;
#141922=TOROIDAL_SURFACE ( 'NONE', #33656, 12.77500000000000036, 0.1000000000000000056 ) ;
#141935=DIRECTION ( 'NONE',  ( 0.000000000000000000, 0.2617529984165031243, 0.9651348961777157509 ) ) ;
#141948=EDGE_LOOP ( 'NONE', ( #256404, #177113, #236808, #41603 ) ) ;
#141960=ORIENTED_EDGE ( 'NONE', *, *, #146174, .F. ) ;
#142001=CARTESIAN_POINT ( 'NONE',  ( 21.05000000000000071, 61.94127660284455317, -221.8315191551248517 ) ) ;
#142009=CARTESIAN_POINT ( 'NONE',  ( -20.64999999999999858, 63.56320957583155717, -222.0641766000055668 ) ) ;
#142063=ORIENTED_EDGE ( 'NONE', *, *, #52596, .T. ) ;
#142090=ORIENTED_EDGE ( 'NONE', *, *, #95234, .T. ) ;
#142097=EDGE_CURVE ( 'NONE', #116117, #12050, #158582, .T. ) ;
#142136=ORIENTED_EDGE ( 'NONE', *, *, #120818, .T. ) ;
#142157=CARTESIAN_POINT ( 'NONE',  ( -20.54999999999999716, 81.80425911359037627, -227.0113082700774783 ) ) ;
#142169=DIRECTION ( 'NONE',  ( -1.000000000000000000, 0.000000000000000000, 0.000000000000000000 ) ) ;
#142178=AXIS2_PLACEMENT_3D ( 'NONE', #229782, #51114, #152851 ) ;
#142181=DIRECTION ( 'NONE',  ( 0.000000000000000000, 0.2617529984165174461, 0.9651348961777118651 ) ) ;
#142186=AXIS2_PLACEMENT_3D ( 'NONE', #85322, #104872, #207899 ) ;
#142195=CIRCLE ( 'NONE', #233801, 0.1000000000000124678 ) ;
#142202=DIRECTION ( 'NONE',  ( 1.000000000000000000, 0.000000000000000000, 0.000000000000000000 ) ) ;
#142240=LINE ( 'NONE', #39321, #12924 ) ;
#142245=ORIENTED_EDGE ( 'NONE', *, *, #205164, .F. ) ;
#142258=ORIENTED_EDGE ( 'NONE', *, *, #221862, .F. ) ;
#142261=VERTEX_POINT ( 'NONE', #251887 ) ;
#142307=CARTESIAN_POINT ( 'NONE',  ( 18.59999999999999787, 84.16003609933891028, -218.3250942044780345 ) ) ;
#142318=CARTESIAN_POINT ( 'NONE',  ( 21.05000000000000071, 59.13236860818124541, -225.8959333647716505 ) ) ;
#142337=ORIENTED_EDGE ( 'NONE', *, *, #243428, .T. ) ;
#142339=ORIENTED_EDGE ( 'NONE', *, *, #56374, .F. ) ;
#142370=FACE_OUTER_BOUND ( 'NONE', #221718, .T. ) ;
#142391=CARTESIAN_POINT ( 'NONE',  ( -21.05000000000000071, 65.56235145718194701, -241.8874454306706525 ) ) ;
#142396=FACE_OUTER_BOUND ( 'NONE', #174307, .T. ) ;
#142416=B_SPLINE_CURVE_WITH_KNOTS ( 'NONE', 3,
 ( #89655, #210904, #152245, #153550 ),
 .UNSPECIFIED., .F., .F.,
 ( 4, 4 ),
 ( 0.000000000000000000, 0.0001048066582182593560 ),
 .UNSPECIFIED. ) ;
#142442=DIRECTION ( 'NONE',  ( 1.000000000000000000, -3.151514657663852580E-16, 8.547182517843351137E-17 ) ) ;
#142478=CARTESIAN_POINT ( 'NONE',  ( -23.25000000000000000, 79.08634564045905790, -228.8189404293001132 ) ) ;
#142479=ORIENTED_EDGE ( 'NONE', *, *, #162870, .F. ) ;
#142496=ORIENTED_EDGE ( 'NONE', *, *, #90933, .T. ) ;
#142518=CARTESIAN_POINT ( 'NONE',  ( -20.64999999999999858, 82.48249193998721296, -215.5326005316167084 ) ) ;
#142527=VECTOR ( 'NONE', #139350, 1000.000000000000000 ) ;
#142543=DIRECTION ( 'NONE',  ( -1.000000000000000000, 0.000000000000000000, 0.000000000000000000 ) ) ;
#142564=VERTEX_POINT ( 'NONE', #226883 ) ;
#142607=DIRECTION ( 'NONE',  ( 0.000000000000000000, 0.9667078373770114919, 0.2558827019434133931 ) ) ;
#142612=VERTEX_POINT ( 'NONE', #173385 ) ;
#142629=EDGE_CURVE ( 'NONE', #160519, #151240, #54660, .T. ) ;
#142647=DIRECTION ( 'NONE',  ( -1.000000000000000000, -0.000000000000000000, -0.000000000000000000 ) ) ;
#142651=DIRECTION ( 'NONE',  ( -1.000000000000000000, 2.849773892568378313E-16, -7.728835255496647986E-17 ) ) ;
#142663=TOROIDAL_SURFACE ( 'NONE', #30275, 7.800000000000000711, 0.1000000000000000056 ) ;
#142669=CARTESIAN_POINT ( 'NONE',  ( 21.53551880898956838, 60.65712384523044420, -234.1747044932786253 ) ) ;
#142678=EDGE_CURVE ( 'NONE', #146093, #221590, #129081, .T. ) ;
#142772=ORIENTED_EDGE ( 'NONE', *, *, #91717, .F. ) ;
#142797=ORIENTED_EDGE ( 'NONE', *, *, #45184, .T. ) ;
#142918=DIRECTION ( 'NONE',  ( 0.000000000000000000, -0.2617529984165024026, -0.9651348961777158619 ) ) ;
#142921=DIRECTION ( 'NONE',  ( 0.000000000000000000, -0.2617529984163859957, -0.9651348961777475033 ) ) ;
#142924=EDGE_CURVE ( 'NONE', #58200, #76073, #257082, .T. ) ;
#142932=CIRCLE ( 'NONE', #30553, 7.720710678118671844 ) ;
#142946=TOROIDAL_SURFACE ( 'NONE', #92896, 7.800000000000000711, 0.1000000000000000056 ) ;
#142952=CARTESIAN_POINT ( 'NONE',  ( 18.59999999999999787, 78.12133356376092763, -231.3112718935514920 ) ) ;
#142954=DIRECTION ( 'NONE',  ( -0.000000000000000000, 0.9651348961777157509, -0.2617529984165031243 ) ) ;
#142979=AXIS2_PLACEMENT_3D ( 'NONE', #40889, #124261, #239063 ) ;
#142984=VERTEX_POINT ( 'NONE', #145743 ) ;
#143003=DIRECTION ( 'NONE',  ( -1.000000000000000000, 2.849773892568378313E-16, -7.728835255496647986E-17 ) ) ;
#143011=ADVANCED_FACE ( 'NONE', ( #182335 ), #102752, .T. ) ;
#143056=ORIENTED_EDGE ( 'NONE', *, *, #120309, .T. ) ;
#143062=EDGE_CURVE ( 'NONE', #189304, #40848, #111773, .T. ) ;
#143074=AXIS2_PLACEMENT_3D ( 'NONE', #102402, #180706, #236804 ) ;
#143111=CARTESIAN_POINT ( 'NONE',  ( 21.46681500593416914, 60.61285123220954318, -234.0601523988351857 ) ) ;
#143114=DIRECTION ( 'NONE',  ( 0.000000000000000000, -0.9651348961777157509, 0.2617529984165031243 ) ) ;
#143126=VERTEX_POINT ( 'NONE', #209588 ) ;
#143128=DIRECTION ( 'NONE',  ( 0.000000000000000000, -0.2617529984165033463, -0.9651348961777156399 ) ) ;
#143131=CARTESIAN_POINT ( 'NONE',  ( -21.46681500597755488, 65.43630044540329038, -242.4735498273712153 ) ) ;
#143155=TOROIDAL_SURFACE ( 'NONE', #59950, 0.2000000000000000111, 0.1000000000000000056 ) ;
#143161=LINE ( 'NONE', #164036, #236915 ) ;
#143173=EDGE_CURVE ( 'NONE', #14440, #205787, #115669, .T. ) ;
#143191=CARTESIAN_POINT ( 'NONE',  ( 20.85000000000000142, 79.11538813396778380, -196.3722783875038544 ) ) ;
#143248=DIRECTION ( 'NONE',  ( 0.000000000000000000, -0.9651348961777157509, 0.2617529984165031243 ) ) ;
#143257=EDGE_CURVE ( 'NONE', #204155, #147319, #169885, .T. ) ;
#143340=CARTESIAN_POINT ( 'NONE',  ( 20.94999999999999929, 86.10439672154322466, -209.4215112426525138 ) ) ;
#143359=CIRCLE ( 'NONE', #201621, 0.09999999999999577283 ) ;
#143387=ORIENTED_EDGE ( 'NONE', *, *, #162173, .T. ) ;
#143422=DIRECTION ( 'NONE',  ( 0.000000000000000000, -0.2617529984165152257, -0.9651348961777124202 ) ) ;
#143447=CYLINDRICAL_SURFACE ( 'NONE', #214126, 11.79999999999999361 ) ;
#143453=CIRCLE ( 'NONE', #206001, 0.1000000000000022676 ) ;
#143466=ORIENTED_EDGE ( 'NONE', *, *, #58815, .F. ) ;
#143468=EDGE_CURVE ( 'NONE', #155936, #71652, #86596, .T. ) ;
#143482=FACE_OUTER_BOUND ( 'NONE', #237642, .T. ) ;
#143494=AXIS2_PLACEMENT_3D ( 'NONE', #198898, #44969, #219739 ) ;
#143579=DIRECTION ( 'NONE',  ( 0.000000000000000000, -0.9651348961777157509, 0.2617529984165031243 ) ) ;
#143588=CARTESIAN_POINT ( 'NONE',  ( -21.64999999999999858, 63.44052078637213299, -222.1345147897817185 ) ) ;
#143600=AXIS2_PLACEMENT_3D ( 'NONE', #29284, #90482, #69666 ) ;
#143614=AXIS2_PLACEMENT_3D ( 'NONE', #200002, #57893, #38360 ) ;
#143636=EDGE_CURVE ( 'NONE', #14172, #210631, #141238, .T. ) ;
#143645=FACE_OUTER_BOUND ( 'NONE', #98902, .T. ) ;
#143647=CARTESIAN_POINT ( 'NONE',  ( -23.25000000000000000, 76.00000000001126921, -203.5231074845248997 ) ) ;
#143666=CARTESIAN_POINT ( 'NONE',  ( 21.14999999999999858, 59.16775194334852728, -221.0793150863668473 ) ) ;
#143668=CARTESIAN_POINT ( 'NONE',  ( -20.99780126800941815, 62.98982820228309265, -207.1569994557045788 ) ) ;
#143672=CARTESIAN_POINT ( 'NONE',  ( -21.13422380238980125, 65.53162686811064930, -242.1220625181933030 ) ) ;
#143677=DIRECTION ( 'NONE',  ( -1.000000000000000000, -0.000000000000000000, 0.000000000000000000 ) ) ;
#143687=VERTEX_POINT ( 'NONE', #146037 ) ;
#143702=ADVANCED_FACE ( 'NONE', ( #213717 ), #112072, .T. ) ;
#143707=VERTEX_POINT ( 'NONE', #251557 ) ;
#143771=VERTEX_POINT ( 'NONE', #14262 ) ;
#143788=DIRECTION ( 'NONE',  ( 0.000000000000000000, 0.7035695228903320331, 0.7106264324241468033 ) ) ;
#143793=DIRECTION ( 'NONE',  ( 0.000000000000000000, -0.2617529984164506107, -0.9651348961777299618 ) ) ;
#143816=DIRECTION ( 'NONE',  ( 1.000000000000000000, -3.151514657663852580E-16, 8.547182517843351137E-17 ) ) ;
#143845=( NAMED_UNIT ( * ) PLANE_ANGLE_UNIT ( ) SI_UNIT ( $, .RADIAN. ) );
#143858=ORIENTED_EDGE ( 'NONE', *, *, #137025, .F. ) ;
#143880=AXIS2_PLACEMENT_3D ( 'NONE', #183064, #166093, #205161 ) ;
#143898=ORIENTED_EDGE ( 'NONE', *, *, #233944, .T. ) ;
#143913=AXIS2_PLACEMENT_3D ( 'NONE', #152726, #56134, #255586 ) ;
#143927=FACE_OUTER_BOUND ( 'NONE', #148324, .T. ) ;
#143937=DIRECTION ( 'NONE',  ( -3.469446951953772592E-14, -0.9651348961777379554, 0.2617529984164210233 ) ) ;
#143966=CARTESIAN_POINT ( 'NONE',  ( 22.47071067811865319, 59.75442326890421896, -233.9300113800879046 ) ) ;
#144030=CARTESIAN_POINT ( 'NONE',  ( 18.49999999999999289, 62.92706838342916598, -212.5665282393149766 ) ) ;
#144044=CYLINDRICAL_SURFACE ( 'NONE', #143494, 0.09999999999999939493 ) ;
#144065=ORIENTED_EDGE ( 'NONE', *, *, #208106, .T. ) ;
#144093=CARTESIAN_POINT ( 'NONE',  ( 18.59999999999999076, 66.44571689960341132, -213.7280413126916017 ) ) ;
#144117=DIRECTION ( 'NONE',  ( 0.000000000000000000, -0.2617529984169731372, -0.9651348961775882973 ) ) ;
#144125=AXIS2_PLACEMENT_3D ( 'NONE', #60671, #218460, #39873 ) ;
#144146=ADVANCED_FACE ( 'NONE', ( #234246 ), #111751, .T. ) ;
#144148=CARTESIAN_POINT ( 'NONE',  ( -20.64999999999999858, 70.60814576644823148, -215.7631455941064189 ) ) ;
#144152=CIRCLE ( 'NONE', #31798, 0.09999999999999939493 ) ;
#144160=EDGE_LOOP ( 'NONE', ( #209191, #134430 ) ) ;
#144186=EDGE_LOOP ( 'NONE', ( #125536, #109374, #138654, #219227 ) ) ;
#144201=DIRECTION ( 'NONE',  ( 0.000000000000000000, 0.2617529984165152257, 0.9651348961777124202 ) ) ;
#144212=CARTESIAN_POINT ( 'NONE',  ( -20.94999999999999929, 57.72708596674831938, -226.0092949359174952 ) ) ;
#144228=EDGE_LOOP ( 'NONE', ( #94273, #214063, #79160, #211168 ) ) ;
#144236=ORIENTED_EDGE ( 'NONE', *, *, #129287, .F. ) ;
#144241=CARTESIAN_POINT ( 'NONE',  ( 18.58703555225035586, 78.17463401018991931, -231.4407306458928701 ) ) ;
#144293=AXIS2_PLACEMENT_3D ( 'NONE', #166556, #27047, #240936 ) ;
#144313=VECTOR ( 'NONE', #86523, 1000.000000000000000 ) ;
#144318=FACE_OUTER_BOUND ( 'NONE', #161286, .T. ) ;
#144320=VERTEX_POINT ( 'NONE', #99850 ) ;
#144324=CARTESIAN_POINT ( 'NONE',  ( 21.14999999999999503, 64.27847795353595473, -247.1247091181747066 ) ) ;
#144329=DIRECTION ( 'NONE',  ( 1.000000000000000000, 0.000000000000000000, 0.000000000000000000 ) ) ;
#144357=AXIS2_PLACEMENT_3D ( 'NONE', #204202, #9858, #149401 ) ;
#144469=DIRECTION ( 'NONE',  ( 1.734723475976817507E-14, 0.2617529984165031243, 0.9651348961777157509 ) ) ;
#144472=CARTESIAN_POINT ( 'NONE',  ( 23.14999999999999858, 72.13946041530040532, -202.4760954908588815 ) ) ;
#144482=ORIENTED_EDGE ( 'NONE', *, *, #20997, .T. ) ;
#144483=FACE_OUTER_BOUND ( 'NONE', #206956, .T. ) ;
#144503=ORIENTED_EDGE ( 'NONE', *, *, #184232, .F. ) ;
#144513=DIRECTION ( 'NONE',  ( -0.000000000000000000, -0.2617529984165028467, -0.9651348961777159730 ) ) ;
#144519=ORIENTED_EDGE ( 'NONE', *, *, #17558, .F. ) ;
#144545=EDGE_LOOP ( 'NONE', ( #30391, #206871, #25506, #62970, #109529, #132930, #87549, #207346, #175547, #58493, #200904, #67635, #154600, #179786, #143858, #230043, #217884, #247312, #72209, #234887, #139925, #30769, #235936, #48555, #182958, #196785, #126936 ) ) ;
#144575=DIRECTION ( 'NONE',  ( 0.000000000000000000, 0.9651348961777148627, -0.2617529984165062329 ) ) ;
#144590=ORIENTED_EDGE ( 'NONE', *, *, #182569, .T. ) ;
#144619=EDGE_CURVE ( 'NONE', #55134, #228509, #203126, .T. ) ;
#144643=LINE ( 'NONE', #49411, #116692 ) ;
#144649=ORIENTED_EDGE ( 'NONE', *, *, #37175, .F. ) ;
#144744=ORIENTED_EDGE ( 'NONE', *, *, #175926, .T. ) ;
#144780=EDGE_CURVE ( 'NONE', #150591, #248567, #27783, .T. ) ;
#144815=VECTOR ( 'NONE', #107925, 1000.000000000000114 ) ;
#144863=FACE_OUTER_BOUND ( 'NONE', #70583, .T. ) ;
#144871=CARTESIAN_POINT ( 'NONE',  ( 21.17356465864818915, 65.45462388619900196, -242.0281076209811033 ) ) ;
#144874=ORIENTED_EDGE ( 'NONE', *, *, #94958, .T. ) ;
#144923=DIRECTION ( 'NONE',  ( 0.000000000000000000, 0.1290532225515392817, 0.9916376685811522096 ) ) ;
#144960=AXIS2_PLACEMENT_3D ( 'NONE', #50626, #153659, #151042 ) ;
#144965=CARTESIAN_POINT ( 'NONE',  ( 21.05000000000000071, 60.06173988932783203, -221.3217724115915814 ) ) ;
#144974=CIRCLE ( 'NONE', #7629, 0.1000000000000124678 ) ;
#144987=AXIS2_PLACEMENT_3D ( 'NONE', #197851, #202988, #118338 ) ;
#144991=DIRECTION ( 'NONE',  ( 0.000000000000000000, -0.2617529984164955192, -0.9651348961777178603 ) ) ;
#145033=CARTESIAN_POINT ( 'NONE',  ( -21.05000000000000071, 79.07891399537199106, -236.0635483022085452 ) ) ;
#145036=EDGE_CURVE ( 'NONE', #81393, #116965, #236617, .T. ) ;
#145043=CARTESIAN_POINT ( 'NONE',  ( -21.05000000000009663, 60.96458334440597326, -234.1404740665545319 ) ) ;
#145058=ORIENTED_EDGE ( 'NONE', *, *, #113141, .F. ) ;
#145100=EDGE_CURVE ( 'NONE', #73566, #152520, #236801, .T. ) ;
#145111=FACE_OUTER_BOUND ( 'NONE', #27695, .T. ) ;
#145134=SPHERICAL_SURFACE ( 'NONE', #83858, 0.1000000000000000056 ) ;
#145164=CARTESIAN_POINT ( 'NONE',  ( -23.15000000000000213, 70.12557831835937350, -215.6322690948981915 ) ) ;
#145168=ORIENTED_EDGE ( 'NONE', *, *, #220097, .T. ) ;
#145180=CIRCLE ( 'NONE', #145366, 4.050000000000000711 ) ;
#145188=DIRECTION ( 'NONE',  ( 0.000000000000000000, -0.2617529984165031243, -0.9651348961777157509 ) ) ;
#145206=CYLINDRICAL_SURFACE ( 'NONE', #224023, 3.999999999999996447 ) ;
#145208=ORIENTED_EDGE ( 'NONE', *, *, #65276, .F. ) ;
#145224=FACE_OUTER_BOUND ( 'NONE', #120423, .T. ) ;
#145234=DIRECTION ( 'NONE',  ( -0.000000000000000000, 0.9651348961777159730, -0.2617529984165026247 ) ) ;
#145239=EDGE_CURVE ( 'NONE', #205311, #23903, #228227, .T. ) ;
#145240=VECTOR ( 'NONE', #174140, 1000.000000000000000 ) ;
#145247=CARTESIAN_POINT ( 'NONE',  ( 21.07928932188134397, 61.09751618602743406, -234.2940654522722639 ) ) ;
#145266=CARTESIAN_POINT ( 'NONE',  ( 21.05000000000001492, 61.01939706577768163, -234.1520516327897496 ) ) ;
#145327=ADVANCED_FACE ( 'NONE', ( #197741 ), #7705, .T. ) ;
#145366=AXIS2_PLACEMENT_3D ( 'NONE', #194257, #57255, #212529 ) ;
#145376=SPHERICAL_SURFACE ( 'NONE', #29623, 0.1000000000000000056 ) ;
#145434=AXIS2_PLACEMENT_3D ( 'NONE', #89807, #229348, #50669 ) ;
#145488=CIRCLE ( 'NONE', #3856, 11.64999999999998970 ) ;
#145490=ORIENTED_EDGE ( 'NONE', *, *, #58696, .F. ) ;
#145502=LINE ( 'NONE', #202914, #96728 ) ;
#145547=DIRECTION ( 'NONE',  ( 0.000000000000000000, 0.9651348961777379554, -0.2617529984164210233 ) ) ;
#145553=ORIENTED_EDGE ( 'NONE', *, *, #147099, .T. ) ;
#145582=CARTESIAN_POINT ( 'NONE',  ( 20.94999999999999929, 72.02722222756959525, -225.1832529173024398 ) ) ;
#145613=CARTESIAN_POINT ( 'NONE',  ( -22.59999999999999787, 55.86495732666938352, -232.8769840133977880 ) ) ;
#145620=VERTEX_POINT ( 'NONE', #249714 ) ;
#145652=CARTESIAN_POINT ( 'NONE',  ( 23.25000000000000000, 75.39949836213487799, -250.2448839681187849 ) ) ;
#145671=ORIENTED_EDGE ( 'NONE', *, *, #22118, .T. ) ;
#145743=CARTESIAN_POINT ( 'NONE',  ( 20.94999999999999929, 87.24382154048164750, -206.5725299160771726 ) ) ;
#145756=PLANE ( 'NONE',  #147347 ) ;
#145767=CARTESIAN_POINT ( 'NONE',  ( -23.15000000000000213, 63.84823067483194592, -203.4394279312818981 ) ) ;
#145772=ORIENTED_EDGE ( 'NONE', *, *, #159782, .T. ) ;
#145777=EDGE_LOOP ( 'NONE', ( #255906, #166548, #113018, #241002 ) ) ;
#145848=CARTESIAN_POINT ( 'NONE',  ( 20.97462148592295961, 61.87364552196481782, -221.7047524508823528 ) ) ;
#145860=ORIENTED_EDGE ( 'NONE', *, *, #84730, .T. ) ;
#145863=ORIENTED_EDGE ( 'NONE', *, *, #182879, .T. ) ;
#145923=ORIENTED_EDGE ( 'NONE', *, *, #121322, .F. ) ;
#145940=ORIENTED_EDGE ( 'NONE', *, *, #125439, .F. ) ;
#145960=ORIENTED_EDGE ( 'NONE', *, *, #210429, .F. ) ;
#145969=DIRECTION ( 'NONE',  ( 0.000000000000000000, 0.2617529984165030132, 0.9651348961777158619 ) ) ;
#145972=CARTESIAN_POINT ( 'NONE',  ( 20.94999999999999574, 79.38304387823771435, -235.9388060597213723 ) ) ;
#145980=CARTESIAN_POINT ( 'NONE',  ( 21.09316766718128022, 61.07293998390336753, -234.2256142562819718 ) ) ;
#145996=EDGE_CURVE ( 'NONE', #115380, #143707, #190751, .T. ) ;
#146011=CARTESIAN_POINT ( 'NONE',  ( 20.94999999999999574, 67.23127455305841238, -235.8551265064783991 ) ) ;
#146026=ADVANCED_FACE ( 'NONE', ( #194603 ), #149043, .T. ) ;
#146027=ORIENTED_EDGE ( 'NONE', *, *, #127930, .T. ) ;
#146037=CARTESIAN_POINT ( 'NONE',  ( 21.05000000000000071, 68.22899648672319017, -213.7884437866858889 ) ) ;
#146039=SPHERICAL_SURFACE ( 'NONE', #63803, 0.1000000000000000056 ) ;
#146045=CARTESIAN_POINT ( 'NONE',  ( 18.49999999999999289, 63.74705046376995199, -209.1848118361201330 ) ) ;
#146093=VERTEX_POINT ( 'NONE', #99297 ) ;
#146100=DIRECTION ( 'NONE',  ( 1.000000000000000000, 0.000000000000000000, 0.000000000000000000 ) ) ;
#146108=VERTEX_POINT ( 'NONE', #197128 ) ;
#146115=ORIENTED_EDGE ( 'NONE', *, *, #209770, .T. ) ;
#146172=DIRECTION ( 'NONE',  ( 1.000000000000000000, 0.000000000000000000, -0.000000000000000000 ) ) ;
#146173=DIRECTION ( 'NONE',  ( 1.000000000000000000, 0.000000000000000000, 0.000000000000000000 ) ) ;
#146174=EDGE_CURVE ( 'NONE', #29748, #128048, #121489, .T. ) ;
#146176=ORIENTED_EDGE ( 'NONE', *, *, #252174, .F. ) ;
#146177=FACE_OUTER_BOUND ( 'NONE', #256688, .T. ) ;
#146232=DIRECTION ( 'NONE',  ( 1.836970198721029934E-16, 0.9651348961777157509, -0.2617529984165031243 ) ) ;
#146244=CARTESIAN_POINT ( 'NONE',  ( 20.94999999999999929, 68.48451787451661232, -224.2224406095231757 ) ) ;
#146259=ADVANCED_FACE ( 'NONE', ( #104431 ), #243965, .F. ) ;
#146290=CARTESIAN_POINT ( 'NONE',  ( -23.25000000000000000, 80.78317333349157536, -192.9003134612049166 ) ) ;
#146311=DIRECTION ( 'NONE',  ( 0.000000000000000000, -0.2617529984165031243, -0.9651348961777157509 ) ) ;
#146330=ORIENTED_EDGE ( 'NONE', *, *, #113753, .T. ) ;
#146338=CARTESIAN_POINT ( 'NONE',  ( -20.54999999999999716, 81.91411460262999356, -215.0718681741873013 ) ) ;
#146367=AXIS2_PLACEMENT_3D ( 'NONE', #190566, #154038, #69328 ) ;
#146387=CARTESIAN_POINT ( 'NONE',  ( 20.94999999999999929, 76.49733069700262433, -201.6893511817872309 ) ) ;
#146409=ORIENTED_EDGE ( 'NONE', *, *, #196357, .F. ) ;
#146446=CIRCLE ( 'NONE', #34084, 0.8750000000000007772 ) ;
#146449=VERTEX_POINT ( 'NONE', #90020 ) ;
#146458=CIRCLE ( 'NONE', #117270, 0.1000000000000040579 ) ;
#146472=DIRECTION ( 'NONE',  ( 0.000000000000000000, -0.2617529984165022361, -0.9651348961777160840 ) ) ;
#146473=DIRECTION ( 'NONE',  ( 0.000000000000000000, -0.9651348961777157509, 0.2617529984165031243 ) ) ;
#146478=ADVANCED_FACE ( 'NONE', ( #159025 ), #196826, .T. ) ;
#146479=ADVANCED_FACE ( 'NONE', ( #156466 ), #18199, .T. ) ;
#146499=DIRECTION ( 'NONE',  ( 0.000000000000000000, -0.2617529984164915779, -0.9651348961777189706 ) ) ;
#146509=DIRECTION ( 'NONE',  ( 1.000000000000000000, -3.151514657663852580E-16, 8.547182517843349904E-17 ) ) ;
#146536=VERTEX_POINT ( 'NONE', #199425 ) ;
#146542=FACE_OUTER_BOUND ( 'NONE', #172503, .T. ) ;
#146594=ORIENTED_EDGE ( 'NONE', *, *, #230259, .F. ) ;
#146636=AXIS2_PLACEMENT_3D ( 'NONE', #187014, #246952, #46185 ) ;
#146649=CYLINDRICAL_SURFACE ( 'NONE', #84598, 0.09999999999999939493 ) ;
#146687=DIRECTION ( 'NONE',  ( 0.000000000000000000, -0.2617529984165031243, -0.9651348961777157509 ) ) ;
#146733=ORIENTED_EDGE ( 'NONE', *, *, #138350, .T. ) ;
#146739=CARTESIAN_POINT ( 'NONE',  ( 21.05000000000000071, 68.05808644172607558, -213.7045301755741491 ) ) ;
#146743=VECTOR ( 'NONE', #136426, 1000.000000000000000 ) ;
#146747=ORIENTED_EDGE ( 'NONE', *, *, #141710, .F. ) ;
#146768=CARTESIAN_POINT ( 'NONE',  ( -21.06715728752538652, 57.72708596674831938, -226.0092949359175236 ) ) ;
#146770=FACE_OUTER_BOUND ( 'NONE', #71411, .T. ) ;
#146808=ADVANCED_FACE ( 'NONE', ( #50574 ), #8909, .T. ) ;
#146816=CARTESIAN_POINT ( 'NONE',  ( -23.15000000000000213, 59.07123845373075000, -221.0531397865252075 ) ) ;
#146854=CARTESIAN_POINT ( 'NONE',  ( -20.94999999999999929, 70.47363787294415260, -228.3418745167492432 ) ) ;
#146874=ORIENTED_EDGE ( 'NONE', *, *, #32683, .T. ) ;
#146888=DIRECTION ( 'NONE',  ( 0.000000000000000000, 0.2617529984165152257, 0.9651348961777124202 ) ) ;
#146908=CARTESIAN_POINT ( 'NONE',  ( -18.58222699835055280, 67.49225400653517681, -195.4205142095401584 ) ) ;
#146935=CARTESIAN_POINT ( 'NONE',  ( 23.14999999999999858, 67.44464249442897597, -214.0562211244547655 ) ) ;
#146940=AXIS2_PLACEMENT_3D ( 'NONE', #23947, #162172, #38358 ) ;
#146974=DIRECTION ( 'NONE',  ( 0.000000000000000000, -0.2617529984165152257, -0.9651348961777124202 ) ) ;
#146976=AXIS2_PLACEMENT_3D ( 'NONE', #164167, #62498, #85869 ) ;
#146978=ORIENTED_EDGE ( 'NONE', *, *, #238731, .F. ) ;
#146983=CARTESIAN_POINT ( 'NONE',  ( -21.07016717457011268, 65.57674933587216515, -241.9556870860043603 ) ) ;
#147058=CYLINDRICAL_SURFACE ( 'NONE', #192914, 0.1000000000000124678 ) ;
#147060=VERTEX_POINT ( 'NONE', #113959 ) ;
#147085=ORIENTED_EDGE ( 'NONE', *, *, #150804, .T. ) ;
#147088=EDGE_CURVE ( 'NONE', #203694, #69974, #42487, .T. ) ;
#147093=FACE_BOUND ( 'NONE', #57509, .T. ) ;
#147097=CARTESIAN_POINT ( 'NONE',  ( -23.15000000000000213, 74.95298800634525094, -207.3836470692357636 ) ) ;
#147099=EDGE_CURVE ( 'NONE', #194221, #193203, #21280, .T. ) ;
#147158=EDGE_CURVE ( 'NONE', #22805, #100463, #384, .T. ) ;
#147166=DIRECTION ( 'NONE',  ( -0.000000000000000000, 0.9651348961777157509, -0.2617529984165031243 ) ) ;
#147167=CIRCLE ( 'NONE', #188866, 12.87500000000000178 ) ;
#147180=DIRECTION ( 'NONE',  ( 0.000000000000000000, -0.9673461469267405910, 0.2534589355812664757 ) ) ;
#147192=ORIENTED_EDGE ( 'NONE', *, *, #41182, .T. ) ;
#147211=VECTOR ( 'NONE', #162345, 1000.000000000000000 ) ;
#147252=CARTESIAN_POINT ( 'NONE',  ( -20.64999999999999858, 68.71679287596359131, -222.9654461259447658 ) ) ;
#147262=EDGE_CURVE ( 'NONE', #159934, #157057, #108556, .T. ) ;
#147270=CARTESIAN_POINT ( 'NONE',  ( 21.08884785362045378, 61.08269451800257599, -234.2391594833300701 ) ) ;
#147318=ORIENTED_EDGE ( 'NONE', *, *, #227647, .T. ) ;
#147319=VERTEX_POINT ( 'NONE', #3903 ) ;
#147321=VECTOR ( 'NONE', #179322, 1000.000000000000000 ) ;
#147334=ORIENTED_EDGE ( 'NONE', *, *, #178964, .T. ) ;
#147347=AXIS2_PLACEMENT_3D ( 'NONE', #89635, #27148, #244863 ) ;
#147364=ADVANCED_FACE ( 'NONE', ( #80849 ), #189703, .F. ) ;
#147367=TOROIDAL_SURFACE ( 'NONE', #205608, 0.4000000000000017431, 0.1000000000000000056 ) ;
#147385=DIRECTION ( 'NONE',  ( 0.000000000000000000, 0.2617529984165152257, 0.9651348961777124202 ) ) ;
#147406=EDGE_CURVE ( 'NONE', #51771, #70810, #69100, .T. ) ;
#147423=VECTOR ( 'NONE', #66426, 1000.000000000000000 ) ;
#147426=ADVANCED_FACE ( 'NONE', ( #148557 ), #194004, .T. ) ;
#147434=ORIENTED_EDGE ( 'NONE', *, *, #153056, .F. ) ;
#147466=ORIENTED_EDGE ( 'NONE', *, *, #52031, .F. ) ;
#147469=CARTESIAN_POINT ( 'NONE',  ( 22.39999999999999858, 59.68594599439719417, -233.9123800762197902 ) ) ;
#147501=CARTESIAN_POINT ( 'NONE',  ( 23.24999999999999645, 78.02678328198446422, -204.0727887811995629 ) ) ;
#147511=CARTESIAN_POINT ( 'NONE',  ( -22.50000000000000000, 65.59531831295525706, -241.8872196075891168 ) ) ;
#147525=DIRECTION ( 'NONE',  ( 0.7071067811865475727, -0.6824534298470373850, 0.1850873201762210096 ) ) ;
#147541=VERTEX_POINT ( 'NONE', #152430 ) ;
#147548=ORIENTED_EDGE ( 'NONE', *, *, #176470, .T. ) ;
#147572=CARTESIAN_POINT ( 'NONE',  ( -20.94999999999999929, 68.51069317435826633, -224.1259271199053842 ) ) ;
#147587=CARTESIAN_POINT ( 'NONE',  ( 20.84999999999999432, 70.22659352830977753, -197.9852579278363578 ) ) ;
#147603=ORIENTED_EDGE ( 'NONE', *, *, #113492, .T. ) ;
#147631=ORIENTED_EDGE ( 'NONE', *, *, #175706, .T. ) ;
#147644=EDGE_LOOP ( 'NONE', ( #72004, #74483, #227453, #12343 ) ) ;
#147677=DIRECTION ( 'NONE',  ( 1.000000000000000000, -2.849773892568378313E-16, 7.728835255496647986E-17 ) ) ;
#147723=AXIS2_PLACEMENT_3D ( 'NONE', #83867, #40965, #65626 ) ;
#147756=VECTOR ( 'NONE', #109022, 1000.000000000000114 ) ;
#147768=EDGE_CURVE ( 'NONE', #2766, #242581, #248327, .T. ) ;
#147782=ORIENTED_EDGE ( 'NONE', *, *, #175474, .T. ) ;
#147827=LINE ( 'NONE', #48702, #144313 ) ;
#147829=CARTESIAN_POINT ( 'NONE',  ( -18.59999999999999787, 80.78317333349157536, -192.9003134612048882 ) ) ;
#147863=ORIENTED_EDGE ( 'NONE', *, *, #112146, .T. ) ;
#147868=CARTESIAN_POINT ( 'NONE',  ( -21.29999999999995808, 68.29137419664525055, -231.9463301769586394 ) ) ;
#147869=DIRECTION ( 'NONE',  ( 0.000000000000000000, -0.5378121776619179117, 0.8430646840892729310 ) ) ;
#147878=ORIENTED_EDGE ( 'NONE', *, *, #128933, .T. ) ;
#147948=ORIENTED_EDGE ( 'NONE', *, *, #36342, .T. ) ;
#147952=CARTESIAN_POINT ( 'NONE',  ( 21.05000000000000071, 61.00122447389660607, -225.2976766370351527 ) ) ;
#147983=ORIENTED_EDGE ( 'NONE', *, *, #147158, .F. ) ;
#148030=ORIENTED_EDGE ( 'NONE', *, *, #130285, .F. ) ;
#148057=EDGE_CURVE ( 'NONE', #241619, #41069, #202362, .T. ) ;
#148081=DIRECTION ( 'NONE',  ( 0.000000000000000000, 0.2617529984165031243, 0.9651348961777157509 ) ) ;
#148082=ORIENTED_EDGE ( 'NONE', *, *, #126979, .T. ) ;
#148100=ORIENTED_EDGE ( 'NONE', *, *, #17523, .F. ) ;
#148131=AXIS2_PLACEMENT_3D ( 'NONE', #113737, #14673, #159311 ) ;
#148140=DIRECTION ( 'NONE',  ( 1.000000000000000000, 0.000000000000000000, 0.000000000000000000 ) ) ;
#148169=VERTEX_POINT ( 'NONE', #162373 ) ;
#148172=EDGE_CURVE ( 'NONE', #252099, #234093, #106855, .T. ) ;
#148187=CARTESIAN_POINT ( 'NONE',  ( -21.45000000000000284, 63.02410583447655767, -221.9179669651492759 ) ) ;
#148223=DIRECTION ( 'NONE',  ( -0.000000000000000000, -0.2617529984165031243, -0.9651348961777157509 ) ) ;
#148228=DIRECTION ( 'NONE',  ( 1.000000000000000000, 0.000000000000000000, 0.000000000000000000 ) ) ;
#148251=DIRECTION ( 'NONE',  ( -1.000000000000000000, -0.000000000000000000, 0.000000000000000000 ) ) ;
#148262=EDGE_CURVE ( 'NONE', #139316, #55604, #152692, .T. ) ;
#148278=CIRCLE ( 'NONE', #239873, 0.09999999999999543976 ) ;
#148296=EDGE_LOOP ( 'NONE', ( #244950, #37819, #112101, #239992 ) ) ;
#148318=DIRECTION ( 'NONE',  ( 0.000000000000000000, -0.9667078373770149335, -0.2558827019434000150 ) ) ;
#148321=CARTESIAN_POINT ( 'NONE',  ( -21.05000000000000071, 79.10508929521364507, -235.9670348125907537 ) ) ;
#148324=EDGE_LOOP ( 'NONE', ( #70434, #132203, #198806, #238488, #182954 ) ) ;
#148350=AXIS2_PLACEMENT_3D ( 'NONE', #26275, #86207, #67955 ) ;
#148375=CYLINDRICAL_SURFACE ( 'NONE', #248435, 0.09999999999999935330 ) ;
#148401=ORIENTED_EDGE ( 'NONE', *, *, #217591, .T. ) ;
#148426=CYLINDRICAL_SURFACE ( 'NONE', #241789, 3.999999999999996447 ) ;
#148440=FACE_OUTER_BOUND ( 'NONE', #182084, .T. ) ;
#148469=VERTEX_POINT ( 'NONE', #159499 ) ;
#148475=CARTESIAN_POINT ( 'NONE',  ( -23.25000000000000000, 68.66552716081216090, -214.3300732090495444 ) ) ;
#148503=ORIENTED_EDGE ( 'NONE', *, *, #202058, .T. ) ;
#148534=CARTESIAN_POINT ( 'NONE',  ( 21.02374657821570025, 62.99095723451777928, -207.1734234075709651 ) ) ;
#148540=DIRECTION ( 'NONE',  ( 3.469446951953728416E-14, 0.7049548389604960441, -0.7092521942343085195 ) ) ;
#148551=DIRECTION ( 'NONE',  ( 1.000000000000000000, 0.000000000000000000, 0.000000000000000000 ) ) ;
#148557=FACE_OUTER_BOUND ( 'NONE', #243415, .T. ) ;
#148565=VERTEX_POINT ( 'NONE', #221994 ) ;
#148566=CARTESIAN_POINT ( 'NONE',  ( 21.11927991906888025, 61.00523113630152494, -234.1759810734909877 ) ) ;
#148574=ADVANCED_FACE ( 'NONE', ( #122935 ), #131630, .T. ) ;
#148575=CIRCLE ( 'NONE', #19388, 11.79999999999999005 ) ;
#148583=EDGE_CURVE ( 'NONE', #116241, #120691, #94564, .T. ) ;
#148586=ADVANCED_FACE ( 'NONE', ( #167221 ), #44683, .T. ) ;
#148625=CARTESIAN_POINT ( 'NONE',  ( 22.16821283564876666, 59.93584560259384375, -233.8765425695785893 ) ) ;
#148644=CARTESIAN_POINT ( 'NONE',  ( 18.50000000000000000, 78.21362219944488459, -231.2727646510690533 ) ) ;
#148648=VERTEX_POINT ( 'NONE', #97886 ) ;
#148662=CARTESIAN_POINT ( 'NONE',  ( 21.05000000000000071, 62.92003201576280702, -207.2439188921395612 ) ) ;
#148731=CARTESIAN_POINT ( 'NONE',  ( -18.59999999999999787, 68.22930980752001062, -227.7331931781284879 ) ) ;
#148735=DIRECTION ( 'NONE',  ( 0.000000000000000000, -0.9209589331071864615, 0.3896596508878908960 ) ) ;
#148759=CARTESIAN_POINT ( 'NONE',  ( -18.59999999999999787, 70.44746257310249860, -228.4383880063670347 ) ) ;
#148770=CIRCLE ( 'NONE', #2990, 0.1000000000000018374 ) ;
#148780=VECTOR ( 'NONE', #241369, 1000.000000000000000 ) ;
#148824=FACE_OUTER_BOUND ( 'NONE', #257298, .T. ) ;
#148839=CARTESIAN_POINT ( 'NONE',  ( 18.59999999999999076, 63.83083047455526327, -209.3924252461221158 ) ) ;
#148845=EDGE_LOOP ( 'NONE', ( #96741, #82104, #35323, #46001 ) ) ;
#148850=CARTESIAN_POINT ( 'NONE',  ( -22.01447462590973103, 60.19480426826893193, -234.0493890886782822 ) ) ;
#148899=AXIS2_PLACEMENT_3D ( 'NONE', #141522, #221053, #200224 ) ;
#148901=EDGE_CURVE ( 'NONE', #155690, #90469, #57136, .T. ) ;
#148909=AXIS2_PLACEMENT_3D ( 'NONE', #19188, #180838, #40069 ) ;
#148917=EDGE_CURVE ( 'NONE', #174276, #117062, #213369, .T. ) ;
#148919=VERTEX_POINT ( 'NONE', #98519 ) ;
#148920=ORIENTED_EDGE ( 'NONE', *, *, #166193, .T. ) ;
#148922=CARTESIAN_POINT ( 'NONE',  ( -21.05000000000000071, 61.16604239670572696, -234.3115055913001470 ) ) ;
#148934=VERTEX_POINT ( 'NONE', #235503 ) ;
#148958=EDGE_CURVE ( 'NONE', #148565, #163993, #113004, .T. ) ;
#148962=VERTEX_POINT ( 'NONE', #103677 ) ;
#148968=AXIS2_PLACEMENT_3D ( 'NONE', #234042, #232789, #55372 ) ;
#148977=DIRECTION ( 'NONE',  ( 0.000000000000000000, 0.9651348961777259650, -0.2617529984164657098 ) ) ;
#149000=DIRECTION ( 'NONE',  ( 1.000000000000000000, 0.000000000000000000, 0.000000000000000000 ) ) ;
#149008=AXIS2_PLACEMENT_3D ( 'NONE', #55602, #176899, #214710 ) ;
#149015=DIRECTION ( 'NONE',  ( 0.000000000000000000, -0.9916376685811618685, 0.1290532225514649800 ) ) ;
#149017=LINE ( 'NONE', #130707, #107178 ) ;
#149021=SHAPE_REPRESENTATION_RELATIONSHIP ( 'NONE' , 'NONE' ,  #241717, #63721 ) ;
#149043=CYLINDRICAL_SURFACE ( 'NONE', #166480, 0.1000000000000124678 ) ;
#149080=DIRECTION ( 'NONE',  ( 1.000000000000000000, 0.000000000000000000, -0.000000000000000000 ) ) ;
#149116=DIRECTION ( 'NONE',  ( 0.000000000000000000, 0.9651348961777379554, -0.2617529984164210233 ) ) ;
#149120=CARTESIAN_POINT ( 'NONE',  ( -23.15000000000000213, 81.82295291318693842, -214.8938525951558915 ) ) ;
#149145=EDGE_CURVE ( 'NONE', #2330, #36582, #204079, .T. ) ;
#149168=ORIENTED_EDGE ( 'NONE', *, *, #168996, .F. ) ;
#149223=CARTESIAN_POINT ( 'NONE',  ( 23.15000000000000213, 82.09643798151613225, -215.4278993322501208 ) ) ;
#149224=CARTESIAN_POINT ( 'NONE',  ( -20.85000000000000497, 62.84855743180813903, -207.1254202119976640 ) ) ;
#149310=CARTESIAN_POINT ( 'NONE',  ( -23.25000000000000000, 80.80934863333322937, -192.8037999715871535 ) ) ;
#149319=ORIENTED_EDGE ( 'NONE', *, *, #93560, .T. ) ;
#149322=DIRECTION ( 'NONE',  ( -1.000000000000000000, 0.000000000000000000, 0.000000000000000000 ) ) ;
#149334=ORIENTED_EDGE ( 'NONE', *, *, #1584, .F. ) ;
#149337=DIRECTION ( 'NONE',  ( 0.000000000000000000, 0.9651348961777148627, -0.2617529984165062329 ) ) ;
#149350=FACE_OUTER_BOUND ( 'NONE', #219860, .T. ) ;
#149378=CARTESIAN_POINT ( 'NONE',  ( -20.15000000000000568, 63.79987548357193816, -213.0104660527734382 ) ) ;
#149400=CARTESIAN_POINT ( 'NONE',  ( 20.85000000000000142, 76.00000000001126921, -203.5231074845248997 ) ) ;
#149401=DIRECTION ( 'NONE',  ( 1.000000000000000000, 7.049440681616512959E-16, -1.911869773728117674E-16 ) ) ;
#149408=VERTEX_POINT ( 'NONE', #112703 ) ;
#149466=DIRECTION ( 'NONE',  ( 0.000000000000000000, 0.2617529984165031243, 0.9651348961777157509 ) ) ;
#149486=CONICAL_SURFACE ( 'NONE', #253499, 7.750000000000033751, 0.7853981633974531640 ) ;
#149505=CARTESIAN_POINT ( 'NONE',  ( 21.05000000000000071, 68.16863917788211324, -213.8681745540812926 ) ) ;
#149521=DIRECTION ( 'NONE',  ( 0.000000000000000000, -0.9651348961777155289, 0.2617529984165036794 ) ) ;
#149561=CARTESIAN_POINT ( 'NONE',  ( -23.25000000000000000, 68.18350826420393673, -222.4110246041809091 ) ) ;
#149602=VECTOR ( 'NONE', #197153, 1000.000000000000000 ) ;
#149657=AXIS2_PLACEMENT_3D ( 'NONE', #234034, #18839, #97051 ) ;
#149680=CARTESIAN_POINT ( 'NONE',  ( -22.50000000000000000, 55.98745301258801987, -232.8057040749261262 ) ) ;
#149714=EDGE_LOOP ( 'NONE', ( #252439, #41759, #194762, #208637, #123245 ) ) ;
#149721=CARTESIAN_POINT ( 'NONE',  ( -21.55000000000000426, 63.02410583447655767, -221.9179669651492759 ) ) ;
#149725=CARTESIAN_POINT ( 'NONE',  ( -20.94999999999999929, 76.00000000001126921, -203.5231074845248997 ) ) ;
#149733=CARTESIAN_POINT ( 'NONE',  ( -21.03922262424669753, 57.80806069346814979, -226.1924746198927778 ) ) ;
#149750=EDGE_CURVE ( 'NONE', #38996, #22560, #240313, .T. ) ;
#149761=DIRECTION ( 'NONE',  ( 1.000000000000000000, 0.000000000000000000, 0.000000000000000000 ) ) ;
#149775=FACE_OUTER_BOUND ( 'NONE', #55428, .T. ) ;
#149823=EDGE_LOOP ( 'NONE', ( #114231, #247091, #235599 ) ) ;
#149836=LINE ( 'NONE', #230649, #160172 ) ;
#149860=VERTEX_POINT ( 'NONE', #140956 ) ;
#149870=AXIS2_PLACEMENT_3D ( 'NONE', #214546, #134992, #158464 ) ;
#149876=DIRECTION ( 'NONE',  ( 1.000000000000000000, 0.000000000000000000, 0.000000000000000000 ) ) ;
#149888=EDGE_CURVE ( 'NONE', #77841, #181022, #48766, .T. ) ;
#149889=FACE_OUTER_BOUND ( 'NONE', #63764, .T. ) ;
#149891=ORIENTED_EDGE ( 'NONE', *, *, #1133, .T. ) ;
#149896=EDGE_CURVE ( 'NONE', #250042, #58070, #222372, .T. ) ;
#149897=CARTESIAN_POINT ( 'NONE',  ( 20.51284917709620004, 59.28817092441780545, -225.7512494052134855 ) ) ;
#149900=ORIENTED_EDGE ( 'NONE', *, *, #210526, .T. ) ;
#149907=CARTESIAN_POINT ( 'NONE',  ( -20.54999999999999716, 63.53703427598990316, -222.1606900896233583 ) ) ;
#149932=EDGE_LOOP ( 'NONE', ( #10487, #229042, #210745 ) ) ;
#149934=CARTESIAN_POINT ( 'NONE',  ( 18.49505832270841310, 78.22446672510398002, -231.3780609907616679 ) ) ;
#149949=ORIENTED_EDGE ( 'NONE', *, *, #38698, .T. ) ;
#149958=LINE ( 'NONE', #115953, #161542 ) ;
#149966=ADVANCED_FACE ( 'NONE', ( #242593 ), #123249, .T. ) ;
#149967=AXIS2_PLACEMENT_3D ( 'NONE', #25530, #162478, #187180 ) ;
#149980=FACE_OUTER_BOUND ( 'NONE', #141704, .T. ) ;
#149983=ORIENTED_EDGE ( 'NONE', *, *, #102026, .T. ) ;
#149987=CARTESIAN_POINT ( 'NONE',  ( 20.84999999999998721, 67.49222854868494892, -195.4187676019683693 ) ) ;
#150006=CYLINDRICAL_SURFACE ( 'NONE', #162250, 0.09999999999999939493 ) ;
#150013=AXIS2_PLACEMENT_3D ( 'NONE', #148187, #29563, #229023 ) ;
#150023=DIRECTION ( 'NONE',  ( -1.000000000000000000, 0.000000000000000000, 0.000000000000000000 ) ) ;
#150039=AXIS2_PLACEMENT_3D ( 'NONE', #41634, #121186, #200692 ) ;
#150051=CYLINDRICAL_SURFACE ( 'NONE', #256934, 0.09999999999999939493 ) ;
#150082=DIRECTION ( 'NONE',  ( 1.000000000000000000, 0.000000000000000000, 0.000000000000000000 ) ) ;
#150107=EDGE_CURVE ( 'NONE', #110910, #258034, #114649, .T. ) ;
#150117=CARTESIAN_POINT ( 'NONE',  ( -21.11101077989000174, 65.53510346643489015, -242.0508478410367275 ) ) ;
#150136=ORIENTED_EDGE ( 'NONE', *, *, #14765, .F. ) ;
#150137=LINE ( 'NONE', #229655, #132437 ) ;
#150149=AXIS2_PLACEMENT_3D ( 'NONE', #254822, #56640, #93230 ) ;
#150176=CARTESIAN_POINT ( 'NONE',  ( 20.95539060131842746, 58.98120222732934792, -225.6874131423334404 ) ) ;
#150222=VERTEX_POINT ( 'NONE', #40282 ) ;
#150233=ORIENTED_EDGE ( 'NONE', *, *, #228535, .T. ) ;
#150269=FACE_OUTER_BOUND ( 'NONE', #122493, .T. ) ;
#150291=ORIENTED_EDGE ( 'NONE', *, *, #86441, .T. ) ;
#150304=LINE ( 'NONE', #107303, #158953 ) ;
#150312=CARTESIAN_POINT ( 'NONE',  ( 23.24999999999999289, 62.92003201576280702, -207.2439188921395612 ) ) ;
#150328=CARTESIAN_POINT ( 'NONE',  ( -18.59999999999999787, 52.81534179157634412, -244.1198638051726277 ) ) ;
#150337=CIRCLE ( 'NONE', #12977, 0.1000000000000124678 ) ;
#150346=FACE_OUTER_BOUND ( 'NONE', #135877, .T. ) ;
#150369=FACE_OUTER_BOUND ( 'NONE', #215260, .T. ) ;
#150388=VECTOR ( 'NONE', #18946, 1000.000000000000000 ) ;
#150401=CARTESIAN_POINT ( 'NONE',  ( 23.14999999999999858, 72.23597390491818260, -202.5022707907005497 ) ) ;
#150410=ORIENTED_EDGE ( 'NONE', *, *, #97112, .F. ) ;
#150442=ORIENTED_EDGE ( 'NONE', *, *, #881, .T. ) ;
#150447=CYLINDRICAL_SURFACE ( 'NONE', #153137, 0.09999999999998657185 ) ;
#150467=ADVANCED_FACE ( 'NONE', ( #76162 ), #69819, .T. ) ;
#150473=ORIENTED_EDGE ( 'NONE', *, *, #85633, .F. ) ;
#150490=DIRECTION ( 'NONE',  ( 0.000000000000000000, -0.2617529984165152257, -0.9651348961777124202 ) ) ;
#150496=AXIS2_PLACEMENT_3D ( 'NONE', #189876, #191185, #152056 ) ;
#150525=ADVANCED_FACE ( 'NONE', ( #114004 ), #119160, .T. ) ;
#150532=DIRECTION ( 'NONE',  ( 0.000000000000000000, -0.9651348961777028723, 0.2617529984165503087 ) ) ;
#150546=DIRECTION ( 'NONE',  ( 0.000000000000000000, 0.9209589331071864615, -0.3896596508878908960 ) ) ;
#150591=VERTEX_POINT ( 'NONE', #179159 ) ;
#150634=ORIENTED_EDGE ( 'NONE', *, *, #73056, .T. ) ;
#150643=( BOUNDED_SURFACE ( )  B_SPLINE_SURFACE ( 3, 2, ( 
 ( #6337, #8924, #184991 ),
 ( #85853, #27235, #46748 ),
 ( #166747, #126288, #183717 ),
 ( #145848, #88423, #243679 ),
 ( #225379, #65036, #84552 ),
 ( #222816, #203265, #142001 ) ),
 .UNSPECIFIED., .F., .F., .F. ) 
 B_SPLINE_SURFACE_WITH_KNOTS ( ( 4, 2, 4 ),
 ( 3, 3 ),
 ( 0.0001381104793128067206, 0.0002947094729387610568, 0.0004513084665647153931 ),
 ( 0.000000000000000000, 1.000000000000000000 ),
 .UNSPECIFIED. ) 
 GEOMETRIC_REPRESENTATION_ITEM ( )  RATIONAL_B_SPLINE_SURFACE ( (
 ( 1.000000000000000000, 0.7071067811865505703, 1.000000000000000000),
 ( 1.000000000000000000, 0.6919563088103167781, 1.000000000000000000),
 ( 1.000000000000000000, 0.6959445945713532700, 1.000000000000000000),
 ( 1.000000000000000000, 0.7137882985316233997, 1.000000000000000000),
 ( 1.000000000000000000, 0.7257496306093990102, 1.000000000000000000),
 ( 1.000000000000000000, 0.7250110520820101101, 1.000000000000000000) ) ) 
 REPRESENTATION_ITEM ( '' )  SURFACE ( )  );
#150651=CARTESIAN_POINT ( 'NONE',  ( 20.94999999999999929, 67.70174932746996888, -211.7710791003628401 ) ) ;
#150684=ORIENTED_EDGE ( 'NONE', *, *, #243558, .F. ) ;
#150730=FACE_OUTER_BOUND ( 'NONE', #34452, .T. ) ;
#150746=CIRCLE ( 'NONE', #67540, 0.09999999999999789613 ) ;
#150752=CARTESIAN_POINT ( 'NONE',  ( 21.04999999999999716, 61.15213033694344347, -234.1846142192326283 ) ) ;
#150762=CARTESIAN_POINT ( 'NONE',  ( 20.94999999999999929, 76.00000000001126921, -203.5231074845248997 ) ) ;
#150793=ORIENTED_EDGE ( 'NONE', *, *, #249033, .F. ) ;
#150804=EDGE_CURVE ( 'NONE', #29169, #162073, #253129, .T. ) ;
#150825=CARTESIAN_POINT ( 'NONE',  ( 18.51024323315077069, 67.49344847133113490, -195.4961807846321733 ) ) ;
#150831=CARTESIAN_POINT ( 'NONE',  ( 18.50000000000000000, 86.87366311306882949, -199.3414869250131858 ) ) ;
#150834=CARTESIAN_POINT ( 'NONE',  ( -20.15000000000000568, 61.49644909750671928, -221.5036531391373273 ) ) ;
#150846=AXIS2_PLACEMENT_3D ( 'NONE', #147252, #170726, #250209 ) ;
#150889=AXIS2_PLACEMENT_3D ( 'NONE', #203421, #65179, #2631 ) ;
#150914=AXIS2_PLACEMENT_3D ( 'NONE', #89360, #11132, #247155 ) ;
#150955=CARTESIAN_POINT ( 'NONE',  ( -23.15000000000000213, 78.98983215084128062, -228.7927651294584450 ) ) ;
#151018=EDGE_LOOP ( 'NONE', ( #54171, #229290, #26930 ) ) ;
#151020=DIRECTION ( 'NONE',  ( 1.000000000000000000, 0.000000000000000000, 0.000000000000000000 ) ) ;
#151042=DIRECTION ( 'NONE',  ( 2.952720810173290098E-16, 0.9651348961777149738, -0.2617529984165062884 ) ) ;
#151044=DIRECTION ( 'NONE',  ( -1.000000000000000000, -0.000000000000000000, 0.000000000000000000 ) ) ;
#151070=CARTESIAN_POINT ( 'NONE',  ( 18.50000000000000000, 86.87366311306882949, -199.3414869250131858 ) ) ;
#151073=EDGE_CURVE ( 'NONE', #130099, #174276, #184047, .T. ) ;
#151096=VERTEX_POINT ( 'NONE', #244011 ) ;
#151118=ORIENTED_EDGE ( 'NONE', *, *, #154585, .T. ) ;
#151125=DIRECTION ( 'NONE',  ( -0.000000000000000000, -0.2617529984165031243, -0.9651348961777157509 ) ) ;
#151133=CYLINDRICAL_SURFACE ( 'NONE', #85478, 0.1000000000000124678 ) ;
#151147=DIRECTION ( 'NONE',  ( 0.000000000000000000, -0.9651348961777157509, 0.2617529984165031243 ) ) ;
#151161=EDGE_LOOP ( 'NONE', ( #70725, #134321, #102047, #222837 ) ) ;
#151193=DIRECTION ( 'NONE',  ( -7.304098846218490641E-16, -0.9651348961777379554, 0.2617529984164210233 ) ) ;
#151195=AXIS2_PLACEMENT_3D ( 'NONE', #128971, #51967, #131524 ) ;
#151196=EDGE_CURVE ( 'NONE', #25796, #114377, #53416, .T. ) ;
#151200=ORIENTED_EDGE ( 'NONE', *, *, #168861, .T. ) ;
#151207=CARTESIAN_POINT ( 'NONE',  ( 18.41356215285960474, 78.24072131640578220, -231.5548844243369047 ) ) ;
#151215=ADVANCED_FACE ( 'NONE', ( #13131 ), #92643, .T. ) ;
#151240=VERTEX_POINT ( 'NONE', #174811 ) ;
#151251=CARTESIAN_POINT ( 'NONE',  ( -18.59999999999999787, 68.49522935589659767, -224.1230159437372436 ) ) ;
#151285=ORIENTED_EDGE ( 'NONE', *, *, #155090, .F. ) ;
#151289=DIRECTION ( 'NONE',  ( 0.000000000000000000, -0.3896596508880098009, -0.9209589331071360574 ) ) ;
#151338=DIRECTION ( 'NONE',  ( 0.000000000000000000, -0.2617529984165031243, -0.9651348961777157509 ) ) ;
#151339=FACE_OUTER_BOUND ( 'NONE', #112375, .T. ) ;
#151342=DIRECTION ( 'NONE',  ( 0.000000000000000000, 0.9651348961777157509, -0.2617529984165031243 ) ) ;
#151363=PLANE ( 'NONE',  #127901 ) ;
#151411=CARTESIAN_POINT ( 'NONE',  ( 20.94999999999999929, 77.04701199367727327, -199.6625678998140359 ) ) ;
#151417=DIRECTION ( 'NONE',  ( 0.000000000000000000, 0.2617529984165031243, 0.9651348961777157509 ) ) ;
#151423=VERTEX_POINT ( 'NONE', #66369 ) ;
#151435=CYLINDRICAL_SURFACE ( 'NONE', #122699, 0.09999999999999939493 ) ;
#151453=VERTEX_POINT ( 'NONE', #25969 ) ;
#151463=CARTESIAN_POINT ( 'NONE',  ( 20.95576188350343116, 58.98444046482349279, -225.7323267698970426 ) ) ;
#151464=AXIS2_PLACEMENT_3D ( 'NONE', #176268, #77133, #236207 ) ;
#151487=( BOUNDED_SURFACE ( )  B_SPLINE_SURFACE ( 3, 2, ( 
 ( #17069, #253075, #156599 ),
 ( #54869, #136988, #117437 ),
 ( #35371, #96558, #99127 ),
 ( #18328, #58713, #178728 ) ),
 .UNSPECIFIED., .F., .F., .F. ) 
 B_SPLINE_SURFACE_WITH_KNOTS ( ( 4, 4 ),
 ( 3, 3 ),
 ( 0.0002700421466196706831, 0.0004789321604330953582 ),
 ( 0.000000000000000000, 1.000000000000000000 ),
 .UNSPECIFIED. ) 
 GEOMETRIC_REPRESENTATION_ITEM ( )  RATIONAL_B_SPLINE_SURFACE ( (
 ( 1.000000000000000000, 0.7071067811865475727, 1.000000000000000000),
 ( 1.000000000000000000, 0.7163411249510942547, 1.000000000000000000),
 ( 1.000000000000000000, 0.7221957104842546826, 1.000000000000000000),
 ( 1.000000000000000000, 0.7250110520819882387, 1.000000000000000000) ) ) 
 REPRESENTATION_ITEM ( '' )  SURFACE ( )  );
#151502=CIRCLE ( 'NONE', #205443, 0.1999999999999981515 ) ;
#151515=ORIENTED_EDGE ( 'NONE', *, *, #60497, .F. ) ;
#151531=EDGE_CURVE ( 'NONE', #4833, #227798, #41147, .T. ) ;
#151550=CARTESIAN_POINT ( 'NONE',  ( -18.59999999999999787, 67.23127455305841238, -235.8551265064783991 ) ) ;
#151593=CARTESIAN_POINT ( 'NONE',  ( 21.14999999999999858, 59.16775194334852017, -221.0793150863668473 ) ) ;
#151641=CONICAL_SURFACE ( 'NONE', #168219, 4.049999999999987388, 0.7853981633974604915 ) ;
#151657=CARTESIAN_POINT ( 'NONE',  ( 20.04142135623730070, 61.57587952878035509, -212.2000740415318774 ) ) ;
#151663=ORIENTED_EDGE ( 'NONE', *, *, #117769, .F. ) ;
#151673=AXIS2_PLACEMENT_3D ( 'NONE', #86984, #204382, #88267 ) ;
#151675=CARTESIAN_POINT ( 'NONE',  ( 20.94999999999999574, 79.13126459505528487, -235.8705213229730191 ) ) ;
#151676=CYLINDRICAL_SURFACE ( 'NONE', #11793, 0.1000000000000124678 ) ;
#151685=CYLINDRICAL_SURFACE ( 'NONE', #41088, 0.09999999999999939493 ) ;
#151692=TOROIDAL_SURFACE ( 'NONE', #26781, 11.70000000000000107, 0.1000000000000000056 ) ;
#151718=CIRCLE ( 'NONE', #18398, 3.899999999999987477 ) ;
#151740=CARTESIAN_POINT ( 'NONE',  ( -20.64999999999999858, 78.17003882911672008, -228.8770135013149911 ) ) ;
#151757=FACE_OUTER_BOUND ( 'NONE', #141491, .T. ) ;
#151828=CARTESIAN_POINT ( 'NONE',  ( 20.94999999999999929, 72.02722222756959525, -225.1832529173024398 ) ) ;
#151836=CIRCLE ( 'NONE', #172708, 4.000000000000000000 ) ;
#151894=ORIENTED_EDGE ( 'NONE', *, *, #139756, .F. ) ;
#151915=B_SPLINE_CURVE_WITH_KNOTS ( 'NONE', 3,
 ( #55354, #197464, #235306, #231482, #112808, #252294, #77495, #157081, #133648, #37140 ),
 .UNSPECIFIED., .F., .F.,
 ( 4, 3, 3, 4 ),
 ( 0.000000000000000000, 0.0002000000000002737706, 0.001000000000045111938, 0.001967863649472118698 ),
 .UNSPECIFIED. ) ;
#151934=ORIENTED_EDGE ( 'NONE', *, *, #148172, .F. ) ;
#151936=EDGE_CURVE ( 'NONE', #35199, #118789, #99533, .T. ) ;
#151959=ORIENTED_EDGE ( 'NONE', *, *, #202958, .T. ) ;
#151961=CIRCLE ( 'NONE', #47854, 0.09999999999999095723 ) ;
#151962=CARTESIAN_POINT ( 'NONE',  ( -23.15000000000000213, 70.80971041069356886, -215.3055740759912453 ) ) ;
#151977=DIRECTION ( 'NONE',  ( 0.000000000000000000, 0.2617529984165152257, 0.9651348961777124202 ) ) ;
#151994=DIRECTION ( 'NONE',  ( 0.000000000000000000, 0.9229812358755983270, -0.3848449534832869001 ) ) ;
#152027=LINE ( 'NONE', #93304, #202742 ) ;
#152056=DIRECTION ( 'NONE',  ( 0.000000000000000000, 0.2617529984165030132, 0.9651348961777157509 ) ) ;
#152075=DIRECTION ( 'NONE',  ( 1.000000000000000000, 0.000000000000000000, 0.000000000000000000 ) ) ;
#152089=VECTOR ( 'NONE', #203116, 1000.000000000000227 ) ;
#152096=FACE_OUTER_BOUND ( 'NONE', #43428, .T. ) ;
#152104=VERTEX_POINT ( 'NONE', #227062 ) ;
#152110=DIRECTION ( 'NONE',  ( 0.000000000000000000, 0.9229812358756199764, -0.3848449534832346086 ) ) ;
#152117=EDGE_CURVE ( 'NONE', #57260, #242049, #212199, .T. ) ;
#152239=CIRCLE ( 'NONE', #218823, 0.1000000000000124678 ) ;
#152245=CARTESIAN_POINT ( 'NONE',  ( -22.59080734064477980, 55.88289069467541736, -232.8092063914161542 ) ) ;
#152259=CIRCLE ( 'NONE', #10766, 0.1000000000000124678 ) ;
#152265=DIRECTION ( 'NONE',  ( 1.000000000000000000, 0.000000000000000000, 0.000000000000000000 ) ) ;
#152297=CARTESIAN_POINT ( 'NONE',  ( -21.00250684356852560, 57.72708596625226818, -226.0092949377465459 ) ) ;
#152311=DIRECTION ( 'NONE',  ( -1.836970198721029934E-16, -0.9651348961777157509, 0.2617529984165031243 ) ) ;
#152313=FACE_OUTER_BOUND ( 'NONE', #199399, .T. ) ;
#152363=DIRECTION ( 'NONE',  ( -1.000000000000000000, -0.000000000000000000, -0.000000000000000000 ) ) ;
#152368=EDGE_CURVE ( 'NONE', #40380, #204366, #133084, .T. ) ;
#152382=ORIENTED_EDGE ( 'NONE', *, *, #136249, .F. ) ;
#152398=ORIENTED_EDGE ( 'NONE', *, *, #229001, .T. ) ;
#152408=CARTESIAN_POINT ( 'NONE',  ( 21.05000000000000071, 86.32947205150912851, -209.3293116780858156 ) ) ;
#152416=ORIENTED_EDGE ( 'NONE', *, *, #111278, .T. ) ;
#152430=CARTESIAN_POINT ( 'NONE',  ( 21.14999999999999858, 60.91865828504416669, -234.1430899377568267 ) ) ;
#152459=CARTESIAN_POINT ( 'NONE',  ( -21.04999999999999716, 78.33723480602354527, -231.5810597241785729 ) ) ;
#152470=CARTESIAN_POINT ( 'NONE',  ( 20.21494484322227692, 60.43554925037637560, -225.3705126911073648 ) ) ;
#152520=VERTEX_POINT ( 'NONE', #203355 ) ;
#152536=DIRECTION ( 'NONE',  ( 0.000000000000000000, -0.2617529984165152257, -0.9651348961777124202 ) ) ;
#152540=CARTESIAN_POINT ( 'NONE',  ( 21.05000000000000071, 62.99095723518624368, -207.1734234082435080 ) ) ;
#152579=DIRECTION ( 'NONE',  ( 0.000000000000000000, 0.2617529984165152257, 0.9651348961777124202 ) ) ;
#152627=CIRCLE ( 'NONE', #11126, 0.09999999999999868716 ) ;
#152637=FACE_OUTER_BOUND ( 'NONE', #114929, .T. ) ;
#152692=CIRCLE ( 'NONE', #156780, 0.09999999999999939493 ) ;
#152714=CARTESIAN_POINT ( 'NONE',  ( 19.99999999999998934, 62.39550153362034735, -208.7959266050682459 ) ) ;
#152726=CARTESIAN_POINT ( 'NONE',  ( -21.05000000000000071, 67.23127455305841238, -235.8551265064783991 ) ) ;
#152781=DIRECTION ( 'NONE',  ( -0.000000000000000000, 0.9651348961777157509, -0.2617529984165031243 ) ) ;
#152786=EDGE_CURVE ( 'NONE', #171580, #12386, #54539, .T. ) ;
#152823=ORIENTED_EDGE ( 'NONE', *, *, #147088, .F. ) ;
#152851=DIRECTION ( 'NONE',  ( 0.000000000000000000, 0.2617529984165033463, 0.9651348961777157509 ) ) ;
#152856=CARTESIAN_POINT ( 'NONE',  ( 21.05000000000000071, 60.94483358488582070, -234.0465764481390636 ) ) ;
#152860=DIRECTION ( 'NONE',  ( -1.000000000000000000, -0.000000000000000000, 0.000000000000000000 ) ) ;
#152886=CARTESIAN_POINT ( 'NONE',  ( -18.50000000000000000, 52.91185528119410719, -244.1460391050142960 ) ) ;
#152897=CARTESIAN_POINT ( 'NONE',  ( -23.25000000000000000, 78.57160958314655375, -238.9307242378722833 ) ) ;
#152945=ORIENTED_EDGE ( 'NONE', *, *, #158933, .T. ) ;
#152946=CARTESIAN_POINT ( 'NONE',  ( 23.14999999999998437, 67.23127455305841238, -235.8551265064783991 ) ) ;
#152967=EDGE_LOOP ( 'NONE', ( #162040, #10812, #145940 ) ) ;
#152972=FACE_OUTER_BOUND ( 'NONE', #87535, .T. ) ;
#153018=ADVANCED_FACE ( 'NONE', ( #131194 ), #32129, .T. ) ;
#153037=CARTESIAN_POINT ( 'NONE',  ( 21.14999999999999858, 56.01362831242965967, -232.7091905853083347 ) ) ;
#153056=EDGE_CURVE ( 'NONE', #210631, #207046, #216820, .T. ) ;
#153099=CARTESIAN_POINT ( 'NONE',  ( -20.85000000000000142, 62.88396779178383156, -206.9948552354529170 ) ) ;
#153100=EDGE_CURVE ( 'NONE', #88353, #220738, #125079, .T. ) ;
#153121=EDGE_LOOP ( 'NONE', ( #234539, #153774, #87616, #168116 ) ) ;
#153123=CIRCLE ( 'NONE', #132811, 0.1999999999999945155 ) ;
#153125=VERTEX_POINT ( 'NONE', #153380 ) ;
#153137=AXIS2_PLACEMENT_3D ( 'NONE', #228698, #89156, #56110 ) ;
#153166=ORIENTED_EDGE ( 'NONE', *, *, #237101, .T. ) ;
#153173=FACE_OUTER_BOUND ( 'NONE', #165575, .T. ) ;
#153205=FACE_OUTER_BOUND ( 'NONE', #167368, .T. ) ;
#153230=ADVANCED_FACE ( 'NONE', ( #137597 ), #59329, .T. ) ;
#153231=ORIENTED_EDGE ( 'NONE', *, *, #207916, .T. ) ;
#153245=EDGE_CURVE ( 'NONE', #99302, #20693, #155927, .T. ) ;
#153275=COLOUR_RGB ( '', 0.66274510, 0.83137255, 0.94901961) ;
#153316=ADVANCED_FACE ( 'NONE', ( #646 ), #42066, .T. ) ;
#153317=CARTESIAN_POINT ( 'NONE',  ( -21.37071067811865532, 65.00420125700266283, -213.2334772433522687 ) ) ;
#153321=CARTESIAN_POINT ( 'NONE',  ( -22.50000000000000000, 59.68594599439717285, -233.9123800762197902 ) ) ;
#153347=AXIS2_PLACEMENT_3D ( 'NONE', #55097, #16034, #38154 ) ;
#153353=CARTESIAN_POINT ( 'NONE',  ( 20.85000000000000142, 80.73028107938317532, -192.7673210925340186 ) ) ;
#153380=CARTESIAN_POINT ( 'NONE',  ( -20.54999999999999716, 68.37653524343949130, -222.4633752038642172 ) ) ;
#153396=DIRECTION ( 'NONE',  ( 1.000000000000000000, 0.000000000000000000, 0.000000000000000000 ) ) ;
#153419=CARTESIAN_POINT ( 'NONE',  ( -23.15000000000000213, 86.27712145182582049, -209.5223386573213702 ) ) ;
#153428=CARTESIAN_POINT ( 'NONE',  ( 22.50000000000000000, 55.96169194136206215, -232.9023299069559130 ) ) ;
#153459=EDGE_LOOP ( 'NONE', ( #27129, #137313, #138604, #80004 ) ) ;
#153492=EDGE_CURVE ( 'NONE', #147319, #223586, #46218, .T. ) ;
#153507=EDGE_CURVE ( 'NONE', #32310, #190202, #87800, .T. ) ;
#153513=CARTESIAN_POINT ( 'NONE',  ( 0.000000000000000000, 0.000000000000000000, 0.000000000000000000 ) ) ;
#153545=VERTEX_POINT ( 'NONE', #135697 ) ;
#153550=CARTESIAN_POINT ( 'NONE',  ( -22.57320508075687115, 55.89093952297024970, -232.7795287750844579 ) ) ;
#153560=FACE_OUTER_BOUND ( 'NONE', #227463, .T. ) ;
#153604=EDGE_CURVE ( 'NONE', #95393, #91550, #91914, .T. ) ;
#153629=CIRCLE ( 'NONE', #141119, 11.74999999999999467 ) ;
#153637=ADVANCED_FACE ( 'NONE', ( #97837 ), #19631, .T. ) ;
#153640=AXIS2_PLACEMENT_3D ( 'NONE', #47283, #167290, #149000 ) ;
#153648=PRODUCT_DEFINITION_SHAPE ( 'NONE', 'NONE',  #121752 ) ;
#153655=CARTESIAN_POINT ( 'NONE',  ( 18.49999999999999645, 76.00000000001126921, -203.5231074845248997 ) ) ;
#153659=DIRECTION ( 'NONE',  ( -1.000000000000000000, 2.849773892568378313E-16, -7.728835255496647986E-17 ) ) ;
#153682=FACE_OUTER_BOUND ( 'NONE', #41474, .T. ) ;
#153684=DIRECTION ( 'NONE',  ( 1.000000000000000000, 0.000000000000000000, 0.000000000000000000 ) ) ;
#153708=DIRECTION ( 'NONE',  ( 1.000000000000000000, 0.000000000000000000, 0.000000000000000000 ) ) ;
#153719=CARTESIAN_POINT ( 'NONE',  ( 21.05000000000000071, 62.82351852614505106, -207.2177435922979214 ) ) ;
#153723=DIRECTION ( 'NONE',  ( 1.000000000000000000, 0.000000000000000000, 0.000000000000000000 ) ) ;
#153737=LINE ( 'NONE', #54569, #238383 ) ;
#153774=ORIENTED_EDGE ( 'NONE', *, *, #101873, .T. ) ;
#153780=CARTESIAN_POINT ( 'NONE',  ( 20.21567752745037794, 59.45201827013453055, -225.5779475914478382 ) ) ;
#153781=FACE_OUTER_BOUND ( 'NONE', #72399, .T. ) ;
#153814=AXIS2_PLACEMENT_3D ( 'NONE', #84472, #164072, #124943 ) ;
#153868=PLANE ( 'NONE',  #257558 ) ;
#153872=AXIS2_PLACEMENT_3D ( 'NONE', #127787, #63954, #86044 ) ;
#153904=EDGE_CURVE ( 'NONE', #88487, #216022, #138066, .T. ) ;
#153915=AXIS2_PLACEMENT_3D ( 'NONE', #167447, #246942, #141426 ) ;
#154038=DIRECTION ( 'NONE',  ( 1.000000000000000000, -2.849773892568378313E-16, 7.728835255496647986E-17 ) ) ;
#154056=DIRECTION ( 'NONE',  ( 1.000000000000000000, 0.000000000000000000, -0.000000000000000000 ) ) ;
#154072=AXIS2_PLACEMENT_3D ( 'NONE', #257208, #156910, #197285 ) ;
#154085=CIRCLE ( 'NONE', #174942, 11.64999999999998614 ) ;
#154108=ORIENTED_EDGE ( 'NONE', *, *, #53445, .F. ) ;
#154145=VECTOR ( 'NONE', #100055, 1000.000000000000000 ) ;
#154151=DIRECTION ( 'NONE',  ( 0.000000000000000000, -0.2617529984165152257, -0.9651348961777124202 ) ) ;
#154153=ORIENTED_EDGE ( 'NONE', *, *, #75895, .T. ) ;
#154168=EDGE_LOOP ( 'NONE', ( #138344, #35258, #67412, #78431 ) ) ;
#154176=ORIENTED_EDGE ( 'NONE', *, *, #240821, .T. ) ;
#154180=DIRECTION ( 'NONE',  ( 0.000000000000000000, 0.9651348961777379554, -0.2617529984164210233 ) ) ;
#154224=DIRECTION ( 'NONE',  ( 0.000000000000000000, 0.8636236514130390951, -0.5041370733441546959 ) ) ;
#154258=LINE ( 'NONE', #195924, #16072 ) ;
#154318=ORIENTED_EDGE ( 'NONE', *, *, #137613, .T. ) ;
#154379=EDGE_CURVE ( 'NONE', #56792, #239682, #109212, .T. ) ;
#154381=DIRECTION ( 'NONE',  ( -1.000000000000000000, -0.000000000000000000, -0.000000000000000000 ) ) ;
#154396=AXIS2_PLACEMENT_3D ( 'NONE', #126838, #111127, #30323 ) ;
#154465=DIRECTION ( 'NONE',  ( 1.000000000000000000, 0.000000000000000000, 0.000000000000000000 ) ) ;
#154470=DIRECTION ( 'NONE',  ( 1.000000000000000000, 0.000000000000000000, 0.000000000000000000 ) ) ;
#154488=DIRECTION ( 'NONE',  ( 1.000000000000000000, 0.000000000000000000, 0.000000000000000000 ) ) ;
#154501=DIRECTION ( 'NONE',  ( 0.000000000000000000, -0.5378121776619179117, 0.8430646840892729310 ) ) ;
#154519=ORIENTED_EDGE ( 'NONE', *, *, #212877, .F. ) ;
#154556=LINE ( 'NONE', #71155, #166749 ) ;
#154581=CARTESIAN_POINT ( 'NONE',  ( -18.43473496883401808, 78.23946247294885836, -231.5402422415359069 ) ) ;
#154585=EDGE_CURVE ( 'NONE', #142261, #47050, #145502, .T. ) ;
#154600=ORIENTED_EDGE ( 'NONE', *, *, #238048, .T. ) ;
#154610=CARTESIAN_POINT ( 'NONE',  ( -23.25000000000000000, 79.19526988099229925, -196.1889237952725296 ) ) ;
#154635=CARTESIAN_POINT ( 'NONE',  ( 21.05000000000000071, 60.94483358488582070, -234.0465764481390636 ) ) ;
#154646=CARTESIAN_POINT ( 'NONE',  ( -20.54999999999999361, 61.57587952878036930, -212.2000740415318774 ) ) ;
#154655=CARTESIAN_POINT ( 'NONE',  ( -21.14999999999999858, 55.91711482281189660, -232.6830152854666949 ) ) ;
#154667=CARTESIAN_POINT ( 'NONE',  ( -18.50000000000000000, 67.49463558145298236, -195.5618716440587548 ) ) ;
#154671=VERTEX_POINT ( 'NONE', #9849 ) ;
#154709=CARTESIAN_POINT ( 'NONE',  ( -20.54999999999999716, 78.98983215084128062, -228.7927651294584450 ) ) ;
#154743=CARTESIAN_POINT ( 'NONE',  ( -20.94999999999999929, 70.17424292862648372, -198.1782849070719124 ) ) ;
#154766=ORIENTED_EDGE ( 'NONE', *, *, #71734, .F. ) ;
#154791=ORIENTED_EDGE ( 'NONE', *, *, #256043, .F. ) ;
#154794=ADVANCED_FACE ( 'NONE', ( #174108 ), #50556, .T. ) ;
#154856=CARTESIAN_POINT ( 'NONE',  ( 21.05000000000000071, 81.91411460262999356, -215.0718681741873013 ) ) ;
#154864=FACE_OUTER_BOUND ( 'NONE', #241031, .T. ) ;
#154920=EDGE_CURVE ( 'NONE', #695, #148919, #87774, .T. ) ;
#154951=CYLINDRICAL_SURFACE ( 'NONE', #95305, 0.1000000000000124678 ) ;
#154989=EDGE_CURVE ( 'NONE', #81393, #221732, #207769, .T. ) ;
#155005=ORIENTED_EDGE ( 'NONE', *, *, #29941, .F. ) ;
#155011=DIRECTION ( 'NONE',  ( 2.952720810173289112E-16, 0.9651348961777146407, -0.2617529984165072321 ) ) ;
#155017=DIRECTION ( 'NONE',  ( 1.000000000000000000, 0.000000000000000000, 0.000000000000000000 ) ) ;
#155043=VECTOR ( 'NONE', #221835, 1000.000000000000000 ) ;
#155048=CARTESIAN_POINT ( 'NONE',  ( 21.05000000000000071, 82.09643798151613225, -215.4278993322501208 ) ) ;
#155069=VECTOR ( 'NONE', #210424, 1000.000000000000000 ) ;
#155090=EDGE_CURVE ( 'NONE', #248567, #110678, #242102, .T. ) ;
#155093=EDGE_LOOP ( 'NONE', ( #18741, #934, #165073, #9796 ) ) ;
#155146=DIRECTION ( 'NONE',  ( 0.000000000000000000, 0.2617529984165027912, 0.9651348961777157509 ) ) ;
#155161=CIRCLE ( 'NONE', #217636, 0.1999999999999945155 ) ;
#155168=AXIS2_PLACEMENT_3D ( 'NONE', #165552, #207251, #222932 ) ;
#155187=ORIENTED_EDGE ( 'NONE', *, *, #176667, .T. ) ;
#155231=SPHERICAL_SURFACE ( 'NONE', #52580, 0.1000000000000000056 ) ;
#155260=VECTOR ( 'NONE', #35920, 1000.000000000000114 ) ;
#155264=ORIENTED_EDGE ( 'NONE', *, *, #136249, .T. ) ;
#155295=FACE_OUTER_BOUND ( 'NONE', #126486, .T. ) ;
#155307=FACE_OUTER_BOUND ( 'NONE', #77165, .T. ) ;
#155311=EDGE_CURVE ( 'NONE', #208387, #159529, #7970, .T. ) ;
#155356=TOROIDAL_SURFACE ( 'NONE', #113798, 0.2000000000000000111, 0.1000000000000000056 ) ;
#155370=ORIENTED_EDGE ( 'NONE', *, *, #11374, .F. ) ;
#155381=ORIENTED_EDGE ( 'NONE', *, *, #115851, .F. ) ;
#155412=B_SPLINE_CURVE_WITH_KNOTS ( 'NONE', 3,
 ( #143966, #65724, #67010, #203948, #164836, #22772, #100942, #142669, #185678, #145247 ),
 .UNSPECIFIED., .F., .F.,
 ( 4, 3, 3, 4 ),
 ( 0.000000000000000000, 0.0002000000000002897355, 0.001000000000045110204, 0.001967863649472100917 ),
 .UNSPECIFIED. ) ;
#155426=AXIS2_PLACEMENT_3D ( 'NONE', #203633, #221885, #125391 ) ;
#155481=ORIENTED_EDGE ( 'NONE', *, *, #224159, .T. ) ;
#155488=DIRECTION ( 'NONE',  ( 0.000000000000000000, -0.9651348961777379554, 0.2617529984164210233 ) ) ;
#155531=AXIS2_PLACEMENT_3D ( 'NONE', #118963, #19866, #99360 ) ;
#155593=ORIENTED_EDGE ( 'NONE', *, *, #26444, .F. ) ;
#155606=ORIENTED_EDGE ( 'NONE', *, *, #254879, .T. ) ;
#155690=VERTEX_POINT ( 'NONE', #122477 ) ;
#155695=ORIENTED_EDGE ( 'NONE', *, *, #22513, .F. ) ;
#155699=CIRCLE ( 'NONE', #39169, 0.09999999999999939493 ) ;
#155707=VERTEX_POINT ( 'NONE', #45493 ) ;
#155752=CARTESIAN_POINT ( 'NONE',  ( -22.47120815636973745, 64.15397383650149266, -247.0913167448723868 ) ) ;
#155755=CIRCLE ( 'NONE', #105812, 0.1000000000000124678 ) ;
#155761=CARTESIAN_POINT ( 'NONE',  ( -20.64999999999999858, 63.53703427598990316, -222.1606900896233583 ) ) ;
#155765=EDGE_LOOP ( 'NONE', ( #255732, #235426, #217260, #183916, #185505 ) ) ;
#155766=CIRCLE ( 'NONE', #43329, 0.1000000000000124678 ) ;
#155772=CARTESIAN_POINT ( 'NONE',  ( -22.49806830649814060, 55.96728299348496449, -232.8804964729971232 ) ) ;
#155802=FACE_OUTER_BOUND ( 'NONE', #79704, .T. ) ;
#155818=ORIENTED_EDGE ( 'NONE', *, *, #225859, .T. ) ;
#155836=DIRECTION ( 'NONE',  ( 0.000000000000000000, -0.7092521942343630315, -0.7049548389604409770 ) ) ;
#155852=DIRECTION ( 'NONE',  ( 0.000000000000000000, 0.2617529984164915779, 0.9651348961777189706 ) ) ;
#155927=LINE ( 'NONE', #112926, #150388 ) ;
#155936=VERTEX_POINT ( 'NONE', #197828 ) ;
#155944=DIRECTION ( 'NONE',  ( 0.000000000000000000, 0.2617529984164856383, 0.9651348961777204138 ) ) ;
#155961=DIRECTION ( 'NONE',  ( -1.000000000000000000, -0.000000000000000000, -0.000000000000000000 ) ) ;
#155987=CARTESIAN_POINT ( 'NONE',  ( 18.49999999999998934, 67.49462292596862767, -195.5612049585272700 ) ) ;
#156005=DIRECTION ( 'NONE',  ( 0.000000000000000000, -0.2617529984165031243, -0.9651348961777157509 ) ) ;
#156048=EDGE_CURVE ( 'NONE', #177022, #104140, #141706, .T. ) ;
#156066=ORIENTED_EDGE ( 'NONE', *, *, #140428, .T. ) ;
#156068=CYLINDRICAL_SURFACE ( 'NONE', #125978, 0.09999999999999939493 ) ;
#156080=AXIS2_PLACEMENT_3D ( 'NONE', #19289, #115824, #38867 ) ;
#156143=AXIS2_PLACEMENT_3D ( 'NONE', #176384, #237626, #214212 ) ;
#156158=CARTESIAN_POINT ( 'NONE',  ( -18.59999999999999787, 68.59681812508419796, -224.1344059333694361 ) ) ;
#156161=CARTESIAN_POINT ( 'NONE',  ( -20.64999999999999858, 76.00000000001126921, -203.5231074845248997 ) ) ;
#156167=VECTOR ( 'NONE', #200308, 1000.000000000000000 ) ;
#156176=CARTESIAN_POINT ( 'NONE',  ( 21.04999999999999716, 58.88961039665833397, -225.7941988232044821 ) ) ;
#156196=CARTESIAN_POINT ( 'NONE',  ( -23.15000000000000213, 70.12557831835937350, -215.6322690948981915 ) ) ;
#156227=VECTOR ( 'NONE', #226397, 1000.000000000000114 ) ;
#156231=ORIENTED_EDGE ( 'NONE', *, *, #165682, .F. ) ;
#156238=AXIS2_PLACEMENT_3D ( 'NONE', #163294, #61617, #221942 ) ;
#156272=EDGE_CURVE ( 'NONE', #20618, #223936, #108992, .T. ) ;
#156276=EDGE_LOOP ( 'NONE', ( #239127, #31303, #158372, #253798 ) ) ;
#156287=CARTESIAN_POINT ( 'NONE',  ( -20.54999999999999716, 68.59518897103603763, -214.2073844195901131 ) ) ;
#156295=VERTEX_POINT ( 'NONE', #71186 ) ;
#156296=CYLINDRICAL_SURFACE ( 'NONE', #131681, 4.049999999999987388 ) ;
#156335=VECTOR ( 'NONE', #136802, 1000.000000000000000 ) ;
#156381=ORIENTED_EDGE ( 'NONE', *, *, #116727, .F. ) ;
#156418=CARTESIAN_POINT ( 'NONE',  ( -22.49999999999999645, 55.86495732666937641, -232.8769840133978164 ) ) ;
#156422=CARTESIAN_POINT ( 'NONE',  ( 21.05000000000000071, 79.33069327855442054, -236.1318330389568985 ) ) ;
#156466=FACE_OUTER_BOUND ( 'NONE', #83126, .T. ) ;
#156476=CIRCLE ( 'NONE', #173044, 0.1000000000000124678 ) ;
#156479=EDGE_CURVE ( 'NONE', #185233, #50777, #180789, .T. ) ;
#156483=VECTOR ( 'NONE', #191246, 1000.000000000000000 ) ;
#156493=ORIENTED_EDGE ( 'NONE', *, *, #27547, .T. ) ;
#156500=CARTESIAN_POINT ( 'NONE',  ( 18.49999999999999289, 70.08587962373171365, -198.1273832143211848 ) ) ;
#156511=EDGE_CURVE ( 'NONE', #133646, #19150, #143359, .T. ) ;
#156527=VECTOR ( 'NONE', #115981, 1000.000000000000114 ) ;
#156562=LINE ( 'NONE', #151411, #78476 ) ;
#156580=ADVANCED_FACE ( 'NONE', ( #134343 ), #36587, .T. ) ;
#156599=CARTESIAN_POINT ( 'NONE',  ( 20.94999999999999929, 60.83337574417770810, -225.3422414619148810 ) ) ;
#156605=FACE_BOUND ( 'NONE', #251107, .T. ) ;
#156606=ORIENTED_EDGE ( 'NONE', *, *, #22050, .F. ) ;
#156617=CYLINDRICAL_SURFACE ( 'NONE', #126424, 0.09999999999999939493 ) ;
#156639=DIRECTION ( 'NONE',  ( 0.000000000000000000, -0.9667078373770112698, -0.2558827019434132821 ) ) ;
#156644=DIRECTION ( 'NONE',  ( 0.7071067811865475727, -0.6824534298470373850, 0.1850873201762210096 ) ) ;
#156674=ORIENTED_EDGE ( 'NONE', *, *, #182569, .F. ) ;
#156690=CARTESIAN_POINT ( 'NONE',  ( -18.59999999999999787, 57.79742415652444265, -226.1319837253768981 ) ) ;
#156696=EDGE_CURVE ( 'NONE', #952, #174802, #168543, .T. ) ;
#156747=ORIENTED_EDGE ( 'NONE', *, *, #190900, .T. ) ;
#156758=CARTESIAN_POINT ( 'NONE',  ( -21.44999999999999929, 65.89281126173843006, -213.4744760240239145 ) ) ;
#156780=AXIS2_PLACEMENT_3D ( 'NONE', #90506, #108791, #85350 ) ;
#156789=EDGE_CURVE ( 'NONE', #84395, #217417, #247599, .T. ) ;
#156791=( BOUNDED_SURFACE ( )  B_SPLINE_SURFACE ( 3, 2, ( 
 ( #9116, #88618, #202176 ),
 ( #168226, #5226, #204726 ),
 ( #6532, #7838, #126485 ),
 ( #225562, #247718, #243859 ),
 ( #223005, #23582, #65224 ),
 ( #103053, #44400, #164345 ),
 ( #104332, #105609, #46928 ),
 ( #183897, #185180, #224298 ),
 ( #206029, #45670, #27431 ),
 ( #50776, #254121, #95058 ) ),
 .UNSPECIFIED., .F., .F., .F. ) 
 B_SPLINE_SURFACE_WITH_KNOTS ( ( 4, 2, 2, 2, 4 ),
 ( 3, 3 ),
 ( 0.0001836757140119138357, 0.0004000170051583584025, 0.0005081876507315807130, 0.0005622729735181917869, 0.0006163582963048029693 ),
 ( 0.000000000000000000, 1.000000000000000000 ),
 .UNSPECIFIED. ) 
 GEOMETRIC_REPRESENTATION_ITEM ( )  RATIONAL_B_SPLINE_SURFACE ( (
 ( 1.000000000000000000, 0.7071067811865933139, 1.000000000000000000),
 ( 1.000000000000000000, 0.6461995200037486953, 1.000000000000000000),
 ( 1.000000000000000000, 0.5776453529538307929, 1.000000000000000000),
 ( 1.000000000000000000, 0.4585233068357276176, 1.000000000000000000),
 ( 1.000000000000000000, 0.4154092989952298254, 1.000000000000000000),
 ( 1.000000000000000000, 0.3550093145831299535, 1.000000000000000000),
 ( 1.000000000000000000, 0.3354498651682248367, 1.000000000000000000),
 ( 1.000000000000000000, 0.3060347992260692429, 1.000000000000000000),
 ( 1.000000000000000000, 0.2963555829624867632, 1.000000000000000000),
 ( 1.000000000000000000, 0.2966190024559665073, 1.000000000000000000) ) ) 
 REPRESENTATION_ITEM ( '' )  SURFACE ( )  );
#156820=AXIS2_PLACEMENT_3D ( 'NONE', #233004, #251240, #191321 ) ;
#156823=LINE ( 'NONE', #40729, #211845 ) ;
#156828=DIRECTION ( 'NONE',  ( 6.938893903906363786E-14, -0.2617529984165152257, -0.9651348961777124202 ) ) ;
#156840=DIRECTION ( 'NONE',  ( 1.836970198721029934E-16, 0.9651348961777157509, -0.2617529984165031243 ) ) ;
#156848=DIRECTION ( 'NONE',  ( 0.000000000000000000, 0.2617529984165046231, 0.9651348961777154178 ) ) ;
#156886=EDGE_CURVE ( 'NONE', #132493, #28102, #28597, .T. ) ;
#156904=AXIS2_PLACEMENT_3D ( 'NONE', #77029, #34103, #177456 ) ;
#156910=DIRECTION ( 'NONE',  ( -1.000000000000000000, -0.000000000000000000, -0.000000000000000000 ) ) ;
#156929=ORIENTED_EDGE ( 'NONE', *, *, #47286, .F. ) ;
#156943=CARTESIAN_POINT ( 'NONE',  ( -23.25000000000000000, 55.89093952297024970, -232.7795287750844579 ) ) ;
#156950=VERTEX_POINT ( 'NONE', #235709 ) ;
#156951=ORIENTED_EDGE ( 'NONE', *, *, #106231, .T. ) ;
#156974=DIRECTION ( 'NONE',  ( 1.000000000000000000, 0.000000000000000000, 0.000000000000000000 ) ) ;
#156979=ORIENTED_EDGE ( 'NONE', *, *, #32969, .T. ) ;
#156988=ORIENTED_EDGE ( 'NONE', *, *, #133924, .T. ) ;
#157005=CARTESIAN_POINT ( 'NONE',  ( 18.59999999999999076, 66.40155400966892785, -213.5088390336144073 ) ) ;
#157011=VECTOR ( 'NONE', #57600, 1000.000000000000000 ) ;
#157030=AXIS2_PLACEMENT_3D ( 'NONE', #65744, #106132, #67032 ) ;
#157036=DIRECTION ( 'NONE',  ( 0.000000000000000000, 0.9651348961777379554, -0.2617529984164210233 ) ) ;
#157046=DIRECTION ( 'NONE',  ( 1.000000000000000000, 0.000000000000000000, 0.000000000000000000 ) ) ;
#157051=TOROIDAL_SURFACE ( 'NONE', #215292, 11.70000000000000462, 0.1000000000000000056 ) ;
#157057=VERTEX_POINT ( 'NONE', #209749 ) ;
#157081=CARTESIAN_POINT ( 'NONE',  ( -21.53551880898958260, 65.35981425085753926, -242.3774659647530996 ) ) ;
#157096=VERTEX_POINT ( 'NONE', #218703 ) ;
#157118=CYLINDRICAL_SURFACE ( 'NONE', #22669, 0.09999999999999149847 ) ;
#157176=ORIENTED_EDGE ( 'NONE', *, *, #161557, .T. ) ;
#157178=AXIS2_PLACEMENT_3D ( 'NONE', #160581, #240096, #220535 ) ;
#157185=EDGE_CURVE ( 'NONE', #235804, #190202, #25664, .T. ) ;
#157202=ADVANCED_FACE ( 'NONE', ( #187315 ), #14775, .T. ) ;
#157223=DIRECTION ( 'NONE',  ( -1.000000000000000000, -0.000000000000000000, 0.000000000000000000 ) ) ;
#157228=FACE_OUTER_BOUND ( 'NONE', #226271, .T. ) ;
#157244=DIRECTION ( 'NONE',  ( -3.265361837132813093E-16, -0.9651348961777146407, 0.2617529984165072321 ) ) ;
#157248=ORIENTED_EDGE ( 'NONE', *, *, #167770, .F. ) ;
#157253=EDGE_LOOP ( 'NONE', ( #112136, #25624, #93120, #86633 ) ) ;
#157262=EDGE_LOOP ( 'NONE', ( #405, #86196, #125550 ) ) ;
#157274=ORIENTED_EDGE ( 'NONE', *, *, #113492, .F. ) ;
#157288=ORIENTED_EDGE ( 'NONE', *, *, #78791, .T. ) ;
#157411=FACE_OUTER_BOUND ( 'NONE', #87048, .T. ) ;
#157430=ORIENTED_EDGE ( 'NONE', *, *, #153245, .T. ) ;
#157470=DIRECTION ( 'NONE',  ( -1.000000000000000000, -0.000000000000000000, -0.000000000000000000 ) ) ;
#157473=CARTESIAN_POINT ( 'NONE',  ( 21.05000000000000071, 67.23127455305841238, -235.8551265064783991 ) ) ;
#157500=AXIS2_PLACEMENT_3D ( 'NONE', #73248, #152781, #232306 ) ;
#157562=CARTESIAN_POINT ( 'NONE',  ( -23.25000000000000000, 76.00000000001126921, -203.5231074845248997 ) ) ;
#157614=CARTESIAN_POINT ( 'NONE',  ( -21.45000000000000284, 63.02410583447655767, -221.9179669651492759 ) ) ;
#157616=ORIENTED_EDGE ( 'NONE', *, *, #256427, .T. ) ;
#157633=ORIENTED_EDGE ( 'NONE', *, *, #106383, .T. ) ;
#157634=EDGE_CURVE ( 'NONE', #125569, #247253, #159826, .T. ) ;
#157649=DIRECTION ( 'NONE',  ( 1.000000000000000000, 0.000000000000000000, 0.000000000000000000 ) ) ;
#157677=ORIENTED_EDGE ( 'NONE', *, *, #104029, .T. ) ;
#157688=ORIENTED_EDGE ( 'NONE', *, *, #172473, .T. ) ;
#157694=AXIS2_PLACEMENT_3D ( 'NONE', #52999, #66487, #204693 ) ;
#157720=EDGE_LOOP ( 'NONE', ( #117703, #187007, #233817, #129934 ) ) ;
#157730=ADVANCED_FACE ( 'NONE', ( #222241 ), #244391, .F. ) ;
#157740=CARTESIAN_POINT ( 'NONE',  ( -21.05000000000000071, 67.23127455305841238, -235.8551265064783991 ) ) ;
#157770=ORIENTED_EDGE ( 'NONE', *, *, #129086, .F. ) ;
#157779=TOROIDAL_SURFACE ( 'NONE', #45290, 2.100000000000002309, 0.1000000000000000056 ) ;
#157798=CARTESIAN_POINT ( 'NONE',  ( -23.24999999999999645, 87.01908966642815813, -199.5693496768551825 ) ) ;
#157813=CIRCLE ( 'NONE', #253425, 11.75000000000000178 ) ;
#157824=DIRECTION ( 'NONE',  ( 1.000000000000000000, 0.000000000000000000, 0.000000000000000000 ) ) ;
#157849=CARTESIAN_POINT ( 'NONE',  ( 21.05000000000000071, 65.63508776066827011, -242.0675804128435971 ) ) ;
#157850=EDGE_CURVE ( 'NONE', #8256, #62695, #53911, .T. ) ;
#157861=ORIENTED_EDGE ( 'NONE', *, *, #133464, .F. ) ;
#157903=DIRECTION ( 'NONE',  ( 1.000000000000000000, 0.000000000000000000, 0.000000000000000000 ) ) ;
#157913=FACE_OUTER_BOUND ( 'NONE', #202129, .T. ) ;
#157928=ORIENTED_EDGE ( 'NONE', *, *, #225668, .F. ) ;
#157935=CARTESIAN_POINT ( 'NONE',  ( -18.59999999999999787, 61.43991280424057777, -221.4883200034892923 ) ) ;
#157965=CARTESIAN_POINT ( 'NONE',  ( -20.07928932188135107, 61.56469444049141515, -221.5221618711549354 ) ) ;
#157982=CARTESIAN_POINT ( 'NONE',  ( 21.11747605621531321, 61.96368823759529221, -221.7396181602011040 ) ) ;
#158004=VERTEX_POINT ( 'NONE', #64037 ) ;
#158016=VECTOR ( 'NONE', #45346, 1000.000000000000000 ) ;
#158032=DIRECTION ( 'NONE',  ( 0.000000000000000000, 0.2617529984165033463, 0.9651348961777156399 ) ) ;
#158033=DIRECTION ( 'NONE',  ( 0.000000000000000000, -0.2617529984165032908, -0.9651348961777156399 ) ) ;
#158043=CARTESIAN_POINT ( 'NONE',  ( -20.54999999999999716, 82.48249193998721296, -215.5326005316167084 ) ) ;
#158051=CARTESIAN_POINT ( 'NONE',  ( -23.25000000000000000, 67.23127455305841238, -235.8551265064783991 ) ) ;
#158117=AXIS2_PLACEMENT_3D ( 'NONE', #228997, #90744, #51596 ) ;
#158152=ADVANCED_FACE ( 'NONE', ( #195781 ), #243668, .T. ) ;
#158165=EDGE_CURVE ( 'NONE', #125182, #223936, #181327, .T. ) ;
#158191=ADVANCED_FACE ( 'NONE', ( #256957 ), #219150, .T. ) ;
#158198=EDGE_CURVE ( 'NONE', #109963, #125, #185411, .T. ) ;
#158210=DIRECTION ( 'NONE',  ( 0.000000000000000000, 0.2617529984165031243, 0.9651348961777157509 ) ) ;
#158240=DIRECTION ( 'NONE',  ( 0.000000000000000000, 0.2617529984164955192, 0.9651348961777178603 ) ) ;
#158260=AXIS2_PLACEMENT_3D ( 'NONE', #40681, #221812, #60188 ) ;
#158266=CARTESIAN_POINT ( 'NONE',  ( 22.39999999999999503, 65.09550114356429162, -243.3481044654562879 ) ) ;
#158289=ORIENTED_EDGE ( 'NONE', *, *, #36196, .T. ) ;
#158333=EDGE_CURVE ( 'NONE', #110369, #129974, #135686, .T. ) ;
#158348=CIRCLE ( 'NONE', #45889, 0.1000000000000124678 ) ;
#158372=ORIENTED_EDGE ( 'NONE', *, *, #80618, .F. ) ;
#158377=FACE_OUTER_BOUND ( 'NONE', #256047, .T. ) ;
#158378=DIRECTION ( 'NONE',  ( 0.000000000000000000, 0.2617529984164915779, 0.9651348961777187485 ) ) ;
#158398=ORIENTED_EDGE ( 'NONE', *, *, #74771, .F. ) ;
#158402=FACE_OUTER_BOUND ( 'NONE', #228845, .T. ) ;
#158431=CARTESIAN_POINT ( 'NONE',  ( -18.43707690579160996, 87.08727414655713517, -199.6327537731850441 ) ) ;
#158444=ORIENTED_EDGE ( 'NONE', *, *, #107735, .F. ) ;
#158459=FACE_OUTER_BOUND ( 'NONE', #233814, .T. ) ;
#158463=VERTEX_POINT ( 'NONE', #70398 ) ;
#158464=DIRECTION ( 'NONE',  ( 0.000000000000000000, 0.9651348961777163060, -0.2617529984165013479 ) ) ;
#158466=EDGE_LOOP ( 'NONE', ( #124012, #172062, #22273, #118228 ) ) ;
#158467=AXIS2_PLACEMENT_3D ( 'NONE', #191306, #192561, #174328 ) ;
#158481=DIRECTION ( 'NONE',  ( 0.7071359030026941328, -0.1850796971396165280, -0.6824253222084246673 ) ) ;
#158510=CARTESIAN_POINT ( 'NONE',  ( -23.15000000000000213, 68.76258920191057200, -222.5680764032308048 ) ) ;
#158544=CARTESIAN_POINT ( 'NONE',  ( 20.94999999999999574, 70.47363787294415260, -228.3418745167492432 ) ) ;
#158547=EDGE_LOOP ( 'NONE', ( #71818, #99645, #10120, #193002, #124228, #122947, #12089, #148082 ) ) ;
#158563=CYLINDRICAL_SURFACE ( 'NONE', #209452, 2.000000000000013323 ) ;
#158572=ORIENTED_EDGE ( 'NONE', *, *, #31124, .F. ) ;
#158582=LINE ( 'NONE', #119442, #73464 ) ;
#158612=ORIENTED_EDGE ( 'NONE', *, *, #52221, .T. ) ;
#158616=CARTESIAN_POINT ( 'NONE',  ( -18.50000000000000000, 61.47936603916259912, -212.1738987416902376 ) ) ;
#158629=CARTESIAN_POINT ( 'NONE',  ( 20.94999999999999929, 82.09643798151613225, -215.4278993322501208 ) ) ;
#158633=B_SPLINE_CURVE_WITH_KNOTS ( 'NONE', 3,
 ( #55719, #79158, #40084, #156176, #136566, #218670 ),
 .UNSPECIFIED., .F., .F.,
 ( 4, 2, 4 ),
 ( 0.000000000000000000, 0.0002113392456165950461, 0.0004226784912331900922 ),
 .UNSPECIFIED. ) ;
#158642=LINE ( 'NONE', #178202, #156167 ) ;
#158647=ORIENTED_EDGE ( 'NONE', *, *, #170606, .F. ) ;
#158658=ORIENTED_EDGE ( 'NONE', *, *, #257363, .T. ) ;
#158696=FACE_OUTER_BOUND ( 'NONE', #91669, .T. ) ;
#158757=DIRECTION ( 'NONE',  ( 0.000000000000000000, 0.7092521942342977503, 0.7049548389605067023 ) ) ;
#158796=CIRCLE ( 'NONE', #92124, 0.09999999999999961697 ) ;
#158799=ORIENTED_EDGE ( 'NONE', *, *, #202284, .T. ) ;
#158808=DIRECTION ( 'NONE',  ( -5.603264701231743991E-32, 0.2617529984165029577, 0.9651348961777157509 ) ) ;
#158824=DIRECTION ( 'NONE',  ( 1.000000000000000000, -2.849773892568378313E-16, 7.728835255496647986E-17 ) ) ;
#158849=ORIENTED_EDGE ( 'NONE', *, *, #165243, .F. ) ;
#158915=ORIENTED_EDGE ( 'NONE', *, *, #182553, .F. ) ;
#158933=EDGE_CURVE ( 'NONE', #101417, #233526, #96579, .T. ) ;
#158951=ORIENTED_EDGE ( 'NONE', *, *, #159619, .F. ) ;
#158953=VECTOR ( 'NONE', #207713, 1000.000000000000000 ) ;
#158961=DIRECTION ( 'NONE',  ( -2.915501640297154283E-16, -0.9651348961777159730, 0.2617529984165023471 ) ) ;
#159025=FACE_OUTER_BOUND ( 'NONE', #45056, .T. ) ;
#159037=VERTEX_POINT ( 'NONE', #82845 ) ;
#159085=CARTESIAN_POINT ( 'NONE',  ( -23.15000000000000213, 86.19075908668452257, -209.4719249499869136 ) ) ;
#159086=DIRECTION ( 'NONE',  ( 0.000000000000000000, 0.2617529984165152257, 0.9651348961777124202 ) ) ;
#159122=EDGE_LOOP ( 'NONE', ( #159330, #27705, #15241, #35459 ) ) ;
#159158=CARTESIAN_POINT ( 'NONE',  ( -20.54999999999999716, 70.12557831835937350, -215.6322690948981915 ) ) ;
#159160=DIRECTION ( 'NONE',  ( 2.952720810173289112E-16, 0.9651348961777157509, -0.2617529984165031243 ) ) ;
#159250=CIRCLE ( 'NONE', #109138, 0.09999999999999939493 ) ;
#159257=ORIENTED_EDGE ( 'NONE', *, *, #610, .F. ) ;
#159266=FACE_OUTER_BOUND ( 'NONE', #202626, .T. ) ;
#159270=CARTESIAN_POINT ( 'NONE',  ( -23.15000000000000213, 68.76258920191057200, -222.5680764032308048 ) ) ;
#159283=ORIENTED_EDGE ( 'NONE', *, *, #99034, .T. ) ;
#159284=ORIENTED_EDGE ( 'NONE', *, *, #39434, .F. ) ;
#159311=DIRECTION ( 'NONE',  ( 0.000000000000000000, -0.2617529984165024026, -0.9651348961777158619 ) ) ;
#159330=ORIENTED_EDGE ( 'NONE', *, *, #47586, .T. ) ;
#159337=CARTESIAN_POINT ( 'NONE',  ( 20.04142135623730070, 61.54970422893870818, -212.2965875311496688 ) ) ;
#159396=CIRCLE ( 'NONE', #42855, 11.64999999999998970 ) ;
#159399=EDGE_LOOP ( 'NONE', ( #19142, #186826, #28514, #16607 ) ) ;
#159412=CIRCLE ( 'NONE', #76168, 0.09999999999999789613 ) ;
#159416=CARTESIAN_POINT ( 'NONE',  ( 20.01093837587850288, 62.37047727546982401, -208.8881959771026686 ) ) ;
#159424=DIRECTION ( 'NONE',  ( 0.000000000000000000, 0.9651348961777118651, -0.2617529984165174461 ) ) ;
#159427=CARTESIAN_POINT ( 'NONE',  ( 21.06089410995839728, 60.07392730735723063, -221.2708047820654826 ) ) ;
#159439=ADVANCED_FACE ( 'NONE', ( #83821 ), #100814, .F. ) ;
#159456=VERTEX_POINT ( 'NONE', #134215 ) ;
#159464=CARTESIAN_POINT ( 'NONE',  ( -21.55000000000000071, 63.34400729675436281, -222.1083394899400503 ) ) ;
#159485=EDGE_CURVE ( 'NONE', #18097, #190202, #19558, .T. ) ;
#159490=ADVANCED_FACE ( 'NONE', ( #186836 ), #9463, .T. ) ;
#159495=AXIS2_PLACEMENT_3D ( 'NONE', #73229, #234841, #37944 ) ;
#159499=CARTESIAN_POINT ( 'NONE',  ( -20.07928932188135107, 63.86812082655664113, -213.0289747847910462 ) ) ;
#159529=VERTEX_POINT ( 'NONE', #212506 ) ;
#159558=CARTESIAN_POINT ( 'NONE',  ( -20.94999999999999929, 86.48473784507379492, -209.3714211149925575 ) ) ;
#159578=( NAMED_UNIT ( * ) SI_UNIT ( $, .STERADIAN. ) SOLID_ANGLE_UNIT ( ) );
#159583=EDGE_CURVE ( 'NONE', #30065, #5530, #118545, .T. ) ;
#159585=ORIENTED_EDGE ( 'NONE', *, *, #71734, .T. ) ;
#159619=EDGE_CURVE ( 'NONE', #252329, #155690, #61240, .T. ) ;
#159669=DIRECTION ( 'NONE',  ( -1.000000000000000000, -0.000000000000000000, 0.000000000000000000 ) ) ;
#159687=ORIENTED_EDGE ( 'NONE', *, *, #133294, .T. ) ;
#159701=CYLINDRICAL_SURFACE ( 'NONE', #191447, 0.1000000000000124678 ) ;
#159703=CARTESIAN_POINT ( 'NONE',  ( 21.05000000000000071, 67.23127455305841238, -235.8551265064783991 ) ) ;
#159718=ADVANCED_FACE ( 'NONE', ( #244875 ), #85768, .T. ) ;
#159728=ORIENTED_EDGE ( 'NONE', *, *, #14990, .F. ) ;
#159734=AXIS2_PLACEMENT_3D ( 'NONE', #95445, #177595, #237538 ) ;
#159751=ORIENTED_EDGE ( 'NONE', *, *, #112336, .T. ) ;
#159761=DIRECTION ( 'NONE',  ( 1.000000000000000000, 0.000000000000000000, -0.000000000000000000 ) ) ;
#159763=AXIS2_PLACEMENT_3D ( 'NONE', #15283, #111807, #93508 ) ;
#159773=ORIENTED_EDGE ( 'NONE', *, *, #96685, .T. ) ;
#159782=EDGE_CURVE ( 'NONE', #87098, #149860, #107196, .T. ) ;
#159793=VERTEX_POINT ( 'NONE', #68829 ) ;
#159819=CIRCLE ( 'NONE', #189035, 11.75000000000000178 ) ;
#159826=( BOUNDED_CURVE ( )  B_SPLINE_CURVE ( 3, ( #215824, #245689, #87868, #48763 ),
 .UNSPECIFIED., .F., .F. ) 
 B_SPLINE_CURVE_WITH_KNOTS ( ( 4, 4 ),
 ( 1.570796326794931197, 3.141592653589758477 ),
 .UNSPECIFIED. ) 
 CURVE ( )  GEOMETRIC_REPRESENTATION_ITEM ( )  RATIONAL_B_SPLINE_CURVE ( ( 1.000000000000000000, 0.8047378541243812577, 0.8047378541243812577, 1.000000000000000000 ) ) 
 REPRESENTATION_ITEM ( '' )  );
#159829=AXIS2_PLACEMENT_3D ( 'NONE', #81401, #3166, #21487 ) ;
#159864=B_SPLINE_CURVE_WITH_KNOTS ( 'NONE', 3,
 ( #36851, #78491, #175094, #98036, #17267, #236293, #137195, #117636 ),
 .UNSPECIFIED., .F., .F.,
 ( 4, 2, 2, 4 ),
 ( 0.000000000000000000, 0.0002181133598169092088, 0.0003271700397253594493, 0.0004362267196338096898 ),
 .UNSPECIFIED. ) ;
#159868=( BOUNDED_SURFACE ( )  B_SPLINE_SURFACE ( 3, 2, ( 
 ( #105365, #182392, #81954 ),
 ( #80687, #164107, #161552 ),
 ( #66289, #23336, #220237 ),
 ( #44162, #184943, #6291 ),
 ( #102814, #181115, #85803 ),
 ( #165389, #41610, #160280 ) ),
 .UNSPECIFIED., .F., .F., .F. ) 
 B_SPLINE_SURFACE_WITH_KNOTS ( ( 4, 2, 4 ),
 ( 3, 3 ),
 ( 6.719893378900182717E-05, 0.0002757154632485606582, 0.0004842319927081195434 ),
 ( 0.000000000000000000, 1.000000000000000000 ),
 .UNSPECIFIED. ) 
 GEOMETRIC_REPRESENTATION_ITEM ( )  RATIONAL_B_SPLINE_SURFACE ( (
 ( 1.000000000000000000, 0.7250110520819763593, 1.000000000000000000),
 ( 1.000000000000000000, 0.7277932058357685641, 1.000000000000000000),
 ( 1.000000000000000000, 0.7278452872619538550, 1.000000000000000000),
 ( 1.000000000000000000, 0.7221445671547270795, 1.000000000000000000),
 ( 1.000000000000000000, 0.7163662143781618363, 1.000000000000000000),
 ( 1.000000000000000000, 0.7071067811865475727, 1.000000000000000000) ) ) 
 REPRESENTATION_ITEM ( '' )  SURFACE ( )  );
#159875=VERTEX_POINT ( 'NONE', #187500 ) ;
#159877=DIRECTION ( 'NONE',  ( 0.000000000000000000, 0.2617529984165030132, 0.9651348961777156399 ) ) ;
#159899=ORIENTED_EDGE ( 'NONE', *, *, #15494, .T. ) ;
#159904=AXIS2_PLACEMENT_3D ( 'NONE', #165539, #32469, #49427 ) ;
#159905=B_SPLINE_CURVE_WITH_KNOTS ( 'NONE', 3,
 ( #193812, #155987, #92134, #234199, #56824, #71316, #249931, #150825, #230357, #51695, #131260, #171709, #240630, #99803, #41177, #38583, #97221, #197643, #162395 ),
 .UNSPECIFIED., .F., .F.,
 ( 4, 3, 3, 3, 3, 3, 4 ),
 ( -2.000416914641864300E-06, 0.000000000000000000, 4.714008503747964783E-05, 9.979203887779479183E-05, 0.0001372215519229583246, 0.0001635031576221121225, 0.0001900083748504222147 ),
 .UNSPECIFIED. ) ;
#159907=LINE ( 'NONE', #138997, #216734 ) ;
#159923=VERTEX_POINT ( 'NONE', #56914 ) ;
#159934=VERTEX_POINT ( 'NONE', #196453 ) ;
#159939=CARTESIAN_POINT ( 'NONE',  ( 22.39999999999999503, 64.18196446391819165, -247.0985338183330668 ) ) ;
#159983=LINE ( 'NONE', #218627, #228285 ) ;
#159993=AXIS2_PLACEMENT_3D ( 'NONE', #211993, #8643, #68622 ) ;
#160011=EDGE_CURVE ( 'NONE', #213246, #2766, #40614, .T. ) ;
#160026=CARTESIAN_POINT ( 'NONE',  ( -21.05000000000000071, 70.65782965956557859, -228.4198064469268559 ) ) ;
#160103=CYLINDRICAL_SURFACE ( 'NONE', #77436, 0.09999999999999939493 ) ;
#160116=ADVANCED_FACE ( 'NONE', ( #149350 ), #50204, .F. ) ;
#160134=CARTESIAN_POINT ( 'NONE',  ( -23.25000000000000000, 67.23127455305841238, -235.8551265064783991 ) ) ;
#160135=CIRCLE ( 'NONE', #134952, 0.2000000000000042577 ) ;
#160165=DIRECTION ( 'NONE',  ( -1.734723475976746257E-13, 0.9228863568391486583, 0.3850724248244262182 ) ) ;
#160172=VECTOR ( 'NONE', #170718, 1000.000000000000000 ) ;
#160173=CARTESIAN_POINT ( 'NONE',  ( -20.54999999999999716, 76.00000000001126921, -203.5231074845248997 ) ) ;
#160202=ORIENTED_EDGE ( 'NONE', *, *, #61908, .F. ) ;
#160230=TOROIDAL_SURFACE ( 'NONE', #101908, 3.899999999999999467, 0.1000000000000000056 ) ;
#160252=CARTESIAN_POINT ( 'NONE',  ( 20.94999999999999929, 68.05808644172607558, -213.7045301755741491 ) ) ;
#160264=EDGE_LOOP ( 'NONE', ( #4869, #93275, #45379 ) ) ;
#160280=CARTESIAN_POINT ( 'NONE',  ( 20.94999999999999929, 59.10678033798691189, -225.7992625810339575 ) ) ;
#160294=VERTEX_POINT ( 'NONE', #231446 ) ;
#160320=DIRECTION ( 'NONE',  ( 0.000000000000000000, 0.7049548389605067023, -0.7092521942342977503 ) ) ;
#160321=CARTESIAN_POINT ( 'NONE',  ( 22.45305468355011413, 64.25313205997872501, -247.2214437328679821 ) ) ;
#160342=CIRCLE ( 'NONE', #43606, 0.1000000000000106498 ) ;
#160367=CARTESIAN_POINT ( 'NONE',  ( 19.75857864376268935, 62.39550153362034735, -208.7959266050682459 ) ) ;
#160437=ORIENTED_EDGE ( 'NONE', *, *, #99597, .T. ) ;
#160462=VECTOR ( 'NONE', #44250, 1000.000000000000000 ) ;
#160488=AXIS2_PLACEMENT_3D ( 'NONE', #1305, #45589, #123852 ) ;
#160519=VERTEX_POINT ( 'NONE', #6935 ) ;
#160581=CARTESIAN_POINT ( 'NONE',  ( 23.15000000000000213, 75.39949836213487799, -250.2448839681187849 ) ) ;
#160591=DIRECTION ( 'NONE',  ( -1.000000000000000000, -0.000000000000000000, 0.000000000000000000 ) ) ;
#160628=CARTESIAN_POINT ( 'NONE',  ( 22.47071067811865319, 65.11488425470513164, -243.2801022963548405 ) ) ;
#160646=VERTEX_POINT ( 'NONE', #156758 ) ;
#160719=CARTESIAN_POINT ( 'NONE',  ( 19.75857864376269646, 62.36932623377868623, -208.8924400946860089 ) ) ;
#160732=CARTESIAN_POINT ( 'NONE',  ( -21.07928932188134041, 61.09751618602744827, -234.2940654522722639 ) ) ;
#160745=CARTESIAN_POINT ( 'NONE',  ( 18.59999999999999076, 62.94087027993914063, -212.6738838931263444 ) ) ;
#160761=AXIS2_PLACEMENT_3D ( 'NONE', #124876, #221381, #143128 ) ;
#160764=EDGE_CURVE ( 'NONE', #250378, #81173, #257349, .T. ) ;
#160777=CIRCLE ( 'NONE', #194078, 0.09999999999999543976 ) ;
#160782=AXIS2_PLACEMENT_3D ( 'NONE', #104012, #68771, #225244 ) ;
#160783=CARTESIAN_POINT ( 'NONE',  ( -20.64999999999999858, 65.86663596189677605, -213.5709895136416776 ) ) ;
#160803=DIRECTION ( 'NONE',  ( 0.000000000000000000, -0.9651348961777157509, 0.2617529984165031243 ) ) ;
#160813=CARTESIAN_POINT ( 'NONE',  ( -20.54999999999999716, 82.57900542960499024, -215.5587758314583482 ) ) ;
#160843=VERTEX_POINT ( 'NONE', #182730 ) ;
#160849=DIRECTION ( 'NONE',  ( 6.938893903906363786E-14, -0.2617529984165152257, -0.9651348961777124202 ) ) ;
#160860=CARTESIAN_POINT ( 'NONE',  ( 23.15000000000000213, 81.82295291318693842, -214.8938525951558915 ) ) ;
#160884=ADVANCED_FACE ( 'NONE', ( #45764 ), #167037, .T. ) ;
#160886=CIRCLE ( 'NONE', #173394, 7.800000000000007816 ) ;
#160892=ORIENTED_EDGE ( 'NONE', *, *, #98746, .F. ) ;
#160893=DIRECTION ( 'NONE',  ( 1.000000000000000000, 0.000000000000000000, 0.000000000000000000 ) ) ;
#160917=ORIENTED_EDGE ( 'NONE', *, *, #137161, .F. ) ;
#160942=DIRECTION ( 'NONE',  ( -1.000000000000000000, 0.000000000000000000, 0.000000000000000000 ) ) ;
#160982=DIRECTION ( 'NONE',  ( 0.000000000000000000, -0.2617529984165031243, -0.9651348961777157509 ) ) ;
#161084=EDGE_LOOP ( 'NONE', ( #87854, #235511, #189641, #23782 ) ) ;
#161098=ORIENTED_EDGE ( 'NONE', *, *, #231296, .F. ) ;
#161154=AXIS2_PLACEMENT_3D ( 'NONE', #40044, #239505, #219930 ) ;
#161181=ORIENTED_EDGE ( 'NONE', *, *, #208638, .T. ) ;
#161220=EDGE_LOOP ( 'NONE', ( #94261, #48741, #196786, #250625 ) ) ;
#161223=CARTESIAN_POINT ( 'NONE',  ( 18.59999999999999787, 79.24821784679177483, -196.3217825494968736 ) ) ;
#161275=CARTESIAN_POINT ( 'NONE',  ( 22.39999999999999503, 55.86476422312858858, -232.8760422647022494 ) ) ;
#161281=ADVANCED_FACE ( 'NONE', ( #248475 ), #115749, .T. ) ;
#161283=CARTESIAN_POINT ( 'NONE',  ( 21.05000000000000071, 67.25744985290005218, -235.7586130168606076 ) ) ;
#161284=FACE_OUTER_BOUND ( 'NONE', #171658, .T. ) ;
#161286=EDGE_LOOP ( 'NONE', ( #149319, #203451, #113641, #50412 ) ) ;
#161292=EDGE_CURVE ( 'NONE', #82116, #97495, #69857, .T. ) ;
#161303=EDGE_CURVE ( 'NONE', #57260, #88879, #49677, .T. ) ;
#161312=ORIENTED_EDGE ( 'NONE', *, *, #168846, .T. ) ;
#161313=DIRECTION ( 'NONE',  ( 0.000000000000000000, -0.2617529984165046231, -0.9651348961777154178 ) ) ;
#161319=DIRECTION ( 'NONE',  ( 0.000000000000000000, 0.2617529984165033463, 0.9651348961777156399 ) ) ;
#161339=EDGE_CURVE ( 'NONE', #242581, #2766, #82404, .T. ) ;
#161351=ORIENTED_EDGE ( 'NONE', *, *, #149750, .T. ) ;
#161357=LINE ( 'NONE', #62243, #161867 ) ;
#161371=EDGE_CURVE ( 'NONE', #242736, #77452, #178716, .T. ) ;
#161405=CARTESIAN_POINT ( 'NONE',  ( 20.94999999999999574, 63.48629093094752562, -224.6400281563320505 ) ) ;
#161408=CARTESIAN_POINT ( 'NONE',  ( -23.15000000000000213, 62.82351852614503684, -207.2177435922979214 ) ) ;
#161458=VERTEX_POINT ( 'NONE', #176656 ) ;
#161505=DIRECTION ( 'NONE',  ( 0.000000000000000000, 0.2617529984165031243, 0.9651348961777157509 ) ) ;
#161508=CARTESIAN_POINT ( 'NONE',  ( 21.97500000000000497, 61.02768354592785727, -221.4801322937404677 ) ) ;
#161514=FACE_OUTER_BOUND ( 'NONE', #23248, .T. ) ;
#161542=VECTOR ( 'NONE', #179783, 1000.000000000000114 ) ;
#161548=DIRECTION ( 'NONE',  ( 1.000000000000000000, -7.049440681616512959E-16, 1.911869773728117674E-16 ) ) ;
#161552=CARTESIAN_POINT ( 'NONE',  ( 20.95595624212415586, 58.97486571184673920, -225.7106661587678218 ) ) ;
#161557=EDGE_CURVE ( 'NONE', #229500, #230038, #187068, .T. ) ;
#161577=AXIS2_PLACEMENT_3D ( 'NONE', #123128, #202647, #103535 ) ;
#161613=AXIS2_PLACEMENT_3D ( 'NONE', #123652, #201897, #23287 ) ;
#161630=CIRCLE ( 'NONE', #215748, 7.791421356237338891 ) ;
#161634=ORIENTED_EDGE ( 'NONE', *, *, #114124, .T. ) ;
#161669=AXIS2_PLACEMENT_3D ( 'NONE', #71665, #132916, #151193 ) ;
#161671=ORIENTED_EDGE ( 'NONE', *, *, #163691, .F. ) ;
#161696=DIRECTION ( 'NONE',  ( -1.000000000000000000, 7.049440681616512959E-16, -1.911869773728117674E-16 ) ) ;
#161740=DIRECTION ( 'NONE',  ( 0.000000000000000000, -0.3896596508879864307, -0.9209589331071459384 ) ) ;
#161751=VECTOR ( 'NONE', #192657, 1000.000000000000000 ) ;
#161764=CYLINDRICAL_SURFACE ( 'NONE', #8595, 0.09999999999999939493 ) ;
#161783=ORIENTED_EDGE ( 'NONE', *, *, #35076, .T. ) ;
#161799=DIRECTION ( 'NONE',  ( 0.000000000000000000, -0.9651348961777379554, 0.2617529984164210233 ) ) ;
#161814=CARTESIAN_POINT ( 'NONE',  ( 21.10710606213542206, 61.96450539493646659, -221.7435352673221587 ) ) ;
#161836=ADVANCED_FACE ( 'NONE', ( #149775 ), #36863, .T. ) ;
#161854=VECTOR ( 'NONE', #160320, 1000.000000000000114 ) ;
#161867=VECTOR ( 'NONE', #235732, 999.9999999999998863 ) ;
#161903=ADVANCED_FACE ( 'NONE', ( #196567 ), #20527, .F. ) ;
#161934=EDGE_CURVE ( 'NONE', #72090, #206303, #136577, .T. ) ;
#161977=ORIENTED_EDGE ( 'NONE', *, *, #68268, .T. ) ;
#162018=DIRECTION ( 'NONE',  ( 0.000000000000000000, 0.9651348961777157509, -0.2617529984165031243 ) ) ;
#162020=DIRECTION ( 'NONE',  ( 0.000000000000000000, -0.2617529984165031243, -0.9651348961777157509 ) ) ;
#162028=EDGE_CURVE ( 'NONE', #40334, #108241, #175753, .T. ) ;
#162035=DIRECTION ( 'NONE',  ( 0.000000000000000000, -0.9651348961777379554, 0.2617529984164210233 ) ) ;
#162040=ORIENTED_EDGE ( 'NONE', *, *, #174223, .F. ) ;
#162073=VERTEX_POINT ( 'NONE', #23096 ) ;
#162095=( BOUNDED_SURFACE ( )  B_SPLINE_SURFACE ( 3, 2, ( 
 ( #118922, #231, #79749 ),
 ( #199750, #134591, #21116 ),
 ( #100587, #1510, #214158 ),
 ( #206149, #165759, #245283 ) ),
 .UNSPECIFIED., .F., .F., .F. ) 
 B_SPLINE_SURFACE_WITH_KNOTS ( ( 4, 4 ),
 ( 3, 3 ),
 ( -1.387778780781445676E-17, 0.001979672783031532872 ),
 ( 0.000000000000000000, 1.000000000000000000 ),
 .UNSPECIFIED. ) 
 GEOMETRIC_REPRESENTATION_ITEM ( )  RATIONAL_B_SPLINE_SURFACE ( (
 ( 1.000000000000000000, 0.7103081912008362142, 1.000000000000000000),
 ( 1.000000000000000000, 0.7104998333558978363, 1.000000000000000000),
 ( 1.000000000000000000, 0.7107238315755931568, 1.000000000000000000),
 ( 1.000000000000000000, 0.7110073749539214116, 1.000000000000000000) ) ) 
 REPRESENTATION_ITEM ( '' )  SURFACE ( )  );
#162097=DIRECTION ( 'NONE',  ( 1.000000000000000000, 0.000000000000000000, 0.000000000000000000 ) ) ;
#162133=EDGE_CURVE ( 'NONE', #126428, #85926, #69927, .T. ) ;
#162155=ORIENTED_EDGE ( 'NONE', *, *, #161339, .T. ) ;
#162172=DIRECTION ( 'NONE',  ( 0.000000000000000000, -0.7049548389605022614, 0.7092521942343023023 ) ) ;
#162173=EDGE_CURVE ( 'NONE', #50332, #74935, #169040, .T. ) ;
#162175=CARTESIAN_POINT ( 'NONE',  ( -20.94999027547553894, 67.49459761544871128, -195.5598716110968951 ) ) ;
#162208=ORIENTED_EDGE ( 'NONE', *, *, #198860, .T. ) ;
#162250=AXIS2_PLACEMENT_3D ( 'NONE', #50849, #130406, #113422 ) ;
#162253=ORIENTED_EDGE ( 'NONE', *, *, #251693, .T. ) ;
#162255=CARTESIAN_POINT ( 'NONE',  ( 18.49999999999999289, 66.54223038922117439, -213.7542166125332415 ) ) ;
#162256=CARTESIAN_POINT ( 'NONE',  ( 20.94999999999999574, 79.03091752131670944, -235.9469187808398942 ) ) ;
#162270=DIRECTION ( 'NONE',  ( -0.000000000000000000, 0.2617529984165031243, 0.9651348961777157509 ) ) ;
#162275=CARTESIAN_POINT ( 'NONE',  ( -18.59999999999999787, 52.91185528119410719, -244.1460391050142960 ) ) ;
#162282=ORIENTED_EDGE ( 'NONE', *, *, #193658, .T. ) ;
#162345=DIRECTION ( 'NONE',  ( -3.265361837132813093E-16, -0.9651348961777157509, 0.2617529984165031243 ) ) ;
#162363=EDGE_LOOP ( 'NONE', ( #148503, #159687, #115268, #92300 ) ) ;
#162364=ORIENTED_EDGE ( 'NONE', *, *, #106822, .F. ) ;
#162370=CARTESIAN_POINT ( 'NONE',  ( -18.50000000000000000, 86.87366311306884370, -199.3414869250131858 ) ) ;
#162373=CARTESIAN_POINT ( 'NONE',  ( 18.59999999999999076, 62.46583972339646351, -208.9186153945276487 ) ) ;
#162395=CARTESIAN_POINT ( 'NONE',  ( 18.59999999999996945, 67.49222854868494892, -195.4187676019683693 ) ) ;
#162400=EDGE_CURVE ( 'NONE', #241262, #220817, #224440, .T. ) ;
#162412=DIRECTION ( 'NONE',  ( 0.000000000000000000, -0.2617529984165033463, -0.9651348961777157509 ) ) ;
#162417=ORIENTED_EDGE ( 'NONE', *, *, #30763, .T. ) ;
#162440=ORIENTED_EDGE ( 'NONE', *, *, #221494, .T. ) ;
#162441=DIRECTION ( 'NONE',  ( 0.000000000000000000, 0.2617529984165031243, 0.9651348961777157509 ) ) ;
#162451=EDGE_LOOP ( 'NONE', ( #147318, #20869, #91170, #240399 ) ) ;
#162465=ORIENTED_EDGE ( 'NONE', *, *, #129655, .F. ) ;
#162466=ORIENTED_EDGE ( 'NONE', *, *, #243109, .T. ) ;
#162478=DIRECTION ( 'NONE',  ( 1.000000000000000000, 0.000000000000000000, -0.000000000000000000 ) ) ;
#162520=CARTESIAN_POINT ( 'NONE',  ( -18.59999999999999787, 71.84303044094815505, -225.1053209871248271 ) ) ;
#162524=CARTESIAN_POINT ( 'NONE',  ( -21.09610168723073897, 61.06592963697848830, -234.2178341264986159 ) ) ;
#162540=ADVANCED_FACE ( 'NONE', ( #135651 ), #54829, .F. ) ;
#162542=CARTESIAN_POINT ( 'NONE',  ( -18.41353343127310893, 78.24072131640579641, -231.5548844243369615 ) ) ;
#162546=ORIENTED_EDGE ( 'NONE', *, *, #206112, .F. ) ;
#162572=CARTESIAN_POINT ( 'NONE',  ( 20.95512820512821150, 61.85802300103158302, -221.7569547192959476 ) ) ;
#162592=DIRECTION ( 'NONE',  ( 1.000000000000000000, 0.000000000000000000, -0.000000000000000000 ) ) ;
#162599=CARTESIAN_POINT ( 'NONE',  ( -21.05000000000000071, 64.21185867012613357, -224.4479740254296303 ) ) ;
#162628=EDGE_CURVE ( 'NONE', #109963, #66884, #211365, .T. ) ;
#162642=FACE_OUTER_BOUND ( 'NONE', #19686, .T. ) ;
#162660=DIRECTION ( 'NONE',  ( 0.000000000000000000, 0.2617529984165152257, 0.9651348961777124202 ) ) ;
#162665=ORIENTED_EDGE ( 'NONE', *, *, #191450, .T. ) ;
#162685=DIRECTION ( 'NONE',  ( -0.000000000000000000, 0.2617529984165031243, 0.9651348961777157509 ) ) ;
#162696=CARTESIAN_POINT ( 'NONE',  ( -23.15000000000000213, 72.62993014539878800, -215.9492192728129965 ) ) ;
#162715=VERTEX_POINT ( 'NONE', #22162 ) ;
#162733=CARTESIAN_POINT ( 'NONE',  ( -21.53752568622129004, 65.35928353582079353, -242.3794047578559514 ) ) ;
#162757=DIRECTION ( 'NONE',  ( 0.000000000000000000, 0.2617529984165033463, 0.9651348961777157509 ) ) ;
#162784=B_SPLINE_CURVE_WITH_KNOTS ( 'NONE', 3,
 ( #150831, #136364, #71320, #94699, #230366, #93414, #51701, #253763, #131265, #95973 ),
 .UNSPECIFIED., .F., .F.,
 ( 4, 2, 2, 2, 4 ),
 ( 0.000000000000000000, 0.0001660831991682683057, 0.0002491247987523607845, 0.0002906455985444082843, 0.0003321663983364558383 ),
 .UNSPECIFIED. ) ;
#162791=VERTEX_POINT ( 'NONE', #182520 ) ;
#162798=AXIS2_PLACEMENT_3D ( 'NONE', #55698, #75341, #114439 ) ;
#162805=ORIENTED_EDGE ( 'NONE', *, *, #247800, .F. ) ;
#162813=EDGE_LOOP ( 'NONE', ( #92985, #57385, #48948, #165051, #90537, #178141, #137975, #126190, #151200, #106185, #194648, #4579, #60266, #97278 ) ) ;
#162843=ORIENTED_EDGE ( 'NONE', *, *, #254845, .F. ) ;
#162862=SPHERICAL_SURFACE ( 'NONE', #250261, 0.1000000000000000056 ) ;
#162870=EDGE_CURVE ( 'NONE', #181475, #188424, #191336, .T. ) ;
#162880=DIRECTION ( 'NONE',  ( -1.000000000000000000, -0.000000000000000000, -0.000000000000000000 ) ) ;
#162886=DIRECTION ( 'NONE',  ( 1.000000000000000000, 0.000000000000000000, 0.000000000000000000 ) ) ;
#162921=DIRECTION ( 'NONE',  ( 1.000000000000000000, 0.000000000000000000, 0.000000000000000000 ) ) ;
#162955=VERTEX_POINT ( 'NONE', #31166 ) ;
#162959=DIRECTION ( 'NONE',  ( 0.000000000000000000, 0.2617529984165180013, 0.9651348961777117541 ) ) ;
#162988=ORIENTED_EDGE ( 'NONE', *, *, #1111, .F. ) ;
#163007=CARTESIAN_POINT ( 'NONE',  ( -20.94999999999999929, 86.45856254523214091, -209.4679346046102921 ) ) ;
#163044=EDGE_CURVE ( 'NONE', #62395, #156950, #29042, .T. ) ;
#163047=AXIS2_PLACEMENT_3D ( 'NONE', #198703, #163437, #61762 ) ;
#163063=VERTEX_POINT ( 'NONE', #117085 ) ;
#163066=DIRECTION ( 'NONE',  ( 1.000000000000000000, 0.000000000000000000, -0.000000000000000000 ) ) ;
#163072=VECTOR ( 'NONE', #163523, 1000.000000000000000 ) ;
#163132=CIRCLE ( 'NONE', #54766, 0.1000000000000124678 ) ;
#163168=EDGE_CURVE ( 'NONE', #133775, #241262, #245660, .T. ) ;
#163239=AXIS2_PLACEMENT_3D ( 'NONE', #4422, #120555, #143937 ) ;
#163250=CIRCLE ( 'NONE', #29984, 0.09999999999999939493 ) ;
#163270=DIRECTION ( 'NONE',  ( 0.000000000000000000, -0.9916376685811618685, 0.1290532225514649800 ) ) ;
#163278=EDGE_CURVE ( 'NONE', #142984, #133447, #129147, .T. ) ;
#163294=CARTESIAN_POINT ( 'NONE',  ( 18.59999999999997655, 79.19526988099229925, -196.1889237952725296 ) ) ;
#163309=EDGE_CURVE ( 'NONE', #137749, #132077, #116660, .T. ) ;
#163371=EDGE_LOOP ( 'NONE', ( #63503, #155818, #231178, #154108 ) ) ;
#163399=CIRCLE ( 'NONE', #38498, 0.6000000000000005329 ) ;
#163406=VERTEX_POINT ( 'NONE', #39829 ) ;
#163414=CARTESIAN_POINT ( 'NONE',  ( -20.54999999999999716, 76.00000000001126921, -203.5231074845248997 ) ) ;
#163437=DIRECTION ( 'NONE',  ( 0.000000000000000000, 0.9651348961777157509, -0.2617529984165031243 ) ) ;
#163441=CARTESIAN_POINT ( 'NONE',  ( -20.85882249326303040, 67.49222854868494892, -195.4187676019683693 ) ) ;
#163450=CARTESIAN_POINT ( 'NONE',  ( 22.39999999999999503, 59.68594599439719417, -233.9123800762197902 ) ) ;
#163457=CARTESIAN_POINT ( 'NONE',  ( -20.64999999999999858, 82.09643798151613225, -215.4278993322501208 ) ) ;
#163466=ORIENTED_EDGE ( 'NONE', *, *, #210429, .T. ) ;
#163468=VERTEX_POINT ( 'NONE', #198868 ) ;
#163471=ORIENTED_EDGE ( 'NONE', *, *, #185670, .T. ) ;
#163477=DIRECTION ( 'NONE',  ( 0.000000000000000000, -0.2617529984165031243, -0.9651348961777158619 ) ) ;
#163512=FACE_OUTER_BOUND ( 'NONE', #90050, .T. ) ;
#163517=DIRECTION ( 'NONE',  ( -1.000000000000000000, -0.000000000000000000, 0.000000000000000000 ) ) ;
#163523=DIRECTION ( 'NONE',  ( 0.000000000000000000, -0.2617529984165031243, -0.9651348961777157509 ) ) ;
#163547=CARTESIAN_POINT ( 'NONE',  ( 19.97071067811864609, 61.50763418579565212, -212.1815653095142693 ) ) ;
#163575=CARTESIAN_POINT ( 'NONE',  ( 18.59999999999999432, 68.58368164137472434, -224.2353459317783120 ) ) ;
#163581=LINE ( 'NONE', #3191, #225753 ) ;
#163609=DIRECTION ( 'NONE',  ( 0.000000000000000000, -0.2617529984164506107, -0.9651348961777299618 ) ) ;
#163613=DIRECTION ( 'NONE',  ( -0.000000000000000000, 0.2493442905258256848, 0.9684149032218436481 ) ) ;
#163617=LINE ( 'NONE', #144030, #147211 ) ;
#163624=EDGE_CURVE ( 'NONE', #225728, #235804, #33499, .T. ) ;
#163625=DIRECTION ( 'NONE',  ( 0.000000000000000000, -0.2617529984165024026, -0.9651348961777158619 ) ) ;
#163666=DIRECTION ( 'NONE',  ( 0.000000000000000000, -0.2617529984164856383, -0.9651348961777204138 ) ) ;
#163667=FACE_OUTER_BOUND ( 'NONE', #241719, .T. ) ;
#163688=ORIENTED_EDGE ( 'NONE', *, *, #106383, .F. ) ;
#163691=EDGE_CURVE ( 'NONE', #64537, #113079, #191716, .T. ) ;
#163706=DIRECTION ( 'NONE',  ( 0.7071067811865474617, -0.6824534298470372740, 0.1850873201762209819 ) ) ;
#163749=ORIENTED_EDGE ( 'NONE', *, *, #22295, .T. ) ;
#163836=CARTESIAN_POINT ( 'NONE',  ( 18.43579564894478295, 78.24390728993300570, -231.6169759425274322 ) ) ;
#163842=CARTESIAN_POINT ( 'NONE',  ( 20.95512820512820440, 61.84489010471549619, -221.8053782964821039 ) ) ;
#163854=AXIS2_PLACEMENT_3D ( 'NONE', #132892, #96296, #234541 ) ;
#163865=EDGE_CURVE ( 'NONE', #67070, #235804, #57763, .T. ) ;
#163881=LINE ( 'NONE', #162599, #207929 ) ;
#163962=DIRECTION ( 'NONE',  ( 1.000000000000000000, 0.000000000000000000, 0.000000000000000000 ) ) ;
#163982=EDGE_CURVE ( 'NONE', #38302, #133775, #216959, .T. ) ;
#163993=VERTEX_POINT ( 'NONE', #181598 ) ;
#164019=ORIENTED_EDGE ( 'NONE', *, *, #208584, .T. ) ;
#164021=DIRECTION ( 'NONE',  ( 0.000000000000000000, 0.2617529984164357892, 0.9651348961777339586 ) ) ;
#164023=DIRECTION ( 'NONE',  ( 0.000000000000000000, 0.9651348961777379554, -0.2617529984164210233 ) ) ;
#164036=CARTESIAN_POINT ( 'NONE',  ( -18.50000000000000000, 59.50933445848280456, -243.9217804674669310 ) ) ;
#164049=VERTEX_POINT ( 'NONE', #114561 ) ;
#164072=DIRECTION ( 'NONE',  ( 1.000000000000000000, 0.000000000000000000, 0.000000000000000000 ) ) ;
#164073=EDGE_CURVE ( 'NONE', #151096, #143707, #42039, .T. ) ;
#164077=ORIENTED_EDGE ( 'NONE', *, *, #200362, .F. ) ;
#164089=CIRCLE ( 'NONE', #80670, 0.1000000000000035028 ) ;
#164092=CARTESIAN_POINT ( 'NONE',  ( 18.49999999999999289, 54.30302133219453964, -244.5233354669909431 ) ) ;
#164107=CARTESIAN_POINT ( 'NONE',  ( 21.05000000000097771, 58.96901243545040927, -225.7107919458293850 ) ) ;
#164109=VERTEX_POINT ( 'NONE', #214938 ) ;
#164149=CIRCLE ( 'NONE', #205621, 11.90000000000000568 ) ;
#164167=CARTESIAN_POINT ( 'NONE',  ( 20.94999999999999929, 67.23127455305841238, -235.8551265064783991 ) ) ;
#164177=EDGE_CURVE ( 'NONE', #77989, #177651, #20611, .T. ) ;
#164185=VERTEX_POINT ( 'NONE', #139224 ) ;
#164214=CARTESIAN_POINT ( 'NONE',  ( 23.24999999999999289, 71.23658437219593509, -236.9414014499068912 ) ) ;
#164234=AXIS2_PLACEMENT_3D ( 'NONE', #240133, #138425, #78467 ) ;
#164298=DIRECTION ( 'NONE',  ( 0.000000000000000000, -0.2617529984165033463, -0.9651348961777157509 ) ) ;
#164310=CARTESIAN_POINT ( 'NONE',  ( 23.24999999999999289, 52.91185528119409298, -244.1460391050142675 ) ) ;
#164319=DIRECTION ( 'NONE',  ( 0.000000000000000000, 0.1071148137998806232, 0.9942466578594150173 ) ) ;
#164338=ORIENTED_EDGE ( 'NONE', *, *, #68489, .F. ) ;
#164345=CARTESIAN_POINT ( 'NONE',  ( -18.48408745364672967, 87.07669050450563475, -199.6027005069816198 ) ) ;
#164363=CIRCLE ( 'NONE', #185016, 0.09999999999999642508 ) ;
#164387=CARTESIAN_POINT ( 'NONE',  ( -20.94999999999999929, 76.00000000001126921, -203.5231074845248997 ) ) ;
#164388=EDGE_CURVE ( 'NONE', #147060, #148919, #138038, .T. ) ;
#164428=AXIS2_PLACEMENT_3D ( 'NONE', #78959, #178115, #114268 ) ;
#164486=VERTEX_POINT ( 'NONE', #30892 ) ;
#164489=ADVANCED_FACE ( 'NONE', ( #49129 ), #200418, .F. ) ;
#164538=CARTESIAN_POINT ( 'NONE',  ( -21.05000000000000071, 62.86885547537412577, -207.0505773246642036 ) ) ;
#164578=EDGE_CURVE ( 'NONE', #232481, #175607, #175528, .T. ) ;
#164608=AXIS2_PLACEMENT_3D ( 'NONE', #18716, #98209, #257272 ) ;
#164625=ORIENTED_EDGE ( 'NONE', *, *, #43733, .T. ) ;
#164650=ORIENTED_EDGE ( 'NONE', *, *, #157185, .F. ) ;
#164702=AXIS2_PLACEMENT_3D ( 'NONE', #202863, #125886, #185869 ) ;
#164738=FACE_OUTER_BOUND ( 'NONE', #97892, .T. ) ;
#164807=FACE_OUTER_BOUND ( 'NONE', #131769, .T. ) ;
#164815=DIRECTION ( 'NONE',  ( -1.000000000000000000, -0.000000000000000000, -0.000000000000000000 ) ) ;
#164816=EDGE_LOOP ( 'NONE', ( #170439, #23613, #233521, #215455 ) ) ;
#164836=CARTESIAN_POINT ( 'NONE',  ( 22.14074124539698829, 60.07292514105704129, -234.0163508767828660 ) ) ;
#164871=AXIS2_PLACEMENT_3D ( 'NONE', #35661, #194724, #76031 ) ;
#164872=VECTOR ( 'NONE', #97667, 1000.000000000000000 ) ;
#164911=DIRECTION ( 'NONE',  ( 0.000000000000000000, 0.2617529984164506107, 0.9651348961777299618 ) ) ;
#164939=CIRCLE ( 'NONE', #27619, 0.09999999999999939493 ) ;
#164940=DIRECTION ( 'NONE',  ( 1.000000000000000000, 0.000000000000000000, 0.000000000000000000 ) ) ;
#164941=ADVANCED_FACE ( 'NONE', ( #70553 ), #242278, .F. ) ;
#164974=DIRECTION ( 'NONE',  ( 0.000000000000000000, 0.2617529984165031243, 0.9651348961777157509 ) ) ;
#164984=TOROIDAL_SURFACE ( 'NONE', #60729, 0.2000000000000000111, 0.1000000000000000056 ) ;
#165041=CIRCLE ( 'NONE', #131735, 12.97500000000001208 ) ;
#165042=AXIS2_PLACEMENT_3D ( 'NONE', #72715, #15298, #94808 ) ;
#165047=CARTESIAN_POINT ( 'NONE',  ( -21.05000000000000071, 86.27712145182582049, -209.5223386573213702 ) ) ;
#165051=ORIENTED_EDGE ( 'NONE', *, *, #52191, .F. ) ;
#165073=ORIENTED_EDGE ( 'NONE', *, *, #217690, .F. ) ;
#165103=AXIS2_PLACEMENT_3D ( 'NONE', #244014, #165802, #87502 ) ;
#165114=CARTESIAN_POINT ( 'NONE',  ( 21.00000000000000000, 61.02768354592784306, -221.4801322937404393 ) ) ;
#165115=CARTESIAN_POINT ( 'NONE',  ( 18.48536876927954964, 78.20985190841274459, -231.5293656822601918 ) ) ;
#165138=( BOUNDED_SURFACE ( )  B_SPLINE_SURFACE ( 3, 2, ( 
 ( #251363, #193978, #234362 ),
 ( #92287, #113143, #135253 ),
 ( #149733, #233118, #192690 ),
 ( #173168, #248817, #70196 ),
 ( #51861, #72769, #152297 ),
 ( #231824, #252637, #77851 ) ),
 .UNSPECIFIED., .F., .F., .T. ) 
 B_SPLINE_SURFACE_WITH_KNOTS ( ( 4, 2, 4 ),
 ( 3, 3 ),
 ( 1.570796326794895448, 2.356194490192343505, 3.141592653589791784 ),
 ( 0.000000000000000000, 1.000000000000000000 ),
 .UNSPECIFIED. ) 
 GEOMETRIC_REPRESENTATION_ITEM ( )  RATIONAL_B_SPLINE_SURFACE ( (
 ( 1.000000000000000000, 0.7071067811865475727, 1.000000000000000000),
 ( 1.000000000000000000, 0.6611148371775555921, 1.000000000000000000),
 ( 1.000000000000000000, 0.6092287576700941010, 1.000000000000000000),
 ( 1.000000000000000000, 0.5278258667053719044, 1.000000000000000000),
 ( 1.000000000000000000, 0.4993418825339194789, 1.000000000000000000),
 ( 1.000000000000000000, 0.5000000000000545120, 1.000000000000000000) ) ) 
 REPRESENTATION_ITEM ( '' )  SURFACE ( )  );
#165139=DIRECTION ( 'NONE',  ( -1.000000000000000000, -0.000000000000000000, -0.000000000000000000 ) ) ;
#165144=CARTESIAN_POINT ( 'NONE',  ( -20.85000000000000142, 67.49222854868494892, -195.4187676019683408 ) ) ;
#165148=AXIS2_PLACEMENT_3D ( 'NONE', #140020, #40976, #120514 ) ;
#165159=CYLINDRICAL_SURFACE ( 'NONE', #222523, 0.09999999999999939493 ) ;
#165170=EDGE_CURVE ( 'NONE', #181858, #61516, #26009, .T. ) ;
#165197=CARTESIAN_POINT ( 'NONE',  ( 20.94999999999999574, 70.65782965956557859, -228.4198064469268559 ) ) ;
#165199=CARTESIAN_POINT ( 'NONE',  ( 18.50000000000001776, 86.96699927712943179, -199.3055931863049466 ) ) ;
#165200=ORIENTED_EDGE ( 'NONE', *, *, #139756, .T. ) ;
#165235=DIRECTION ( 'NONE',  ( 0.000000000000000000, -0.9651348961777157509, 0.2617529984165031243 ) ) ;
#165243=EDGE_CURVE ( 'NONE', #40333, #198131, #138398, .T. ) ;
#165250=CIRCLE ( 'NONE', #248635, 0.09999999999999935330 ) ;
#165262=AXIS2_PLACEMENT_3D ( 'NONE', #102766, #161505, #48904 ) ;
#165270=VERTEX_POINT ( 'NONE', #31583 ) ;
#165281=CARTESIAN_POINT ( 'NONE',  ( -22.47007471830798764, 65.21035539001040604, -243.3066537799435878 ) ) ;
#165282=AXIS2_PLACEMENT_3D ( 'NONE', #98780, #158824, #177109 ) ;
#165341=DIRECTION ( 'NONE',  ( 0.000000000000000000, 0.3994087351226822125, 0.9167729611565227366 ) ) ;
#165389=CARTESIAN_POINT ( 'NONE',  ( 21.05000000000000071, 59.13236860818125251, -225.8959333647716505 ) ) ;
#165421=CARTESIAN_POINT ( 'NONE',  ( 23.25000000000000355, 90.68298050906625463, -235.1761083729927861 ) ) ;
#165426=VECTOR ( 'NONE', #67613, 1000.000000000000000 ) ;
#165483=ADVANCED_FACE ( 'NONE', ( #187764 ), #156791, .T. ) ;
#165521=DIRECTION ( 'NONE',  ( 0.000000000000000000, -0.9651348961777158619, 0.2617529984165032353 ) ) ;
#165523=DIRECTION ( 'NONE',  ( -0.000000000000000000, 0.2617529984165031243, 0.9651348961777157509 ) ) ;
#165539=CARTESIAN_POINT ( 'NONE',  ( -18.59999999999999787, 72.02722222756958104, -225.1832529173024398 ) ) ;
#165552=CARTESIAN_POINT ( 'NONE',  ( -18.50000000000000000, 61.43991280424057777, -221.4883200034892923 ) ) ;
#165569=ORIENTED_EDGE ( 'NONE', *, *, #35526, .T. ) ;
#165575=EDGE_LOOP ( 'NONE', ( #152382, #133156, #113842, #35445 ) ) ;
#165643=EDGE_CURVE ( 'NONE', #166612, #258034, #109475, .T. ) ;
#165654=CIRCLE ( 'NONE', #236366, 0.09999999999999939493 ) ;
#165669=DIRECTION ( 'NONE',  ( -1.000000000000000000, -0.000000000000000000, 0.000000000000000000 ) ) ;
#165682=EDGE_CURVE ( 'NONE', #133293, #161458, #221787, .T. ) ;
#165706=ORIENTED_EDGE ( 'NONE', *, *, #213221, .T. ) ;
#165707=ORIENTED_EDGE ( 'NONE', *, *, #46479, .F. ) ;
#165716=ORIENTED_EDGE ( 'NONE', *, *, #220957, .F. ) ;
#165733=FACE_OUTER_BOUND ( 'NONE', #430, .T. ) ;
#165743=CARTESIAN_POINT ( 'NONE',  ( -20.85000000000000142, 67.49222854868494892, -195.4187676019683693 ) ) ;
#165757=CARTESIAN_POINT ( 'NONE',  ( 21.07928932188134397, 65.47931918658503037, -241.9371126717015841 ) ) ;
#165759=CARTESIAN_POINT ( 'NONE',  ( 21.07016717457010202, 65.57674933587217936, -241.9556870860043603 ) ) ;
#165761=EDGE_CURVE ( 'NONE', #137090, #193211, #58477, .T. ) ;
#165767=CARTESIAN_POINT ( 'NONE',  ( 21.05000000000000071, 67.63082410804655353, -211.8415745842588649 ) ) ;
#165769=ORIENTED_EDGE ( 'NONE', *, *, #17112, .T. ) ;
#165775=AXIS2_PLACEMENT_3D ( 'NONE', #187008, #227388, #116121 ) ;
#165781=ORIENTED_EDGE ( 'NONE', *, *, #52830, .T. ) ;
#165802=DIRECTION ( 'NONE',  ( 0.000000000000000000, -0.9651348961777157509, 0.2617529984165031243 ) ) ;
#165830=FACE_OUTER_BOUND ( 'NONE', #228980, .T. ) ;
#165831=CARTESIAN_POINT ( 'NONE',  ( -21.05315837191484363, 62.86884414000814303, -207.0506191381281837 ) ) ;
#165848=CARTESIAN_POINT ( 'NONE',  ( -23.25000000000000000, 70.85002333954264486, -215.2140597723681879 ) ) ;
#165859=AXIS2_PLACEMENT_3D ( 'NONE', #116210, #58756, #176184 ) ;
#165864=VERTEX_POINT ( 'NONE', #3654 ) ;
#165881=EDGE_LOOP ( 'NONE', ( #213337, #195624, #182928, #138045 ) ) ;
#165882=CARTESIAN_POINT ( 'NONE',  ( -21.05000000000000071, 64.23744694032046709, -224.5446448091673233 ) ) ;
#165883=CARTESIAN_POINT ( 'NONE',  ( 20.94999999999999929, 68.48451787451661232, -224.2224406095231757 ) ) ;
#165910=ORIENTED_EDGE ( 'NONE', *, *, #223347, .F. ) ;
#165925=AXIS2_PLACEMENT_3D ( 'NONE', #221764, #5282, #123993 ) ;
#165928=DIRECTION ( 'NONE',  ( 1.000000000000000000, 0.000000000000000000, 0.000000000000000000 ) ) ;
#165956=CYLINDRICAL_SURFACE ( 'NONE', #127184, 0.09999999999999868716 ) ;
#165999=EDGE_LOOP ( 'NONE', ( #236919, #10783, #67989, #175941 ) ) ;
#166011=AXIS2_PLACEMENT_3D ( 'NONE', #148839, #104528, #28929 ) ;
#166012=DIRECTION ( 'NONE',  ( -1.000000000000000000, -0.000000000000000000, -0.000000000000000000 ) ) ;
#166022=ORIENTED_EDGE ( 'NONE', *, *, #109352, .T. ) ;
#166028=CARTESIAN_POINT ( 'NONE',  ( 22.39999999999999503, 64.27847795353595473, -247.1247091181747066 ) ) ;
#166093=DIRECTION ( 'NONE',  ( 4.336808689942128177E-15, -0.7049548389604990417, 0.7092521942343054109 ) ) ;
#166098=CARTESIAN_POINT ( 'NONE',  ( -23.15000000000000213, 82.57900542960499024, -215.5587758314583482 ) ) ;
#166105=CARTESIAN_POINT ( 'NONE',  ( -20.64999999999999858, 66.26558728512915764, -222.7970849955717938 ) ) ;
#166139=CARTESIAN_POINT ( 'NONE',  ( 23.14999999999999503, 62.94620731560446103, -207.1474054025217697 ) ) ;
#166140=CARTESIAN_POINT ( 'NONE',  ( 20.94999999999999574, 72.06821323333463170, -225.0920403225231610 ) ) ;
#166147=CARTESIAN_POINT ( 'NONE',  ( -18.60000000000000142, 78.12133356376092763, -231.3112718935514920 ) ) ;
#166169=CARTESIAN_POINT ( 'NONE',  ( 21.15000000000000213, 60.91865828504416669, -234.1430899377568551 ) ) ;
#166193=EDGE_CURVE ( 'NONE', #153545, #206475, #30320, .T. ) ;
#166212=DIRECTION ( 'NONE',  ( 3.469446951953622393E-14, 0.9684149032218615227, -0.2493442905257554076 ) ) ;
#166288=ORIENTED_EDGE ( 'NONE', *, *, #170963, .T. ) ;
#166312=CIRCLE ( 'NONE', #137243, 12.87499999999998579 ) ;
#166374=CIRCLE ( 'NONE', #195018, 0.09999999999999939493 ) ;
#166406=VERTEX_POINT ( 'NONE', #152856 ) ;
#166426=DIRECTION ( 'NONE',  ( -7.304098846218490641E-16, -0.9651348961777379554, 0.2617529984164210233 ) ) ;
#166454=CARTESIAN_POINT ( 'NONE',  ( -18.50000000000000000, 67.49463558145298236, -195.5618716440587548 ) ) ;
#166460=B_SPLINE_CURVE_WITH_KNOTS ( 'NONE', 3,
 ( #171190, #128168, #31663, #246814, #250665, #32962, #227254, #109866 ),
 .UNSPECIFIED., .F., .F.,
 ( 4, 2, 2, 4 ),
 ( 0.000000000000000000, 0.0001049670497870086627, 0.0002099340995740173253, 0.0004198681991480253265 ),
 .UNSPECIFIED. ) ;
#166474=SPHERICAL_SURFACE ( 'NONE', #188003, 0.1000000000000000056 ) ;
#166480=AXIS2_PLACEMENT_3D ( 'NONE', #228572, #215414, #41942 ) ;
#166523=DIRECTION ( 'NONE',  ( 0.000000000000000000, 0.2617529984164506107, 0.9651348961777299618 ) ) ;
#166548=ORIENTED_EDGE ( 'NONE', *, *, #197449, .F. ) ;
#166556=CARTESIAN_POINT ( 'NONE',  ( 20.94999999999999929, 62.44369217491800583, -212.5390448563743746 ) ) ;
#166559=CARTESIAN_POINT ( 'NONE',  ( -18.59999999999999787, 72.10920423909969657, -225.0008277277438822 ) ) ;
#166564=DIRECTION ( 'NONE',  ( -0.000000000000000000, -0.2617529984165031243, -0.9651348961777157509 ) ) ;
#166578=ORIENTED_EDGE ( 'NONE', *, *, #15009, .T. ) ;
#166612=VERTEX_POINT ( 'NONE', #168276 ) ;
#166722=CARTESIAN_POINT ( 'NONE',  ( 21.05000000000000071, 68.19849547655701372, -211.6586561550524834 ) ) ;
#166732=CIRCLE ( 'NONE', #233360, 0.1000000000000018374 ) ;
#166738=( BOUNDED_SURFACE ( )  B_SPLINE_SURFACE ( 3, 2, ( 
 ( #238480, #156418, #235901 ),
 ( #117259, #179811, #58541 ),
 ( #217608, #119844, #196776 ),
 ( #18149, #177260, #97661 ) ),
 .UNSPECIFIED., .F., .F., .F. ) 
 B_SPLINE_SURFACE_WITH_KNOTS ( ( 4, 4 ),
 ( 3, 3 ),
 ( 0.0006461284895274125748, 0.0007503702773986283599 ),
 ( 0.000000000000000000, 1.000000000000000000 ),
 .UNSPECIFIED. ) 
 GEOMETRIC_REPRESENTATION_ITEM ( )  RATIONAL_B_SPLINE_SURFACE ( (
 ( 1.000000000000000000, 0.7071067811865475727, 1.000000000000000000),
 ( 1.000000000000000000, 0.7076476444649285602, 1.000000000000000000),
 ( 1.000000000000000000, 0.7075727925191765966, 1.000000000000000000),
 ( 1.000000000000000000, 0.7071067811865670016, 1.000000000000000000) ) ) 
 REPRESENTATION_ITEM ( '' )  SURFACE ( )  );
#166740=AXIS2_PLACEMENT_3D ( 'NONE', #150401, #172570, #149116 ) ;
#166747=CARTESIAN_POINT ( 'NONE',  ( 21.04105312098488056, 61.89240493045525682, -221.6333095009565284 ) ) ;
#166749=VECTOR ( 'NONE', #55378, 1000.000000000000000 ) ;
#166850=AXIS2_PLACEMENT_3D ( 'NONE', #140900, #156644, #220440 ) ;
#166855=VERTEX_POINT ( 'NONE', #16874 ) ;
#166873=FACE_OUTER_BOUND ( 'NONE', #249639, .T. ) ;
#166918=VECTOR ( 'NONE', #52548, 1000.000000000000000 ) ;
#166922=DIRECTION ( 'NONE',  ( 1.000000000000000000, 0.000000000000000000, -0.000000000000000000 ) ) ;
#166931=ORIENTED_EDGE ( 'NONE', *, *, #64242, .T. ) ;
#166965=FACE_OUTER_BOUND ( 'NONE', #100384, .T. ) ;
#166972=CARTESIAN_POINT ( 'NONE',  ( 18.59999999999999787, 80.78317333349157536, -192.9003134612049166 ) ) ;
#166991=CARTESIAN_POINT ( 'NONE',  ( -23.25000000000000000, 82.67551891922275331, -215.5849511313000164 ) ) ;
#167037=CYLINDRICAL_SURFACE ( 'NONE', #32789, 0.09999999999999868716 ) ;
#167046=EDGE_LOOP ( 'NONE', ( #96452, #22569, #21118, #8464, #85746 ) ) ;
#167047=AXIS2_PLACEMENT_3D ( 'NONE', #162520, #202902, #242027 ) ;
#167048=EDGE_CURVE ( 'NONE', #121064, #231796, #47641, .T. ) ;
#167112=CARTESIAN_POINT ( 'NONE',  ( -23.15000000000000213, 67.23127455305841238, -235.8551265064783991 ) ) ;
#167114=EDGE_LOOP ( 'NONE', ( #188593, #215527, #226569, #125907 ) ) ;
#167118=ORIENTED_EDGE ( 'NONE', *, *, #26444, .T. ) ;
#167129=CARTESIAN_POINT ( 'NONE',  ( -21.05000000000000071, 65.63226930301911466, -242.1330134503736247 ) ) ;
#167153=ORIENTED_EDGE ( 'NONE', *, *, #92629, .T. ) ;
#167162=FACE_OUTER_BOUND ( 'NONE', #243635, .T. ) ;
#167215=ORIENTED_EDGE ( 'NONE', *, *, #35282, .F. ) ;
#167221=FACE_OUTER_BOUND ( 'NONE', #202621, .T. ) ;
#167229=CARTESIAN_POINT ( 'NONE',  ( 20.94999999999999929, 63.62814136979439184, -224.4990371885399441 ) ) ;
#167290=DIRECTION ( 'NONE',  ( -0.000000000000000000, 0.2617529984165031243, 0.9651348961777157509 ) ) ;
#167316=CARTESIAN_POINT ( 'NONE',  ( -20.89878130938411616, 67.49249915771264341, -195.4369143829851510 ) ) ;
#167349=ORIENTED_EDGE ( 'NONE', *, *, #162628, .T. ) ;
#167366=DIRECTION ( 'NONE',  ( 0.000000000000000000, -0.2617529984164506107, -0.9651348961777299618 ) ) ;
#167368=EDGE_LOOP ( 'NONE', ( #255901, #143056, #140914, #9775 ) ) ;
#167409=ORIENTED_EDGE ( 'NONE', *, *, #196171, .F. ) ;
#167414=VECTOR ( 'NONE', #87462, 1000.000000000000000 ) ;
#167447=CARTESIAN_POINT ( 'NONE',  ( 21.05000000000000071, 82.09643798151613225, -215.4278993322501208 ) ) ;
#167469=CARTESIAN_POINT ( 'NONE',  ( -20.54999999999999716, 63.76951449014745066, -212.8986194275075832 ) ) ;
#167579=DIRECTION ( 'NONE',  ( 0.000000000000000000, -0.2617529984165152257, -0.9651348961777124202 ) ) ;
#167589=DIRECTION ( 'NONE',  ( 1.000000000000000000, 0.000000000000000000, 0.000000000000000000 ) ) ;
#167591=DIRECTION ( 'NONE',  ( 0.000000000000000000, 0.2617529984165031243, 0.9651348961777157509 ) ) ;
#167614=EDGE_LOOP ( 'NONE', ( #37575, #41672, #27639, #84124 ) ) ;
#167635=EDGE_LOOP ( 'NONE', ( #190672, #120438, #214621, #70261 ) ) ;
#167643=ADVANCED_FACE ( 'NONE', ( #174075 ), #91913, .F. ) ;
#167654=SURFACE_STYLE_USAGE ( .BOTH. , #65965 ) ;
#167672=CARTESIAN_POINT ( 'NONE',  ( -20.64999999999999858, 70.60134440767087938, -223.4290147181903308 ) ) ;
#167690=CARTESIAN_POINT ( 'NONE',  ( -23.25000000000000000, 70.02906482874161043, -215.6060937950565233 ) ) ;
#167705=ORIENTED_EDGE ( 'NONE', *, *, #163168, .F. ) ;
#167730=EDGE_CURVE ( 'NONE', #46377, #204366, #146458, .T. ) ;
#167738=ADVANCED_FACE ( 'NONE', ( #44486 ), #4796, .T. ) ;
#167749=CARTESIAN_POINT ( 'NONE',  ( 23.14999999999999503, 64.14229051353817113, -222.2212283990554624 ) ) ;
#167770=EDGE_CURVE ( 'NONE', #72258, #152104, #34101, .T. ) ;
#167793=AXIS2_PLACEMENT_3D ( 'NONE', #257980, #217595, #123665 ) ;
#167820=LINE ( 'NONE', #68693, #123052 ) ;
#167908=CIRCLE ( 'NONE', #9656, 0.1999999999999987899 ) ;
#167909=AXIS2_PLACEMENT_3D ( 'NONE', #20145, #37150, #197474 ) ;
#167917=CARTESIAN_POINT ( 'NONE',  ( 23.24999999999999645, 76.00000000001126921, -203.5231074845248997 ) ) ;
#167923=VERTEX_POINT ( 'NONE', #213818 ) ;
#167977=CIRCLE ( 'NONE', #192894, 3.999999999999996447 ) ;
#167991=DIRECTION ( 'NONE',  ( 0.000000000000000000, -0.9651348961777157509, 0.2617529984165031243 ) ) ;
#168003=ORIENTED_EDGE ( 'NONE', *, *, #145036, .F. ) ;
#168012=EDGE_LOOP ( 'NONE', ( #168003, #15599, #33411, #236107 ) ) ;
#168060=EDGE_CURVE ( 'NONE', #64537, #124804, #78139, .T. ) ;
#168093=DIRECTION ( 'NONE',  ( 1.000000000000000000, 0.000000000000000000, 0.000000000000000000 ) ) ;
#168115=CARTESIAN_POINT ( 'NONE',  ( 20.94999999999999574, 68.49522935589659767, -224.1230159437372436 ) ) ;
#168116=ORIENTED_EDGE ( 'NONE', *, *, #201857, .T. ) ;
#168136=FACE_OUTER_BOUND ( 'NONE', #174094, .T. ) ;
#168152=CARTESIAN_POINT ( 'NONE',  ( 21.05000000000000071, 78.93126476241668854, -235.8702625865613243 ) ) ;
#168157=LINE ( 'NONE', #71598, #68531 ) ;
#168159=DIRECTION ( 'NONE',  ( -0.000000000000000000, 0.9651348961777161950, -0.2617529984165014589 ) ) ;
#168168=CARTESIAN_POINT ( 'NONE',  ( 21.09813707148777340, 61.06062195154343897, -234.2140757814696883 ) ) ;
#168174=ORIENTED_EDGE ( 'NONE', *, *, #115851, .T. ) ;
#168175=EDGE_LOOP ( 'NONE', ( #152398, #75905, #202731, #220158 ) ) ;
#168219=AXIS2_PLACEMENT_3D ( 'NONE', #82753, #249263, #163625 ) ;
#168225=DIRECTION ( 'NONE',  ( -0.000000000000000000, -0.9651348961777157509, 0.2617529984165028467 ) ) ;
#168226=CARTESIAN_POINT ( 'NONE',  ( -18.49999999999999645, 86.87898763699993765, -199.4031916457581985 ) ) ;
#168229=ORIENTED_EDGE ( 'NONE', *, *, #53830, .F. ) ;
#168232=CARTESIAN_POINT ( 'NONE',  ( 18.52928932304084242, 63.76945704520649372, -209.3485784096579891 ) ) ;
#168234=DIRECTION ( 'NONE',  ( -4.336808689942053235E-15, 0.9667078373770151556, 0.2558827019433999594 ) ) ;
#168263=DIRECTION ( 'NONE',  ( -1.000000000000000000, -2.671448610905051031E-14, -6.406987848362951272E-14 ) ) ;
#168266=ORIENTED_EDGE ( 'NONE', *, *, #96685, .F. ) ;
#168276=CARTESIAN_POINT ( 'NONE',  ( 18.59999999999999076, 70.15623657602074559, -198.0563205710787713 ) ) ;
#168280=CYLINDRICAL_SURFACE ( 'NONE', #94070, 0.1000000000000124678 ) ;
#168292=DIRECTION ( 'NONE',  ( -1.000000000000000000, -0.000000000000000000, -0.000000000000000000 ) ) ;
#168293=DIRECTION ( 'NONE',  ( 0.000000000000000000, 0.2617529984165031243, 0.9651348961777157509 ) ) ;
#168316=ORIENTED_EDGE ( 'NONE', *, *, #106491, .F. ) ;
#168331=ORIENTED_EDGE ( 'NONE', *, *, #56372, .F. ) ;
#168345=AXIS2_PLACEMENT_3D ( 'NONE', #28453, #68837, #85774 ) ;
#168382=VECTOR ( 'NONE', #51693, 1000.000000000000000 ) ;
#168383=EDGE_CURVE ( 'NONE', #231688, #162715, #74582, .T. ) ;
#168393=FACE_OUTER_BOUND ( 'NONE', #133894, .T. ) ;
#168407=DIRECTION ( 'NONE',  ( 0.000000000000000000, -0.2617529984165031243, -0.9651348961777158619 ) ) ;
#168412=EDGE_CURVE ( 'NONE', #93031, #160519, #129893, .T. ) ;
#168417=ORIENTED_EDGE ( 'NONE', *, *, #165643, .F. ) ;
#168441=DIRECTION ( 'NONE',  ( -1.000000000000000000, -0.000000000000000000, -0.000000000000000000 ) ) ;
#168488=CARTESIAN_POINT ( 'NONE',  ( 20.95203847575071521, 59.07703819446410876, -225.8031978033470182 ) ) ;
#168495=CARTESIAN_POINT ( 'NONE',  ( 21.05000000000000071, 70.60134440767089359, -223.4290147181903023 ) ) ;
#168518=CARTESIAN_POINT ( 'NONE',  ( -21.05000000000000071, 61.06362902394928938, -234.0937223954992987 ) ) ;
#168543=CIRCLE ( 'NONE', #101827, 12.87500000000000178 ) ;
#168552=ADVANCED_FACE ( 'NONE', ( #20463 ), #97372, .F. ) ;
#168560=AXIS2_PLACEMENT_3D ( 'NONE', #38520, #18938, #140159 ) ;
#168599=DIRECTION ( 'NONE',  ( 0.000000000000000000, 0.2617529984165045120, 0.9651348961777153068 ) ) ;
#168614=EDGE_LOOP ( 'NONE', ( #78866, #59655, #227084, #224341, #7774, #40849, #162665, #246959, #147192, #151959, #228352, #38638 ) ) ;
#168667=DIRECTION ( 'NONE',  ( 1.000000000000000000, 0.000000000000000000, 0.000000000000000000 ) ) ;
#168689=CARTESIAN_POINT ( 'NONE',  ( 20.94999999999999929, 63.99342642423710714, -222.3880800784493772 ) ) ;
#168697=CARTESIAN_POINT ( 'NONE',  ( -21.05000000000000426, 65.60136641074581121, -241.9452829207083937 ) ) ;
#168721=ORIENTED_EDGE ( 'NONE', *, *, #14990, .T. ) ;
#168728=EDGE_CURVE ( 'NONE', #252057, #153545, #255062, .T. ) ;
#168758=VECTOR ( 'NONE', #89453, 1000.000000000000000 ) ;
#168779=LINE ( 'NONE', #167469, #104917 ) ;
#168784=AXIS2_PLACEMENT_3D ( 'NONE', #51686, #213341, #93400 ) ;
#168820=CARTESIAN_POINT ( 'NONE',  ( -21.00023020733438983, 61.06322362754159627, -234.1822973190417088 ) ) ;
#168846=EDGE_CURVE ( 'NONE', #30986, #187774, #238425, .T. ) ;
#168852=CARTESIAN_POINT ( 'NONE',  ( -20.64999999999999858, 70.22209180797715078, -215.6584443947398313 ) ) ;
#168861=EDGE_CURVE ( 'NONE', #177586, #206303, #59506, .T. ) ;
#168910=DIRECTION ( 'NONE',  ( 0.000000000000000000, 0.2617529984165031243, 0.9651348961777157509 ) ) ;
#168914=ORIENTED_EDGE ( 'NONE', *, *, #98376, .F. ) ;
#168956=AXIS2_PLACEMENT_3D ( 'NONE', #172980, #97200, #214619 ) ;
#168963=DIRECTION ( 'NONE',  ( -0.000000000000000000, 0.9667078373770112698, 0.2558827019434132821 ) ) ;
#168970=CARTESIAN_POINT ( 'NONE',  ( -21.05000000000000071, 68.11887992016828264, -227.8068560890360175 ) ) ;
#168996=EDGE_CURVE ( 'NONE', #147541, #184831, #27928, .T. ) ;
#169040=LINE ( 'NONE', #248535, #186864 ) ;
#169049=DIRECTION ( 'NONE',  ( 0.000000000000000000, 0.2617529984165058998, 0.9651348961777149738 ) ) ;
#169076=AXIS2_PLACEMENT_3D ( 'NONE', #47132, #69306, #203668 ) ;
#169121=DIRECTION ( 'NONE',  ( -1.000000000000000000, 0.000000000000000000, 0.000000000000000000 ) ) ;
#169161=CARTESIAN_POINT ( 'NONE',  ( 18.55857864376268296, 63.70395599151300559, -209.2544033210146210 ) ) ;
#169171=AXIS2_PLACEMENT_3D ( 'NONE', #251303, #11438, #90954 ) ;
#169175=CARTESIAN_POINT ( 'NONE',  ( 21.05000000000000071, 75.50266930301991408, -205.3568637872625686 ) ) ;
#169228=ORIENTED_EDGE ( 'NONE', *, *, #220109, .F. ) ;
#169249=DIRECTION ( 'NONE',  ( 1.000000000000000000, 0.000000000000000000, 0.000000000000000000 ) ) ;
#169258=EDGE_LOOP ( 'NONE', ( #887, #87918 ) ) ;
#169284=DIRECTION ( 'NONE',  ( 1.000000000000000000, 0.000000000000000000, -0.000000000000000000 ) ) ;
#169287=CIRCLE ( 'NONE', #189910, 4.049999999999987388 ) ;
#169290=VERTEX_POINT ( 'NONE', #186142 ) ;
#169319=DIRECTION ( 'NONE',  ( 0.000000000000000000, 0.2617529984165152257, 0.9651348961777124202 ) ) ;
#169334=ORIENTED_EDGE ( 'NONE', *, *, #9843, .T. ) ;
#169336=CYLINDRICAL_SURFACE ( 'NONE', #241531, 0.1000000000000124678 ) ;
#169343=VECTOR ( 'NONE', #175413, 1000.000000000000000 ) ;
#169356=EDGE_CURVE ( 'NONE', #79096, #99302, #68764, .T. ) ;
#169388=DIRECTION ( 'NONE',  ( -0.000000000000000000, 0.3896596508880098009, 0.9209589331071360574 ) ) ;
#169397=CARTESIAN_POINT ( 'NONE',  ( 18.59999999999998366, 76.00000000001126921, -203.5231074845248997 ) ) ;
#169404=CARTESIAN_POINT ( 'NONE',  ( -22.50485643085239573, 64.23176994213648072, -247.2158861856937051 ) ) ;
#169409=EDGE_LOOP ( 'NONE', ( #57625, #227750, #177268, #89205 ) ) ;
#169436=ADVANCED_FACE ( 'NONE', ( #29665 ), #189994, .F. ) ;
#169448=CARTESIAN_POINT ( 'NONE',  ( 21.08035267497491105, 61.09867933414660257, -234.2775889333592829 ) ) ;
#169459=DIRECTION ( 'NONE',  ( 0.000000000000000000, 0.2617529984165035684, 0.9651348961777156399 ) ) ;
#169473=DIRECTION ( 'NONE',  ( 1.000000000000000000, 0.000000000000000000, 0.000000000000000000 ) ) ;
#169485=CARTESIAN_POINT ( 'NONE',  ( 20.97217846901852312, 60.89049786204130044, -225.3271215246448094 ) ) ;
#169507=ORIENTED_EDGE ( 'NONE', *, *, #156048, .F. ) ;
#169514=ORIENTED_EDGE ( 'NONE', *, *, #151196, .T. ) ;
#169517=CARTESIAN_POINT ( 'NONE',  ( 18.49999999999999289, 63.68186668325585487, -209.1448000494835355 ) ) ;
#169550=CARTESIAN_POINT ( 'NONE',  ( -23.15000000000000213, 67.23127455305841238, -235.8551265064783991 ) ) ;
#169590=FACE_OUTER_BOUND ( 'NONE', #195207, .T. ) ;
#169612=DIRECTION ( 'NONE',  ( 0.000000000000000000, 0.2617529984165031243, 0.9651348961777157509 ) ) ;
#169628=AXIS2_PLACEMENT_3D ( 'NONE', #233365, #108570, #54690 ) ;
#169637=CIRCLE ( 'NONE', #240331, 0.1000000000000124678 ) ;
#169643=AXIS2_PLACEMENT_3D ( 'NONE', #27467, #165669, #106941 ) ;
#169692=EDGE_CURVE ( 'NONE', #41329, #229500, #181990, .T. ) ;
#169749=LINE ( 'NONE', #70643, #207136 ) ;
#169756=ORIENTED_EDGE ( 'NONE', *, *, #115364, .T. ) ;
#169758=FACE_OUTER_BOUND ( 'NONE', #226624, .T. ) ;
#169781=EDGE_CURVE ( 'NONE', #234655, #103686, #234894, .T. ) ;
#169794=ORIENTED_EDGE ( 'NONE', *, *, #144780, .F. ) ;
#169822=ADVANCED_FACE ( 'NONE', ( #231395 ), #255678, .F. ) ;
#169872=AXIS2_PLACEMENT_3D ( 'NONE', #213385, #252505, #92162 ) ;
#169882=AXIS2_PLACEMENT_3D ( 'NONE', #194754, #196026, #95617 ) ;
#169885=CIRCLE ( 'NONE', #178235, 11.64999999999998970 ) ;
#169930=ORIENTED_EDGE ( 'NONE', *, *, #182553, .T. ) ;
#169944=CIRCLE ( 'NONE', #199119, 0.1000000000000124678 ) ;
#169951=ORIENTED_EDGE ( 'NONE', *, *, #78191, .F. ) ;
#169974=DIRECTION ( 'NONE',  ( 0.000000000000000000, 0.2617529984165031243, 0.9651348961777158619 ) ) ;
#169980=CARTESIAN_POINT ( 'NONE',  ( 21.05000000000000071, 82.48249193998721296, -215.5326005316167084 ) ) ;
#169983=AXIS2_PLACEMENT_3D ( 'NONE', #32123, #174219, #77612 ) ;
#170018=CIRCLE ( 'NONE', #57518, 0.1999999999999987899 ) ;
#170032=EDGE_LOOP ( 'NONE', ( #43562, #44447, #145058, #74276 ) ) ;
#170041=DIRECTION ( 'NONE',  ( -3.469446951953245002E-14, -0.2617529984164506107, -0.9651348961777299618 ) ) ;
#170043=EDGE_CURVE ( 'NONE', #140929, #26421, #196114, .T. ) ;
#170073=ORIENTED_EDGE ( 'NONE', *, *, #197750, .F. ) ;
#170092=CARTESIAN_POINT ( 'NONE',  ( 23.14999999999998437, 67.23127455305841238, -235.8551265064783991 ) ) ;
#170097=AXIS2_PLACEMENT_3D ( 'NONE', #143647, #139785, #219330 ) ;
#170107=ORIENTED_EDGE ( 'NONE', *, *, #139148, .T. ) ;
#170116=VERTEX_POINT ( 'NONE', #159558 ) ;
#170134=ORIENTED_EDGE ( 'NONE', *, *, #102026, .F. ) ;
#170136=DIRECTION ( 'NONE',  ( -1.000000000000000000, -0.000000000000000000, 0.000000000000000000 ) ) ;
#170137=DIRECTION ( 'NONE',  ( -1.000000000000000000, 0.000000000000000000, 0.000000000000000000 ) ) ;
#170147=DIRECTION ( 'NONE',  ( 1.000000000000000000, 0.000000000000000000, 0.000000000000000000 ) ) ;
#170155=CIRCLE ( 'NONE', #249409, 0.09999999999999939493 ) ;
#170184=CARTESIAN_POINT ( 'NONE',  ( -21.14999999999999858, 56.01362831242966678, -232.7091905853083347 ) ) ;
#170237=LINE ( 'NONE', #171498, #230515 ) ;
#170254=CARTESIAN_POINT ( 'NONE',  ( 21.05000000000000071, 68.35681244624937847, -231.7050464529141891 ) ) ;
#170292=CARTESIAN_POINT ( 'NONE',  ( 23.14999999999999858, 76.00000000001126921, -203.5231074845248997 ) ) ;
#170341=ORIENTED_EDGE ( 'NONE', *, *, #60497, .T. ) ;
#170343=DIRECTION ( 'NONE',  ( 0.000000000000000000, -0.9209589331071864615, 0.3896596508878908960 ) ) ;
#170399=PLANE ( 'NONE',  #47113 ) ;
#170417=ADVANCED_FACE ( 'NONE', ( #159266 ), #60273, .T. ) ;
#170439=ORIENTED_EDGE ( 'NONE', *, *, #60511, .F. ) ;
#170442=LINE ( 'NONE', #230355, #168382 ) ;
#170486=DIRECTION ( 'NONE',  ( 1.000000000000000000, 0.000000000000000000, 0.000000000000000000 ) ) ;
#170488=CARTESIAN_POINT ( 'NONE',  ( 21.14999999999999503, 75.39949836213487799, -250.2448839681187849 ) ) ;
#170496=LINE ( 'NONE', #13946, #242407 ) ;
#170521=DIRECTION ( 'NONE',  ( 0.000000000000000000, -0.2617529984165035684, -0.9651348961777156399 ) ) ;
#170535=CYLINDRICAL_SURFACE ( 'NONE', #114314, 0.5000000000000014433 ) ;
#170551=ORIENTED_EDGE ( 'NONE', *, *, #117769, .T. ) ;
#170565=AXIS2_PLACEMENT_3D ( 'NONE', #209411, #132449, #170343 ) ;
#170576=FACE_OUTER_BOUND ( 'NONE', #445, .T. ) ;
#170587=AXIS2_PLACEMENT_3D ( 'NONE', #10459, #105670, #146100 ) ;
#170598=DIRECTION ( 'NONE',  ( 0.000000000000000000, -0.9942466578594181259, 0.1071148137998542138 ) ) ;
#170606=EDGE_CURVE ( 'NONE', #115375, #216022, #87399, .T. ) ;
#170632=DIRECTION ( 'NONE',  ( 0.000000000000000000, -0.2617529984165035128, -0.9651348961777155289 ) ) ;
#170660=AXIS2_PLACEMENT_3D ( 'NONE', #248423, #222751, #44140 ) ;
#170677=CARTESIAN_POINT ( 'NONE',  ( 20.94999999999999929, 68.16863917788211324, -213.8681745540812926 ) ) ;
#170709=EDGE_CURVE ( 'NONE', #26421, #255695, #158642, .T. ) ;
#170713=AXIS2_PLACEMENT_3D ( 'NONE', #250657, #211553, #92869 ) ;
#170714=DIRECTION ( 'NONE',  ( 0.000000000000000000, -0.9651348961777379554, 0.2617529984164210233 ) ) ;
#170718=DIRECTION ( 'NONE',  ( -0.000000000000000000, 0.2617529984165031243, 0.9651348961777157509 ) ) ;
#170726=DIRECTION ( 'NONE',  ( 0.000000000000000000, 0.9934243067848629316, -0.1144908148674594617 ) ) ;
#170737=EDGE_CURVE ( 'NONE', #249301, #227798, #177019, .T. ) ;
#170754=TOROIDAL_SURFACE ( 'NONE', #253880, 4.099999999999999645, 0.1000000000000000056 ) ;
#170778=AXIS2_PLACEMENT_3D ( 'NONE', #83462, #80909, #44381 ) ;
#170780=DIRECTION ( 'NONE',  ( 0.000000000000000000, 0.2617529984165152257, 0.9651348961777124202 ) ) ;
#170787=DIRECTION ( 'NONE',  ( 0.000000000000000000, 0.2617529984165031243, 0.9651348961777157509 ) ) ;
#170803=CARTESIAN_POINT ( 'NONE',  ( 18.59999999999999787, 67.23127455305841238, -235.8551265064783991 ) ) ;
#170808=EDGE_CURVE ( 'NONE', #4559, #231216, #85544, .T. ) ;
#170815=CARTESIAN_POINT ( 'NONE',  ( 18.44364597020195262, 78.23832191996586971, -231.5273892603947559 ) ) ;
#170818=DIRECTION ( 'NONE',  ( 0.7071067811865475727, 0.6824534298470373850, -0.1850873201762210096 ) ) ;
#170845=DIRECTION ( 'NONE',  ( -1.000000000000000000, -0.000000000000000000, 0.000000000000000000 ) ) ;
#170858=DIRECTION ( 'NONE',  ( -3.440080580676165868E-14, 0.3848449534832963370, 0.9229812358755945523 ) ) ;
#170921=VECTOR ( 'NONE', #126273, 1000.000000000000000 ) ;
#170962=AXIS2_PLACEMENT_3D ( 'NONE', #141865, #40237, #101409 ) ;
#170963=EDGE_CURVE ( 'NONE', #4469, #78065, #181289, .T. ) ;
#170971=ORIENTED_EDGE ( 'NONE', *, *, #55953, .T. ) ;
#170991=CARTESIAN_POINT ( 'NONE',  ( -21.12757541349819590, 65.53186650915749567, -242.1014610283184254 ) ) ;
#170996=DIRECTION ( 'NONE',  ( 0.000000000000000000, -0.2617529984165035684, -0.9651348961777156399 ) ) ;
#170997=EDGE_CURVE ( 'NONE', #142984, #2330, #222945, .T. ) ;
#171024=ORIENTED_EDGE ( 'NONE', *, *, #245706, .T. ) ;
#171064=FACE_OUTER_BOUND ( 'NONE', #24658, .T. ) ;
#171078=ADVANCED_FACE ( 'NONE', ( #77451 ), #99578, .T. ) ;
#171082=EDGE_CURVE ( 'NONE', #128967, #185020, #197998, .T. ) ;
#171123=EDGE_LOOP ( 'NONE', ( #25744, #234849, #110584, #172829 ) ) ;
#171127=ORIENTED_EDGE ( 'NONE', *, *, #47631, .F. ) ;
#171138=CIRCLE ( 'NONE', #229366, 0.09999999999999949207 ) ;
#171141=ORIENTED_EDGE ( 'NONE', *, *, #144780, .T. ) ;
#171168=ORIENTED_EDGE ( 'NONE', *, *, #195879, .T. ) ;
#171178=CARTESIAN_POINT ( 'NONE',  ( 18.59999999999999076, 79.19526988099229925, -196.1889237952725296 ) ) ;
#171190=CARTESIAN_POINT ( 'NONE',  ( -18.39999999999999858, 78.24390740893980478, -231.6169762517609172 ) ) ;
#171200=AXIS2_PLACEMENT_3D ( 'NONE', #12554, #210733, #232890 ) ;
#171205=DIRECTION ( 'NONE',  ( 1.000000000000000000, 0.000000000000000000, 0.000000000000000000 ) ) ;
#171229=CARTESIAN_POINT ( 'NONE',  ( 22.39999999999999503, 55.98745301258800566, -232.8057040749260977 ) ) ;
#171270=DIRECTION ( 'NONE',  ( -1.000000000000000000, 0.000000000000000000, 0.000000000000000000 ) ) ;
#171280=LINE ( 'NONE', #13447, #166918 ) ;
#171335=ORIENTED_EDGE ( 'NONE', *, *, #138898, .T. ) ;
#171340=ORIENTED_EDGE ( 'NONE', *, *, #210155, .T. ) ;
#171344=CARTESIAN_POINT ( 'NONE',  ( -20.54999999999999716, 68.76258920191057200, -222.5680764032308048 ) ) ;
#171363=DIRECTION ( 'NONE',  ( 1.000000000000000000, -3.151514657663852580E-16, 8.547182517843351137E-17 ) ) ;
#171365=DIRECTION ( 'NONE',  ( 0.000000000000000000, 0.2617529984165152257, 0.9651348961777124202 ) ) ;
#171404=ORIENTED_EDGE ( 'NONE', *, *, #153100, .F. ) ;
#171412=CARTESIAN_POINT ( 'NONE',  ( -23.25000000000000000, 79.38304387823772856, -235.9388060597213723 ) ) ;
#171416=DIRECTION ( 'NONE',  ( -1.000000000000000000, -0.000000000000000000, 0.000000000000000000 ) ) ;
#171424=VERTEX_POINT ( 'NONE', #73363 ) ;
#171441=ORIENTED_EDGE ( 'NONE', *, *, #157634, .T. ) ;
#171469=ORIENTED_EDGE ( 'NONE', *, *, #222009, .F. ) ;
#171478=CARTESIAN_POINT ( 'NONE',  ( 18.59999999999999787, 79.37986612816742138, -196.2658927859692142 ) ) ;
#171482=LINE ( 'NONE', #238815, #220325 ) ;
#171488=DIRECTION ( 'NONE',  ( 2.952720810173289112E-16, 0.9651348961777191926, -0.2617529984164898571 ) ) ;
#171498=CARTESIAN_POINT ( 'NONE',  ( 20.94999999999999574, 68.59681812508419796, -224.1344059333694361 ) ) ;
#171500=ORIENTED_EDGE ( 'NONE', *, *, #126075, .T. ) ;
#171505=ADVANCED_FACE ( 'NONE', ( #236254 ), #193932, .T. ) ;
#171552=CIRCLE ( 'NONE', #204829, 0.09999999999999939493 ) ;
#171580=VERTEX_POINT ( 'NONE', #234982 ) ;
#171637=( BOUNDED_SURFACE ( )  B_SPLINE_SURFACE ( 3, 2, ( 
 ( #240977, #165281, #27092 ),
 ( #81854, #204393, #3629 ),
 ( #162733, #106569, #143131 ),
 ( #23234, #146983, #242242 ) ),
 .UNSPECIFIED., .F., .F., .T. ) 
 B_SPLINE_SURFACE_WITH_KNOTS ( ( 4, 4 ),
 ( 3, 3 ),
 ( 6.938893903907228378E-18, 0.001979672783031562362 ),
 ( 0.000000000000000000, 1.000000000000000000 ),
 .UNSPECIFIED. ) 
 GEOMETRIC_REPRESENTATION_ITEM ( )  RATIONAL_B_SPLINE_SURFACE ( (
 ( 1.000000000000000000, 0.7103081912008362142, 1.000000000000000000),
 ( 1.000000000000000000, 0.7104998333558624202, 1.000000000000000000),
 ( 1.000000000000000000, 0.7107238315756159164, 1.000000000000000000),
 ( 1.000000000000000000, 0.7110073749539299603, 1.000000000000000000) ) ) 
 REPRESENTATION_ITEM ( '' )  SURFACE ( )  );
#171658=EDGE_LOOP ( 'NONE', ( #154176, #141509, #69992, #133163 ) ) ;
#171677=EDGE_LOOP ( 'NONE', ( #4145, #42593, #234421, #71404 ) ) ;
#171695=CARTESIAN_POINT ( 'NONE',  ( 22.49999999999999289, 55.96443555106008461, -232.8914797391818752 ) ) ;
#171709=CARTESIAN_POINT ( 'NONE',  ( 18.54148534481893762, 67.49261718274587452, -195.4446851895584416 ) ) ;
#171727=VERTEX_POINT ( 'NONE', #208710 ) ;
#171738=CARTESIAN_POINT ( 'NONE',  ( 18.59999999999999787, 72.05339752741123505, -225.0867394276846483 ) ) ;
#171749=DIRECTION ( 'NONE',  ( 1.000000000000000000, 0.000000000000000000, -0.000000000000000000 ) ) ;
#171813=EDGE_CURVE ( 'NONE', #82125, #203694, #127461, .T. ) ;
#171815=DIRECTION ( 'NONE',  ( 0.000000000000000000, 0.2617529984165031243, 0.9651348961777157509 ) ) ;
#171821=CARTESIAN_POINT ( 'NONE',  ( 20.95512820512820440, 60.15812638745688901, -221.3479132702343009 ) ) ;
#171826=CIRCLE ( 'NONE', #205084, 0.8750000000000007772 ) ;
#171854=DIRECTION ( 'NONE',  ( 0.000000000000000000, 0.2617529984165152257, 0.9651348961777124202 ) ) ;
#171879=ADVANCED_FACE ( 'NONE', ( #165733 ), #71768, .T. ) ;
#171900=PLANE ( 'NONE',  #1435 ) ;
#171969=CYLINDRICAL_SURFACE ( 'NONE', #250884, 0.1000000000000048767 ) ;
#171988=DIRECTION ( 'NONE',  ( 0.000000000000000000, 0.3994087351226822125, 0.9167729611565227366 ) ) ;
#172046=DIRECTION ( 'NONE',  ( -1.000000000000000000, -0.000000000000000000, -0.000000000000000000 ) ) ;
#172062=ORIENTED_EDGE ( 'NONE', *, *, #208725, .T. ) ;
#172089=AXIS2_PLACEMENT_3D ( 'NONE', #204072, #63279, #103669 ) ;
#172093=CARTESIAN_POINT ( 'NONE',  ( -21.55000000000000426, 65.32753222054176945, -213.4247798787853867 ) ) ;
#172126=ORIENTED_EDGE ( 'NONE', *, *, #91758, .T. ) ;
#172136=CARTESIAN_POINT ( 'NONE',  ( 23.24999999999999289, 52.81534179157632991, -244.1198638051726277 ) ) ;
#172174=EDGE_LOOP ( 'NONE', ( #181611, #137225, #152945, #7634, #158444, #248984, #242398 ) ) ;
#172178=EDGE_CURVE ( 'NONE', #186373, #36582, #194317, .T. ) ;
#172230=DIRECTION ( 'NONE',  ( -1.000000000000000000, -0.000000000000000000, -0.000000000000000000 ) ) ;
#172235=DIRECTION ( 'NONE',  ( 1.000000000000000000, 0.000000000000000000, 0.000000000000000000 ) ) ;
#172272=CARTESIAN_POINT ( 'NONE',  ( -21.13498764882296044, 65.52942838307841100, -242.1238406827027063 ) ) ;
#172277=SPHERICAL_SURFACE ( 'NONE', #70215, 0.1000000000000000056 ) ;
#172305=ORIENTED_EDGE ( 'NONE', *, *, #78191, .T. ) ;
#172310=AXIS2_PLACEMENT_3D ( 'NONE', #29197, #31752, #68285 ) ;
#172332=ORIENTED_EDGE ( 'NONE', *, *, #217294, .F. ) ;
#172473=EDGE_CURVE ( 'NONE', #229500, #231654, #57065, .T. ) ;
#172476=CIRCLE ( 'NONE', #80828, 11.65000000000000391 ) ;
#172480=EDGE_CURVE ( 'NONE', #155936, #97513, #2912, .T. ) ;
#172503=EDGE_LOOP ( 'NONE', ( #60402, #92733, #14643, #166578 ) ) ;
#172516=AXIS2_PLACEMENT_3D ( 'NONE', #73828, #232897, #133761 ) ;
#172528=ADVANCED_FACE ( 'NONE', ( #224728 ), #140271, .F. ) ;
#172536=DIRECTION ( 'NONE',  ( -1.000000000000000000, -0.000000000000000000, -0.000000000000000000 ) ) ;
#172552=DIRECTION ( 'NONE',  ( -1.000000000000000000, 0.000000000000000000, 0.000000000000000000 ) ) ;
#172570=DIRECTION ( 'NONE',  ( 2.465190328815662439E-32, -0.2617529984165030132, -0.9651348961777158619 ) ) ;
#172589=DIRECTION ( 'NONE',  ( 0.000000000000000000, 0.2617529984165021806, 0.9651348961777159730 ) ) ;
#172621=ORIENTED_EDGE ( 'NONE', *, *, #192225, .T. ) ;
#172623=ORIENTED_EDGE ( 'NONE', *, *, #194139, .T. ) ;
#172631=EDGE_CURVE ( 'NONE', #248447, #79198, #106573, .T. ) ;
#172634=DIRECTION ( 'NONE',  ( 0.000000000000000000, 0.9229812358755983270, -0.3848449534832869001 ) ) ;
#172637=VECTOR ( 'NONE', #100203, 1000.000000000000000 ) ;
#172649=CARTESIAN_POINT ( 'NONE',  ( 23.14999999999999503, 60.99662849158838895, -205.1669373764474642 ) ) ;
#172674=CARTESIAN_POINT ( 'NONE',  ( -22.47071067811866385, 59.75442326890419764, -233.9300113800878762 ) ) ;
#172708=AXIS2_PLACEMENT_3D ( 'NONE', #128466, #185865, #149337 ) ;
#172721=ORIENTED_EDGE ( 'NONE', *, *, #37632, .F. ) ;
#172731=AXIS2_PLACEMENT_3D ( 'NONE', #224655, #241660, #3031 ) ;
#172780=CYLINDRICAL_SURFACE ( 'NONE', #245619, 0.1000000000000124678 ) ;
#172828=EDGE_CURVE ( 'NONE', #159529, #104826, #113410, .T. ) ;
#172829=ORIENTED_EDGE ( 'NONE', *, *, #66209, .F. ) ;
#172835=ORIENTED_EDGE ( 'NONE', *, *, #126075, .F. ) ;
#172842=ORIENTED_EDGE ( 'NONE', *, *, #163168, .T. ) ;
#172844=CARTESIAN_POINT ( 'NONE',  ( 22.40000000000020819, 64.25313205997866817, -247.2214437328679537 ) ) ;
#172873=CARTESIAN_POINT ( 'NONE',  ( -18.59999999999999787, 80.78317333349157536, -192.9003134612048882 ) ) ;
#172876=CIRCLE ( 'NONE', #255968, 0.1000000000000106498 ) ;
#172914=CARTESIAN_POINT ( 'NONE',  ( 18.59999999999997655, 76.00000000001126921, -203.5231074845248997 ) ) ;
#172947=ORIENTED_EDGE ( 'NONE', *, *, #234518, .T. ) ;
#172976=VERTEX_POINT ( 'NONE', #2423 ) ;
#172980=CARTESIAN_POINT ( 'NONE',  ( 18.59999999999999787, 72.02722222756958104, -225.1832529173024398 ) ) ;
#173002=CARTESIAN_POINT ( 'NONE',  ( 22.48508240969612615, 64.13718632996433655, -247.0868454141091490 ) ) ;
#173006=EDGE_CURVE ( 'NONE', #79058, #38302, #241075, .T. ) ;
#173034=DIRECTION ( 'NONE',  ( 0.000000000000000000, -0.3896596508880098009, -0.9209589331071360574 ) ) ;
#173044=AXIS2_PLACEMENT_3D ( 'NONE', #236100, #157903, #216536 ) ;
#173086=EDGE_CURVE ( 'NONE', #135164, #247253, #6276, .T. ) ;
#173103=ADVANCED_FACE ( 'NONE', ( #44146 ), #148375, .T. ) ;
#173108=ORIENTED_EDGE ( 'NONE', *, *, #22513, .T. ) ;
#173117=CARTESIAN_POINT ( 'NONE',  ( 21.03670563405603033, 60.20313529934050223, -221.1782316337949794 ) ) ;
#173127=EDGE_CURVE ( 'NONE', #128036, #134983, #53119, .T. ) ;
#173138=ORIENTED_EDGE ( 'NONE', *, *, #61425, .T. ) ;
#173142=ADVANCED_FACE ( 'NONE', ( #153560 ), #111824, .F. ) ;
#173168=CARTESIAN_POINT ( 'NONE',  ( -21.00219873199061738, 57.83991513803482576, -226.1457439616172849 ) ) ;
#173169=TOROIDAL_SURFACE ( 'NONE', #68905, 7.800000000000000711, 0.1000000000000000056 ) ;
#173196=DIRECTION ( 'NONE',  ( 0.000000000000000000, 0.9651348961777157509, -0.2617529984165031243 ) ) ;
#173249=CIRCLE ( 'NONE', #160761, 4.100000000000008527 ) ;
#173253=EDGE_CURVE ( 'NONE', #220738, #245391, #56855, .T. ) ;
#173265=FACE_OUTER_BOUND ( 'NONE', #187902, .T. ) ;
#173279=DIRECTION ( 'NONE',  ( -0.000000000000000000, -0.9651348961777157509, 0.2617529984165031243 ) ) ;
#173302=ORIENTED_EDGE ( 'NONE', *, *, #162400, .T. ) ;
#173335=DIRECTION ( 'NONE',  ( -1.000000000000000000, -0.000000000000000000, -0.000000000000000000 ) ) ;
#173340=LINE ( 'NONE', #237112, #222597 ) ;
#173342=CARTESIAN_POINT ( 'NONE',  ( 20.12518398540832010, 59.69712022869846635, -225.5262535407554765 ) ) ;
#173373=DIRECTION ( 'NONE',  ( 1.000000000000000000, 0.000000000000000000, 0.000000000000000000 ) ) ;
#173385=CARTESIAN_POINT ( 'NONE',  ( 20.94999999999999929, 81.91411460262999356, -215.0718681741873013 ) ) ;
#173394=AXIS2_PLACEMENT_3D ( 'NONE', #153655, #14105, #59590 ) ;
#173407=ORIENTED_EDGE ( 'NONE', *, *, #5235, .T. ) ;
#173412=DIRECTION ( 'NONE',  ( 0.000000000000000000, 0.4099100576504394744, 0.9121259477928547188 ) ) ;
#173424=CARTESIAN_POINT ( 'NONE',  ( 20.85000000000000142, 80.78317333349157536, -192.9003134612049166 ) ) ;
#173440=B_SPLINE_CURVE_WITH_KNOTS ( 'NONE', 3,
 ( #197401, #77438, #99565, #201254, #240398, #22652, #61751, #21368, #155752, #180422, #98269, #141293, #219527, #81283, #39654, #116592 ),
 .UNSPECIFIED., .F., .F.,
 ( 4, 3, 3, 3, 3, 4 ),
 ( 0.000000000000000000, 2.209075297431153384E-05, 5.594258369009587762E-05, 8.979524372342081605E-05, 0.0001236472815274580067, 0.0001574990747609520314 ),
 .UNSPECIFIED. ) ;
#173451=DIRECTION ( 'NONE',  ( -1.000000000000000000, -0.000000000000000000, -0.000000000000000000 ) ) ;
#173501=VECTOR ( 'NONE', #96576, 1000.000000000000000 ) ;
#173526=CIRCLE ( 'NONE', #78166, 12.87500000000000178 ) ;
#173536=CARTESIAN_POINT ( 'NONE',  ( -22.39999999999999858, 56.01362831242966678, -232.7091905853083347 ) ) ;
#173572=CARTESIAN_POINT ( 'NONE',  ( 21.05000000000000071, 65.49889199258034012, -241.8691648588986425 ) ) ;
#173593=ADVANCED_FACE ( 'NONE', ( #68532, #23679 ), #182738, .F. ) ;
#173614=AXIS2_PLACEMENT_3D ( 'NONE', #185474, #5526, #85050 ) ;
#173640=FACE_OUTER_BOUND ( 'NONE', #203838, .T. ) ;
#173665=VERTEX_POINT ( 'NONE', #203568 ) ;
#173671=FACE_OUTER_BOUND ( 'NONE', #67254, .T. ) ;
#173719=ADVANCED_FACE ( 'NONE', ( #144863 ), #44622, .T. ) ;
#173724=LINE ( 'NONE', #134522, #125327 ) ;
#173740=ORIENTED_EDGE ( 'NONE', *, *, #35076, .F. ) ;
#173762=ORIENTED_EDGE ( 'NONE', *, *, #182879, .F. ) ;
#173768=ORIENTED_EDGE ( 'NONE', *, *, #156479, .F. ) ;
#173917=ORIENTED_EDGE ( 'NONE', *, *, #221020, .F. ) ;
#173934=EDGE_CURVE ( 'NONE', #45881, #108241, #110885, .T. ) ;
#173950=ORIENTED_EDGE ( 'NONE', *, *, #6170, .T. ) ;
#173960=CARTESIAN_POINT ( 'NONE',  ( -20.85000000000000142, 78.06784868750165174, -195.8985418047209350 ) ) ;
#173992=VECTOR ( 'NONE', #106140, 1000.000000000000000 ) ;
#174018=EDGE_CURVE ( 'NONE', #143707, #128967, #140453, .T. ) ;
#174036=CIRCLE ( 'NONE', #86652, 0.1000000000000124678 ) ;
#174075=FACE_OUTER_BOUND ( 'NONE', #91431, .T. ) ;
#174094=EDGE_LOOP ( 'NONE', ( #238511, #199140, #17447, #233578 ) ) ;
#174105=CARTESIAN_POINT ( 'NONE',  ( -22.39999999999999858, 59.71212129423881976, -233.8158665866020272 ) ) ;
#174108=FACE_OUTER_BOUND ( 'NONE', #42201, .T. ) ;
#174125=FACE_OUTER_BOUND ( 'NONE', #177062, .T. ) ;
#174140=DIRECTION ( 'NONE',  ( -2.952720810173289112E-16, -0.9651348961777157509, 0.2617529984165031243 ) ) ;
#174161=VECTOR ( 'NONE', #127779, 1000.000000000000000 ) ;
#174179=ORIENTED_EDGE ( 'NONE', *, *, #90356, .T. ) ;
#174186=DIRECTION ( 'NONE',  ( 1.000000000000000000, 7.049440681616514931E-16, -1.911869773728115948E-16 ) ) ;
#174209=DIRECTION ( 'NONE',  ( 0.000000000000000000, 0.9651348961777157509, -0.2617529984165031243 ) ) ;
#174219=DIRECTION ( 'NONE',  ( -0.000000000000000000, 0.3848449534832963370, 0.9229812358755945523 ) ) ;
#174223=EDGE_CURVE ( 'NONE', #231873, #255695, #132457, .T. ) ;
#174251=ORIENTED_EDGE ( 'NONE', *, *, #44126, .T. ) ;
#174252=DIRECTION ( 'NONE',  ( 0.000000000000000000, -0.9651348961777157509, 0.2617529984165031243 ) ) ;
#174261=DIRECTION ( 'NONE',  ( 0.000000000000000000, -0.2617529984165031243, -0.9651348961777157509 ) ) ;
#174267=ORIENTED_EDGE ( 'NONE', *, *, #256793, .F. ) ;
#174270=ADVANCED_FACE ( 'NONE', ( #154864 ), #165138, .T. ) ;
#174276=VERTEX_POINT ( 'NONE', #177000 ) ;
#174278=EDGE_LOOP ( 'NONE', ( #109093, #177957, #216173, #246953, #216618 ) ) ;
#174307=EDGE_LOOP ( 'NONE', ( #200159, #20008, #171469, #200815 ) ) ;
#174328=DIRECTION ( 'NONE',  ( 0.000000000000000000, -0.2617529984165152257, -0.9651348961777124202 ) ) ;
#174345=FACE_OUTER_BOUND ( 'NONE', #100085, .T. ) ;
#174377=ORIENTED_EDGE ( 'NONE', *, *, #164177, .F. ) ;
#174409=EDGE_LOOP ( 'NONE', ( #228187, #59688 ) ) ;
#174437=ORIENTED_EDGE ( 'NONE', *, *, #82656, .T. ) ;
#174456=ORIENTED_EDGE ( 'NONE', *, *, #128582, .T. ) ;
#174482=CARTESIAN_POINT ( 'NONE',  ( 21.05000000000000071, 76.49733069700262433, -201.6893511817872309 ) ) ;
#174495=DIRECTION ( 'NONE',  ( 0.000000000000000000, -0.2617529984165031243, -0.9651348961777157509 ) ) ;
#174544=FACE_OUTER_BOUND ( 'NONE', #131267, .T. ) ;
#174550=CARTESIAN_POINT ( 'NONE',  ( 18.59999999999999076, 55.11435547888746811, -226.8560373590520101 ) ) ;
#174566=CARTESIAN_POINT ( 'NONE',  ( 20.96428641294277995, 62.87317279473580811, -207.0346585172396487 ) ) ;
#174580=CYLINDRICAL_SURFACE ( 'NONE', #134272, 0.1000000000000124678 ) ;
#174586=DIRECTION ( 'NONE',  ( -0.000000000000000000, 0.3848449534832868446, 0.9229812358755982160 ) ) ;
#174601=EDGE_CURVE ( 'NONE', #148962, #9861, #224213, .T. ) ;
#174603=CARTESIAN_POINT ( 'NONE',  ( 21.05000000000000071, 58.76097767208403866, -233.5579081436841022 ) ) ;
#174629=CARTESIAN_POINT ( 'NONE',  ( 20.30466543256828160, 60.41185174759706911, -225.4538167435136415 ) ) ;
#174630=DIRECTION ( 'NONE',  ( 0.000000000000000000, 0.2617529984165030132, 0.9651348961777157509 ) ) ;
#174641=EDGE_CURVE ( 'NONE', #221167, #257696, #66002, .T. ) ;
#174666=EDGE_LOOP ( 'NONE', ( #78059, #60599, #98043, #161181 ) ) ;
#174678=CARTESIAN_POINT ( 'NONE',  ( -23.25000000000000000, 67.49222854868494892, -195.4187676019683693 ) ) ;
#174679=ORIENTED_EDGE ( 'NONE', *, *, #192729, .T. ) ;
#174702=EDGE_LOOP ( 'NONE', ( #161634, #125232, #197224, #107039 ) ) ;
#174715=CARTESIAN_POINT ( 'NONE',  ( -21.07928932188134041, 61.09751618602744827, -234.2940654522722639 ) ) ;
#174719=CARTESIAN_POINT ( 'NONE',  ( 20.94999999999999574, 70.53171716061257257, -228.4612385850772682 ) ) ;
#174802=VERTEX_POINT ( 'NONE', #39741 ) ;
#174811=CARTESIAN_POINT ( 'NONE',  ( 23.15000000000000213, 82.22731448072437388, -214.9453318841612486 ) ) ;
#174820=FACE_OUTER_BOUND ( 'NONE', #98574, .T. ) ;
#174842=CARTESIAN_POINT ( 'NONE',  ( -21.07933241753356413, 65.48460859884913532, -241.9386811690302181 ) ) ;
#174851=CARTESIAN_POINT ( 'NONE',  ( -20.64999999999999858, 63.46669608621377279, -222.0380013001639270 ) ) ;
#174854=CARTESIAN_POINT ( 'NONE',  ( 21.07954640115354294, 65.51085817920615284, -241.9464652145973957 ) ) ;
#174896=CARTESIAN_POINT ( 'NONE',  ( 20.94999999999999574, 60.83337574417771521, -225.3422414619149095 ) ) ;
#174902=ADVANCED_FACE ( 'NONE', ( #163512 ), #111993, .T. ) ;
#174926=EDGE_LOOP ( 'NONE', ( #196049, #128268 ) ) ;
#174931=CARTESIAN_POINT ( 'NONE',  ( -21.98333005346336577, 65.30108822512866595, -242.9721039335941555 ) ) ;
#174937=LINE ( 'NONE', #236134, #226512 ) ;
#174939=DIRECTION ( 'NONE',  ( -0.000000000000000000, 0.9651348961777157509, -0.2617529984165031243 ) ) ;
#174942=AXIS2_PLACEMENT_3D ( 'NONE', #183653, #123676, #83222 ) ;
#174976=ORIENTED_EDGE ( 'NONE', *, *, #203372, .F. ) ;
#175034=EDGE_CURVE ( 'NONE', #217417, #216635, #193396, .T. ) ;
#175090=CARTESIAN_POINT ( 'NONE',  ( -18.59999999999999787, 70.56573376625485139, -228.3808404818380779 ) ) ;
#175094=CARTESIAN_POINT ( 'NONE',  ( 18.58719872626881298, 87.01890647199485329, -199.4425935546263986 ) ) ;
#175097=ADVANCED_FACE ( 'NONE', ( #152972 ), #151685, .T. ) ;
#175113=LINE ( 'NONE', #231205, #35861 ) ;
#175146=ORIENTED_EDGE ( 'NONE', *, *, #13916, .T. ) ;
#175153=CARTESIAN_POINT ( 'NONE',  ( -23.25000000000000000, 76.00000000001126921, -203.5231074845248997 ) ) ;
#175189=AXIS2_PLACEMENT_3D ( 'NONE', #208190, #111638, #29569 ) ;
#175195=CIRCLE ( 'NONE', #91919, 0.1000000000000027117 ) ;
#175246=DIRECTION ( 'NONE',  ( 1.000000000000000000, -2.849773892568378313E-16, 7.728835255496647986E-17 ) ) ;
#175265=DIRECTION ( 'NONE',  ( 1.000000000000000000, -2.824170522722115425E-14, 2.841386468225606068E-14 ) ) ;
#175311=AXIS2_PLACEMENT_3D ( 'NONE', #73132, #92650, #104804 ) ;
#175312=CARTESIAN_POINT ( 'NONE',  ( 23.24999999999999289, 56.01362831242965967, -232.7091905853083347 ) ) ;
#175322=CARTESIAN_POINT ( 'NONE',  ( 21.12769345151713196, 60.09153065753968548, -221.2288501437841717 ) ) ;
#175336=DIRECTION ( 'NONE',  ( -1.000000000000000000, 0.000000000000000000, 0.000000000000000000 ) ) ;
#175344=AXIS2_PLACEMENT_3D ( 'NONE', #99433, #224531, #108445 ) ;
#175349=CYLINDRICAL_SURFACE ( 'NONE', #140072, 7.900000000000010125 ) ;
#175350=FACE_OUTER_BOUND ( 'NONE', #179652, .T. ) ;
#175366=DIRECTION ( 'NONE',  ( 0.000000000000000000, 0.2617529984165031243, 0.9651348961777157509 ) ) ;
#175378=EDGE_CURVE ( 'NONE', #128048, #251815, #33105, .T. ) ;
#175382=ORIENTED_EDGE ( 'NONE', *, *, #231957, .T. ) ;
#175389=ORIENTED_EDGE ( 'NONE', *, *, #154920, .F. ) ;
#175394=PLANE ( 'NONE',  #257225 ) ;
#175402=EDGE_CURVE ( 'NONE', #129497, #191603, #216192, .T. ) ;
#175413=DIRECTION ( 'NONE',  ( -1.000000000000000000, -0.000000000000000000, 0.000000000000000000 ) ) ;
#175423=CYLINDRICAL_SURFACE ( 'NONE', #204296, 0.5000000000000014433 ) ;
#175438=CARTESIAN_POINT ( 'NONE',  ( -18.59999999999999787, 61.45319073932094511, -212.2704122313080006 ) ) ;
#175439=EDGE_LOOP ( 'NONE', ( #124489, #81945, #206395, #253403 ) ) ;
#175468=DIRECTION ( 'NONE',  ( 3.469446951953492389E-14, 0.9228863568391486583, 0.3850724248244262182 ) ) ;
#175474=EDGE_CURVE ( 'NONE', #25862, #235134, #141719, .T. ) ;
#175478=CIRCLE ( 'NONE', #125408, 3.999999999999996447 ) ;
#175498=AXIS2_PLACEMENT_3D ( 'NONE', #153419, #75149, #169121 ) ;
#175528=LINE ( 'NONE', #60669, #13004 ) ;
#175531=FACE_OUTER_BOUND ( 'NONE', #117686, .T. ) ;
#175547=ORIENTED_EDGE ( 'NONE', *, *, #26231, .F. ) ;
#175561=DIRECTION ( 'NONE',  ( -1.000000000000000000, -0.000000000000000000, 0.000000000000000000 ) ) ;
#175579=EDGE_LOOP ( 'NONE', ( #198438, #97813, #135675, #158647 ) ) ;
#175607=VERTEX_POINT ( 'NONE', #222526 ) ;
#175612=CARTESIAN_POINT ( 'NONE',  ( 20.94999999999999574, 68.48451787451661232, -224.2224406095231757 ) ) ;
#175613=FACE_OUTER_BOUND ( 'NONE', #189459, .T. ) ;
#175649=ORIENTED_EDGE ( 'NONE', *, *, #73348, .F. ) ;
#175661=B_SPLINE_CURVE_WITH_KNOTS ( 'NONE', 3,
 ( #121947, #44977, #202758, #224873, #227449, #82770, #124519, #46244, #244446, #162370 ),
 .UNSPECIFIED., .F., .F.,
 ( 4, 2, 2, 2, 4 ),
 ( 0.000000000000000000, 4.221631689684808797E-05, 8.443263379369617594E-05, 0.0001688652675874713902, 0.0003377305351750226319 ),
 .UNSPECIFIED. ) ;
#175677=LINE ( 'NONE', #119557, #16956 ) ;
#175678=VERTEX_POINT ( 'NONE', #153321 ) ;
#175706=EDGE_CURVE ( 'NONE', #6907, #16586, #7948, .T. ) ;
#175753=LINE ( 'NONE', #156196, #28687 ) ;
#175776=ORIENTED_EDGE ( 'NONE', *, *, #69972, .F. ) ;
#175800=ORIENTED_EDGE ( 'NONE', *, *, #52665, .F. ) ;
#175821=EDGE_LOOP ( 'NONE', ( #240441, #130328, #90812, #166931 ) ) ;
#175900=EDGE_LOOP ( 'NONE', ( #201628, #25172, #20190, #37, #144519 ) ) ;
#175926=EDGE_CURVE ( 'NONE', #211251, #4726, #20792, .T. ) ;
#175941=ORIENTED_EDGE ( 'NONE', *, *, #235077, .F. ) ;
#176003=VERTEX_POINT ( 'NONE', #250787 ) ;
#176007=DIRECTION ( 'NONE',  ( 0.000000000000000000, 0.2617529984164955192, 0.9651348961777178603 ) ) ;
#176022=CARTESIAN_POINT ( 'NONE',  ( -20.54999999999999716, 70.12557831835937350, -215.6322690948981915 ) ) ;
#176035=DIRECTION ( 'NONE',  ( 0.000000000000000000, 0.9651348961777157509, -0.2617529984165031243 ) ) ;
#176050=ORIENTED_EDGE ( 'NONE', *, *, #148917, .T. ) ;
#176056=CARTESIAN_POINT ( 'NONE',  ( -18.50000000000000000, 70.22659352830977753, -197.9852579278363578 ) ) ;
#176058=ORIENTED_EDGE ( 'NONE', *, *, #234538, .T. ) ;
#176069=AXIS2_PLACEMENT_3D ( 'NONE', #206452, #209023, #126921 ) ;
#176083=ORIENTED_EDGE ( 'NONE', *, *, #23373, .T. ) ;
#176088=DIRECTION ( 'NONE',  ( 0.000000000000000000, 0.2617529984165035684, 0.9651348961777156399 ) ) ;
#176099=AXIS2_PLACEMENT_3D ( 'NONE', #165197, #204305, #141767 ) ;
#176107=CARTESIAN_POINT ( 'NONE',  ( -18.59999999999999787, 61.57587952878036930, -212.2000740415318774 ) ) ;
#176136=VERTEX_POINT ( 'NONE', #38184 ) ;
#176144=DIRECTION ( 'NONE',  ( 0.000000000000000000, 0.2617529984165174461, 0.9651348961777118651 ) ) ;
#176158=CARTESIAN_POINT ( 'NONE',  ( -18.59999999999999787, 68.48451787451661232, -224.2224406095231757 ) ) ;
#176165=FACE_OUTER_BOUND ( 'NONE', #162813, .T. ) ;
#176171=CARTESIAN_POINT ( 'NONE',  ( 21.05000000000000071, 78.47509609352879068, -238.9045489380306435 ) ) ;
#176184=DIRECTION ( 'NONE',  ( 0.000000000000000000, 0.2617529984164915779, 0.9651348961777189706 ) ) ;
#176199=DIRECTION ( 'NONE',  ( -0.000000000000000000, 0.7106264324241465813, -0.7035695228903323661 ) ) ;
#176265=CARTESIAN_POINT ( 'NONE',  ( 23.14999999999998792, 55.98745301258801987, -232.8057040749261262 ) ) ;
#176268=CARTESIAN_POINT ( 'NONE',  ( -23.15000000000000213, 76.00000000001126921, -203.5231074845248997 ) ) ;
#176272=CARTESIAN_POINT ( 'NONE',  ( -21.05000000000000071, 67.23127455305841238, -235.8551265064783991 ) ) ;
#176299=ORIENTED_EDGE ( 'NONE', *, *, #82869, .T. ) ;
#176335=AXIS2_PLACEMENT_3D ( 'NONE', #236718, #58073, #118068 ) ;
#176365=EDGE_LOOP ( 'NONE', ( #106915, #207199, #215348, #84948, #248800 ) ) ;
#176384=CARTESIAN_POINT ( 'NONE',  ( 20.94999999999999929, 63.62814136979439184, -224.4990371885399441 ) ) ;
#176414=AXIS2_PLACEMENT_3D ( 'NONE', #85067, #207641, #6851 ) ;
#176419=AXIS2_PLACEMENT_3D ( 'NONE', #6898, #70761, #68161 ) ;
#176445=CIRCLE ( 'NONE', #138961, 0.5000000000000014433 ) ;
#176470=EDGE_CURVE ( 'NONE', #194529, #143771, #4186, .T. ) ;
#176488=ORIENTED_EDGE ( 'NONE', *, *, #120753, .T. ) ;
#176489=CIRCLE ( 'NONE', #238842, 11.74999999999999822 ) ;
#176498=FACE_OUTER_BOUND ( 'NONE', #213034, .T. ) ;
#176520=ADVANCED_FACE ( 'NONE', ( #71082 ), #125648, .F. ) ;
#176534=CARTESIAN_POINT ( 'NONE',  ( 20.94999999999999929, 67.23127455305841238, -235.8551265064783991 ) ) ;
#176612=CARTESIAN_POINT ( 'NONE',  ( -21.05000000000000071, 68.49522935589659767, -224.1230159437372436 ) ) ;
#176633=CIRCLE ( 'NONE', #55771, 0.1000000000000124678 ) ;
#176640=CARTESIAN_POINT ( 'NONE',  ( 23.15000000000000213, 79.08634564045904369, -228.8189404293001132 ) ) ;
#176645=CARTESIAN_POINT ( 'NONE',  ( -23.25000000000000000, 76.00000000001126921, -203.5231074845248997 ) ) ;
#176656=CARTESIAN_POINT ( 'NONE',  ( 20.94999999999999574, 79.03126467873600802, -235.8703919547671717 ) ) ;
#176667=EDGE_CURVE ( 'NONE', #116965, #160646, #84833, .T. ) ;
#176677=AXIS2_PLACEMENT_3D ( 'NONE', #230831, #131708, #211245 ) ;
#176680=ORIENTED_EDGE ( 'NONE', *, *, #33820, .F. ) ;
#176685=EDGE_CURVE ( 'NONE', #47050, #163993, #225578, .T. ) ;
#176690=CARTESIAN_POINT ( 'NONE',  ( 20.94983749550516450, 67.49429988484537546, -195.5441618131978601 ) ) ;
#176697=CARTESIAN_POINT ( 'NONE',  ( -18.52186455169006152, 78.22055546782374336, -231.5567229729791165 ) ) ;
#176700=ORIENTED_EDGE ( 'NONE', *, *, #177141, .F. ) ;
#176701=ORIENTED_EDGE ( 'NONE', *, *, #129655, .T. ) ;
#176708=CARTESIAN_POINT ( 'NONE',  ( -23.25000000000000000, 78.00142589229885459, -228.9845759368473637 ) ) ;
#176726=VECTOR ( 'NONE', #252477, 1000.000000000000000 ) ;
#176745=DIRECTION ( 'NONE',  ( -1.000000000000000000, 0.000000000000000000, 0.000000000000000000 ) ) ;
#176748=AXIS2_PLACEMENT_3D ( 'NONE', #36814, #233707, #74664 ) ;
#176752=AXIS2_PLACEMENT_3D ( 'NONE', #50707, #155961, #91148 ) ;
#176754=AXIS2_PLACEMENT_3D ( 'NONE', #195223, #98612, #96071 ) ;
#176771=VERTEX_POINT ( 'NONE', #6613 ) ;
#176811=EDGE_LOOP ( 'NONE', ( #172623, #124765, #222712, #7155 ) ) ;
#176824=CARTESIAN_POINT ( 'NONE',  ( 22.47110162079220785, 64.15407550225560840, -247.0913484080595026 ) ) ;
#176826=CARTESIAN_POINT ( 'NONE',  ( -20.94999999999999929, 68.48451787451661232, -224.2224406095231757 ) ) ;
#176887=DIRECTION ( 'NONE',  ( -1.000000000000000000, -0.000000000000000000, 0.000000000000000000 ) ) ;
#176899=DIRECTION ( 'NONE',  ( 1.000000000000000000, 0.000000000000000000, -0.000000000000000000 ) ) ;
#176970=EDGE_LOOP ( 'NONE', ( #210931, #190246, #222742, #25114 ) ) ;
#176989=EDGE_LOOP ( 'NONE', ( #210805, #250460, #30741, #128942 ) ) ;
#176993=LINE ( 'NONE', #24324, #55178 ) ;
#177000=CARTESIAN_POINT ( 'NONE',  ( -23.15000000000000213, 55.89093952297024970, -232.7795287750844579 ) ) ;
#177018=FACE_OUTER_BOUND ( 'NONE', #238952, .T. ) ;
#177019=CIRCLE ( 'NONE', #222759, 12.87500000000000178 ) ;
#177022=VERTEX_POINT ( 'NONE', #62444 ) ;
#177051=AXIS2_PLACEMENT_3D ( 'NONE', #24186, #238070, #257579 ) ;
#177062=EDGE_LOOP ( 'NONE', ( #202686, #234166, #138028, #100931 ) ) ;
#177080=DIRECTION ( 'NONE',  ( 0.000000000000000000, 0.2617529984165152257, 0.9651348961777124202 ) ) ;
#177085=CARTESIAN_POINT ( 'NONE',  ( -20.85000000000000142, 80.78317333349157536, -192.9003134612049166 ) ) ;
#177090=EDGE_LOOP ( 'NONE', ( #123850, #100435, #117537 ) ) ;
#177103=CARTESIAN_POINT ( 'NONE',  ( 20.94999999999998508, 62.88396779178383156, -206.9948552354528886 ) ) ;
#177109=DIRECTION ( 'NONE',  ( 0.000000000000000000, 0.9651348961776958779, -0.2617529984165761214 ) ) ;
#177113=ORIENTED_EDGE ( 'NONE', *, *, #52191, .T. ) ;
#177116=CARTESIAN_POINT ( 'NONE',  ( -18.59999999999999787, 57.82359945636609666, -226.0354702357591350 ) ) ;
#177136=CARTESIAN_POINT ( 'NONE',  ( 20.95512820512820440, 62.54007867304706281, -212.5651857150171224 ) ) ;
#177141=EDGE_CURVE ( 'NONE', #123153, #211510, #66294, .T. ) ;
#177142=CARTESIAN_POINT ( 'NONE',  ( -18.50000000000000711, 57.72708596674832648, -226.0092949359174952 ) ) ;
#177177=DIRECTION ( 'NONE',  ( -1.000000000000000000, -0.000000000000000000, -0.000000000000000000 ) ) ;
#177228=CARTESIAN_POINT ( 'NONE',  ( 19.58285714285715073, 60.73471314953822997, -225.3683569544359671 ) ) ;
#177238=ADVANCED_FACE ( 'NONE', ( #10173 ), #248785, .F. ) ;
#177260=CARTESIAN_POINT ( 'NONE',  ( -22.48660254037844552, 55.87785187304944401, -232.8277855198933253 ) ) ;
#177268=ORIENTED_EDGE ( 'NONE', *, *, #70279, .F. ) ;
#177270=AXIS2_PLACEMENT_3D ( 'NONE', #243796, #82124, #63878 ) ;
#177302=FACE_OUTER_BOUND ( 'NONE', #194465, .T. ) ;
#177328=CARTESIAN_POINT ( 'NONE',  ( -21.05000000000000071, 86.58125133469155799, -209.3975964148341973 ) ) ;
#177400=CARTESIAN_POINT ( 'NONE',  ( 21.04999999999978755, 65.55631946098660023, -241.9747880272848022 ) ) ;
#177406=DIRECTION ( 'NONE',  ( 0.000000000000000000, -0.9651348961780373825, 0.2617529984153167399 ) ) ;
#177407=ORIENTED_EDGE ( 'NONE', *, *, #212202, .F. ) ;
#177408=DIRECTION ( 'NONE',  ( 1.000000000000000000, 0.000000000000000000, 0.000000000000000000 ) ) ;
#177443=DIRECTION ( 'NONE',  ( 0.000000000000000000, 0.9651348961777157509, -0.2617529984165031243 ) ) ;
#177445=PLANE ( 'NONE',  #193322 ) ;
#177449=ORIENTED_EDGE ( 'NONE', *, *, #17876, .T. ) ;
#177456=DIRECTION ( 'NONE',  ( 0.000000000000000000, 0.2617529984165031243, 0.9651348961777157509 ) ) ;
#177468=AXIS2_PLACEMENT_3D ( 'NONE', #186502, #249052, #152536 ) ;
#177505=EDGE_CURVE ( 'NONE', #120691, #154671, #227608, .T. ) ;
#177512=EDGE_CURVE ( 'NONE', #232566, #219655, #223749, .T. ) ;
#177534=ORIENTED_EDGE ( 'NONE', *, *, #252009, .T. ) ;
#177540=CARTESIAN_POINT ( 'NONE',  ( 21.12802099929860944, 61.96285729424215560, -221.7356349687620138 ) ) ;
#177586=VERTEX_POINT ( 'NONE', #150651 ) ;
#177590=CARTESIAN_POINT ( 'NONE',  ( 18.59999999999999076, 63.62814136979439184, -224.4990371885399441 ) ) ;
#177595=DIRECTION ( 'NONE',  ( 1.000000000000000000, 0.000000000000000000, -0.000000000000000000 ) ) ;
#177613=CARTESIAN_POINT ( 'NONE',  ( -21.44999999999999929, 63.37018259659601682, -222.0118260003222872 ) ) ;
#177622=LINE ( 'NONE', #257069, #90383 ) ;
#177650=CARTESIAN_POINT ( 'NONE',  ( -23.25000000000000000, 78.57160958314655375, -238.9307242378722833 ) ) ;
#177651=VERTEX_POINT ( 'NONE', #50243 ) ;
#177720=FACE_OUTER_BOUND ( 'NONE', #223616, .T. ) ;
#177725=VECTOR ( 'NONE', #4616, 1000.000000000000000 ) ;
#177736=VECTOR ( 'NONE', #252969, 1000.000000000000114 ) ;
#177745=CYLINDRICAL_SURFACE ( 'NONE', #221944, 11.75000000000000178 ) ;
#177769=EDGE_CURVE ( 'NONE', #193142, #88353, #173526, .T. ) ;
#177774=VERTEX_POINT ( 'NONE', #38404 ) ;
#177813=DIRECTION ( 'NONE',  ( 0.000000000000000000, 0.2617529984165030688, 0.9651348961777157509 ) ) ;
#177823=ORIENTED_EDGE ( 'NONE', *, *, #96295, .F. ) ;
#177828=EDGE_LOOP ( 'NONE', ( #43007, #189005, #21176, #236822 ) ) ;
#177858=CARTESIAN_POINT ( 'NONE',  ( -18.59999999999999787, 72.05339752741123505, -225.0867394276846483 ) ) ;
#177862=VECTOR ( 'NONE', #208630, 1000.000000000000000 ) ;
#177883=ORIENTED_EDGE ( 'NONE', *, *, #214757, .T. ) ;
#177885=DIRECTION ( 'NONE',  ( 1.000000000000000000, 0.000000000000000000, 0.000000000000000000 ) ) ;
#177890=LINE ( 'NONE', #256063, #41721 ) ;
#177902=ORIENTED_EDGE ( 'NONE', *, *, #209585, .F. ) ;
#177922=CARTESIAN_POINT ( 'NONE',  ( 21.08479644141221954, 65.51392872348355922, -241.9636179317403162 ) ) ;
#177927=CARTESIAN_POINT ( 'NONE',  ( -20.85000000000000142, 80.82423061532404063, -192.8091306798888525 ) ) ;
#177932=CARTESIAN_POINT ( 'NONE',  ( -18.59999999999999787, 79.16909458115064524, -196.2854372848902926 ) ) ;
#177957=ORIENTED_EDGE ( 'NONE', *, *, #12277, .F. ) ;
#177969=CARTESIAN_POINT ( 'NONE',  ( 20.86777300164945004, 67.49225400653517681, -195.4205142095401868 ) ) ;
#177977=CARTESIAN_POINT ( 'NONE',  ( -18.49346865148359598, 78.22586126723579980, -231.3921957456194889 ) ) ;
#177991=VECTOR ( 'NONE', #248970, 1000.000000000000000 ) ;
#178002=DIRECTION ( 'NONE',  ( 0.000000000000000000, 0.9651348961777157509, -0.2617529984165031243 ) ) ;
#178010=VERTEX_POINT ( 'NONE', #34282 ) ;
#178022=DIRECTION ( 'NONE',  ( 0.000000000000000000, -0.2617529984165031243, -0.9651348961777157509 ) ) ;
#178028=ORIENTED_EDGE ( 'NONE', *, *, #182613, .F. ) ;
#178036=ORIENTED_EDGE ( 'NONE', *, *, #221862, .T. ) ;
#178055=CARTESIAN_POINT ( 'NONE',  ( -18.59999999999999787, 57.82359945636609666, -226.0354702357591350 ) ) ;
#178061=CARTESIAN_POINT ( 'NONE',  ( 23.15000000000000213, 81.77808381374872226, -227.1078217596952697 ) ) ;
#178066=DIRECTION ( 'NONE',  ( -0.000000000000000000, -0.9651348961777157509, 0.2617529984165031243 ) ) ;
#178084=EDGE_CURVE ( 'NONE', #135481, #202597, #52836, .T. ) ;
#178088=DIRECTION ( 'NONE',  ( -0.000000000000000000, 0.6922311945860614157, 0.7216758089626911232 ) ) ;
#178092=FACE_OUTER_BOUND ( 'NONE', #171677, .T. ) ;
#178110=CARTESIAN_POINT ( 'NONE',  ( 22.44352723754029810, 64.17297141203522415, -247.0962508001766480 ) ) ;
#178112=DIRECTION ( 'NONE',  ( 0.000000000000000000, -0.2617529984165031243, -0.9651348961777157509 ) ) ;
#178113=EDGE_CURVE ( 'NONE', #76073, #241619, #231937, .T. ) ;
#178115=DIRECTION ( 'NONE',  ( 0.000000000000000000, -0.5041370733442398500, -0.8636236514129894681 ) ) ;
#178125=VECTOR ( 'NONE', #13590, 1000.000000000000000 ) ;
#178141=ORIENTED_EDGE ( 'NONE', *, *, #5902, .T. ) ;
#178174=VERTEX_POINT ( 'NONE', #175090 ) ;
#178202=CARTESIAN_POINT ( 'NONE',  ( -20.64999999999999858, 66.33592547490526670, -222.9197737850312251 ) ) ;
#178235=AXIS2_PLACEMENT_3D ( 'NONE', #59448, #75234, #77750 ) ;
#178237=VERTEX_POINT ( 'NONE', #110583 ) ;
#178259=CARTESIAN_POINT ( 'NONE',  ( -21.05000000000000071, 64.23744694032046709, -224.5446448091673233 ) ) ;
#178293=CARTESIAN_POINT ( 'NONE',  ( 21.08489247129321242, 61.89576995986235630, -221.6119524385055399 ) ) ;
#178316=ADVANCED_FACE ( 'NONE', ( #152313 ), #127876, .F. ) ;
#178375=LINE ( 'NONE', #40154, #181024 ) ;
#178386=LINE ( 'NONE', #222589, #69294 ) ;
#178433=DIRECTION ( 'NONE',  ( 0.000000000000000000, -0.9651348961777157509, 0.2617529984165031243 ) ) ;
#178437=ADVANCED_FACE ( 'NONE', ( #79140 ), #61409, .F. ) ;
#178460=AXIS2_PLACEMENT_3D ( 'NONE', #111548, #133674, #15030 ) ;
#178482=CARTESIAN_POINT ( 'NONE',  ( 21.05000000000000071, 67.92720994251783395, -214.1870976236629929 ) ) ;
#178520=ADVANCED_FACE ( 'NONE', ( #161284 ), #201669, .T. ) ;
#178524=DIRECTION ( 'NONE',  ( 1.000000000000000000, -3.151514657663852580E-16, 8.547182517843351137E-17 ) ) ;
#178532=DIRECTION ( 'NONE',  ( 0.7071067811865475727, 0.6824534298470373850, -0.1850873201762210096 ) ) ;
#178568=DIRECTION ( 'NONE',  ( 1.000000000000000000, 0.000000000000000000, 0.000000000000000000 ) ) ;
#178582=CARTESIAN_POINT ( 'NONE',  ( 23.14999999999999858, 76.00000000001126921, -203.5231074845248997 ) ) ;
#178592=DIRECTION ( 'NONE',  ( 0.000000000000000000, 0.2617529984164915779, 0.9651348961777187485 ) ) ;
#178608=FACE_OUTER_BOUND ( 'NONE', #123923, .T. ) ;
#178611=EDGE_CURVE ( 'NONE', #58070, #45271, #53019, .T. ) ;
#178636=EDGE_LOOP ( 'NONE', ( #246682, #18419 ) ) ;
#178646=CIRCLE ( 'NONE', #91126, 2.000000000000009326 ) ;
#178649=CARTESIAN_POINT ( 'NONE',  ( -21.05000000000000071, 70.44746257310249860, -228.4383880063670347 ) ) ;
#178654=DIRECTION ( 'NONE',  ( -1.000000000000000000, 0.000000000000000000, 0.000000000000000000 ) ) ;
#178657=ORIENTED_EDGE ( 'NONE', *, *, #218, .F. ) ;
#178660=FACE_OUTER_BOUND ( 'NONE', #168012, .T. ) ;
#178664=DIRECTION ( 'NONE',  ( 1.000000000000000000, 0.000000000000000000, 0.000000000000000000 ) ) ;
#178675=CIRCLE ( 'NONE', #232825, 0.09999999999999939493 ) ;
#178680=LINE ( 'NONE', #216474, #221281 ) ;
#178716=CIRCLE ( 'NONE', #149657, 0.1000000000000124678 ) ;
#178728=CARTESIAN_POINT ( 'NONE',  ( 20.95512820512820440, 60.90483797576755620, -225.2715357783924333 ) ) ;
#178744=ORIENTED_EDGE ( 'NONE', *, *, #192496, .F. ) ;
#178749=DIRECTION ( 'NONE',  ( 2.952720810173289112E-16, 0.9651348961777157509, -0.2617529984165031243 ) ) ;
#178829=ORIENTED_EDGE ( 'NONE', *, *, #24457, .F. ) ;
#178853=DIRECTION ( 'NONE',  ( 0.000000000000000000, 0.2617529984165152257, 0.9651348961777124202 ) ) ;
#178859=EDGE_CURVE ( 'NONE', #110910, #88904, #182182, .T. ) ;
#178864=ORIENTED_EDGE ( 'NONE', *, *, #234766, .F. ) ;
#178869=ORIENTED_EDGE ( 'NONE', *, *, #141710, .T. ) ;
#178900=LINE ( 'NONE', #121487, #245340 ) ;
#178903=CARTESIAN_POINT ( 'NONE',  ( 21.05000000000000071, 76.00000000001126921, -203.5231074845248997 ) ) ;
#178935=ORIENTED_EDGE ( 'NONE', *, *, #153507, .T. ) ;
#178964=EDGE_CURVE ( 'NONE', #73870, #695, #257174, .T. ) ;
#178992=CARTESIAN_POINT ( 'NONE',  ( 23.25000000000000000, 79.08634564045904369, -228.8189404293001132 ) ) ;
#179005=CARTESIAN_POINT ( 'NONE',  ( 19.99999999738033551, 62.35288080320960802, -208.9530776385553850 ) ) ;
#179024=EDGE_CURVE ( 'NONE', #110447, #19933, #86498, .T. ) ;
#179058=ORIENTED_EDGE ( 'NONE', *, *, #226798, .F. ) ;
#179070=EDGE_CURVE ( 'NONE', #91550, #239682, #128238, .T. ) ;
#179094=ORIENTED_EDGE ( 'NONE', *, *, #29765, .F. ) ;
#179159=CARTESIAN_POINT ( 'NONE',  ( 21.30000000000002558, 66.17117490947157421, -239.7639228359981303 ) ) ;
#179169=AXIS2_PLACEMENT_3D ( 'NONE', #251508, #149876, #169459 ) ;
#179178=CARTESIAN_POINT ( 'NONE',  ( -20.94999999999999929, 67.49463558145296815, -195.5618716440587548 ) ) ;
#179181=DIRECTION ( 'NONE',  ( 0.000000000000000000, -0.2617529984165030132, -0.9651348961777157509 ) ) ;
#179214=DIRECTION ( 'NONE',  ( -1.000000000000000000, 0.000000000000000000, 0.000000000000000000 ) ) ;
#179237=EDGE_CURVE ( 'NONE', #84318, #230992, #120075, .T. ) ;
#179258=DIRECTION ( 'NONE',  ( -0.8660254037844724584, -0.1308764992082773471, -0.4825674480887902629 ) ) ;
#179277=AXIS2_PLACEMENT_3D ( 'NONE', #146290, #206275, #107163 ) ;
#179284=FACE_OUTER_BOUND ( 'NONE', #240076, .T. ) ;
#179304=CYLINDRICAL_SURFACE ( 'NONE', #132245, 0.1000000000000124678 ) ;
#179322=DIRECTION ( 'NONE',  ( -1.000000000000000000, -0.000000000000000000, -0.000000000000000000 ) ) ;
#179331=EDGE_LOOP ( 'NONE', ( #2080, #230500, #138802, #8865 ) ) ;
#179365=DIRECTION ( 'NONE',  ( 1.000000000000000000, 0.000000000000000000, 0.000000000000000000 ) ) ;
#179372=CARTESIAN_POINT ( 'NONE',  ( -18.59999999999999787, 70.37092869010230345, -198.1237041667535550 ) ) ;
#179424=VECTOR ( 'NONE', #161696, 1000.000000000000000 ) ;
#179425=AXIS2_PLACEMENT_3D ( 'NONE', #136994, #239962, #61317 ) ;
#179453=ADVANCED_FACE ( 'NONE', ( #142370 ), #69988, .T. ) ;
#179468=DIRECTION ( 'NONE',  ( 0.000000000000000000, -0.2617529984165031243, -0.9651348961777157509 ) ) ;
#179489=DIRECTION ( 'NONE',  ( 0.000000000000000000, 0.2617529984165035128, 0.9651348961777155289 ) ) ;
#179491=AXIS2_PLACEMENT_3D ( 'NONE', #257276, #117815, #17432 ) ;
#179571=DIRECTION ( 'NONE',  ( 0.000000000000000000, -0.9651348961777157509, 0.2617529984165031243 ) ) ;
#179627=EDGE_CURVE ( 'NONE', #77258, #163063, #170155, .T. ) ;
#179643=CARTESIAN_POINT ( 'NONE',  ( -20.85000000000000142, 64.75617845954087670, -200.4736850529726269 ) ) ;
#179645=CARTESIAN_POINT ( 'NONE',  ( 18.41815437325352534, 86.89613897263180320, -199.6357246881775040 ) ) ;
#179646=VERTEX_POINT ( 'NONE', #85761 ) ;
#179652=EDGE_LOOP ( 'NONE', ( #241234, #23535, #218558, #41616 ) ) ;
#179655=DIRECTION ( 'NONE',  ( 1.000000000000000000, 2.379049338482476317E-14, 0.000000000000000000 ) ) ;
#179657=DIRECTION ( 'NONE',  ( -1.000000000000000000, 0.000000000000000000, 0.000000000000000000 ) ) ;
#179662=DIRECTION ( 'NONE',  ( 0.000000000000000000, 0.9651348961777157509, -0.2617529984165031243 ) ) ;
#179687=EDGE_LOOP ( 'NONE', ( #144744, #122364 ) ) ;
#179694=EDGE_CURVE ( 'NONE', #11008, #70163, #207040, .T. ) ;
#179708=CARTESIAN_POINT ( 'NONE',  ( 21.07094088545304444, 61.10557489434067691, -234.2962495489933872 ) ) ;
#179737=ORIENTED_EDGE ( 'NONE', *, *, #52830, .F. ) ;
#179783=DIRECTION ( 'NONE',  ( -0.000000000000000000, -0.3896596508880098009, -0.9209589331071360574 ) ) ;
#179786=ORIENTED_EDGE ( 'NONE', *, *, #152786, .T. ) ;
#179790=CARTESIAN_POINT ( 'NONE',  ( -23.25000000000000000, 76.00000000001126921, -203.5231074845248997 ) ) ;
#179792=ORIENTED_EDGE ( 'NONE', *, *, #244532, .T. ) ;
#179809=CIRCLE ( 'NONE', #71483, 0.1000000000000040579 ) ;
#179811=CARTESIAN_POINT ( 'NONE',  ( -22.50014994443974103, 55.86946353937208443, -232.8597856945306432 ) ) ;
#179819=AXIS2_PLACEMENT_3D ( 'NONE', #69934, #206853, #169049 ) ;
#179886=DIRECTION ( 'NONE',  ( 0.000000000000000000, 0.2617529984165031243, 0.9651348961777157509 ) ) ;
#179941=ORIENTED_EDGE ( 'NONE', *, *, #256061, .F. ) ;
#179992=DIRECTION ( 'NONE',  ( 0.000000000000000000, 0.2617529984165031243, 0.9651348961777157509 ) ) ;
#179994=DIRECTION ( 'NONE',  ( -1.000000000000000000, 2.849773892568378313E-16, -7.728835255496647986E-17 ) ) ;
#180014=DIRECTION ( 'NONE',  ( -1.000000000000000000, -0.000000000000000000, 0.000000000000000000 ) ) ;
#180027=ORIENTED_EDGE ( 'NONE', *, *, #161371, .F. ) ;
#180032=LINE ( 'NONE', #138296, #250199 ) ;
#180044=CARTESIAN_POINT ( 'NONE',  ( 18.60000000000000142, 78.12133356376091342, -231.3112718935514636 ) ) ;
#180045=ORIENTED_EDGE ( 'NONE', *, *, #1111, .T. ) ;
#180057=DIRECTION ( 'NONE',  ( 0.000000000000000000, -0.9651348961777028723, 0.2617529984165503087 ) ) ;
#180078=CARTESIAN_POINT ( 'NONE',  ( 21.14999999999999858, 61.95748721176698126, -221.7323031544521541 ) ) ;
#180150=CARTESIAN_POINT ( 'NONE',  ( -20.54999999999999716, 76.49733069700262433, -201.6893511817872309 ) ) ;
#180191=DIRECTION ( 'NONE',  ( -1.000000000000000000, 2.849773892568378313E-16, -7.728835255496647986E-17 ) ) ;
#180204=CARTESIAN_POINT ( 'NONE',  ( 18.49999999999999289, 66.34920340998563404, -213.7018660128499334 ) ) ;
#180210=EDGE_CURVE ( 'NONE', #223586, #159037, #13377, .T. ) ;
#180224=AXIS2_PLACEMENT_3D ( 'NONE', #162275, #241784, #63135 ) ;
#180234=FACE_OUTER_BOUND ( 'NONE', #195217, .T. ) ;
#180268=EDGE_LOOP ( 'NONE', ( #93752, #119764, #53198, #129384 ) ) ;
#180273=VECTOR ( 'NONE', #35051, 1000.000000000000000 ) ;
#180303=DIRECTION ( 'NONE',  ( 0.000000000000000000, 0.2617529984164996826, 0.9651348961777166391 ) ) ;
#180335=AXIS2_PLACEMENT_3D ( 'NONE', #57654, #135904, #216739 ) ;
#180349=DIRECTION ( 'NONE',  ( 0.000000000000000000, -0.9651348961777157509, 0.2617529984165031243 ) ) ;
#180378=ADVANCED_FACE ( 'NONE', ( #229818 ), #120609, .T. ) ;
#180410=EDGE_CURVE ( 'NONE', #162073, #48041, #55015, .T. ) ;
#180422=CARTESIAN_POINT ( 'NONE',  ( -22.46246831459151494, 64.16073937605142419, -247.0930817548480150 ) ) ;
#180424=AXIS2_PLACEMENT_3D ( 'NONE', #199359, #183641, #241052 ) ;
#180445=DIRECTION ( 'NONE',  ( 0.000000000000000000, 0.2617529984165152257, 0.9651348961777124202 ) ) ;
#180461=EDGE_CURVE ( 'NONE', #234918, #163063, #107232, .T. ) ;
#180472=CARTESIAN_POINT ( 'NONE',  ( 21.05000000000000071, 82.09643798151613225, -215.4278993322501208 ) ) ;
#180479=DIRECTION ( 'NONE',  ( 0.000000000000000000, -0.2558827019434435912, 0.9667078373770033872 ) ) ;
#180497=CIRCLE ( 'NONE', #14099, 2.000000000000013323 ) ;
#180536=CARTESIAN_POINT ( 'NONE',  ( 23.14999999999999858, 65.72352950616313194, -223.1694128933794730 ) ) ;
#180540=FACE_OUTER_BOUND ( 'NONE', #202879, .T. ) ;
#180542=DIRECTION ( 'NONE',  ( 1.000000000000000000, 0.000000000000000000, 0.000000000000000000 ) ) ;
#180549=EDGE_CURVE ( 'NONE', #204625, #252057, #223094, .T. ) ;
#180550=CARTESIAN_POINT ( 'NONE',  ( -21.05000000000000071, 64.27847795353595473, -247.1247091181747066 ) ) ;
#180560=ORIENTED_EDGE ( 'NONE', *, *, #165170, .T. ) ;
#180562=DIRECTION ( 'NONE',  ( -1.000000000000000000, -0.000000000000000000, 0.000000000000000000 ) ) ;
#180610=ORIENTED_EDGE ( 'NONE', *, *, #91803, .F. ) ;
#180677=EDGE_LOOP ( 'NONE', ( #159283, #194408, #104286, #205537 ) ) ;
#180687=EDGE_LOOP ( 'NONE', ( #89245, #116590, #129097, #27416 ) ) ;
#180706=DIRECTION ( 'NONE',  ( 1.000000000000000000, 0.000000000000000000, 0.000000000000000000 ) ) ;
#180725=ORIENTED_EDGE ( 'NONE', *, *, #83754, .F. ) ;
#180736=VERTEX_POINT ( 'NONE', #18180 ) ;
#180789=CIRCLE ( 'NONE', #97542, 4.299999999999945643 ) ;
#180803=DIRECTION ( 'NONE',  ( 0.000000000000000000, -0.2617529984165034573, -0.9651348961777156399 ) ) ;
#180819=EDGE_LOOP ( 'NONE', ( #84493, #108800, #141220, #138852 ) ) ;
#180838=DIRECTION ( 'NONE',  ( 0.000000000000000000, 0.3848449534832868446, 0.9229812358755983270 ) ) ;
#180862=CARTESIAN_POINT ( 'NONE',  ( -18.59999999999999787, 80.78317333349157536, -192.9003134612049166 ) ) ;
#180863=TOROIDAL_SURFACE ( 'NONE', #101716, 0.2000000000000000111, 0.1000000000000000056 ) ;
#180865=CARTESIAN_POINT ( 'NONE',  ( 23.14999999999999858, 76.00000000001126921, -203.5231074845248997 ) ) ;
#180888=ORIENTED_EDGE ( 'NONE', *, *, #50248, .F. ) ;
#180926=CARTESIAN_POINT ( 'NONE',  ( 21.00000000000000000, 61.05385884576949707, -221.3836188041226762 ) ) ;
#180927=AXIS2_PLACEMENT_3D ( 'NONE', #190910, #171363, #93053 ) ;
#180985=VERTEX_POINT ( 'NONE', #7602 ) ;
#181022=VERTEX_POINT ( 'NONE', #147097 ) ;
#181024=VECTOR ( 'NONE', #195371, 1000.000000000000000 ) ;
#181059=ORIENTED_EDGE ( 'NONE', *, *, #5359, .T. ) ;
#181067=VECTOR ( 'NONE', #224462, 1000.000000000000114 ) ;
#181080=DIRECTION ( 'NONE',  ( 0.000000000000000000, 0.9651348961777157509, -0.2617529984165031243 ) ) ;
#181115=CARTESIAN_POINT ( 'NONE',  ( 21.04999999999999716, 59.07346110239164716, -225.8107669182993789 ) ) ;
#181141=EDGE_CURVE ( 'NONE', #160519, #59315, #21024, .T. ) ;
#181149=ORIENTED_EDGE ( 'NONE', *, *, #229601, .F. ) ;
#181156=EDGE_LOOP ( 'NONE', ( #181059, #75180, #136744, #129738 ) ) ;
#181180=AXIS2_PLACEMENT_3D ( 'NONE', #84091, #86690, #223639 ) ;
#181195=AXIS2_PLACEMENT_3D ( 'NONE', #100077, #179662, #80507 ) ;
#181210=CARTESIAN_POINT ( 'NONE',  ( -20.64999999999999858, 68.63171270270233038, -223.0506438513196770 ) ) ;
#181250=FACE_OUTER_BOUND ( 'NONE', #94072, .T. ) ;
#181289=CIRCLE ( 'NONE', #77199, 0.09999999999999939493 ) ;
#181310=AXIS2_PLACEMENT_3D ( 'NONE', #98232, #95695, #215641 ) ;
#181321=FACE_OUTER_BOUND ( 'NONE', #37210, .T. ) ;
#181327=CIRCLE ( 'NONE', #135318, 0.1000000000000106498 ) ;
#181337=CARTESIAN_POINT ( 'NONE',  ( -23.15000000000000213, 68.56901367119438362, -214.3038979092079046 ) ) ;
#181340=CARTESIAN_POINT ( 'NONE',  ( 18.46921299892754220, 78.23786519927757865, -231.6012438402944724 ) ) ;
#181354=FACE_OUTER_BOUND ( 'NONE', #31777, .T. ) ;
#181412=FACE_OUTER_BOUND ( 'NONE', #240265, .T. ) ;
#181413=FACE_OUTER_BOUND ( 'NONE', #243936, .T. ) ;
#181429=DIRECTION ( 'NONE',  ( 0.000000000000000000, 0.2617529984165033463, 0.9651348961777157509 ) ) ;
#181475=VERTEX_POINT ( 'NONE', #159337 ) ;
#181480=DIRECTION ( 'NONE',  ( 0.000000000000000000, -0.9651348961776677893, 0.2617529984166795387 ) ) ;
#181523=DIRECTION ( 'NONE',  ( 1.000000000000000000, -2.849773892568378313E-16, 7.728835255496647986E-17 ) ) ;
#181538=CARTESIAN_POINT ( 'NONE',  ( -20.87155475150660777, 62.85241404162280077, -207.1112001314805582 ) ) ;
#181545=CARTESIAN_POINT ( 'NONE',  ( -21.05000000000000071, 65.60141603934033583, -241.9453590735340924 ) ) ;
#181555=ADVANCED_FACE ( 'NONE', ( #215434 ), #162095, .F. ) ;
#181563=CARTESIAN_POINT ( 'NONE',  ( 21.13461538461538325, 60.21941965847795331, -221.1573116214326546 ) ) ;
#181564=EDGE_CURVE ( 'NONE', #102375, #41172, #202297, .T. ) ;
#181581=CARTESIAN_POINT ( 'NONE',  ( 21.05000000000000071, 63.62814136979439184, -224.4990371885399441 ) ) ;
#181588=AXIS2_PLACEMENT_3D ( 'NONE', #208357, #169249, #188765 ) ;
#181598=CARTESIAN_POINT ( 'NONE',  ( -21.29999999999995808, 66.17117490947157421, -239.7639228359981303 ) ) ;
#181611=ORIENTED_EDGE ( 'NONE', *, *, #114243, .T. ) ;
#181639=EDGE_LOOP ( 'NONE', ( #142245, #127852, #82529, #193426 ) ) ;
#181666=VECTOR ( 'NONE', #215342, 1000.000000000000000 ) ;
#181672=DIRECTION ( 'NONE',  ( 0.000000000000000000, -0.9651348961777157509, 0.2617529984165032353 ) ) ;
#181709=ORIENTED_EDGE ( 'NONE', *, *, #254265, .F. ) ;
#181716=CIRCLE ( 'NONE', #115082, 3.999999999999996447 ) ;
#181740=DIRECTION ( 'NONE',  ( 0.000000000000000000, -0.2617529984165031243, -0.9651348961777157509 ) ) ;
#181747=TOROIDAL_SURFACE ( 'NONE', #69335, 0.6000000000000009770, 0.1000000000000000056 ) ;
#181761=CYLINDRICAL_SURFACE ( 'NONE', #198356, 0.1000000000000066530 ) ;
#181779=CARTESIAN_POINT ( 'NONE',  ( -20.64999999999999858, 78.08573236070779444, -228.9307947190811774 ) ) ;
#181784=DIRECTION ( 'NONE',  ( 0.000000000000000000, 0.2617529984165030132, 0.9651348961777157509 ) ) ;
#181808=CARTESIAN_POINT ( 'NONE',  ( 20.93302460841143287, 67.49317130920637453, -195.4795610751097286 ) ) ;
#181815=DIRECTION ( 'NONE',  ( 1.000000000000000000, 0.000000000000000000, 0.000000000000000000 ) ) ;
#181816=CIRCLE ( 'NONE', #81814, 0.1000000000000079159 ) ;
#181826=DIRECTION ( 'NONE',  ( 1.000000000000000000, 0.000000000000000000, 0.000000000000000000 ) ) ;
#181847=DIRECTION ( 'NONE',  ( -1.000000000000000000, 0.000000000000000000, 0.000000000000000000 ) ) ;
#181850=ORIENTED_EDGE ( 'NONE', *, *, #209808, .F. ) ;
#181858=VERTEX_POINT ( 'NONE', #56028 ) ;
#181861=EDGE_CURVE ( 'NONE', #143707, #121787, #125587, .T. ) ;
#181920=ADVANCED_FACE ( 'NONE', ( #140728 ), #79607, .T. ) ;
#181934=CARTESIAN_POINT ( 'NONE',  ( 20.94999999999999574, 72.02722222756958104, -225.1832529173024398 ) ) ;
#181951=AXIS2_PLACEMENT_3D ( 'NONE', #109319, #190174, #11540 ) ;
#181990=LINE ( 'NONE', #4612, #130642 ) ;
#182009=EDGE_LOOP ( 'NONE', ( #58302, #204891, #199321, #169507 ) ) ;
#182013=AXIS2_PLACEMENT_3D ( 'NONE', #171178, #188124, #14649 ) ;
#182053=CARTESIAN_POINT ( 'NONE',  ( 21.05000000000000071, 68.17695920783671681, -227.9262201573640141 ) ) ;
#182065=ORIENTED_EDGE ( 'NONE', *, *, #146174, .T. ) ;
#182072=CARTESIAN_POINT ( 'NONE',  ( -21.14999999999999858, 60.91865828504416669, -234.1430899377568551 ) ) ;
#182084=EDGE_LOOP ( 'NONE', ( #240594, #139094, #7796, #83654 ) ) ;
#182085=DIRECTION ( 'NONE',  ( 1.000000000000000000, 0.000000000000000000, 0.000000000000000000 ) ) ;
#182089=CIRCLE ( 'NONE', #140373, 0.1999999999999908795 ) ;
#182137=CARTESIAN_POINT ( 'NONE',  ( -20.64999999999999858, 66.36210077474692071, -222.8232602954134336 ) ) ;
#182158=FACE_OUTER_BOUND ( 'NONE', #210539, .T. ) ;
#182161=DIRECTION ( 'NONE',  ( 1.000000000000000000, 0.000000000000000000, 0.000000000000000000 ) ) ;
#182182=B_SPLINE_CURVE_WITH_KNOTS ( 'NONE', 3,
 ( #11184, #90704, #177969, #97089, #81382, #257428, #22761, #77539, #120572, #241773, #181808, #42300, #82668, #99670, #176690, #200092, #57983, #61867, #218340 ),
 .UNSPECIFIED., .F., .F.,
 ( 4, 3, 3, 3, 3, 3, 4 ),
 ( 1.387778780781445676E-17, 2.646747978908967593E-05, 5.271166642128211505E-05, 9.008788829882676842E-05, 0.0001426648776560830647, 0.0001897378458659620612, 0.0001917382627806005289 ),
 .UNSPECIFIED. ) ;
#182233=DIRECTION ( 'NONE',  ( 1.000000000000000000, 0.000000000000000000, 0.000000000000000000 ) ) ;
#182243=DIRECTION ( 'NONE',  ( 0.000000000000000000, -0.9651348961777155289, 0.2617529984165036794 ) ) ;
#182263=TOROIDAL_SURFACE ( 'NONE', #19777, 0.6000000000000015321, 0.1000000000000000056 ) ;
#182274=DIRECTION ( 'NONE',  ( -1.000000000000000000, -0.000000000000000000, -0.000000000000000000 ) ) ;
#182297=ADVANCED_FACE ( 'NONE', ( #177018 ), #212280, .F. ) ;
#182325=DIRECTION ( 'NONE',  ( 0.000000000000000000, 0.2558827019434435912, -0.9667078373770033872 ) ) ;
#182326=ORIENTED_EDGE ( 'NONE', *, *, #148057, .T. ) ;
#182335=FACE_OUTER_BOUND ( 'NONE', #122525, .T. ) ;
#182336=TOROIDAL_SURFACE ( 'NONE', #40718, 11.65000000000000036, 0.1000000000000000056 ) ;
#182378=ORIENTED_EDGE ( 'NONE', *, *, #56608, .T. ) ;
#182382=ORIENTED_EDGE ( 'NONE', *, *, #103792, .T. ) ;
#182387=CARTESIAN_POINT ( 'NONE',  ( -22.59999999999999787, 55.96169194136206215, -232.9023299069559130 ) ) ;
#182392=CARTESIAN_POINT ( 'NONE',  ( 21.05000000000000071, 58.97943978561187350, -225.6753515332448217 ) ) ;
#182397=ADVANCED_FACE ( 'NONE', ( #80407 ), #222500, .T. ) ;
#182446=SPHERICAL_SURFACE ( 'NONE', #197256, 0.1000000000000000056 ) ;
#182483=CARTESIAN_POINT ( 'NONE',  ( -23.25000000000000000, 70.76519756549812712, -215.1840646563997836 ) ) ;
#182520=CARTESIAN_POINT ( 'NONE',  ( 18.49999999999999645, 79.11538813396778380, -196.3722783875038544 ) ) ;
#182544=DIRECTION ( 'NONE',  ( 0.000000000000000000, 0.9167729611565434977, -0.3994087351226345284 ) ) ;
#182549=VERTEX_POINT ( 'NONE', #91996 ) ;
#182553=EDGE_CURVE ( 'NONE', #136295, #87098, #242290, .T. ) ;
#182569=EDGE_CURVE ( 'NONE', #100977, #164049, #42029, .T. ) ;
#182578=AXIS2_PLACEMENT_3D ( 'NONE', #143191, #6244, #165341 ) ;
#182587=DIRECTION ( 'NONE',  ( 1.000000000000000000, 0.000000000000000000, 0.000000000000000000 ) ) ;
#182589=ORIENTED_EDGE ( 'NONE', *, *, #171082, .T. ) ;
#182600=PLANE ( 'NONE',  #157694 ) ;
#182613=EDGE_CURVE ( 'NONE', #159456, #77841, #83661, .T. ) ;
#182620=CARTESIAN_POINT ( 'NONE',  ( 18.43565242384933711, 78.24390740893980478, -231.6169762517608888 ) ) ;
#182626=DIRECTION ( 'NONE',  ( 0.000000000000000000, -0.8636236514130390951, 0.5041370733441546959 ) ) ;
#182631=AXIS2_PLACEMENT_3D ( 'NONE', #67854, #7909, #168293 ) ;
#182650=ORIENTED_EDGE ( 'NONE', *, *, #143636, .T. ) ;
#182730=CARTESIAN_POINT ( 'NONE',  ( 18.49999999999999645, 70.47363787294415260, -228.3418745167492432 ) ) ;
#182738=PLANE ( 'NONE',  #27892 ) ;
#182743=ADVANCED_FACE ( 'NONE', ( #95831 ), #175423, .F. ) ;
#182761=CARTESIAN_POINT ( 'NONE',  ( 20.94999999999999929, 68.03191114188443578, -213.8010436651919122 ) ) ;
#182765=DIRECTION ( 'NONE',  ( 0.000000000000000000, 0.7106264324241465813, -0.7035695228903323661 ) ) ;
#182805=FACE_OUTER_BOUND ( 'NONE', #201525, .T. ) ;
#182811=CARTESIAN_POINT ( 'NONE',  ( -21.05000000000000071, 66.97496366775517629, -235.8217698210967512 ) ) ;
#182863=EDGE_CURVE ( 'NONE', #113079, #77452, #200222, .T. ) ;
#182876=CIRCLE ( 'NONE', #203522, 0.1000000000000124678 ) ;
#182879=EDGE_CURVE ( 'NONE', #89267, #215885, #19171, .T. ) ;
#182883=DIRECTION ( 'NONE',  ( 0.000000000000000000, -0.9651348961777157509, 0.2617529984165031243 ) ) ;
#182900=ORIENTED_EDGE ( 'NONE', *, *, #15160, .F. ) ;
#182922=EDGE_CURVE ( 'NONE', #169290, #54640, #254371, .T. ) ;
#182928=ORIENTED_EDGE ( 'NONE', *, *, #151531, .T. ) ;
#182943=DIRECTION ( 'NONE',  ( 0.000000000000000000, -0.3896596508880098009, -0.9209589331071361684 ) ) ;
#182945=EDGE_CURVE ( 'NONE', #52103, #207394, #175478, .T. ) ;
#182954=ORIENTED_EDGE ( 'NONE', *, *, #2918, .T. ) ;
#182958=ORIENTED_EDGE ( 'NONE', *, *, #173006, .T. ) ;
#182971=ORIENTED_EDGE ( 'NONE', *, *, #44807, .T. ) ;
#182976=FACE_OUTER_BOUND ( 'NONE', #194568, .T. ) ;
#182993=CIRCLE ( 'NONE', #232885, 11.90000000000000568 ) ;
#183012=CARTESIAN_POINT ( 'NONE',  ( 18.59999999999999076, 62.49201502323811752, -208.8221019049098857 ) ) ;
#183021=CARTESIAN_POINT ( 'NONE',  ( -23.15000000000000213, 86.43238724539048690, -209.5644480942280836 ) ) ;
#183058=CARTESIAN_POINT ( 'NONE',  ( 23.24999999999999645, 79.76402609510435582, -204.5439441783492498 ) ) ;
#183064=CARTESIAN_POINT ( 'NONE',  ( -21.05000000000000071, 67.70174932746996888, -211.7710791003628401 ) ) ;
#183125=ORIENTED_EDGE ( 'NONE', *, *, #129431, .F. ) ;
#183137=ORIENTED_EDGE ( 'NONE', *, *, #101046, .F. ) ;
#183140=CARTESIAN_POINT ( 'NONE',  ( 21.05000000000000071, 61.00573819068043235, -234.0630943441842646 ) ) ;
#183239=DIRECTION ( 'NONE',  ( 0.000000000000000000, -0.2617529984165031243, -0.9651348961777157509 ) ) ;
#183252=ORIENTED_EDGE ( 'NONE', *, *, #25384, .F. ) ;
#183273=DIRECTION ( 'NONE',  ( 1.000000000000000000, 0.000000000000000000, -0.000000000000000000 ) ) ;
#183274=LINE ( 'NONE', #43759, #177725 ) ;
#183343=CIRCLE ( 'NONE', #208284, 0.1000000000000018374 ) ;
#183370=CARTESIAN_POINT ( 'NONE',  ( -21.14999999999999858, 57.66663670110953888, -226.2321832927624712 ) ) ;
#183379=DIRECTION ( 'NONE',  ( 1.000000000000000000, 8.153259210133937167E-16, 2.158126701439427224E-16 ) ) ;
#183391=CARTESIAN_POINT ( 'NONE',  ( 23.14999999999999858, 70.60134440767089359, -223.4290147181903023 ) ) ;
#183401=CARTESIAN_POINT ( 'NONE',  ( 18.46947024752512334, 78.23781598975503471, -231.6011157545027856 ) ) ;
#183408=AXIS2_PLACEMENT_3D ( 'NONE', #223355, #176887, #58172 ) ;
#183426=DIRECTION ( 'NONE',  ( 1.000000000000000000, 5.945622153099073960E-16, -5.981866248895712861E-16 ) ) ;
#183433=EDGE_LOOP ( 'NONE', ( #46934, #214804, #145671, #138235 ) ) ;
#183491=AXIS2_PLACEMENT_3D ( 'NONE', #5783, #82738, #163609 ) ;
#183557=LINE ( 'NONE', #188680, #39241 ) ;
#183575=DIRECTION ( 'NONE',  ( 1.000000000000000000, 0.000000000000000000, 0.000000000000000000 ) ) ;
#183582=DIRECTION ( 'NONE',  ( -1.000000000000000000, -0.000000000000000000, -0.000000000000000000 ) ) ;
#183593=ORIENTED_EDGE ( 'NONE', *, *, #96245, .T. ) ;
#183628=DIRECTION ( 'NONE',  ( 0.000000000000000000, -0.2617529984165031243, -0.9651348961777157509 ) ) ;
#183641=DIRECTION ( 'NONE',  ( 0.7070776581708964059, -0.1850949428989398515, -0.6824815363281259151 ) ) ;
#183649=ORIENTED_EDGE ( 'NONE', *, *, #210155, .F. ) ;
#183653=CARTESIAN_POINT ( 'NONE',  ( -18.50000000000000000, 76.00000000001126921, -203.5231074845248997 ) ) ;
#183663=ORIENTED_EDGE ( 'NONE', *, *, #7291, .F. ) ;
#183717=CARTESIAN_POINT ( 'NONE',  ( 21.09787244211714352, 61.96551932823614095, -221.7456163672507898 ) ) ;
#183765=CIRCLE ( 'NONE', #117123, 0.09999999999999789613 ) ;
#183783=ORIENTED_EDGE ( 'NONE', *, *, #154920, .T. ) ;
#183790=LINE ( 'NONE', #224187, #234317 ) ;
#183832=CARTESIAN_POINT ( 'NONE',  ( 21.08621493067296626, 61.08863989881826484, -234.2474152884988996 ) ) ;
#183842=ORIENTED_EDGE ( 'NONE', *, *, #105583, .T. ) ;
#183889=DIRECTION ( 'NONE',  ( -1.000000000000000000, 0.000000000000000000, 0.000000000000000000 ) ) ;
#183897=CARTESIAN_POINT ( 'NONE',  ( -18.41817142474038249, 86.89613756584731163, -199.6357039480042488 ) ) ;
#183912=VECTOR ( 'NONE', #160591, 1000.000000000000000 ) ;
#183916=ORIENTED_EDGE ( 'NONE', *, *, #205891, .F. ) ;
#183922=FACE_OUTER_BOUND ( 'NONE', #164816, .T. ) ;
#183941=EDGE_CURVE ( 'NONE', #235080, #70430, #71802, .T. ) ;
#183964=FACE_OUTER_BOUND ( 'NONE', #18339, .T. ) ;
#184012=DIRECTION ( 'NONE',  ( -1.000000000000000000, -0.000000000000000000, 0.000000000000000000 ) ) ;
#184021=ORIENTED_EDGE ( 'NONE', *, *, #153056, .T. ) ;
#184037=ORIENTED_EDGE ( 'NONE', *, *, #95848, .F. ) ;
#184047=LINE ( 'NONE', #104484, #11747 ) ;
#184064=DIRECTION ( 'NONE',  ( 0.000000000000000000, 0.2617529984165031243, 0.9651348961777157509 ) ) ;
#184067=CIRCLE ( 'NONE', #209013, 0.1000000000000106498 ) ;
#184080=CARTESIAN_POINT ( 'NONE',  ( -21.07928932188134041, 67.23127455305841238, -235.8551265064783991 ) ) ;
#184083=CARTESIAN_POINT ( 'NONE',  ( -21.02374657821572868, 62.99095723451760165, -207.1734234075708230 ) ) ;
#184084=ORIENTED_EDGE ( 'NONE', *, *, #134458, .T. ) ;
#184087=CARTESIAN_POINT ( 'NONE',  ( -21.04999999999939320, 65.54489249088371139, -242.1291417229003287 ) ) ;
#184174=ORIENTED_EDGE ( 'NONE', *, *, #70239, .F. ) ;
#184195=DIRECTION ( 'NONE',  ( 0.000000000000000000, 0.7106264324241465813, -0.7035695228903324772 ) ) ;
#184196=CARTESIAN_POINT ( 'NONE',  ( -20.94999999999999929, 64.21185867012613357, -224.4479740254296303 ) ) ;
#184202=CIRCLE ( 'NONE', #71811, 0.09999999999999949207 ) ;
#184203=AXIS2_PLACEMENT_3D ( 'NONE', #215162, #234730, #198163 ) ;
#184232=EDGE_CURVE ( 'NONE', #19933, #188240, #21899, .T. ) ;
#184266=( NAMED_UNIT ( * ) SI_UNIT ( $, .STERADIAN. ) SOLID_ANGLE_UNIT ( ) );
#184271=DIRECTION ( 'NONE',  ( 1.000000000000000000, 0.000000000000000000, 0.000000000000000000 ) ) ;
#184276=CARTESIAN_POINT ( 'NONE',  ( -20.86777300164945004, 67.49225400653517681, -195.4205142095401868 ) ) ;
#184297=EDGE_CURVE ( 'NONE', #97495, #218378, #250827, .T. ) ;
#184301=ORIENTED_EDGE ( 'NONE', *, *, #57206, .F. ) ;
#184365=VERTEX_POINT ( 'NONE', #136096 ) ;
#184386=AXIS2_PLACEMENT_3D ( 'NONE', #23204, #203094, #222638 ) ;
#184626=CARTESIAN_POINT ( 'NONE',  ( -21.08479644141223375, 61.09212952597296464, -234.2508065485932889 ) ) ;
#184635=CARTESIAN_POINT ( 'NONE',  ( 18.49999999999998934, 63.53162788017662166, -224.4728618886983043 ) ) ;
#184664=CARTESIAN_POINT ( 'NONE',  ( 18.59999994388910238, 78.14805800158373472, -231.3753211930361999 ) ) ;
#184675=CARTESIAN_POINT ( 'NONE',  ( -21.05000000000000071, 62.99095723518624368, -207.1734234082435080 ) ) ;
#184677=CARTESIAN_POINT ( 'NONE',  ( -20.54999999999999716, 70.60814576644823148, -215.7631455941064189 ) ) ;
#184704=FACE_OUTER_BOUND ( 'NONE', #232672, .T. ) ;
#184733=TOROIDAL_SURFACE ( 'NONE', #151464, 11.89999999999999858, 0.1000000000000000056 ) ;
#184742=CARTESIAN_POINT ( 'NONE',  ( 21.05000000000000071, 81.86853375790846599, -214.9828603846715964 ) ) ;
#184757=DIRECTION ( 'NONE',  ( -1.000000000000000000, -0.000000000000000000, -0.000000000000000000 ) ) ;
#184768=CARTESIAN_POINT ( 'NONE',  ( -18.55121869061588669, 67.49249915771264341, -195.4369143829851510 ) ) ;
#184783=AXIS2_PLACEMENT_3D ( 'NONE', #230238, #30784, #111583 ) ;
#184784=CARTESIAN_POINT ( 'NONE',  ( 21.14999999999999858, 59.19392724319016708, -220.9828015967491126 ) ) ;
#184788=ORIENTED_EDGE ( 'NONE', *, *, #138201, .F. ) ;
#184831=VERTEX_POINT ( 'NONE', #140981 ) ;
#184840=CIRCLE ( 'NONE', #72443, 0.1000000000000124678 ) ;
#184849=DIRECTION ( 'NONE',  ( 0.000000000000000000, -0.1290532225515392817, -0.9916376685811520986 ) ) ;
#184863=ORIENTED_EDGE ( 'NONE', *, *, #120220, .F. ) ;
#184871=ORIENTED_EDGE ( 'NONE', *, *, #134714, .F. ) ;
#184881=AXIS2_PLACEMENT_3D ( 'NONE', #228747, #12272, #30552 ) ;
#184910=CARTESIAN_POINT ( 'NONE',  ( 20.94999999999999929, 68.48451787451661232, -224.2224406095231757 ) ) ;
#184943=CARTESIAN_POINT ( 'NONE',  ( 21.05000000000000071, 59.03303942657512238, -225.8023344323644324 ) ) ;
#184963=CARTESIAN_POINT ( 'NONE',  ( 23.24999999999999645, 67.34812900481119868, -214.0300458246130972 ) ) ;
#184987=ADVANCED_FACE ( 'NONE', ( #240074 ), #184733, .T. ) ;
#184991=CARTESIAN_POINT ( 'NONE',  ( 21.14999999999999858, 61.95748721176698837, -221.7323031544521825 ) ) ;
#184994=EDGE_LOOP ( 'NONE', ( #92534, #29192, #31992, #111419 ) ) ;
#185012=LINE ( 'NONE', #248844, #201327 ) ;
#185016=AXIS2_PLACEMENT_3D ( 'NONE', #19283, #91777, #9667 ) ;
#185020=VERTEX_POINT ( 'NONE', #24897 ) ;
#185035=AXIS2_PLACEMENT_3D ( 'NONE', #88173, #109042, #6089 ) ;
#185058=DIRECTION ( 'NONE',  ( -1.000000000000000000, -0.000000000000000000, 0.000000000000000000 ) ) ;
#185107=DIRECTION ( 'NONE',  ( 1.000000000000000000, 0.000000000000000000, 0.000000000000000000 ) ) ;
#185134=CARTESIAN_POINT ( 'NONE',  ( -23.25000000000000000, 80.80934863333322937, -192.8037999715871535 ) ) ;
#185140=EDGE_LOOP ( 'NONE', ( #40609, #203387, #15930, #120537 ) ) ;
#185178=DIRECTION ( 'NONE',  ( 1.000000000000000000, 0.000000000000000000, 0.000000000000000000 ) ) ;
#185180=CARTESIAN_POINT ( 'NONE',  ( -18.33682934331556780, 86.98715295972735362, -199.3478004332870341 ) ) ;
#185203=CARTESIAN_POINT ( 'NONE',  ( -22.50875500270926821, 64.25313161950418817, -247.2214436174568277 ) ) ;
#185204=ORIENTED_EDGE ( 'NONE', *, *, #197697, .T. ) ;
#185214=ORIENTED_EDGE ( 'NONE', *, *, #162028, .F. ) ;
#185233=VERTEX_POINT ( 'NONE', #218897 ) ;
#185245=CIRCLE ( 'NONE', #235292, 0.1000000000000124678 ) ;
#185249=ORIENTED_EDGE ( 'NONE', *, *, #100541, .F. ) ;
#185263=CARTESIAN_POINT ( 'NONE',  ( 20.94999999999999574, 79.13126459505528487, -235.8705213229730191 ) ) ;
#185312=CARTESIAN_POINT ( 'NONE',  ( -18.59999999999999787, 67.49222854868494892, -195.4187676019683693 ) ) ;
#185340=DIRECTION ( 'NONE',  ( 0.000000000000000000, -0.9651348961777028723, 0.2617529984165503087 ) ) ;
#185370=CARTESIAN_POINT ( 'NONE',  ( -20.85000000000000142, 62.88396779178383156, -206.9948552354529454 ) ) ;
#185375=CARTESIAN_POINT ( 'NONE',  ( -21.05000000000000071, 65.48742650828276624, -241.9089677661029043 ) ) ;
#185387=EDGE_CURVE ( 'NONE', #12386, #219655, #213991, .T. ) ;
#185411=CIRCLE ( 'NONE', #106267, 0.1000000000000124678 ) ;
#185434=DIRECTION ( 'NONE',  ( -1.836970198721029934E-16, -0.9651348961777157509, 0.2617529984165031243 ) ) ;
#185450=CARTESIAN_POINT ( 'NONE',  ( -20.94999999999999929, 68.22930980752001062, -227.7331931781284879 ) ) ;
#185468=CARTESIAN_POINT ( 'NONE',  ( -21.05000000000000071, 61.00523048461932518, -234.0629566809490143 ) ) ;
#185474=CARTESIAN_POINT ( 'NONE',  ( 21.05000000000000071, 76.00000000001126921, -203.5231074845248997 ) ) ;
#185505=ORIENTED_EDGE ( 'NONE', *, *, #69969, .F. ) ;
#185514=CARTESIAN_POINT ( 'NONE',  ( -20.64999999999999858, 75.50266930301991408, -205.3568637872625686 ) ) ;
#185543=EDGE_CURVE ( 'NONE', #90831, #117062, #142416, .T. ) ;
#185548=DIRECTION ( 'NONE',  ( -1.000000000000000000, -0.000000000000000000, -0.000000000000000000 ) ) ;
#185618=EDGE_CURVE ( 'NONE', #231873, #177651, #39407, .T. ) ;
#185637=VERTEX_POINT ( 'NONE', #159939 ) ;
#185644=DIRECTION ( 'NONE',  ( 0.000000000000000000, 0.2617529984165031243, 0.9651348961777157509 ) ) ;
#185651=CYLINDRICAL_SURFACE ( 'NONE', #79595, 0.5000000000000014433 ) ;
#185666=CIRCLE ( 'NONE', #19053, 0.1000000000000106498 ) ;
#185670=EDGE_CURVE ( 'NONE', #147060, #95393, #14462, .T. ) ;
#185678=CARTESIAN_POINT ( 'NONE',  ( 21.30740335185486245, 60.87731878144036557, -234.2343867990592798 ) ) ;
#185733=ORIENTED_EDGE ( 'NONE', *, *, #187873, .F. ) ;
#185761=AXIS2_PLACEMENT_3D ( 'NONE', #58082, #174252, #137623 ) ;
#185762=VERTEX_POINT ( 'NONE', #182053 ) ;
#185798=LINE ( 'NONE', #21603, #11053 ) ;
#185821=AXIS2_PLACEMENT_3D ( 'NONE', #186801, #8155, #88947 ) ;
#185856=ORIENTED_EDGE ( 'NONE', *, *, #206547, .F. ) ;
#185865=DIRECTION ( 'NONE',  ( -1.000000000000000000, 2.849773892568378313E-16, -7.728835255496647986E-17 ) ) ;
#185866=VERTEX_POINT ( 'NONE', #202887 ) ;
#185869=DIRECTION ( 'NONE',  ( 0.000000000000000000, 0.9651348961777160840, -0.2617529984165018475 ) ) ;
#185875=DIRECTION ( 'NONE',  ( 0.000000000000000000, 0.9651348961777379554, -0.2617529984164210233 ) ) ;
#185878=DIRECTION ( 'NONE',  ( 3.469446951953635015E-14, -0.2617529984165031243, -0.9651348961777157509 ) ) ;
#185940=DIRECTION ( 'NONE',  ( 0.7071067811865460184, 0.6824534298470606997, -0.1850873201761399356 ) ) ;
#185946=CARTESIAN_POINT ( 'NONE',  ( 20.85000000000000142, 70.08587962373171365, -198.1273832143211848 ) ) ;
#185960=CARTESIAN_POINT ( 'NONE',  ( 18.42595409746851587, 78.23215996841915398, -231.5864510857097684 ) ) ;
#185962=DIRECTION ( 'NONE',  ( -4.408576920032448588E-17, -0.3896596508880098009, -0.9209589331071360574 ) ) ;
#186042=DIRECTION ( 'NONE',  ( 0.000000000000000000, 0.9667078373770113808, 0.2558827019434133376 ) ) ;
#186046=DIRECTION ( 'NONE',  ( 0.000000000000000000, 0.2617529984164915779, 0.9651348961777189706 ) ) ;
#186073=ORIENTED_EDGE ( 'NONE', *, *, #101046, .T. ) ;
#186090=DIRECTION ( 'NONE',  ( 0.000000000000000000, 0.7035695228903320331, 0.7106264324241468033 ) ) ;
#186095=ORIENTED_EDGE ( 'NONE', *, *, #90844, .F. ) ;
#186126=ORIENTED_EDGE ( 'NONE', *, *, #143062, .F. ) ;
#186142=CARTESIAN_POINT ( 'NONE',  ( 22.48660254037844197, 55.97436536266718576, -232.8539608197349935 ) ) ;
#186145=DIRECTION ( 'NONE',  ( 0.000000000000000000, 0.9651348961777157509, -0.2617529984165031243 ) ) ;
#186171=EDGE_CURVE ( 'NONE', #82116, #42365, #110283, .T. ) ;
#186212=VERTEX_POINT ( 'NONE', #180150 ) ;
#186231=CYLINDRICAL_SURFACE ( 'NONE', #219679, 0.1000000000000124678 ) ;
#186238=CARTESIAN_POINT ( 'NONE',  ( -21.05000000000000782, 61.17395774131533415, -234.2804044302905311 ) ) ;
#186308=CARTESIAN_POINT ( 'NONE',  ( -23.15000000000000213, 79.08634564045905790, -228.8189404293001132 ) ) ;
#186316=AXIS2_PLACEMENT_3D ( 'NONE', #102534, #21770, #3462 ) ;
#186347=ORIENTED_EDGE ( 'NONE', *, *, #122702, .T. ) ;
#186358=CIRCLE ( 'NONE', #73949, 0.1000000000000124678 ) ;
#186373=VERTEX_POINT ( 'NONE', #250380 ) ;
#186374=DIRECTION ( 'NONE',  ( 1.000000000000000000, -1.772924042024179204E-16, 4.808324575169891715E-17 ) ) ;
#186415=CIRCLE ( 'NONE', #107283, 0.1000000000000012546 ) ;
#186429=ORIENTED_EDGE ( 'NONE', *, *, #54381, .T. ) ;
#186475=CARTESIAN_POINT ( 'NONE',  ( 18.49999999999999289, 63.61019970229973808, -209.1253633388161006 ) ) ;
#186476=ADVANCED_FACE ( 'NONE', ( #16919 ), #2122, .F. ) ;
#186490=CIRCLE ( 'NONE', #11528, 0.1000000000000066530 ) ;
#186498=ORIENTED_EDGE ( 'NONE', *, *, #133771, .F. ) ;
#186502=CARTESIAN_POINT ( 'NONE',  ( -23.15000000000000213, 75.45031870333662027, -205.5498907664980948 ) ) ;
#186503=AXIS2_PLACEMENT_3D ( 'NONE', #206506, #145234, #65711 ) ;
#186508=ORIENTED_EDGE ( 'NONE', *, *, #26948, .F. ) ;
#186509=EDGE_CURVE ( 'NONE', #7014, #204625, #139675, .T. ) ;
#186513=ORIENTED_EDGE ( 'NONE', *, *, #190363, .T. ) ;
#186517=AXIS2_PLACEMENT_3D ( 'NONE', #136114, #38347, #154465 ) ;
#186532=CARTESIAN_POINT ( 'NONE',  ( -20.64999999999999858, 65.86663596189677605, -213.5709895136416776 ) ) ;
#186534=LINE ( 'NONE', #11766, #224300 ) ;
#186565=CIRCLE ( 'NONE', #40831, 0.09999999999999935330 ) ;
#186594=EDGE_CURVE ( 'NONE', #178174, #94242, #89609, .T. ) ;
#186595=EDGE_CURVE ( 'NONE', #110369, #193988, #122955, .T. ) ;
#186599=CARTESIAN_POINT ( 'NONE',  ( -21.05000000000000071, 72.05339752741123505, -225.0867394276846483 ) ) ;
#186605=CYLINDRICAL_SURFACE ( 'NONE', #95365, 0.09999999999999939493 ) ;
#186616=AXIS2_PLACEMENT_3D ( 'NONE', #26002, #105492, #15432 ) ;
#186636=AXIS2_PLACEMENT_3D ( 'NONE', #151675, #33028, #192071 ) ;
#186647=DIRECTION ( 'NONE',  ( -1.000000000000000000, 0.000000000000000000, 0.000000000000000000 ) ) ;
#186653=DIRECTION ( 'NONE',  ( 0.000000000000000000, 0.2466408114429753939, 0.9691069652678959701 ) ) ;
#186674=CARTESIAN_POINT ( 'NONE',  ( -21.05000000000138627, 65.53264477812935240, -241.9222181873227555 ) ) ;
#186724=DIRECTION ( 'NONE',  ( -1.000000000000000000, -0.000000000000000000, 0.000000000000000000 ) ) ;
#186755=ORIENTED_EDGE ( 'NONE', *, *, #96188, .F. ) ;
#186765=CARTESIAN_POINT ( 'NONE',  ( -21.05000000000001492, 61.01966792176285992, -234.1522517536919565 ) ) ;
#186795=DIRECTION ( 'NONE',  ( 0.000000000000000000, 0.9209589331071864615, -0.3896596508878908960 ) ) ;
#186801=CARTESIAN_POINT ( 'NONE',  ( -20.94999999999999929, 76.00000000001126921, -203.5231074845248997 ) ) ;
#186826=ORIENTED_EDGE ( 'NONE', *, *, #151073, .F. ) ;
#186836=FACE_OUTER_BOUND ( 'NONE', #193226, .T. ) ;
#186863=CIRCLE ( 'NONE', #140886, 0.1999999999999981515 ) ;
#186864=VECTOR ( 'NONE', #227680, 1000.000000000000000 ) ;
#186906=AXIS2_PLACEMENT_3D ( 'NONE', #65622, #61777, #141316 ) ;
#186928=CARTESIAN_POINT ( 'NONE',  ( 22.39999999999999503, 56.01362831242965967, -232.7091905853083347 ) ) ;
#186942=CARTESIAN_POINT ( 'NONE',  ( -23.25000000000000000, 70.57516910782925379, -223.5255282078080654 ) ) ;
#186985=CARTESIAN_POINT ( 'NONE',  ( 23.14999999999999858, 74.06973020765583726, -202.9996014876918480 ) ) ;
#187002=DIRECTION ( 'NONE',  ( 0.000000000000000000, 0.7049548389605068133, -0.7092521942342976393 ) ) ;
#187007=ORIENTED_EDGE ( 'NONE', *, *, #43470, .T. ) ;
#187008=CARTESIAN_POINT ( 'NONE',  ( 21.05000000000000071, 67.54115598404673904, -214.0823964242964053 ) ) ;
#187014=CARTESIAN_POINT ( 'NONE',  ( 18.59999999999999787, 84.35952707724818822, -212.2592855339655671 ) ) ;
#187028=DIRECTION ( 'NONE',  ( 0.000000000000000000, -0.2617529984165036239, -0.9651348961777156399 ) ) ;
#187068=CIRCLE ( 'NONE', #141261, 0.09999999999999939493 ) ;
#187128=EDGE_CURVE ( 'NONE', #220166, #184365, #218744, .T. ) ;
#187136=ORIENTED_EDGE ( 'NONE', *, *, #40547, .F. ) ;
#187138=LINE ( 'NONE', #86701, #97256 ) ;
#187166=AXIS2_PLACEMENT_3D ( 'NONE', #35024, #153708, #188926 ) ;
#187180=DIRECTION ( 'NONE',  ( 0.000000000000000000, -0.2617529984164856383, -0.9651348961777204138 ) ) ;
#187199=DIRECTION ( 'NONE',  ( 0.000000000000000000, -0.2617529984164955192, -0.9651348961777178603 ) ) ;
#187209=VECTOR ( 'NONE', #209458, 1000.000000000000000 ) ;
#187215=ORIENTED_EDGE ( 'NONE', *, *, #3243, .T. ) ;
#187218=FACE_OUTER_BOUND ( 'NONE', #140624, .T. ) ;
#187273=DIRECTION ( 'NONE',  ( 0.000000000000000000, 0.9651348961777158619, -0.2617529984165031243 ) ) ;
#187279=AXIS2_PLACEMENT_3D ( 'NONE', #177613, #75914, #155488 ) ;
#187295=ORIENTED_EDGE ( 'NONE', *, *, #45535, .T. ) ;
#187314=( BOUNDED_SURFACE ( )  B_SPLINE_SURFACE ( 3, 2, ( 
 ( #101232, #201665, #142952 ),
 ( #84229, #105096, #184664 ),
 ( #6021, #4728, #144241 ),
 ( #103829, #21765, #43884 ),
 ( #123421, #165115, #81681 ),
 ( #240805, #24339, #183401 ),
 ( #106396, #185960, #163836 ),
 ( #223784, #46435, #205509 ) ),
 .UNSPECIFIED., .F., .F., .F. ) 
 B_SPLINE_SURFACE_WITH_KNOTS ( ( 4, 2, 2, 4 ),
 ( 3, 3 ),
 ( 0.0001704874539069756818, 0.0003809798300636538649, 0.0004862260181419929836, 0.0005914722062203320481 ),
 ( 0.000000000000000000, 1.000000000000000000 ),
 .UNSPECIFIED. ) 
 GEOMETRIC_REPRESENTATION_ITEM ( )  RATIONAL_B_SPLINE_SURFACE ( (
 ( 1.000000000000000000, 0.7071067811864569785, 1.000000000000000000),
 ( 1.000000000000000000, 0.7670648383580433993, 1.000000000000000000),
 ( 1.000000000000000000, 0.8204820770247034378, 1.000000000000000000),
 ( 1.000000000000000000, 0.8877218296116180518, 1.000000000000000000),
 ( 1.000000000000000000, 0.9080815932668236945, 1.000000000000000000),
 ( 1.000000000000000000, 0.9395541505859680287, 1.000000000000000000),
 ( 1.000000000000000000, 0.9506520335380508335, 1.000000000000000000),
 ( 1.000000000000000000, 0.9504532311154547664, 1.000000000000000000) ) ) 
 REPRESENTATION_ITEM ( '' )  SURFACE ( )  );
#187315=FACE_OUTER_BOUND ( 'NONE', #148845, .T. ) ;
#187318=ORIENTED_EDGE ( 'NONE', *, *, #191450, .F. ) ;
#187322=CARTESIAN_POINT ( 'NONE',  ( 18.39999999999999858, 78.24072131640578220, -231.5548844243369047 ) ) ;
#187325=AXIS2_PLACEMENT_3D ( 'NONE', #232033, #14272, #173373 ) ;
#187369=ORIENTED_EDGE ( 'NONE', *, *, #182922, .T. ) ;
#187373=ADVANCED_FACE ( 'NONE', ( #6854 ), #165956, .F. ) ;
#187374=CIRCLE ( 'NONE', #49990, 0.1000000000000124678 ) ;
#187377=DIRECTION ( 'NONE',  ( 1.000000000000000000, 0.000000000000000000, 0.000000000000000000 ) ) ;
#187387=CARTESIAN_POINT ( 'NONE',  ( 18.59999999999999787, 67.23127455305841238, -235.8551265064783991 ) ) ;
#187392=VECTOR ( 'NONE', #59517, 1000.000000000000114 ) ;
#187407=DIRECTION ( 'NONE',  ( 0.000000000000000000, -0.9651348961777157509, 0.2617529984165031243 ) ) ;
#187500=CARTESIAN_POINT ( 'NONE',  ( 23.24999999999999645, 65.07363471106805264, -222.4165545841253220 ) ) ;
#187510=DIRECTION ( 'NONE',  ( 0.000000000000000000, 0.9651348961777157509, -0.2617529984165031243 ) ) ;
#187511=DIRECTION ( 'NONE',  ( 0.000000000000000000, -0.9651348961777161950, 0.2617529984165015700 ) ) ;
#187514=ORIENTED_EDGE ( 'NONE', *, *, #168412, .F. ) ;
#187547=DIRECTION ( 'NONE',  ( -0.000000000000000000, 0.9667078373770112698, 0.2558827019434132821 ) ) ;
#187581=DIRECTION ( 'NONE',  ( 0.000000000000000000, 0.9651348961777158619, -0.2617529984165031243 ) ) ;
#187650=EDGE_CURVE ( 'NONE', #16549, #156950, #73246, .T. ) ;
#187667=DIRECTION ( 'NONE',  ( 1.000000000000000000, 0.000000000000000000, 0.000000000000000000 ) ) ;
#187673=DIRECTION ( 'NONE',  ( 0.000000000000000000, -0.6035730884107395333, -0.7973076739542406255 ) ) ;
#187706=CARTESIAN_POINT ( 'NONE',  ( 21.10320863425824811, 61.04759385288372187, -234.2039845577155859 ) ) ;
#187715=AXIS2_PLACEMENT_3D ( 'NONE', #86392, #31625, #105963 ) ;
#187731=LINE ( 'NONE', #188998, #52213 ) ;
#187755=AXIS2_PLACEMENT_3D ( 'NONE', #20830, #256789, #100317 ) ;
#187764=FACE_OUTER_BOUND ( 'NONE', #83421, .T. ) ;
#187774=VERTEX_POINT ( 'NONE', #147501 ) ;
#187802=DIRECTION ( 'NONE',  ( -0.000000000000000000, -0.9121259477928193027, 0.4099100576505185778 ) ) ;
#187831=VECTOR ( 'NONE', #185962, 1000.000000000000114 ) ;
#187834=ADVANCED_FACE ( 'NONE', ( #77894 ), #98711, .T. ) ;
#187873=EDGE_CURVE ( 'NONE', #129900, #162791, #160886, .T. ) ;
#187882=VECTOR ( 'NONE', #218614, 1000.000000000000000 ) ;
#187902=EDGE_LOOP ( 'NONE', ( #200937, #193961, #251892, #129249 ) ) ;
#187927=CARTESIAN_POINT ( 'NONE',  ( 23.14999999999999858, 67.34812900481119868, -214.0300458246130972 ) ) ;
#187930=DIRECTION ( 'NONE',  ( 0.000000000000000000, 0.2617529984165027912, 0.9651348961777158619 ) ) ;
#187974=CARTESIAN_POINT ( 'NONE',  ( 21.05000000000000071, 63.67931791018308019, -224.6923787560153585 ) ) ;
#188003=AXIS2_PLACEMENT_3D ( 'NONE', #145582, #106435, #209412 ) ;
#188005=EDGE_LOOP ( 'NONE', ( #114832, #98132, #177823, #201887, #185733 ) ) ;
#188010=FACE_OUTER_BOUND ( 'NONE', #176811, .T. ) ;
#188012=ADVANCED_FACE ( 'NONE', ( #141722 ), #102566, .F. ) ;
#188020=EDGE_CURVE ( 'NONE', #101319, #43432, #256674, .T. ) ;
#188026=ORIENTED_EDGE ( 'NONE', *, *, #83471, .T. ) ;
#188063=CARTESIAN_POINT ( 'NONE',  ( 20.84999999999998721, 87.34033503009941057, -206.5987052159188124 ) ) ;
#188083=ORIENTED_EDGE ( 'NONE', *, *, #41153, .T. ) ;
#188124=DIRECTION ( 'NONE',  ( 1.000000000000000000, -3.151514657663852580E-16, 8.547182517843351137E-17 ) ) ;
#188240=VERTEX_POINT ( 'NONE', #129855 ) ;
#188260=EDGE_CURVE ( 'NONE', #92812, #171727, #152027, .T. ) ;
#188265=FACE_OUTER_BOUND ( 'NONE', #248411, .T. ) ;
#188266=SPHERICAL_SURFACE ( 'NONE', #201213, 0.1000000000000000056 ) ;
#188270=LINE ( 'NONE', #51298, #155069 ) ;
#188295=ORIENTED_EDGE ( 'NONE', *, *, #214991, .F. ) ;
#188303=AXIS2_PLACEMENT_3D ( 'NONE', #31071, #170598, #54437 ) ;
#188335=CARTESIAN_POINT ( 'NONE',  ( -22.00411653962178704, 60.20480020221445017, -234.0521012187911651 ) ) ;
#188367=CARTESIAN_POINT ( 'NONE',  ( -18.59999999999999787, 79.19526988099229925, -196.1889237952725296 ) ) ;
#188388=DIRECTION ( 'NONE',  ( 1.000000000000000000, 0.000000000000000000, 0.000000000000000000 ) ) ;
#188397=DIRECTION ( 'NONE',  ( 0.000000000000000000, -0.2617529984165031243, -0.9651348961777158619 ) ) ;
#188406=CARTESIAN_POINT ( 'NONE',  ( -20.15000000000000568, 63.82605078341359217, -212.9139525631556751 ) ) ;
#188424=VERTEX_POINT ( 'NONE', #241805 ) ;
#188458=ORIENTED_EDGE ( 'NONE', *, *, #172480, .F. ) ;
#188473=CARTESIAN_POINT ( 'NONE',  ( 21.05000000000000071, 60.91498325274309877, -225.4240842350366165 ) ) ;
#188481=DIRECTION ( 'NONE',  ( -1.000000000000000000, -0.000000000000000000, 0.000000000000000000 ) ) ;
#188497=FACE_OUTER_BOUND ( 'NONE', #220337, .T. ) ;
#188525=CARTESIAN_POINT ( 'NONE',  ( 20.04142135623730070, 62.34315093393704643, -208.9889535843037720 ) ) ;
#188542=VERTEX_POINT ( 'NONE', #70911 ) ;
#188547=DIRECTION ( 'NONE',  ( 0.000000000000000000, 0.2617529984164915779, 0.9651348961777189706 ) ) ;
#188593=ORIENTED_EDGE ( 'NONE', *, *, #16380, .F. ) ;
#188604=CARTESIAN_POINT ( 'NONE',  ( 18.58725287972329454, 87.01889655985287675, -199.4425632957462540 ) ) ;
#188607=DIRECTION ( 'NONE',  ( -0.000000000000000000, -0.2617529984165031243, -0.9651348961777157509 ) ) ;
#188618=CARTESIAN_POINT ( 'NONE',  ( -22.50000000000000000, 67.23127455305841238, -235.8551265064783991 ) ) ;
#188619=FACE_OUTER_BOUND ( 'NONE', #6091, .T. ) ;
#188667=CIRCLE ( 'NONE', #205222, 0.1000000000000124678 ) ;
#188680=CARTESIAN_POINT ( 'NONE',  ( -20.54999999999999716, 76.52350599684427834, -201.5928376921694678 ) ) ;
#188702=CARTESIAN_POINT ( 'NONE',  ( -22.39999999999999858, 59.68594599439717285, -233.9123800762197902 ) ) ;
#188723=ORIENTED_EDGE ( 'NONE', *, *, #233129, .F. ) ;
#188765=DIRECTION ( 'NONE',  ( 0.000000000000000000, 0.2617529984165033463, 0.9651348961777157509 ) ) ;
#188784=DIRECTION ( 'NONE',  ( 0.000000000000000000, -0.2617529984165152257, -0.9651348961777124202 ) ) ;
#188799=PLANE ( 'NONE',  #60119 ) ;
#188806=ORIENTED_EDGE ( 'NONE', *, *, #135989, .F. ) ;
#188820=CIRCLE ( 'NONE', #26514, 0.09999999999999939493 ) ;
#188824=DIRECTION ( 'NONE',  ( 0.000000000000000000, -0.2617529984165031243, -0.9651348961777157509 ) ) ;
#188825=AXIS2_PLACEMENT_3D ( 'NONE', #5702, #142651, #201360 ) ;
#188843=ADVANCED_FACE ( 'NONE', ( #68005 ), #239790, .T. ) ;
#188860=CIRCLE ( 'NONE', #76407, 3.899999999999996803 ) ;
#188866=AXIS2_PLACEMENT_3D ( 'NONE', #122332, #1066, #162757 ) ;
#188870=VERTEX_POINT ( 'NONE', #70607 ) ;
#188897=CIRCLE ( 'NONE', #43152, 0.1000000000000066530 ) ;
#188913=CARTESIAN_POINT ( 'NONE',  ( -20.54999999999999716, 64.71492276886415596, -217.8175830568236506 ) ) ;
#188926=DIRECTION ( 'NONE',  ( 0.000000000000000000, 0.2617529984165152257, 0.9651348961777124202 ) ) ;
#188977=CARTESIAN_POINT ( 'NONE',  ( -20.94999999999999929, 68.48451787451661232, -224.2224406095231757 ) ) ;
#188993=CIRCLE ( 'NONE', #89007, 0.1000000000000124678 ) ;
#188998=CARTESIAN_POINT ( 'NONE',  ( -18.50000000000000000, 59.07123845373075710, -221.0531397865252075 ) ) ;
#189005=ORIENTED_EDGE ( 'NONE', *, *, #19191, .F. ) ;
#189006=CARTESIAN_POINT ( 'NONE',  ( 20.13684514580243246, 60.19795610438474398, -225.5104338443611596 ) ) ;
#189035=AXIS2_PLACEMENT_3D ( 'NONE', #71863, #213917, #170996 ) ;
#189039=CARTESIAN_POINT ( 'NONE',  ( 18.56308993302911503, 63.68807297684761437, -209.2612623977875614 ) ) ;
#189053=ORIENTED_EDGE ( 'NONE', *, *, #253638, .F. ) ;
#189091=SPHERICAL_SURFACE ( 'NONE', #170587, 0.1000000000000000056 ) ;
#189143=CIRCLE ( 'NONE', #255721, 0.1000000000000079159 ) ;
#189146=EDGE_CURVE ( 'NONE', #42365, #125683, #36618, .T. ) ;
#189167=EDGE_CURVE ( 'NONE', #134983, #17708, #164939, .T. ) ;
#189180=CARTESIAN_POINT ( 'NONE',  ( 23.14999999999999503, 66.40155400966892785, -213.5088390336144073 ) ) ;
#189214=ADVANCED_FACE ( 'NONE', ( #181250 ), #37890, .T. ) ;
#189304=VERTEX_POINT ( 'NONE', #226766 ) ;
#189315=EDGE_LOOP ( 'NONE', ( #196351, #176488, #217760 ) ) ;
#189326=CARTESIAN_POINT ( 'NONE',  ( -21.05000000000000071, 61.15173430017006240, -234.1841440743729379 ) ) ;
#189332=LINE ( 'NONE', #96607, #26616 ) ;
#189364=EDGE_LOOP ( 'NONE', ( #45135, #180045, #96343, #195920 ) ) ;
#189402=CIRCLE ( 'NONE', #230936, 0.6000000000000139666 ) ;
#189452=AXIS2_PLACEMENT_3D ( 'NONE', #228354, #147525, #49707 ) ;
#189459=EDGE_LOOP ( 'NONE', ( #38318, #178864, #9584, #141815 ) ) ;
#189464=ORIENTED_EDGE ( 'NONE', *, *, #76556, .T. ) ;
#189470=( BOUNDED_CURVE ( )  B_SPLINE_CURVE ( 3, ( #97631, #196751, #177228, #80638 ),
 .UNSPECIFIED., .F., .F. ) 
 B_SPLINE_CURVE_WITH_KNOTS ( ( 4, 4 ),
 ( 0.06456096931748304957, 3.077031684272310219 ),
 .UNSPECIFIED. ) 
 CURVE ( )  GEOMETRIC_REPRESENTATION_ITEM ( )  RATIONAL_B_SPLINE_CURVE ( ( 1.000000000000000000, 0.3763440860215093164, 0.3763440860215093164, 1.000000000000000000 ) ) 
 REPRESENTATION_ITEM ( '' )  );
#189480=DIRECTION ( 'NONE',  ( -1.000000000000000000, 0.000000000000000000, 0.000000000000000000 ) ) ;
#189490=VECTOR ( 'NONE', #203719, 1000.000000000000000 ) ;
#189507=FACE_OUTER_BOUND ( 'NONE', #124221, .T. ) ;
#189511=CARTESIAN_POINT ( 'NONE',  ( 21.05000000000000071, 66.10573665986744629, -240.0052065600425806 ) ) ;
#189568=DIRECTION ( 'NONE',  ( 0.000000000000000000, -0.9151430362303984989, 0.4031292884906871321 ) ) ;
#189582=DIRECTION ( 'NONE',  ( 0.000000000000000000, -0.2617529984164915779, -0.9651348961777189706 ) ) ;
#189601=DIRECTION ( 'NONE',  ( 0.000000000000000000, 0.2617529984165152257, 0.9651348961777124202 ) ) ;
#189641=ORIENTED_EDGE ( 'NONE', *, *, #78201, .F. ) ;
#189661=CARTESIAN_POINT ( 'NONE',  ( 23.14999999999999503, 60.92570327216495230, -205.2374328603434890 ) ) ;
#189670=ORIENTED_EDGE ( 'NONE', *, *, #179694, .F. ) ;
#189698=CARTESIAN_POINT ( 'NONE',  ( 20.94999999999999574, 68.22930980752001062, -227.7331931781284879 ) ) ;
#189703=TOROIDAL_SURFACE ( 'NONE', #177270, 0.4000000000000012990, 0.1000000000000000056 ) ;
#189751=VECTOR ( 'NONE', #10643, 1000.000000000000000 ) ;
#189814=ORIENTED_EDGE ( 'NONE', *, *, #13488, .T. ) ;
#189818=CARTESIAN_POINT ( 'NONE',  ( 19.92426406871192412, 62.39550153362034024, -208.7959266050682743 ) ) ;
#189839=DIRECTION ( 'NONE',  ( -0.000000000000000000, -0.7106264324241465813, 0.7035695228903323661 ) ) ;
#189874=CARTESIAN_POINT ( 'NONE',  ( -18.59999999999999787, 52.91185528119410719, -244.1460391050142960 ) ) ;
#189876=CARTESIAN_POINT ( 'NONE',  ( 21.05000000000000071, 76.00000000001126921, -203.5231074845248997 ) ) ;
#189900=ORIENTED_EDGE ( 'NONE', *, *, #147262, .T. ) ;
#189910=AXIS2_PLACEMENT_3D ( 'NONE', #245817, #64593, #67176 ) ;
#189915=VECTOR ( 'NONE', #15702, 1000.000000000000000 ) ;
#189957=DIRECTION ( 'NONE',  ( 0.000000000000000000, 0.9651348961777159730, -0.2617529984165021806 ) ) ;
#189967=VERTEX_POINT ( 'NONE', #165882 ) ;
#189984=EDGE_LOOP ( 'NONE', ( #157928, #144590, #257617, #32844, #112360 ) ) ;
#189994=SPHERICAL_SURFACE ( 'NONE', #193016, 0.1000000000000000056 ) ;
#190000=DIRECTION ( 'NONE',  ( 0.000000000000000000, 0.2617529984165031243, 0.9651348961777157509 ) ) ;
#190021=ORIENTED_EDGE ( 'NONE', *, *, #145100, .T. ) ;
#190050=CARTESIAN_POINT ( 'NONE',  ( 18.59999999999999432, 68.22930980752001062, -227.7331931781284879 ) ) ;
#190110=ORIENTED_EDGE ( 'NONE', *, *, #136240, .T. ) ;
#190138=EDGE_CURVE ( 'NONE', #193211, #225653, #194747, .T. ) ;
#190174=DIRECTION ( 'NONE',  ( 8.673617379884087537E-15, -0.2617529984165031243, -0.9651348961777157509 ) ) ;
#190202=VERTEX_POINT ( 'NONE', #74511 ) ;
#190207=ORIENTED_EDGE ( 'NONE', *, *, #173086, .T. ) ;
#190214=DIRECTION ( 'NONE',  ( 0.000000000000000000, -0.2617529984165152257, -0.9651348961777124202 ) ) ;
#190228=CARTESIAN_POINT ( 'NONE',  ( 20.96077737575322786, 62.98594959644118774, -207.1005776826179670 ) ) ;
#190232=DIRECTION ( 'NONE',  ( 0.000000000000000000, 0.9167729611565434977, -0.3994087351226345284 ) ) ;
#190243=VECTOR ( 'NONE', #79374, 1000.000000000000000 ) ;
#190246=ORIENTED_EDGE ( 'NONE', *, *, #180210, .F. ) ;
#190266=CARTESIAN_POINT ( 'NONE',  ( -23.24999999999999645, 86.99291436658650412, -199.6658631664729739 ) ) ;
#190279=DIRECTION ( 'NONE',  ( 0.000000000000000000, 0.2617529984164915779, 0.9651348961777189706 ) ) ;
#190289=ORIENTED_EDGE ( 'NONE', *, *, #46014, .F. ) ;
#190301=CARTESIAN_POINT ( 'NONE',  ( 20.59588692710267566, 59.22361013210799996, -225.7683383221924203 ) ) ;
#190319=ORIENTED_EDGE ( 'NONE', *, *, #85512, .F. ) ;
#190363=EDGE_CURVE ( 'NONE', #76927, #143126, #186358, .T. ) ;
#190368=CARTESIAN_POINT ( 'NONE',  ( -20.64999999999999858, 81.86853375790846599, -214.9828603846715964 ) ) ;
#190373=DIRECTION ( 'NONE',  ( -0.000000000000000000, 0.3848449534832665830, 0.9229812358756067647 ) ) ;
#190402=ORIENTED_EDGE ( 'NONE', *, *, #223060, .T. ) ;
#190413=ORIENTED_EDGE ( 'NONE', *, *, #227048, .T. ) ;
#190428=EDGE_LOOP ( 'NONE', ( #46030, #63781, #35866, #168316 ) ) ;
#190460=CARTESIAN_POINT ( 'NONE',  ( 20.04142135623730070, 61.57587952878035509, -212.2000740415318774 ) ) ;
#190499=AXIS2_PLACEMENT_3D ( 'NONE', #23634, #1452, #43167 ) ;
#190515=CARTESIAN_POINT ( 'NONE',  ( -21.05000000000000071, 67.23127455305841238, -235.8551265064783991 ) ) ;
#190566=CARTESIAN_POINT ( 'NONE',  ( 23.14999999999999858, 76.00000000001126921, -203.5231074845248997 ) ) ;
#190580=ORIENTED_EDGE ( 'NONE', *, *, #21415, .F. ) ;
#190595=LINE ( 'NONE', #176171, #101169 ) ;
#190623=AXIS2_PLACEMENT_3D ( 'NONE', #16230, #10106, #216950 ) ;
#190634=DIRECTION ( 'NONE',  ( 0.000000000000000000, 0.2617529984165152257, 0.9651348961777124202 ) ) ;
#190639=EDGE_CURVE ( 'NONE', #159934, #6279, #249095, .T. ) ;
#190672=ORIENTED_EDGE ( 'NONE', *, *, #186595, .T. ) ;
#190682=EDGE_CURVE ( 'NONE', #233526, #168, #221341, .T. ) ;
#190719=CARTESIAN_POINT ( 'NONE',  ( -18.59999999999999787, 68.68284540823283635, -224.2482512540334767 ) ) ;
#190751=LINE ( 'NONE', #233714, #108018 ) ;
#190777=DIRECTION ( 'NONE',  ( 0.000000000000000000, 0.2617529984165152257, 0.9651348961777124202 ) ) ;
#190791=DIRECTION ( 'NONE',  ( 0.000000000000000000, 0.2617529984164915779, 0.9651348961777189706 ) ) ;
#190872=DIRECTION ( 'NONE',  ( 1.000000000000000000, 0.000000000000000000, 0.000000000000000000 ) ) ;
#190877=EDGE_CURVE ( 'NONE', #55134, #35438, #86722, .T. ) ;
#190885=DIRECTION ( 'NONE',  ( -1.000000000000000000, -0.000000000000000000, 0.000000000000000000 ) ) ;
#190892=CARTESIAN_POINT ( 'NONE',  ( -23.25000000000000000, 79.24821784679178904, -196.3217825494968736 ) ) ;
#190900=EDGE_CURVE ( 'NONE', #16586, #169290, #255191, .T. ) ;
#190910=CARTESIAN_POINT ( 'NONE',  ( 18.49999999999999645, 67.23127455305841238, -235.8551265064783991 ) ) ;
#190939=CARTESIAN_POINT ( 'NONE',  ( 18.59999999999999432, 70.47363787294415260, -228.3418745167492432 ) ) ;
#190953=ORIENTED_EDGE ( 'NONE', *, *, #89221, .F. ) ;
#190959=DIRECTION ( 'NONE',  ( 0.000000000000000000, 0.2617529984165031243, 0.9651348961777157509 ) ) ;
#191015=VERTEX_POINT ( 'NONE', #189511 ) ;
#191030=CARTESIAN_POINT ( 'NONE',  ( 21.06490991615909536, 60.07466569438444992, -221.2696263483812515 ) ) ;
#191083=DIRECTION ( 'NONE',  ( -2.578261006436899437E-14, 0.1290532225515364784, 0.9916376685811524316 ) ) ;
#191095=DIRECTION ( 'NONE',  ( 1.000000000000000000, 0.000000000000000000, -0.000000000000000000 ) ) ;
#191135=CIRCLE ( 'NONE', #211970, 0.3999999999999926392 ) ;
#191144=DIRECTION ( 'NONE',  ( 0.000000000000000000, -0.2617529984165031243, -0.9651348961777157509 ) ) ;
#191158=DIRECTION ( 'NONE',  ( -1.000000000000000000, 1.809991526360996944E-16, -4.908854824437060108E-17 ) ) ;
#191175=DIRECTION ( 'NONE',  ( -0.000000000000000000, 0.7106264324241465813, -0.7035695228903323661 ) ) ;
#191178=CARTESIAN_POINT ( 'NONE',  ( 22.59999999999999432, 55.86495732666938352, -232.8769840133977880 ) ) ;
#191185=DIRECTION ( 'NONE',  ( 1.000000000000000000, 0.000000000000000000, 0.000000000000000000 ) ) ;
#191233=PLANE ( 'NONE',  #31500 ) ;
#191246=DIRECTION ( 'NONE',  ( 0.000000000000000000, -0.2617529984165031243, -0.9651348961777157509 ) ) ;
#191273=DIRECTION ( 'NONE',  ( 0.000000000000000000, -0.2617529984165031243, -0.9651348961777157509 ) ) ;
#191306=CARTESIAN_POINT ( 'NONE',  ( 21.05000000000000071, 74.92681270650359693, -207.4801605588535551 ) ) ;
#191321=DIRECTION ( 'NONE',  ( 1.000000000000000000, 0.000000000000000000, 0.000000000000000000 ) ) ;
#191332=ORIENTED_EDGE ( 'NONE', *, *, #192868, .F. ) ;
#191336=CIRCLE ( 'NONE', #249759, 0.1000000000000106498 ) ;
#191362=EDGE_CURVE ( 'NONE', #171424, #116117, #66282, .T. ) ;
#191371=CARTESIAN_POINT ( 'NONE',  ( 20.94999999999999929, 82.09643798151613225, -215.4278993322501208 ) ) ;
#191376=LINE ( 'NONE', #53107, #227398 ) ;
#191403=ORIENTED_EDGE ( 'NONE', *, *, #169356, .T. ) ;
#191407=DIRECTION ( 'NONE',  ( 0.000000000000000000, 0.2617529984165432588, 0.9651348961777048707 ) ) ;
#191408=EDGE_CURVE ( 'NONE', #104140, #40848, #12137, .T. ) ;
#191447=AXIS2_PLACEMENT_3D ( 'NONE', #239226, #223501, #3163 ) ;
#191450=EDGE_CURVE ( 'NONE', #56792, #147060, #182993, .T. ) ;
#191475=CARTESIAN_POINT ( 'NONE',  ( 20.94999999999999929, 78.17003882911672008, -228.8770135013149911 ) ) ;
#191502=EDGE_CURVE ( 'NONE', #177022, #76927, #220414, .T. ) ;
#191522=CARTESIAN_POINT ( 'NONE',  ( -22.60000000000080433, 64.10952111376602147, -247.1829669476428251 ) ) ;
#191572=CARTESIAN_POINT ( 'NONE',  ( -18.59999999999999787, 61.57587952878036930, -212.2000740415318774 ) ) ;
#191582=AXIS2_PLACEMENT_3D ( 'NONE', #190050, #90938, #227890 ) ;
#191587=DIRECTION ( 'NONE',  ( 0.000000000000000000, -0.2617529984165152257, -0.9651348961777124202 ) ) ;
#191602=ADVANCED_FACE ( 'NONE', ( #161514 ), #204456, .F. ) ;
#191603=VERTEX_POINT ( 'NONE', #144472 ) ;
#191606=AXIS2_PLACEMENT_3D ( 'NONE', #15536, #95042, #16812 ) ;
#191616=DIRECTION ( 'NONE',  ( -1.000000000000000000, 0.000000000000000000, 0.000000000000000000 ) ) ;
#191622=CIRCLE ( 'NONE', #70993, 0.1000000000000051958 ) ;
#191647=ORIENTED_EDGE ( 'NONE', *, *, #57426, .F. ) ;
#191649=VERTEX_POINT ( 'NONE', #25844 ) ;
#191670=DIRECTION ( 'NONE',  ( 0.000000000000000000, -0.2617529984165152257, -0.9651348961777124202 ) ) ;
#191696=DIRECTION ( 'NONE',  ( 0.000000000000000000, 0.2617529984165031243, 0.9651348961777157509 ) ) ;
#191700=VERTEX_POINT ( 'NONE', #50502 ) ;
#191716=CIRCLE ( 'NONE', #83491, 0.1000000000000124678 ) ;
#191727=DIRECTION ( 'NONE',  ( 0.7071359030027629666, -0.6824253222083883630, 0.1850796971394867152 ) ) ;
#191737=CARTESIAN_POINT ( 'NONE',  ( 19.99999999999998934, 61.54970422893870818, -212.2965875311496688 ) ) ;
#191758=VECTOR ( 'NONE', #108321, 1000.000000000000000 ) ;
#191776=EDGE_LOOP ( 'NONE', ( #171335, #63240, #141116 ) ) ;
#191799=DIRECTION ( 'NONE',  ( 1.000000000000000000, 0.000000000000000000, 0.000000000000000000 ) ) ;
#191809=ORIENTED_EDGE ( 'NONE', *, *, #238439, .T. ) ;
#191843=CARTESIAN_POINT ( 'NONE',  ( -23.15000000000000213, 61.57587952878036219, -212.2000740415318774 ) ) ;
#191847=ORIENTED_EDGE ( 'NONE', *, *, #179237, .T. ) ;
#191885=CARTESIAN_POINT ( 'NONE',  ( 20.94999999999999574, 59.10678033798691189, -225.7992625810339575 ) ) ;
#191892=DIRECTION ( 'NONE',  ( -1.000000000000000000, 0.000000000000000000, 0.000000000000000000 ) ) ;
#191916=ORIENTED_EDGE ( 'NONE', *, *, #156886, .T. ) ;
#191937=VECTOR ( 'NONE', #57453, 1000.000000000000000 ) ;
#191950=ADVANCED_FACE ( 'NONE', ( #244558 ), #112446, .T. ) ;
#192021=DIRECTION ( 'NONE',  ( 1.000000000000000000, 0.000000000000000000, 0.000000000000000000 ) ) ;
#192035=CIRCLE ( 'NONE', #29539, 11.75000000000000533 ) ;
#192043=CARTESIAN_POINT ( 'NONE',  ( -21.05000000000000071, 86.43238724539048690, -209.5644480942280836 ) ) ;
#192068=AXIS2_PLACEMENT_3D ( 'NONE', #52977, #112969, #13866 ) ;
#192071=DIRECTION ( 'NONE',  ( 0.000000000000000000, 0.2617529984165152257, 0.9651348961777124202 ) ) ;
#192072=DIRECTION ( 'NONE',  ( 1.000000000000000000, 0.000000000000000000, 0.000000000000000000 ) ) ;
#192086=CARTESIAN_POINT ( 'NONE',  ( -18.59999999999999787, 78.12133356376091342, -231.3112718935514636 ) ) ;
#192112=EDGE_LOOP ( 'NONE', ( #10428, #116321, #183137, #131203 ) ) ;
#192190=ADVANCED_FACE ( 'NONE', ( #97003 ), #229140, .F. ) ;
#192198=CIRCLE ( 'NONE', #79734, 0.1000000000000124678 ) ;
#192215=ORIENTED_EDGE ( 'NONE', *, *, #120904, .F. ) ;
#192225=EDGE_CURVE ( 'NONE', #148648, #221167, #58420, .T. ) ;
#192287=EDGE_LOOP ( 'NONE', ( #13721, #49904, #30893 ) ) ;
#192302=CARTESIAN_POINT ( 'NONE',  ( 20.85000000000000142, 87.24382154048164750, -206.5725299160771726 ) ) ;
#192303=ORIENTED_EDGE ( 'NONE', *, *, #72032, .T. ) ;
#192331=ORIENTED_EDGE ( 'NONE', *, *, #147262, .F. ) ;
#192350=CARTESIAN_POINT ( 'NONE',  ( -23.15000000000000213, 62.86885547537413288, -207.0505773246641752 ) ) ;
#192354=DIRECTION ( 'NONE',  ( 0.000000000000000000, -0.2617529984165026247, -0.9651348961777158619 ) ) ;
#192359=CARTESIAN_POINT ( 'NONE',  ( 22.50927854361890113, 64.25313177404581211, -247.2214436579493224 ) ) ;
#192383=DIRECTION ( 'NONE',  ( 0.000000000000000000, -0.2617529984164506107, -0.9651348961777299618 ) ) ;
#192493=CYLINDRICAL_SURFACE ( 'NONE', #88992, 0.09999999999999939493 ) ;
#192496=EDGE_CURVE ( 'NONE', #223374, #186212, #108512, .T. ) ;
#192544=CARTESIAN_POINT ( 'NONE',  ( 18.59999999999999432, 72.10920423909969657, -225.0008277277438822 ) ) ;
#192561=DIRECTION ( 'NONE',  ( 0.000000000000000000, -0.9651348961777157509, 0.2617529984165032353 ) ) ;
#192570=DIRECTION ( 'NONE',  ( -1.000000000000000000, 0.000000000000000000, 0.000000000000000000 ) ) ;
#192578=ORIENTED_EDGE ( 'NONE', *, *, #53564, .F. ) ;
#192599=DIRECTION ( 'NONE',  ( 0.000000000000000000, 0.2617529984165055668, 0.9651348961777150848 ) ) ;
#192638=CARTESIAN_POINT ( 'NONE',  ( 21.08489834409762409, 60.21194861419059663, -221.1552854090853657 ) ) ;
#192648=ORIENTED_EDGE ( 'NONE', *, *, #67164, .F. ) ;
#192657=DIRECTION ( 'NONE',  ( 1.000000000000000000, 0.000000000000000000, 0.000000000000000000 ) ) ;
#192690=CARTESIAN_POINT ( 'NONE',  ( -21.12844524849339223, 57.69819045127058388, -226.1158383967348016 ) ) ;
#192701=VERTEX_POINT ( 'NONE', #88394 ) ;
#192705=DIRECTION ( 'NONE',  ( 1.875376730785737966E-16, 0.9651348961777157509, -0.2617529984165031243 ) ) ;
#192710=ORIENTED_EDGE ( 'NONE', *, *, #177769, .F. ) ;
#192729=EDGE_CURVE ( 'NONE', #108241, #4288, #200280, .T. ) ;
#192769=ORIENTED_EDGE ( 'NONE', *, *, #175706, .F. ) ;
#192780=AXIS2_PLACEMENT_3D ( 'NONE', #204059, #25446, #163666 ) ;
#192806=ORIENTED_EDGE ( 'NONE', *, *, #147768, .T. ) ;
#192830=DIRECTION ( 'NONE',  ( 1.000000000000000000, 0.000000000000000000, 0.000000000000000000 ) ) ;
#192842=EDGE_CURVE ( 'NONE', #189967, #163063, #38727, .T. ) ;
#192860=CARTESIAN_POINT ( 'NONE',  ( -18.50000000000000000, 70.17424292862648372, -198.1782849070719124 ) ) ;
#192868=EDGE_CURVE ( 'NONE', #248032, #58200, #175677, .T. ) ;
#192894=AXIS2_PLACEMENT_3D ( 'NONE', #113313, #91188, #174630 ) ;
#192896=DIRECTION ( 'NONE',  ( 2.952720810173289112E-16, 0.9651348961777157509, -0.2617529984165031243 ) ) ;
#192914=AXIS2_PLACEMENT_3D ( 'NONE', #89653, #187510, #124954 ) ;
#192917=ORIENTED_EDGE ( 'NONE', *, *, #34645, .T. ) ;
#192921=CARTESIAN_POINT ( 'NONE',  ( 20.94999999999999929, 76.00000000001126921, -203.5231074845248997 ) ) ;
#192922=DIRECTION ( 'NONE',  ( 0.000000000000000000, 0.2617529984165031243, 0.9651348961777157509 ) ) ;
#192927=ORIENTED_EDGE ( 'NONE', *, *, #159583, .T. ) ;
#192941=ORIENTED_EDGE ( 'NONE', *, *, #40273, .T. ) ;
#193002=ORIENTED_EDGE ( 'NONE', *, *, #42364, .T. ) ;
#193016=AXIS2_PLACEMENT_3D ( 'NONE', #188702, #89588, #10068 ) ;
#193028=CARTESIAN_POINT ( 'NONE',  ( 23.15000000000000213, 86.30329675166747450, -209.4258251677035787 ) ) ;
#193068=DIRECTION ( 'NONE',  ( 0.000000000000000000, 0.2617529984164980728, 0.9651348961777171942 ) ) ;
#193069=EDGE_CURVE ( 'NONE', #239682, #251232, #128525, .T. ) ;
#193081=AXIS2_PLACEMENT_3D ( 'NONE', #158510, #60643, #224545 ) ;
#193142=VERTEX_POINT ( 'NONE', #167672 ) ;
#193179=LINE ( 'NONE', #11980, #220960 ) ;
#193203=VERTEX_POINT ( 'NONE', #177932 ) ;
#193211=VERTEX_POINT ( 'NONE', #55359 ) ;
#193226=EDGE_LOOP ( 'NONE', ( #69084, #142339, #167705, #16186 ) ) ;
#193261=AXIS2_PLACEMENT_3D ( 'NONE', #82831, #42453, #119441 ) ;
#193271=ORIENTED_EDGE ( 'NONE', *, *, #1803, .F. ) ;
#193322=AXIS2_PLACEMENT_3D ( 'NONE', #18337, #179994, #159160 ) ;
#193335=DIRECTION ( 'NONE',  ( -0.000000000000000000, -0.2617529984165031243, -0.9651348961777157509 ) ) ;
#193339=ORIENTED_EDGE ( 'NONE', *, *, #76111, .T. ) ;
#193342=DIRECTION ( 'NONE',  ( 1.000000000000000000, 0.000000000000000000, 0.000000000000000000 ) ) ;
#193361=CARTESIAN_POINT ( 'NONE',  ( 20.85000000000000142, 64.75617845954087670, -200.4736850529726269 ) ) ;
#193396=B_SPLINE_CURVE_WITH_KNOTS ( 'NONE', 3,
 ( #94233, #9563, #168697, #248187, #91673, #228640 ),
 .UNSPECIFIED., .F., .F.,
 ( 4, 2, 4 ),
 ( 0.000000000000000000, 0.0001891491689349576852, 0.0003782983378699153704 ),
 .UNSPECIFIED. ) ;
#193401=ORIENTED_EDGE ( 'NONE', *, *, #111278, .F. ) ;
#193418=CIRCLE ( 'NONE', #10424, 0.1000000000000124678 ) ;
#193426=ORIENTED_EDGE ( 'NONE', *, *, #153904, .F. ) ;
#193460=CARTESIAN_POINT ( 'NONE',  ( -20.94999999999999929, 68.48451787451661232, -224.2224406095231757 ) ) ;
#193483=ORIENTED_EDGE ( 'NONE', *, *, #75342, .T. ) ;
#193485=FACE_OUTER_BOUND ( 'NONE', #56040, .T. ) ;
#193489=ORIENTED_EDGE ( 'NONE', *, *, #88754, .T. ) ;
#193527=DIRECTION ( 'NONE',  ( 0.000000000000000000, -0.2617529984165031243, -0.9651348961777158619 ) ) ;
#193551=CARTESIAN_POINT ( 'NONE',  ( -23.15000000000000213, 76.00000000001126921, -203.5231074845248997 ) ) ;
#193573=ORIENTED_EDGE ( 'NONE', *, *, #119771, .T. ) ;
#193588=DIRECTION ( 'NONE',  ( 0.000000000000000000, -0.9651348961777157509, 0.2617529984165031243 ) ) ;
#193601=ORIENTED_EDGE ( 'NONE', *, *, #213114, .F. ) ;
#193608=ORIENTED_EDGE ( 'NONE', *, *, #37874, .F. ) ;
#193615=VECTOR ( 'NONE', #164974, 1000.000000000000000 ) ;
#193657=DIRECTION ( 'NONE',  ( 0.000000000000000000, 0.2617529984165152257, 0.9651348961777124202 ) ) ;
#193658=EDGE_CURVE ( 'NONE', #94125, #66196, #196004, .T. ) ;
#193664=DIRECTION ( 'NONE',  ( 2.952720810173289112E-16, 0.9651348961777174162, -0.2617529984164969070 ) ) ;
#193681=AXIS2_PLACEMENT_3D ( 'NONE', #238359, #141822, #23196 ) ;
#193698=CARTESIAN_POINT ( 'NONE',  ( 21.14999999999999858, 67.32778804267617545, -235.8813018063200388 ) ) ;
#193729=CARTESIAN_POINT ( 'NONE',  ( 22.49999999999999645, 55.96597777900657888, -232.8853806925633307 ) ) ;
#193779=AXIS2_PLACEMENT_3D ( 'NONE', #130777, #252005, #189480 ) ;
#193796=DIRECTION ( 'NONE',  ( -0.000000000000000000, 0.6922311945860614157, 0.7216758089626911232 ) ) ;
#193797=DIRECTION ( 'NONE',  ( 0.000000000000000000, -0.2617529984165031243, -0.9651348961777158619 ) ) ;
#193798=VERTEX_POINT ( 'NONE', #182761 ) ;
#193809=EDGE_CURVE ( 'NONE', #208387, #16660, #175195, .T. ) ;
#193812=CARTESIAN_POINT ( 'NONE',  ( 18.49999999999999289, 67.49463558145296815, -195.5618716440587548 ) ) ;
#193835=AXIS2_PLACEMENT_3D ( 'NONE', #8713, #226444, #88214 ) ;
#193845=ORIENTED_EDGE ( 'NONE', *, *, #174601, .T. ) ;
#193858=DIRECTION ( 'NONE',  ( 0.000000000000000000, -0.3848449534832868446, -0.9229812358755982160 ) ) ;
#193922=VERTEX_POINT ( 'NONE', #243991 ) ;
#193932=TOROIDAL_SURFACE ( 'NONE', #148131, 11.90000000000000213, 0.1000000000000000056 ) ;
#193939=CARTESIAN_POINT ( 'NONE',  ( 21.14999999999999503, 56.01362831242965967, -232.7091905853083347 ) ) ;
#193947=ORIENTED_EDGE ( 'NONE', *, *, #190138, .F. ) ;
#193953=DIRECTION ( 'NONE',  ( 0.000000000000000000, -0.9667078373770112698, -0.2558827019434132821 ) ) ;
#193954=EDGE_CURVE ( 'NONE', #252254, #249301, #8546, .T. ) ;
#193961=ORIENTED_EDGE ( 'NONE', *, *, #91758, .F. ) ;
#193978=CARTESIAN_POINT ( 'NONE',  ( -21.05000000000000071, 57.66663670110953177, -226.2321832927624996 ) ) ;
#193987=DIRECTION ( 'NONE',  ( 1.000000000000000000, 0.000000000000000000, 0.000000000000000000 ) ) ;
#193988=VERTEX_POINT ( 'NONE', #193028 ) ;
#194004=TOROIDAL_SURFACE ( 'NONE', #10651, 11.65000000000000036, 0.1000000000000000056 ) ;
#194011=CARTESIAN_POINT ( 'NONE',  ( -23.25000000000000000, 86.52890073500824997, -209.5906233940697234 ) ) ;
#194019=CIRCLE ( 'NONE', #110607, 0.4999999999999978351 ) ;
#194068=( BOUNDED_SURFACE ( )  B_SPLINE_SURFACE ( 3, 2, ( 
 ( #203965, #106134, #4475 ),
 ( #65746, #44906, #25361 ),
 ( #222224, #224805, #29235 ),
 ( #223517, #145266, #241810 ),
 ( #246940, #128303, #183140 ),
 ( #166169, #63162, #125714 ) ),
 .UNSPECIFIED., .F., .F., .F. ) 
 B_SPLINE_SURFACE_WITH_KNOTS ( ( 4, 2, 4 ),
 ( 3, 3 ),
 ( 0.0001792624049599400582, 0.0003686986002124377883, 0.0005581347954649355184 ),
 ( 0.000000000000000000, 1.000000000000000000 ),
 .UNSPECIFIED. ) 
 GEOMETRIC_REPRESENTATION_ITEM ( )  RATIONAL_B_SPLINE_SURFACE ( (
 ( 1.000000000000000000, 0.9238795325112714174, 1.000000000000000000),
 ( 1.000000000000000000, 0.9229318695242134662, 1.000000000000000000),
 ( 1.000000000000000000, 0.8926288119225641582, 1.000000000000000000),
 ( 1.000000000000000000, 0.8123777807277360319, 1.000000000000000000),
 ( 1.000000000000000000, 0.7629087100926377207, 1.000000000000000000),
 ( 1.000000000000000000, 0.7071067811865352493, 1.000000000000000000) ) ) 
 REPRESENTATION_ITEM ( '' )  SURFACE ( )  );
#194074=CARTESIAN_POINT ( 'NONE',  ( -18.59999999999999787, 71.93512633425886804, -225.1442869522136334 ) ) ;
#194078=AXIS2_PLACEMENT_3D ( 'NONE', #124394, #169974, #203910 ) ;
#194080=CARTESIAN_POINT ( 'NONE',  ( -22.45305610364635740, 64.25313205997782973, -247.2214437328673569 ) ) ;
#194121=CARTESIAN_POINT ( 'NONE',  ( 18.49999999999996803, 70.15623657602074559, -198.0563205710787713 ) ) ;
#194127=DIRECTION ( 'NONE',  ( 0.000000000000000000, 0.2617529984165152257, 0.9651348961777124202 ) ) ;
#194139=EDGE_CURVE ( 'NONE', #206482, #66196, #117063, .T. ) ;
#194157=CARTESIAN_POINT ( 'NONE',  ( 20.44999100639885015, 59.18650678360199890, -225.6339461820924157 ) ) ;
#194171=EDGE_CURVE ( 'NONE', #47300, #114917, #25485, .T. ) ;
#194202=AXIS2_PLACEMENT_3D ( 'NONE', #109507, #92513, #73000 ) ;
#194221=VERTEX_POINT ( 'NONE', #3806 ) ;
#194233=DIRECTION ( 'NONE',  ( 0.000000000000000000, 0.9229812358756199764, -0.3848449534832346086 ) ) ;
#194243=DIRECTION ( 'NONE',  ( 1.000000000000000000, -2.849773892568378313E-16, 7.728835255496647986E-17 ) ) ;
#194257=CARTESIAN_POINT ( 'NONE',  ( 23.14999999999998437, 67.23127455305841238, -235.8551265064783991 ) ) ;
#194280=CARTESIAN_POINT ( 'NONE',  ( -23.15000000000000213, 75.47649400317826007, -205.4533772768803317 ) ) ;
#194317=CIRCLE ( 'NONE', #98554, 0.09999999999999939493 ) ;
#194342=AXIS2_PLACEMENT_3D ( 'NONE', #253520, #149322, #231418 ) ;
#194381=CARTESIAN_POINT ( 'NONE',  ( -21.07971444708686093, 65.48967103324704908, -241.9412416822181058 ) ) ;
#194382=AXIS2_PLACEMENT_3D ( 'NONE', #114029, #248424, #110183 ) ;
#194385=DIRECTION ( 'NONE',  ( 0.000000000000000000, 0.2558827019433787542, -0.9667078373770204847 ) ) ;
#194408=ORIENTED_EDGE ( 'NONE', *, *, #198071, .F. ) ;
#194435=LINE ( 'NONE', #90151, #189751 ) ;
#194450=EDGE_CURVE ( 'NONE', #232566, #176771, #25663, .T. ) ;
#194458=CIRCLE ( 'NONE', #181951, 0.09999999999999939493 ) ;
#194465=EDGE_LOOP ( 'NONE', ( #89623, #53956, #110541, #227046 ) ) ;
#194506=EDGE_CURVE ( 'NONE', #201773, #244346, #125610, .T. ) ;
#194529=VERTEX_POINT ( 'NONE', #53708 ) ;
#194539=DIRECTION ( 'NONE',  ( 0.000000000000000000, 0.2617529984165033463, 0.9651348961777157509 ) ) ;
#194545=DIRECTION ( 'NONE',  ( 1.000000000000000000, 0.000000000000000000, 0.000000000000000000 ) ) ;
#194556=DIRECTION ( 'NONE',  ( 1.000000000000000000, 0.000000000000000000, 0.000000000000000000 ) ) ;
#194568=EDGE_LOOP ( 'NONE', ( #124321, #217737, #63188, #37402 ) ) ;
#194603=FACE_OUTER_BOUND ( 'NONE', #52699, .T. ) ;
#194604=TOROIDAL_SURFACE ( 'NONE', #82111, 11.65000000000000036, 0.1000000000000000056 ) ;
#194638=CARTESIAN_POINT ( 'NONE',  ( 23.14999999999999503, 59.16775194334852017, -221.0793150863668473 ) ) ;
#194645=VERTEX_POINT ( 'NONE', #133993 ) ;
#194648=ORIENTED_EDGE ( 'NONE', *, *, #5715, .T. ) ;
#194650=DIRECTION ( 'NONE',  ( 0.000000000000000000, 0.2617529984165031243, 0.9651348961777157509 ) ) ;
#194693=DIRECTION ( 'NONE',  ( -1.000000000000000000, -0.000000000000000000, -0.000000000000000000 ) ) ;
#194697=ORIENTED_EDGE ( 'NONE', *, *, #63824, .T. ) ;
#194724=DIRECTION ( 'NONE',  ( 0.000000000000000000, 0.9651348961777158619, -0.2617529984165031243 ) ) ;
#194725=CIRCLE ( 'NONE', #207362, 11.80000000000000604 ) ;
#194747=CIRCLE ( 'NONE', #244594, 0.1000000000000124678 ) ;
#194751=CARTESIAN_POINT ( 'NONE',  ( -23.25000000000000000, 52.91185528119410009, -244.1460391050142960 ) ) ;
#194754=CARTESIAN_POINT ( 'NONE',  ( -18.59999999999999787, 76.00000000001126921, -203.5231074845248997 ) ) ;
#194762=ORIENTED_EDGE ( 'NONE', *, *, #58696, .T. ) ;
#194775=CARTESIAN_POINT ( 'NONE',  ( -20.93284271247462058, 62.82351852614505106, -207.2177435922979214 ) ) ;
#194785=FACE_OUTER_BOUND ( 'NONE', #151161, .T. ) ;
#194789=DIRECTION ( 'NONE',  ( 1.000000000000000000, -7.049440681616512959E-16, 1.911869773728117674E-16 ) ) ;
#194812=CYLINDRICAL_SURFACE ( 'NONE', #57801, 0.09999999999999939493 ) ;
#194820=DIRECTION ( 'NONE',  ( 0.000000000000000000, -0.2617529984165031243, -0.9651348961777157509 ) ) ;
#194822=CARTESIAN_POINT ( 'NONE',  ( 23.15000000000000213, 86.43238724539048690, -209.5644480942280836 ) ) ;
#194828=FACE_OUTER_BOUND ( 'NONE', #112670, .T. ) ;
#194833=ORIENTED_EDGE ( 'NONE', *, *, #100567, .F. ) ;
#194866=FACE_OUTER_BOUND ( 'NONE', #116141, .T. ) ;
#194875=CARTESIAN_POINT ( 'NONE',  ( 21.07888907270776002, 60.07907005675570389, -221.2527070780202223 ) ) ;
#194905=EDGE_CURVE ( 'NONE', #166406, #69945, #42601, .T. ) ;
#194906=DIRECTION ( 'NONE',  ( 0.000000000000000000, 0.2617529984165036239, 0.9651348961777156399 ) ) ;
#194908=DIRECTION ( 'NONE',  ( -0.000000000000000000, 0.2617529984165037349, 0.9651348961777156399 ) ) ;
#194923=CARTESIAN_POINT ( 'NONE',  ( 21.14999999999999858, 65.51923798433685420, -242.1677427744926092 ) ) ;
#194926=CARTESIAN_POINT ( 'NONE',  ( -23.15000000000000213, 76.00000000001126921, -203.5231074845248997 ) ) ;
#194930=B_SPLINE_CURVE_WITH_KNOTS ( 'NONE', 3,
 ( #174896, #58714, #238664, #237383, #18330, #1316, #118736, #217791, #37921, #255604 ),
 .UNSPECIFIED., .F., .F.,
 ( 4, 3, 3, 4 ),
 ( 0.000000000000000000, 3.394313611810855516E-05, 6.779740500699835842E-05, 0.0001049857339142647140 ),
 .UNSPECIFIED. ) ;
#194936=CARTESIAN_POINT ( 'NONE',  ( 22.50000000000000000, 67.23127455305841238, -235.8551265064783991 ) ) ;
#194952=EDGE_CURVE ( 'NONE', #76927, #194221, #67295, .T. ) ;
#194969=ORIENTED_EDGE ( 'NONE', *, *, #254264, .F. ) ;
#194971=AXIS2_PLACEMENT_3D ( 'NONE', #146244, #223375, #44763 ) ;
#194977=SPHERICAL_SURFACE ( 'NONE', #252574, 0.1000000000000000056 ) ;
#194983=CARTESIAN_POINT ( 'NONE',  ( -18.47079683080326262, 78.23347366783373502, -231.4733536058482173 ) ) ;
#194995=CARTESIAN_POINT ( 'NONE',  ( 20.94999999999999929, 82.48249193998721296, -215.5326005316167084 ) ) ;
#194997=B_SPLINE_CURVE_WITH_KNOTS ( 'NONE', 3,
 ( #231428, #31954, #115308, #129741, #133587, #191030, #252245, #194875, #250952, #90598, #214406, #14948, #175322, #91893, #51459, #72359 ),
 .UNSPECIFIED., .F., .F.,
 ( 4, 3, 3, 3, 3, 4 ),
 ( 0.000000000000000000, 3.357088238233777529E-05, 6.714213034887866539E-05, 0.0001007408646121051249, 0.0001343627955914316685, 0.0001573956632896109326 ),
 .UNSPECIFIED. ) ;
#195016=CIRCLE ( 'NONE', #153347, 0.1000000000000124678 ) ;
#195018=AXIS2_PLACEMENT_3D ( 'NONE', #82840, #162441, #239397 ) ;
#195028=CARTESIAN_POINT ( 'NONE',  ( -22.39999999999999858, 65.09550114356427741, -243.3481044654562879 ) ) ;
#195030=ORIENTED_EDGE ( 'NONE', *, *, #253638, .T. ) ;
#195073=DIRECTION ( 'NONE',  ( 0.000000000000000000, 0.9651348961777379554, -0.2617529984164210233 ) ) ;
#195074=CARTESIAN_POINT ( 'NONE',  ( 20.94999999999999929, 87.19425987394825484, -209.6674621343692024 ) ) ;
#195119=ORIENTED_EDGE ( 'NONE', *, *, #206112, .T. ) ;
#195145=CIRCLE ( 'NONE', #224340, 0.1999999999999945155 ) ;
#195146=ORIENTED_EDGE ( 'NONE', *, *, #22118, .F. ) ;
#195161=EDGE_CURVE ( 'NONE', #204435, #197715, #96730, .T. ) ;
#195207=EDGE_LOOP ( 'NONE', ( #146874, #220310, #175776, #185249 ) ) ;
#195217=EDGE_LOOP ( 'NONE', ( #146176, #246969, #197177, #85359, #151285 ) ) ;
#195218=VERTEX_POINT ( 'NONE', #116690 ) ;
#195223=CARTESIAN_POINT ( 'NONE',  ( -23.15000000000000213, 86.27712145182582049, -209.5223386573213702 ) ) ;
#195258=ORIENTED_EDGE ( 'NONE', *, *, #122772, .T. ) ;
#195272=TOROIDAL_SURFACE ( 'NONE', #74482, 11.70000000000000639, 0.1000000000000000056 ) ;
#195320=CARTESIAN_POINT ( 'NONE',  ( 20.94999999999999929, 61.00122447389660607, -225.2976766370351527 ) ) ;
#195353=CIRCLE ( 'NONE', #237025, 0.1000000000000016154 ) ;
#195354=ORIENTED_EDGE ( 'NONE', *, *, #227017, .T. ) ;
#195371=DIRECTION ( 'NONE',  ( -0.000000000000000000, 0.2617529984165031243, 0.9651348961777157509 ) ) ;
#195408=DIRECTION ( 'NONE',  ( 1.000000000000000000, 0.000000000000000000, 0.000000000000000000 ) ) ;
#195474=CIRCLE ( 'NONE', #95483, 0.09999999999999543976 ) ;
#195476=DIRECTION ( 'NONE',  ( -2.840903330521632269E-16, -0.7106264324241465813, 0.7035695228903323661 ) ) ;
#195489=ORIENTED_EDGE ( 'NONE', *, *, #59342, .T. ) ;
#195508=DIRECTION ( 'NONE',  ( 0.000000000000000000, -0.2617529984165152257, -0.9651348961777124202 ) ) ;
#195535=FACE_OUTER_BOUND ( 'NONE', #90845, .T. ) ;
#195539=AXIS2_PLACEMENT_3D ( 'NONE', #236166, #211474, #53679 ) ;
#195550=FACE_OUTER_BOUND ( 'NONE', #98858, .T. ) ;
#195573=CARTESIAN_POINT ( 'NONE',  ( -20.54999999999999716, 65.79629777212066699, -213.4483007241822747 ) ) ;
#195604=ORIENTED_EDGE ( 'NONE', *, *, #100567, .T. ) ;
#195618=EDGE_CURVE ( 'NONE', #185762, #150222, #57687, .T. ) ;
#195624=ORIENTED_EDGE ( 'NONE', *, *, #234518, .F. ) ;
#195635=DIRECTION ( 'NONE',  ( 1.000000000000000000, 0.000000000000000000, 0.000000000000000000 ) ) ;
#195638=CIRCLE ( 'NONE', #128985, 0.09999999999999939493 ) ;
#195648=DIRECTION ( 'NONE',  ( 0.000000000000000000, 0.9651348961777156399, -0.2617529984165037349 ) ) ;
#195748=DIRECTION ( 'NONE',  ( 0.000000000000000000, 0.2617529984165152257, 0.9651348961777124202 ) ) ;
#195754=DIRECTION ( 'NONE',  ( -6.938893903907222856E-15, -0.9651348961777158619, 0.2617529984165028467 ) ) ;
#195781=FACE_OUTER_BOUND ( 'NONE', #66808, .T. ) ;
#195782=ADVANCED_FACE ( 'NONE', ( #120287 ), #221987, .T. ) ;
#195818=EDGE_CURVE ( 'NONE', #176136, #121787, #217901, .T. ) ;
#195821=ORIENTED_EDGE ( 'NONE', *, *, #40804, .T. ) ;
#195835=CYLINDRICAL_SURFACE ( 'NONE', #49623, 0.1000000000000124678 ) ;
#195838=CARTESIAN_POINT ( 'NONE',  ( -20.85000000000000142, 70.29876110920605470, -198.0544810472949564 ) ) ;
#195879=EDGE_CURVE ( 'NONE', #229929, #52, #100647, .T. ) ;
#195887=ADVANCED_FACE ( 'NONE', ( #180234 ), #97073, .T. ) ;
#195918=CARTESIAN_POINT ( 'NONE',  ( 18.49999999999998934, 66.47189219944506533, -213.6315278230738102 ) ) ;
#195920=ORIENTED_EDGE ( 'NONE', *, *, #136189, .F. ) ;
#195924=CARTESIAN_POINT ( 'NONE',  ( -20.94999999999999929, 70.15854073567089699, -198.1993227616376885 ) ) ;
#195925=ORIENTED_EDGE ( 'NONE', *, *, #53744, .T. ) ;
#195952=CARTESIAN_POINT ( 'NONE',  ( -20.05000000000000426, 61.53642629385834795, -221.5144953033309321 ) ) ;
#195985=ORIENTED_EDGE ( 'NONE', *, *, #165170, .F. ) ;
#196003=ORIENTED_EDGE ( 'NONE', *, *, #195818, .F. ) ;
#196004=CIRCLE ( 'NONE', #12848, 0.09999999999999939493 ) ;
#196011=CARTESIAN_POINT ( 'NONE',  ( -18.59999999999999787, 59.07123845373075710, -221.0531397865252075 ) ) ;
#196012=B_SPLINE_CURVE_WITH_KNOTS ( 'NONE', 3,
 ( #29921, #229393, #67738, #66454, #148566, #106847, #187706, #168168, #145980, #147270, #183832, #246379, #70342, #207269, #226805, #169448, #228110, #208552, #48165 ),
 .UNSPECIFIED., .F., .F.,
 ( 4, 3, 3, 3, 3, 3, 4 ),
 ( 0.000000000000000000, 7.110282409889993145E-05, 0.0001508797727291377874, 0.0002027344179858592635, 0.0002343294522349093773, 0.0002454816334821335877, 0.0002619873080085596676 ),
 .UNSPECIFIED. ) ;
#196026=DIRECTION ( 'NONE',  ( -1.000000000000000000, -0.000000000000000000, 0.000000000000000000 ) ) ;
#196049=ORIENTED_EDGE ( 'NONE', *, *, #231296, .T. ) ;
#196056=DIRECTION ( 'NONE',  ( 2.978066053179066765E-16, 0.9651348961777157509, -0.2617529984165031243 ) ) ;
#196098=CARTESIAN_POINT ( 'NONE',  ( 20.84999999999999787, 62.84855743180811771, -207.1254202119976640 ) ) ;
#196106=AXIS2_PLACEMENT_3D ( 'NONE', #151657, #116364, #92920 ) ;
#196114=LINE ( 'NONE', #138661, #18226 ) ;
#196154=CYLINDRICAL_SURFACE ( 'NONE', #120471, 2.000000000000013323 ) ;
#196171=EDGE_CURVE ( 'NONE', #167923, #147541, #222537, .T. ) ;
#196186=CARTESIAN_POINT ( 'NONE',  ( 20.94999999999999929, 76.00000000001126921, -203.5231074845248997 ) ) ;
#196196=ORIENTED_EDGE ( 'NONE', *, *, #67790, .T. ) ;
#196206=DIRECTION ( 'NONE',  ( -3.890533409366484652E-14, 0.3848449534832963370, 0.9229812358755945523 ) ) ;
#196221=DIRECTION ( 'NONE',  ( 2.879366945564059217E-14, 0.9118278131605125347, -0.4105728183244932161 ) ) ;
#196231=CARTESIAN_POINT ( 'NONE',  ( -18.46946985241241279, 78.23782832475592386, -231.6011469542054897 ) ) ;
#196249=TOROIDAL_SURFACE ( 'NONE', #225457, 0.2000000000000000111, 0.1000000000000000056 ) ;
#196269=EDGE_CURVE ( 'NONE', #206711, #217493, #52899, .T. ) ;
#196286=CARTESIAN_POINT ( 'NONE',  ( 22.59066674512239814, 55.88295497714577920, -232.8089693692780600 ) ) ;
#196318=AXIS2_PLACEMENT_3D ( 'NONE', #105417, #83297, #44215 ) ;
#196325=ORIENTED_EDGE ( 'NONE', *, *, #145239, .F. ) ;
#196334=DIRECTION ( 'NONE',  ( 0.000000000000000000, 0.2617529984164955192, 0.9651348961777177493 ) ) ;
#196351=ORIENTED_EDGE ( 'NONE', *, *, #55190, .T. ) ;
#196357=EDGE_CURVE ( 'NONE', #71652, #97513, #247811, .T. ) ;
#196361=CARTESIAN_POINT ( 'NONE',  ( 22.45301702632625762, 64.16722595661912010, -247.0947660219591739 ) ) ;
#196406=CARTESIAN_POINT ( 'NONE',  ( 20.12500000000000355, 59.40384239514754938, -225.5881082859534956 ) ) ;
#196410=AXIS2_PLACEMENT_3D ( 'NONE', #142307, #86164, #44514 ) ;
#196453=CARTESIAN_POINT ( 'NONE',  ( -20.94999999999999929, 79.03126467873600802, -235.8703919547671717 ) ) ;
#196458=ORIENTED_EDGE ( 'NONE', *, *, #170606, .T. ) ;
#196484=DIRECTION ( 'NONE',  ( 0.000000000000000000, -0.9651348961777157509, 0.2617529984165031243 ) ) ;
#196485=CYLINDRICAL_SURFACE ( 'NONE', #133217, 0.1000000000000124678 ) ;
#196502=ORIENTED_EDGE ( 'NONE', *, *, #74771, .T. ) ;
#196536=DIRECTION ( 'NONE',  ( 0.000000000000000000, -0.4558084472153119959, 0.8900778951570285091 ) ) ;
#196558=DIRECTION ( 'NONE',  ( 0.000000000000000000, 0.9651348961777148627, -0.2617529984165062329 ) ) ;
#196567=FACE_OUTER_BOUND ( 'NONE', #232063, .T. ) ;
#196596=ADVANCED_FACE ( 'NONE', ( #211706 ), #188266, .T. ) ;
#196625=CARTESIAN_POINT ( 'NONE',  ( 20.94999999999999929, 62.98048128140158752, -207.0210305352945568 ) ) ;
#196626=LINE ( 'NONE', #17988, #93245 ) ;
#196629=DIRECTION ( 'NONE',  ( 0.000000000000000000, 0.2617529984165055668, 0.9651348961777149738 ) ) ;
#196654=CARTESIAN_POINT ( 'NONE',  ( -20.54999999999999716, 82.09643798151613225, -215.4278993322501208 ) ) ;
#196677=CARTESIAN_POINT ( 'NONE',  ( 19.97071067811864609, 62.39759438041176765, -208.9001066625100123 ) ) ;
#196684=DIRECTION ( 'NONE',  ( 0.000000000000000000, -0.2617529984165032908, -0.9651348961777156399 ) ) ;
#196699=AXIS2_PLACEMENT_3D ( 'NONE', #253743, #34302, #53838 ) ;
#196727=ORIENTED_EDGE ( 'NONE', *, *, #52260, .T. ) ;
#196733=EDGE_CURVE ( 'NONE', #212838, #211733, #142932, .T. ) ;
#196751=CARTESIAN_POINT ( 'NONE',  ( 19.58285714285715073, 59.20544293262641133, -225.7731470885128715 ) ) ;
#196764=ORIENTED_EDGE ( 'NONE', *, *, #192225, .F. ) ;
#196776=CARTESIAN_POINT ( 'NONE',  ( -22.59066674512246209, 55.88295497714577920, -232.8089693692780600 ) ) ;
#196785=ORIENTED_EDGE ( 'NONE', *, *, #62653, .T. ) ;
#196786=ORIENTED_EDGE ( 'NONE', *, *, #55339, .T. ) ;
#196804=DIRECTION ( 'NONE',  ( -1.000000000000000000, -0.000000000000000000, -0.000000000000000000 ) ) ;
#196826=PLANE ( 'NONE',  #91626 ) ;
#196845=CARTESIAN_POINT ( 'NONE',  ( -20.54999999999999716, 68.76258920191057200, -222.5680764032308048 ) ) ;
#196853=CARTESIAN_POINT ( 'NONE',  ( -18.59999999999999787, 72.02722222756958104, -225.1832529173024398 ) ) ;
#196860=DIRECTION ( 'NONE',  ( 0.000000000000000000, -0.2617529984164856383, -0.9651348961777204138 ) ) ;
#196874=ORIENTED_EDGE ( 'NONE', *, *, #142678, .T. ) ;
#196877=AXIS2_PLACEMENT_3D ( 'NONE', #249446, #129491, #190777 ) ;
#196917=EDGE_LOOP ( 'NONE', ( #200237, #12479, #1225, #231826, #187318 ) ) ;
#196923=CARTESIAN_POINT ( 'NONE',  ( 21.05000000000000071, 65.63213158188987961, -242.1335211407336772 ) ) ;
#196965=ORIENTED_EDGE ( 'NONE', *, *, #138912, .T. ) ;
#196980=CARTESIAN_POINT ( 'NONE',  ( -20.85000000000000142, 79.19526988099229925, -196.1889237952725296 ) ) ;
#196996=TOROIDAL_SURFACE ( 'NONE', #121996, 0.2000000000000000111, 0.1000000000000000056 ) ;
#197030=ADVANCED_FACE ( 'NONE', ( #108431 ), #70617, .F. ) ;
#197045=CARTESIAN_POINT ( 'NONE',  ( -22.39999999999999858, 64.18196446391819165, -247.0985338183330668 ) ) ;
#197059=AXIS2_PLACEMENT_3D ( 'NONE', #200884, #40573, #137064 ) ;
#197069=VERTEX_POINT ( 'NONE', #187974 ) ;
#197111=ADVANCED_FACE ( 'NONE', ( #71884 ), #226318, .T. ) ;
#197122=DIRECTION ( 'NONE',  ( 0.000000000000000000, 0.2617529984165031243, 0.9651348961777157509 ) ) ;
#197128=CARTESIAN_POINT ( 'NONE',  ( 18.59999999999998721, 70.29876110920605470, -198.0544810472949564 ) ) ;
#197133=ORIENTED_EDGE ( 'NONE', *, *, #62636, .T. ) ;
#197153=DIRECTION ( 'NONE',  ( 0.000000000000000000, 0.2617529984165031243, 0.9651348961777157509 ) ) ;
#197155=ORIENTED_EDGE ( 'NONE', *, *, #31581, .T. ) ;
#197177=ORIENTED_EDGE ( 'NONE', *, *, #161339, .F. ) ;
#197190=DIRECTION ( 'NONE',  ( -0.000000000000000000, -0.9651348961777157509, 0.2617529984165031243 ) ) ;
#197211=DIRECTION ( 'NONE',  ( 1.000000000000000000, 0.000000000000000000, 0.000000000000000000 ) ) ;
#197224=ORIENTED_EDGE ( 'NONE', *, *, #38212, .T. ) ;
#197242=CARTESIAN_POINT ( 'NONE',  ( 19.75857864376269646, 62.46583972339645641, -208.9186153945276487 ) ) ;
#197256=AXIS2_PLACEMENT_3D ( 'NONE', #142009, #22088, #83298 ) ;
#197285=DIRECTION ( 'NONE',  ( 0.000000000000000000, 0.2617529984165059553, 0.9651348961777148627 ) ) ;
#197331=ADVANCED_FACE ( 'NONE', ( #10319 ), #226497, .T. ) ;
#197332=ORIENTED_EDGE ( 'NONE', *, *, #143636, .F. ) ;
#197341=CARTESIAN_POINT ( 'NONE',  ( 21.14999999999999503, 64.25313205997782973, -247.2214437328673853 ) ) ;
#197375=ORIENTED_EDGE ( 'NONE', *, *, #226547, .T. ) ;
#197385=DIRECTION ( 'NONE',  ( 0.000000000000000000, 0.9651348961777157509, -0.2617529984165031243 ) ) ;
#197386=DIRECTION ( 'NONE',  ( -1.000000000000000000, -0.000000000000000000, 0.000000000000000000 ) ) ;
#197390=AXIS2_PLACEMENT_3D ( 'NONE', #82087, #100366, #5109 ) ;
#197401=CARTESIAN_POINT ( 'NONE',  ( -22.50000000000000000, 64.08545097430041437, -247.0723585184913986 ) ) ;
#197439=ORIENTED_EDGE ( 'NONE', *, *, #102791, .F. ) ;
#197449=EDGE_CURVE ( 'NONE', #223936, #100463, #106817, .T. ) ;
#197464=CARTESIAN_POINT ( 'NONE',  ( -22.42357213249529480, 65.12722920756738176, -243.2346049986351204 ) ) ;
#197474=DIRECTION ( 'NONE',  ( 0.000000000000000000, -0.9651348961777379554, 0.2617529984164210233 ) ) ;
#197486=EDGE_CURVE ( 'NONE', #88490, #222045, #196626, .T. ) ;
#197491=AXIS2_PLACEMENT_3D ( 'NONE', #30067, #50855, #11789 ) ;
#197504=CARTESIAN_POINT ( 'NONE',  ( -21.05000000000000071, 56.01362831242967388, -232.7091905853083347 ) ) ;
#197512=CARTESIAN_POINT ( 'NONE',  ( -18.41799967126741677, 78.24072142544075348, -231.5548840223034972 ) ) ;
#197516=EDGE_CURVE ( 'NONE', #72090, #194645, #47614, .T. ) ;
#197520=CARTESIAN_POINT ( 'NONE',  ( -21.05000000000000071, 68.48451787451661232, -224.2224406095231757 ) ) ;
#197545=LINE ( 'NONE', #198834, #215621 ) ;
#197547=CARTESIAN_POINT ( 'NONE',  ( -18.59999999999999787, 57.82359945636609666, -226.0354702357591350 ) ) ;
#197568=ORIENTED_EDGE ( 'NONE', *, *, #125439, .T. ) ;
#197584=DIRECTION ( 'NONE',  ( 1.000000000000000000, 0.000000000000000000, 0.000000000000000000 ) ) ;
#197599=LINE ( 'NONE', #77636, #246764 ) ;
#197639=ORIENTED_EDGE ( 'NONE', *, *, #148901, .T. ) ;
#197643=CARTESIAN_POINT ( 'NONE',  ( 18.59117750673696534, 67.49222854868494892, -195.4187676019683693 ) ) ;
#197662=CARTESIAN_POINT ( 'NONE',  ( -20.64999999999999858, 70.12557831835937350, -215.6322690948981915 ) ) ;
#197696=AXIS2_PLACEMENT_3D ( 'NONE', #220333, #123796, #41701 ) ;
#197697=EDGE_CURVE ( 'NONE', #7048, #257242, #164363, .T. ) ;
#197715=VERTEX_POINT ( 'NONE', #69663 ) ;
#197741=FACE_OUTER_BOUND ( 'NONE', #112106, .T. ) ;
#197750=EDGE_CURVE ( 'NONE', #142564, #70430, #230836, .T. ) ;
#197765=ORIENTED_EDGE ( 'NONE', *, *, #52499, .F. ) ;
#197773=LINE ( 'NONE', #19139, #161751 ) ;
#197806=EDGE_CURVE ( 'NONE', #211751, #137090, #193418, .T. ) ;
#197812=CARTESIAN_POINT ( 'NONE',  ( 18.39999999999999858, 78.24390740893980478, -231.6169762517609172 ) ) ;
#197826=ORIENTED_EDGE ( 'NONE', *, *, #36179, .T. ) ;
#197828=CARTESIAN_POINT ( 'NONE',  ( -18.59999999999999787, 57.72708596674832648, -226.0092949359174952 ) ) ;
#197846=EDGE_LOOP ( 'NONE', ( #172621, #119553, #162546, #243452 ) ) ;
#197851=CARTESIAN_POINT ( 'NONE',  ( -23.15000000000000213, 76.00000000001126921, -203.5231074845248997 ) ) ;
#197896=CARTESIAN_POINT ( 'NONE',  ( 18.40916198585727059, 86.89640093994682957, -199.6396876344186637 ) ) ;
#197913=LINE ( 'NONE', #74165, #211273 ) ;
#197921=DIRECTION ( 'NONE',  ( 0.000000000000000000, 0.2617529984164955192, 0.9651348961777178603 ) ) ;
#197928=ORIENTED_EDGE ( 'NONE', *, *, #121257, .T. ) ;
#197941=ORIENTED_EDGE ( 'NONE', *, *, #115334, .T. ) ;
#197947=LINE ( 'NONE', #177142, #204431 ) ;
#197969=EDGE_CURVE ( 'NONE', #2377, #221167, #221960, .T. ) ;
#197973=CIRCLE ( 'NONE', #93926, 0.09999999999999543976 ) ;
#197998=CIRCLE ( 'NONE', #247901, 0.1000000000000124678 ) ;
#198046=CARTESIAN_POINT ( 'NONE',  ( 18.49999999999999645, 67.23127455305841238, -235.8551265064783991 ) ) ;
#198056=ORIENTED_EDGE ( 'NONE', *, *, #174018, .F. ) ;
#198066=CYLINDRICAL_SURFACE ( 'NONE', #79328, 0.09999999999999543976 ) ;
#198071=EDGE_CURVE ( 'NONE', #43706, #188542, #140693, .T. ) ;
#198079=CARTESIAN_POINT ( 'NONE',  ( -23.25000000000000000, 67.23127455305841238, -235.8551265064783991 ) ) ;
#198086=CARTESIAN_POINT ( 'NONE',  ( 20.94999999999999929, 87.24382154048164750, -206.5725299160771726 ) ) ;
#198104=DIRECTION ( 'NONE',  ( 1.000000000000000000, 0.000000000000000000, 0.000000000000000000 ) ) ;
#198111=AXIS2_PLACEMENT_3D ( 'NONE', #5815, #224866, #164911 ) ;
#198131=VERTEX_POINT ( 'NONE', #57317 ) ;
#198163=DIRECTION ( 'NONE',  ( 0.000000000000000000, 0.2617529984165031798, 0.9651348961777156399 ) ) ;
#198193=DIRECTION ( 'NONE',  ( 1.000000000000000000, 0.000000000000000000, 0.000000000000000000 ) ) ;
#198194=ADVANCED_FACE ( 'NONE', ( #104149 ), #150643, .F. ) ;
#198224=ORIENTED_EDGE ( 'NONE', *, *, #125975, .F. ) ;
#198249=FACE_BOUND ( 'NONE', #44914, .T. ) ;
#198259=ORIENTED_EDGE ( 'NONE', *, *, #190877, .T. ) ;
#198271=ADVANCED_FACE ( 'NONE', ( #24663 ), #226671, .T. ) ;
#198341=CARTESIAN_POINT ( 'NONE',  ( -22.45437739390952103, 64.18196446285904244, -247.0985338222384087 ) ) ;
#198356=AXIS2_PLACEMENT_3D ( 'NONE', #63082, #142607, #180479 ) ;
#198381=CARTESIAN_POINT ( 'NONE',  ( -21.05000000000000071, 67.23127455305841238, -235.8551265064783991 ) ) ;
#198392=CARTESIAN_POINT ( 'NONE',  ( 20.94999999999999929, 76.52350599684427834, -201.5928376921694678 ) ) ;
#198430=ORIENTED_EDGE ( 'NONE', *, *, #237142, .F. ) ;
#198438=ORIENTED_EDGE ( 'NONE', *, *, #113796, .T. ) ;
#198527=ORIENTED_EDGE ( 'NONE', *, *, #247748, .T. ) ;
#198528=VERTEX_POINT ( 'NONE', #88430 ) ;
#198532=LINE ( 'NONE', #77293, #209657 ) ;
#198542=CARTESIAN_POINT ( 'NONE',  ( -23.15000000000000213, 66.26558728512915764, -222.7970849955717938 ) ) ;
#198543=DIRECTION ( 'NONE',  ( -1.000000000000000000, 2.849773892568378313E-16, -7.728835255496647986E-17 ) ) ;
#198597=EDGE_LOOP ( 'NONE', ( #122063, #184871, #238743, #202290 ) ) ;
#198626=CARTESIAN_POINT ( 'NONE',  ( 22.39999999999999858, 67.23127455305841238, -235.8551265064783991 ) ) ;
#198641=ORIENTED_EDGE ( 'NONE', *, *, #44587, .F. ) ;
#198685=VECTOR ( 'NONE', #33873, 1000.000000000000000 ) ;
#198687=EDGE_CURVE ( 'NONE', #52103, #172976, #22711, .T. ) ;
#198697=TOROIDAL_SURFACE ( 'NONE', #86247, 12.77499999999999858, 0.1000000000000000056 ) ;
#198703=CARTESIAN_POINT ( 'NONE',  ( 20.94999999999999929, 72.02722222756959525, -225.1832529173024398 ) ) ;
#198718=CARTESIAN_POINT ( 'NONE',  ( -23.25000000000000000, 86.43238724539048690, -209.5644480942280836 ) ) ;
#198735=CIRCLE ( 'NONE', #86288, 0.1999999999999981515 ) ;
#198740=CYLINDRICAL_SURFACE ( 'NONE', #237909, 0.1000000000000124678 ) ;
#198752=ORIENTED_EDGE ( 'NONE', *, *, #203372, .T. ) ;
#198770=VECTOR ( 'NONE', #61890, 1000.000000000000000 ) ;
#198806=ORIENTED_EDGE ( 'NONE', *, *, #40418, .T. ) ;
#198814=ORIENTED_EDGE ( 'NONE', *, *, #32998, .F. ) ;
#198824=TOROIDAL_SURFACE ( 'NONE', #148968, 11.89999999999999858, 0.1000000000000000056 ) ;
#198834=CARTESIAN_POINT ( 'NONE',  ( -23.25000000000000000, 70.29876110920605470, -198.0544810472949564 ) ) ;
#198837=ADVANCED_FACE ( 'NONE', ( #189507 ), #123430, .F. ) ;
#198855=CIRCLE ( 'NONE', #98862, 2.000000000000013323 ) ;
#198860=EDGE_CURVE ( 'NONE', #146449, #92812, #68270, .T. ) ;
#198868=CARTESIAN_POINT ( 'NONE',  ( 21.05000000000000071, 64.23744694032046709, -224.5446448091673233 ) ) ;
#198884=FACE_OUTER_BOUND ( 'NONE', #60444, .T. ) ;
#198893=DIRECTION ( 'NONE',  ( -1.000000000000000000, 0.000000000000000000, 0.000000000000000000 ) ) ;
#198898=CARTESIAN_POINT ( 'NONE',  ( 23.15000000000000213, 87.16808457410660083, -209.7639756239869939 ) ) ;
#198941=VERTEX_POINT ( 'NONE', #73433 ) ;
#198977=CARTESIAN_POINT ( 'NONE',  ( -23.15000000000000213, 67.23127455305841238, -235.8551265064783991 ) ) ;
#199009=CIRCLE ( 'NONE', #40665, 2.000000000000000000 ) ;
#199018=LINE ( 'NONE', #20396, #211783 ) ;
#199019=DIRECTION ( 'NONE',  ( 0.000000000000000000, 0.2617529984165027912, 0.9651348961777158619 ) ) ;
#199080=CIRCLE ( 'NONE', #20033, 0.1000000000000012546 ) ;
#199084=CARTESIAN_POINT ( 'NONE',  ( 18.59999999999999076, 70.53171716061257257, -228.4612385850772682 ) ) ;
#199096=AXIS2_PLACEMENT_3D ( 'NONE', #135933, #53854, #134642 ) ;
#199119=AXIS2_PLACEMENT_3D ( 'NONE', #220183, #97633, #195508 ) ;
#199140=ORIENTED_EDGE ( 'NONE', *, *, #1754, .T. ) ;
#199142=ORIENTED_EDGE ( 'NONE', *, *, #31124, .T. ) ;
#199146=CARTESIAN_POINT ( 'NONE',  ( 18.49999999999998934, 64.04577702392042227, -222.1950530992138226 ) ) ;
#199161=AXIS2_PLACEMENT_3D ( 'NONE', #28881, #31436, #227023 ) ;
#199195=DIRECTION ( 'NONE',  ( 2.827886303505248766E-16, 0.9667078373770112698, 0.2558827019434132821 ) ) ;
#199196=CYLINDRICAL_SURFACE ( 'NONE', #95567, 0.09999999999999543976 ) ;
#199197=CARTESIAN_POINT ( 'NONE',  ( 18.36493879433392706, 86.98067545911243315, -199.3289539518750644 ) ) ;
#199221=CARTESIAN_POINT ( 'NONE',  ( -22.50000000000000000, 55.98745301258804119, -232.8057040749261262 ) ) ;
#199224=DIRECTION ( 'NONE',  ( 0.000000000000000000, -0.2617529984165036239, -0.9651348961777156399 ) ) ;
#199227=FACE_OUTER_BOUND ( 'NONE', #148296, .T. ) ;
#199234=CARTESIAN_POINT ( 'NONE',  ( 23.24999999999999645, 67.23127455305841238, -235.8551265064783991 ) ) ;
#199244=CARTESIAN_POINT ( 'NONE',  ( -20.94999999999999929, 68.48451787451661232, -224.2224406095231757 ) ) ;
#199249=DIRECTION ( 'NONE',  ( -1.000000000000000000, -0.000000000000000000, 0.000000000000000000 ) ) ;
#199266=CARTESIAN_POINT ( 'NONE',  ( 22.00411653962174796, 60.20480020221229012, -234.0521012187997769 ) ) ;
#199267=DIRECTION ( 'NONE',  ( -2.081668171172242982E-13, -0.7092521942343974484, -0.7049548389604062271 ) ) ;
#199277=EDGE_CURVE ( 'NONE', #102375, #134983, #201943, .T. ) ;
#199279=EDGE_LOOP ( 'NONE', ( #27485, #168417, #41234, #86221 ) ) ;
#199288=EDGE_LOOP ( 'NONE', ( #167409, #4478, #204404, #58963 ) ) ;
#199321=ORIENTED_EDGE ( 'NONE', *, *, #191408, .F. ) ;
#199331=ORIENTED_EDGE ( 'NONE', *, *, #213883, .T. ) ;
#199359=CARTESIAN_POINT ( 'NONE',  ( 22.39999999999999503, 65.09550114356429162, -243.3481044654562879 ) ) ;
#199378=EDGE_CURVE ( 'NONE', #123166, #156295, #83330, .T. ) ;
#199399=EDGE_LOOP ( 'NONE', ( #142136, #27116, #208061, #251351, #54566 ) ) ;
#199425=CARTESIAN_POINT ( 'NONE',  ( -18.59999999999999787, 63.83985267992358104, -213.0213082169670145 ) ) ;
#199438=CARTESIAN_POINT ( 'NONE',  ( 20.94999999999999929, 67.70174932746996888, -211.7710791003628401 ) ) ;
#199489=CARTESIAN_POINT ( 'NONE',  ( 23.14999999999999503, 61.57587952878035509, -212.2000740415318774 ) ) ;
#199512=CARTESIAN_POINT ( 'NONE',  ( -23.25000000000000000, 80.82423061532404063, -192.8091306798888525 ) ) ;
#199524=CARTESIAN_POINT ( 'NONE',  ( -20.94999999999999929, 67.23127455305841238, -235.8551265064783991 ) ) ;
#199526=ORIENTED_EDGE ( 'NONE', *, *, #84218, .T. ) ;
#199586=CARTESIAN_POINT ( 'NONE',  ( -18.59999999999999787, 80.78317333349157536, -192.9003134612048882 ) ) ;
#199594=LINE ( 'NONE', #100431, #230006 ) ;
#199606=CYLINDRICAL_SURFACE ( 'NONE', #166850, 0.09999999999999789613 ) ;
#199616=ORIENTED_EDGE ( 'NONE', *, *, #50493, .F. ) ;
#199623=ORIENTED_EDGE ( 'NONE', *, *, #218707, .T. ) ;
#199654=CARTESIAN_POINT ( 'NONE',  ( 21.09706851349341861, 61.96409884441155214, -221.7490514850052534 ) ) ;
#199688=CARTESIAN_POINT ( 'NONE',  ( -18.59999999999999787, 79.58035499750722863, -226.6153910028758958 ) ) ;
#199689=CIRCLE ( 'NONE', #141392, 0.1000000000000124678 ) ;
#199690=CARTESIAN_POINT ( 'NONE',  ( 23.14999999999999858, 76.00000000001126921, -203.5231074845248997 ) ) ;
#199704=DIRECTION ( 'NONE',  ( 1.000000000000000000, 0.000000000000000000, 0.000000000000000000 ) ) ;
#199750=CARTESIAN_POINT ( 'NONE',  ( 21.93340585899577988, 65.31415710917552531, -242.9239163822612682 ) ) ;
#199752=AXIS2_PLACEMENT_3D ( 'NONE', #24299, #62128, #144201 ) ;
#199766=CARTESIAN_POINT ( 'NONE',  ( -20.54999999999999716, 67.23127455305841238, -235.8551265064783991 ) ) ;
#199843=CARTESIAN_POINT ( 'NONE',  ( 23.14999999999999858, 67.92720994251783395, -214.1870976236629929 ) ) ;
#199858=CARTESIAN_POINT ( 'NONE',  ( 21.05000000000000071, 61.00620644593068675, -234.0632213031365438 ) ) ;
#199862=ORIENTED_EDGE ( 'NONE', *, *, #33504, .F. ) ;
#199879=DIRECTION ( 'NONE',  ( -1.000000000000000000, 0.000000000000000000, 0.000000000000000000 ) ) ;
#199960=CARTESIAN_POINT ( 'NONE',  ( 21.05000000000000071, 62.82351852614503684, -207.2177435922979214 ) ) ;
#199965=ORIENTED_EDGE ( 'NONE', *, *, #113571, .F. ) ;
#199977=TOROIDAL_SURFACE ( 'NONE', #183408, 4.099999999999999645, 0.1000000000000000056 ) ;
#199981=EDGE_CURVE ( 'NONE', #228509, #121064, #152259, .T. ) ;
#200002=CARTESIAN_POINT ( 'NONE',  ( -21.05000000000000071, 76.00000000001126921, -203.5231074845248997 ) ) ;
#200007=DIRECTION ( 'NONE',  ( 0.000000000000000000, -0.2617529984165152257, -0.9651348961777124202 ) ) ;
#200019=FACE_OUTER_BOUND ( 'NONE', #137458, .T. ) ;
#200021=ORIENTED_EDGE ( 'NONE', *, *, #189146, .T. ) ;
#200024=CIRCLE ( 'NONE', #62656, 0.5000000000000051070 ) ;
#200026=EDGE_LOOP ( 'NONE', ( #154766, #218560, #28822, #144065 ) ) ;
#200092=CARTESIAN_POINT ( 'NONE',  ( 20.94999027547553894, 67.49459761544871128, -195.5598716110968951 ) ) ;
#200094=DIRECTION ( 'NONE',  ( 1.000000000000000000, 0.000000000000000000, 0.000000000000000000 ) ) ;
#200153=AXIS2_PLACEMENT_3D ( 'NONE', #77130, #216643, #154151 ) ;
#200156=AXIS2_PLACEMENT_3D ( 'NONE', #141013, #5301, #181429 ) ;
#200159=ORIENTED_EDGE ( 'NONE', *, *, #73458, .F. ) ;
#200220=ORIENTED_EDGE ( 'NONE', *, *, #238048, .F. ) ;
#200222=CIRCLE ( 'NONE', #87776, 0.9750000000000036415 ) ;
#200224=DIRECTION ( 'NONE',  ( 0.000000000000000000, -0.2617529984164994050, -0.9651348961777166391 ) ) ;
#200237=ORIENTED_EDGE ( 'NONE', *, *, #154379, .T. ) ;
#200249=VERTEX_POINT ( 'NONE', #99716 ) ;
#200278=DIRECTION ( 'NONE',  ( -1.000000000000000000, -0.000000000000000000, -0.000000000000000000 ) ) ;
#200280=CIRCLE ( 'NONE', #125279, 0.5000000000000087708 ) ;
#200299=ORIENTED_EDGE ( 'NONE', *, *, #65055, .F. ) ;
#200308=DIRECTION ( 'NONE',  ( 0.000000000000000000, 0.2617529984165031243, 0.9651348961777157509 ) ) ;
#200311=DIRECTION ( 'NONE',  ( 1.000000000000000000, 0.000000000000000000, 0.000000000000000000 ) ) ;
#200316=CARTESIAN_POINT ( 'NONE',  ( -21.14999999999999858, 67.23127455305841238, -235.8551265064783991 ) ) ;
#200362=EDGE_CURVE ( 'NONE', #78065, #130099, #222234, .T. ) ;
#200363=ORIENTED_EDGE ( 'NONE', *, *, #95518, .T. ) ;
#200418=TOROIDAL_SURFACE ( 'NONE', #192068, 0.4000000000000009104, 0.1000000000000000056 ) ;
#200420=AXIS2_PLACEMENT_3D ( 'NONE', #152946, #96750, #34279 ) ;
#200437=DIRECTION ( 'NONE',  ( 2.952720810173289112E-16, 0.9651348961777191926, -0.2617529984164898571 ) ) ;
#200468=EDGE_LOOP ( 'NONE', ( #60935, #204602, #34736, #100487 ) ) ;
#200513=SPHERICAL_SURFACE ( 'NONE', #127035, 0.1000000000000000056 ) ;
#200531=DIRECTION ( 'NONE',  ( 0.000000000000000000, -0.2617529984165152257, -0.9651348961777124202 ) ) ;
#200537=CARTESIAN_POINT ( 'NONE',  ( 21.93340585971789736, 60.16248467656392052, -233.9380090624025001 ) ) ;
#200549=AXIS2_PLACEMENT_3D ( 'NONE', #87752, #227271, #68210 ) ;
#200563=VERTEX_POINT ( 'NONE', #134701 ) ;
#200565=CIRCLE ( 'NONE', #108795, 0.1000000000000124678 ) ;
#200579=CARTESIAN_POINT ( 'NONE',  ( -21.05000000000000071, 68.51069317435826633, -224.1259271199053842 ) ) ;
#200656=ORIENTED_EDGE ( 'NONE', *, *, #35122, .F. ) ;
#200679=AXIS2_PLACEMENT_3D ( 'NONE', #11095, #9800, #255762 ) ;
#200683=ORIENTED_EDGE ( 'NONE', *, *, #103341, .T. ) ;
#200692=DIRECTION ( 'NONE',  ( 1.000000000000000000, 0.000000000000000000, 0.000000000000000000 ) ) ;
#200731=FACE_OUTER_BOUND ( 'NONE', #78002, .T. ) ;
#200741=CIRCLE ( 'NONE', #150846, 0.1000000000000086514 ) ;
#200747=LINE ( 'NONE', #100331, #111117 ) ;
#200803=LINE ( 'NONE', #22183, #246240 ) ;
#200815=ORIENTED_EDGE ( 'NONE', *, *, #234164, .T. ) ;
#200831=ADVANCED_FACE ( 'NONE', ( #162642 ), #44021, .T. ) ;
#200882=ORIENTED_EDGE ( 'NONE', *, *, #43825, .T. ) ;
#200884=CARTESIAN_POINT ( 'NONE',  ( -23.25000000000000000, 67.23127455305841238, -235.8551265064783991 ) ) ;
#200887=ORIENTED_EDGE ( 'NONE', *, *, #70734, .F. ) ;
#200904=ORIENTED_EDGE ( 'NONE', *, *, #203497, .F. ) ;
#200928=EDGE_CURVE ( 'NONE', #194221, #79198, #165250, .T. ) ;
#200932=ORIENTED_EDGE ( 'NONE', *, *, #49871, .F. ) ;
#200937=ORIENTED_EDGE ( 'NONE', *, *, #83027, .T. ) ;
#200958=CYLINDRICAL_SURFACE ( 'NONE', #157178, 0.09999999999999939493 ) ;
#200994=AXIS2_PLACEMENT_3D ( 'NONE', #108042, #25940, #125041 ) ;
#200998=CARTESIAN_POINT ( 'NONE',  ( -23.25000000000000000, 62.82351852614503684, -207.2177435922979214 ) ) ;
#201001=DIRECTION ( 'NONE',  ( 1.000000000000000000, 0.000000000000000000, 0.000000000000000000 ) ) ;
#201015=CARTESIAN_POINT ( 'NONE',  ( 21.40925344232283578, 65.39288699657993220, -242.2555949059684508 ) ) ;
#201023=ORIENTED_EDGE ( 'NONE', *, *, #131174, .T. ) ;
#201067=DIRECTION ( 'NONE',  ( 1.000000000000000000, 0.000000000000000000, 0.000000000000000000 ) ) ;
#201102=CARTESIAN_POINT ( 'NONE',  ( 21.04116576186321197, 60.20408469978575283, -221.1753446031674173 ) ) ;
#201103=CARTESIAN_POINT ( 'NONE',  ( -21.22070241538126112, 60.96101127587400015, -234.2570688782265051 ) ) ;
#201113=DIRECTION ( 'NONE',  ( 0.000000000000000000, 0.2617529984164955192, 0.9651348961777178603 ) ) ;
#201125=FACE_OUTER_BOUND ( 'NONE', #54641, .T. ) ;
#201151=CIRCLE ( 'NONE', #97053, 11.75000000000000178 ) ;
#201164=ORIENTED_EDGE ( 'NONE', *, *, #164388, .T. ) ;
#201171=CIRCLE ( 'NONE', #180335, 0.09999999999999939493 ) ;
#201176=ORIENTED_EDGE ( 'NONE', *, *, #125693, .T. ) ;
#201213=AXIS2_PLACEMENT_3D ( 'NONE', #153037, #209110, #190872 ) ;
#201214=EDGE_LOOP ( 'NONE', ( #192917, #132644, #183252 ) ) ;
#201220=EDGE_LOOP ( 'NONE', ( #90192, #81821, #121645, #88609 ) ) ;
#201245=CIRCLE ( 'NONE', #134597, 0.1999999999999981515 ) ;
#201254=CARTESIAN_POINT ( 'NONE',  ( -22.49756042579671700, 64.10656222496838552, -247.0783888534666062 ) ) ;
#201269=CARTESIAN_POINT ( 'NONE',  ( -20.91682497891423154, 67.49276774653023381, -195.4544018784149841 ) ) ;
#201278=CARTESIAN_POINT ( 'NONE',  ( -18.59999999999999787, 86.87366311306884370, -199.3414869250131858 ) ) ;
#201280=CARTESIAN_POINT ( 'NONE',  ( -20.94999999999999929, 70.15623657602074559, -198.0563205710787713 ) ) ;
#201294=LINE ( 'NONE', #25251, #222274 ) ;
#201317=FACE_OUTER_BOUND ( 'NONE', #152967, .T. ) ;
#201327=VECTOR ( 'NONE', #68937, 999.9999999999998863 ) ;
#201360=DIRECTION ( 'NONE',  ( 0.000000000000000000, 0.9651348961777159730, -0.2617529984165021806 ) ) ;
#201381=CARTESIAN_POINT ( 'NONE',  ( 23.15000000000000213, 86.19075908668452257, -209.4719249499869136 ) ) ;
#201430=AXIS2_PLACEMENT_3D ( 'NONE', #155048, #177177, #54621 ) ;
#201468=DIRECTION ( 'NONE',  ( -1.000000000000000000, 2.849773892568378313E-16, -7.728835255496647986E-17 ) ) ;
#201471=EDGE_CURVE ( 'NONE', #256658, #46658, #78620, .T. ) ;
#201496=FACE_OUTER_BOUND ( 'NONE', #233306, .T. ) ;
#201515=DIRECTION ( 'NONE',  ( -0.000000000000000000, -0.2617529984165031243, -0.9651348961777157509 ) ) ;
#201525=EDGE_LOOP ( 'NONE', ( #89665, #21069, #162440, #128050 ) ) ;
#201565=EDGE_CURVE ( 'NONE', #181475, #12569, #232097, .T. ) ;
#201570=ORIENTED_EDGE ( 'NONE', *, *, #131149, .T. ) ;
#201611=EDGE_CURVE ( 'NONE', #1095, #16549, #174036, .T. ) ;
#201621=AXIS2_PLACEMENT_3D ( 'NONE', #228339, #186653, #225736 ) ;
#201628=ORIENTED_EDGE ( 'NONE', *, *, #218005, .T. ) ;
#201634=DIRECTION ( 'NONE',  ( 0.000000000000000000, 0.3994087351226822125, 0.9167729611565227366 ) ) ;
#201665=CARTESIAN_POINT ( 'NONE',  ( 18.49999999999997513, 78.12133356376092763, -231.3112718935514920 ) ) ;
#201669=CYLINDRICAL_SURFACE ( 'NONE', #148909, 0.09999999999999935330 ) ;
#201701=DIRECTION ( 'NONE',  ( 0.000000000000000000, -0.9651348961777157509, 0.2617529984165031243 ) ) ;
#201722=CIRCLE ( 'NONE', #230979, 6.329289321881358177 ) ;
#201741=DIRECTION ( 'NONE',  ( 1.000000000000000000, 0.000000000000000000, 0.000000000000000000 ) ) ;
#201768=DIRECTION ( 'NONE',  ( -1.000000000000000000, -0.000000000000000000, 0.000000000000000000 ) ) ;
#201773=VERTEX_POINT ( 'NONE', #190368 ) ;
#201775=AXIS2_PLACEMENT_3D ( 'NONE', #157740, #139386, #58567 ) ;
#201783=EDGE_CURVE ( 'NONE', #200249, #129114, #35681, .T. ) ;
#201818=CARTESIAN_POINT ( 'NONE',  ( 22.47007471830798764, 59.77974727959318813, -233.8342073434304211 ) ) ;
#201820=CARTESIAN_POINT ( 'NONE',  ( -20.64999999999999858, 76.52350599684427834, -201.5928376921694678 ) ) ;
#201853=DIRECTION ( 'NONE',  ( 0.000000000000000000, 0.9916376685811618685, -0.1290532225514649800 ) ) ;
#201857=EDGE_CURVE ( 'NONE', #222045, #178174, #149958, .T. ) ;
#201887=ORIENTED_EDGE ( 'NONE', *, *, #7, .F. ) ;
#201895=EDGE_CURVE ( 'NONE', #11153, #61360, #169944, .T. ) ;
#201897=DIRECTION ( 'NONE',  ( -4.408576920032448588E-17, -0.3896596508880098009, -0.9209589331071361684 ) ) ;
#201912=CARTESIAN_POINT ( 'NONE',  ( -18.59999999999999787, 79.19526988099229925, -196.1889237952725296 ) ) ;
#201943=CIRCLE ( 'NONE', #89481, 0.1000000000000106498 ) ;
#201953=ORIENTED_EDGE ( 'NONE', *, *, #124539, .F. ) ;
#201980=CARTESIAN_POINT ( 'NONE',  ( 21.05000000000000071, 78.50726470275242264, -228.6618886302502176 ) ) ;
#201983=AXIS2_PLACEMENT_3D ( 'NONE', #37911, #59995, #39198 ) ;
#201998=FACE_OUTER_BOUND ( 'NONE', #15836, .T. ) ;
#202003=DIRECTION ( 'NONE',  ( 0.000000000000000000, -0.2617529984165035128, -0.9651348961777155289 ) ) ;
#202022=ORIENTED_EDGE ( 'NONE', *, *, #152368, .F. ) ;
#202051=EDGE_CURVE ( 'NONE', #60484, #10835, #95057, .T. ) ;
#202053=CIRCLE ( 'NONE', #35672, 0.1000000000000124678 ) ;
#202058=EDGE_CURVE ( 'NONE', #128967, #176136, #86850, .T. ) ;
#202070=DIRECTION ( 'NONE',  ( 1.000000000000000000, 0.000000000000000000, 0.000000000000000000 ) ) ;
#202115=LINE ( 'NONE', #121332, #210080 ) ;
#202129=EDGE_LOOP ( 'NONE', ( #168721, #125524, #157274, #233195 ) ) ;
#202148=FACE_OUTER_BOUND ( 'NONE', #84167, .T. ) ;
#202153=CIRCLE ( 'NONE', #77233, 0.09999999999999543976 ) ;
#202159=ORIENTED_EDGE ( 'NONE', *, *, #187873, .T. ) ;
#202176=CARTESIAN_POINT ( 'NONE',  ( -18.59999999999999787, 86.96699927712943179, -199.3055931863049466 ) ) ;
#202214=ORIENTED_EDGE ( 'NONE', *, *, #114369, .F. ) ;
#202256=ORIENTED_EDGE ( 'NONE', *, *, #40961, .F. ) ;
#202269=AXIS2_PLACEMENT_3D ( 'NONE', #117813, #104328, #183889 ) ;
#202272=DIRECTION ( 'NONE',  ( -0.000000000000000000, 0.2617529984165031243, 0.9651348961777157509 ) ) ;
#202274=DIRECTION ( 'NONE',  ( -1.000000000000000000, -0.000000000000000000, 0.000000000000000000 ) ) ;
#202284=EDGE_CURVE ( 'NONE', #18158, #65394, #199018, .T. ) ;
#202290=ORIENTED_EDGE ( 'NONE', *, *, #42357, .F. ) ;
#202297=LINE ( 'NONE', #104447, #233579 ) ;
#202348=CARTESIAN_POINT ( 'NONE',  ( 23.14999999999998437, 67.23127455305841238, -235.8551265064783991 ) ) ;
#202357=ORIENTED_EDGE ( 'NONE', *, *, #194171, .F. ) ;
#202362=CIRCLE ( 'NONE', #248512, 12.87499999999999822 ) ;
#202363=B_SPLINE_CURVE_WITH_KNOTS ( 'NONE', 3,
 ( #179178, #489, #60466, #162175, #241688, #120489, #136134, #81294, #240411, #42214, #201269, #121764, #167316, #202561, #64341, #83851, #184276, #163441, #87731 ),
 .UNSPECIFIED., .F., .F.,
 ( 4, 3, 3, 3, 3, 3, 4 ),
 ( -2.000416914638703597E-06, 0.000000000000000000, 4.714008503745425717E-05, 9.979203887779529328E-05, 0.0001372215519229583788, 0.0001635031576221022021, 0.0001900083748504252776 ),
 .UNSPECIFIED. ) ;
#202402=ORIENTED_EDGE ( 'NONE', *, *, #57426, .T. ) ;
#202412=CIRCLE ( 'NONE', #123309, 0.1000000000000124678 ) ;
#202419=FACE_OUTER_BOUND ( 'NONE', #175821, .T. ) ;
#202444=DIRECTION ( 'NONE',  ( 0.000000000000000000, -0.2617529984165031243, -0.9651348961777157509 ) ) ;
#202467=ORIENTED_EDGE ( 'NONE', *, *, #225350, .T. ) ;
#202511=ORIENTED_EDGE ( 'NONE', *, *, #238707, .T. ) ;
#202535=CARTESIAN_POINT ( 'NONE',  ( -21.05000000000000071, 55.11435547888748232, -226.8560373590520101 ) ) ;
#202561=CARTESIAN_POINT ( 'NONE',  ( -20.89192007715128341, 67.49241595948059569, -195.4314365843280541 ) ) ;
#202589=ORIENTED_EDGE ( 'NONE', *, *, #167730, .F. ) ;
#202597=VERTEX_POINT ( 'NONE', #35805 ) ;
#202601=CARTESIAN_POINT ( 'NONE',  ( -20.54999999999999716, 63.56320957583155717, -222.0641766000055668 ) ) ;
#202603=CARTESIAN_POINT ( 'NONE',  ( -23.25000000000000000, 86.43238724539048690, -209.5644480942280836 ) ) ;
#202616=CIRCLE ( 'NONE', #60947, 0.1000000000000124678 ) ;
#202621=EDGE_LOOP ( 'NONE', ( #67047, #27296, #187136 ) ) ;
#202626=EDGE_LOOP ( 'NONE', ( #214726, #85170, #21574, #226949 ) ) ;
#202647=DIRECTION ( 'NONE',  ( -1.000000000000000000, -0.000000000000000000, -0.000000000000000000 ) ) ;
#202663=DIRECTION ( 'NONE',  ( 0.000000000000000000, -0.2617529984165034573, -0.9651348961777156399 ) ) ;
#202686=ORIENTED_EDGE ( 'NONE', *, *, #169781, .T. ) ;
#202689=AXIS2_PLACEMENT_3D ( 'NONE', #240159, #180191, #40707 ) ;
#202707=LINE ( 'NONE', #121909, #218157 ) ;
#202710=VECTOR ( 'NONE', #76429, 1000.000000000000000 ) ;
#202731=ORIENTED_EDGE ( 'NONE', *, *, #148262, .F. ) ;
#202742=VECTOR ( 'NONE', #178002, 1000.000000000000000 ) ;
#202758=CARTESIAN_POINT ( 'NONE',  ( -18.42637059832562940, 86.89577927498417864, -199.6303102917484011 ) ) ;
#202788=CIRCLE ( 'NONE', #86056, 7.720710678118691384 ) ;
#202796=ORIENTED_EDGE ( 'NONE', *, *, #118265, .T. ) ;
#202824=DIRECTION ( 'NONE',  ( 0.000000000000000000, 0.2617529984165031243, 0.9651348961777157509 ) ) ;
#202851=CARTESIAN_POINT ( 'NONE',  ( 21.05000000000000071, 67.23127455305841238, -235.8551265064783991 ) ) ;
#202860=AXIS2_PLACEMENT_3D ( 'NONE', #86839, #225064, #67296 ) ;
#202863=CARTESIAN_POINT ( 'NONE',  ( 23.24999999999999645, 76.00000000001126921, -203.5231074845248997 ) ) ;
#202867=EDGE_CURVE ( 'NONE', #122792, #38996, #166460, .T. ) ;
#202879=EDGE_LOOP ( 'NONE', ( #72753, #223038, #131944, #77575 ) ) ;
#202887=CARTESIAN_POINT ( 'NONE',  ( 18.49999999999999289, 63.62814136979439184, -224.4990371885399441 ) ) ;
#202899=AXIS2_PLACEMENT_3D ( 'NONE', #192544, #135109, #38601 ) ;
#202902=DIRECTION ( 'NONE',  ( 0.000000000000000000, 0.3896596508880124654, 0.9209589331071350582 ) ) ;
#202911=CARTESIAN_POINT ( 'NONE',  ( 21.05000000000000071, 60.98273731152020360, -225.3658424485014109 ) ) ;
#202914=CARTESIAN_POINT ( 'NONE',  ( -23.25000000000000000, 68.29137419664525055, -231.9463301769586394 ) ) ;
#202917=CARTESIAN_POINT ( 'NONE',  ( -22.50000000000000000, 67.13476106344063510, -235.8289512066367024 ) ) ;
#202929=LINE ( 'NONE', #199084, #215781 ) ;
#202946=EDGE_CURVE ( 'NONE', #53100, #27906, #253235, .T. ) ;
#202954=CARTESIAN_POINT ( 'NONE',  ( 20.97239005616515328, 61.87236729066745511, -221.7090595676594944 ) ) ;
#202958=EDGE_CURVE ( 'NONE', #90836, #67070, #145488, .T. ) ;
#202960=CARTESIAN_POINT ( 'NONE',  ( -18.50000000000000000, 65.50527602196416410, -248.6645148362614748 ) ) ;
#202975=VECTOR ( 'NONE', #151044, 1000.000000000000000 ) ;
#202988=DIRECTION ( 'NONE',  ( 1.000000000000000000, 0.000000000000000000, 0.000000000000000000 ) ) ;
#203038=EDGE_LOOP ( 'NONE', ( #54942, #3755, #216179, #54852 ) ) ;
#203049=DIRECTION ( 'NONE',  ( -1.000000000000000000, 7.049440681616512959E-16, -1.911869773728122357E-16 ) ) ;
#203087=ORIENTED_EDGE ( 'NONE', *, *, #228860, .T. ) ;
#203091=DIRECTION ( 'NONE',  ( 1.000000000000000000, 0.000000000000000000, 0.000000000000000000 ) ) ;
#203094=DIRECTION ( 'NONE',  ( 0.000000000000000000, 0.9651348961777157509, -0.2617529984165031243 ) ) ;
#203095=UNCERTAINTY_MEASURE_WITH_UNIT (LENGTH_MEASURE( 1.000000000000000082E-05 ), #48959, 'distance_accuracy_value', 'NONE');
#203116=DIRECTION ( 'NONE',  ( 0.000000000000000000, 0.9667078373770112698, 0.2558827019434133376 ) ) ;
#203121=AXIS2_PLACEMENT_3D ( 'NONE', #33051, #70875, #250754 ) ;
#203126=CIRCLE ( 'NONE', #119765, 0.1999999999999945155 ) ;
#203128=CARTESIAN_POINT ( 'NONE',  ( -21.55000000000000426, 65.31373032403179479, -213.3174242249740189 ) ) ;
#203159=DIRECTION ( 'NONE',  ( 0.000000000000000000, 0.9651348961777157509, -0.2617529984165031243 ) ) ;
#203163=ORIENTED_EDGE ( 'NONE', *, *, #65223, .F. ) ;
#203175=ORIENTED_EDGE ( 'NONE', *, *, #181564, .T. ) ;
#203201=CARTESIAN_POINT ( 'NONE',  ( -18.59999999999999787, 59.16775194334852728, -221.0793150863668473 ) ) ;
#203208=DIRECTION ( 'NONE',  ( -0.000000000000000000, 0.2617529984165031243, 0.9651348961777157509 ) ) ;
#203265=CARTESIAN_POINT ( 'NONE',  ( 21.04999999999999716, 61.84959188511203365, -221.8066534603183868 ) ) ;
#203302=DIRECTION ( 'NONE',  ( -0.000000000000000000, -0.9667078373770112698, -0.2558827019434132821 ) ) ;
#203315=AXIS2_PLACEMENT_3D ( 'NONE', #216982, #236552, #111820 ) ;
#203352=ADVANCED_FACE ( 'NONE', ( #157411 ), #196485, .F. ) ;
#203355=CARTESIAN_POINT ( 'NONE',  ( -21.05000000000000071, 61.16604239671104892, -234.3115055913011417 ) ) ;
#203372=EDGE_CURVE ( 'NONE', #16586, #181858, #17844, .T. ) ;
#203387=ORIENTED_EDGE ( 'NONE', *, *, #213883, .F. ) ;
#203406=DIRECTION ( 'NONE',  ( -0.000000000000000000, 0.9651348961777157509, -0.2617529984165031243 ) ) ;
#203421=CARTESIAN_POINT ( 'NONE',  ( 18.59999999999999076, 63.61019970229975229, -209.1253633388161006 ) ) ;
#203451=ORIENTED_EDGE ( 'NONE', *, *, #24001, .T. ) ;
#203462=CARTESIAN_POINT ( 'NONE',  ( 23.15000000000000213, 86.27712145182582049, -209.5223386573213702 ) ) ;
#203497=EDGE_CURVE ( 'NONE', #1926, #209826, #122549, .T. ) ;
#203505=VECTOR ( 'NONE', #191696, 1000.000000000000000 ) ;
#203522=AXIS2_PLACEMENT_3D ( 'NONE', #166105, #125651, #245610 ) ;
#203540=CARTESIAN_POINT ( 'NONE',  ( -21.29999999999995808, 67.23127455305841238, -235.8551265064783991 ) ) ;
#203547=DIRECTION ( 'NONE',  ( -1.000000000000000000, -0.000000000000000000, 0.000000000000000000 ) ) ;
#203568=CARTESIAN_POINT ( 'NONE',  ( -23.15000000000000213, 78.57160958314655375, -238.9307242378722833 ) ) ;
#203581=FACE_OUTER_BOUND ( 'NONE', #119973, .T. ) ;
#203591=ORIENTED_EDGE ( 'NONE', *, *, #168060, .T. ) ;
#203596=CARTESIAN_POINT ( 'NONE',  ( 20.94999999999999929, 70.62751970751253339, -223.3325012285725109 ) ) ;
#203598=ORIENTED_EDGE ( 'NONE', *, *, #10772, .T. ) ;
#203599=DIRECTION ( 'NONE',  ( 1.000000000000000000, 0.000000000000000000, 0.000000000000000000 ) ) ;
#203600=AXIS2_PLACEMENT_3D ( 'NONE', #35325, #75708, #215206 ) ;
#203633=CARTESIAN_POINT ( 'NONE',  ( 20.94999999999999929, 76.00000000001126921, -203.5231074845248997 ) ) ;
#203644=FACE_OUTER_BOUND ( 'NONE', #13203, .T. ) ;
#203652=CARTESIAN_POINT ( 'NONE',  ( -20.94560253601877164, 62.83003337064300808, -207.1937220765705661 ) ) ;
#203653=EDGE_LOOP ( 'NONE', ( #177449, #145490, #233301, #34795 ) ) ;
#203656=FACE_OUTER_BOUND ( 'NONE', #156276, .T. ) ;
#203664=CARTESIAN_POINT ( 'NONE',  ( -23.15000000000000213, 68.28002175382172823, -222.4371999040225774 ) ) ;
#203668=DIRECTION ( 'NONE',  ( 0.000000000000000000, 0.2617529984165035128, 0.9651348961777155289 ) ) ;
#203694=VERTEX_POINT ( 'NONE', #174105 ) ;
#203696=ADVANCED_FACE ( 'NONE', ( #39710 ), #137475, .T. ) ;
#203716=EDGE_LOOP ( 'NONE', ( #165769, #155593, #58832, #56077 ) ) ;
#203719=DIRECTION ( 'NONE',  ( -6.938893903907224433E-15, -0.9651348961777157509, 0.2617529984165031243 ) ) ;
#203720=DIRECTION ( 'NONE',  ( 1.000000000000000000, 0.000000000000000000, 0.000000000000000000 ) ) ;
#203722=CARTESIAN_POINT ( 'NONE',  ( 18.59999999999999076, 63.81702857804527440, -209.2850695923107480 ) ) ;
#203743=DIRECTION ( 'NONE',  ( -0.000000000000000000, 0.2617529984165031243, 0.9651348961777157509 ) ) ;
#203747=CARTESIAN_POINT ( 'NONE',  ( -21.07928932188134041, 61.09751618602216894, -234.2940654522710986 ) ) ;
#203752=DIRECTION ( 'NONE',  ( 0.000000000000000000, 0.2617529984165045120, 0.9651348961777153068 ) ) ;
#203775=ORIENTED_EDGE ( 'NONE', *, *, #151936, .F. ) ;
#203787=VECTOR ( 'NONE', #139694, 1000.000000000000000 ) ;
#203788=ORIENTED_EDGE ( 'NONE', *, *, #14282, .F. ) ;
#203838=EDGE_LOOP ( 'NONE', ( #229148, #47387, #224836, #120869, #33549, #103465 ) ) ;
#203842=DIRECTION ( 'NONE',  ( 0.000000000000000000, -0.2617529984165031243, -0.9651348961777158619 ) ) ;
#203905=DIRECTION ( 'NONE',  ( 1.000000000000000000, 0.000000000000000000, 0.000000000000000000 ) ) ;
#203910=DIRECTION ( 'NONE',  ( 0.000000000000000000, -0.9651348961777379554, 0.2617529984164210233 ) ) ;
#203948=CARTESIAN_POINT ( 'NONE',  ( 22.32929514600007792, 59.89092396606481117, -233.9670141766093536 ) ) ;
#203949=DIRECTION ( 'NONE',  ( 1.000000000000000000, 0.000000000000000000, 0.000000000000000000 ) ) ;
#203965=CARTESIAN_POINT ( 'NONE',  ( 21.07928932188134397, 61.09751618602741985, -234.2940654522722639 ) ) ;
#204059=CARTESIAN_POINT ( 'NONE',  ( -20.94999999999999929, 79.19526988099229925, -196.1889237952725296 ) ) ;
#204072=CARTESIAN_POINT ( 'NONE',  ( -23.25000000000000000, 76.00000000001126921, -203.5231074845248997 ) ) ;
#204079=LINE ( 'NONE', #5871, #257025 ) ;
#204088=EDGE_CURVE ( 'NONE', #219655, #66786, #255807, .T. ) ;
#204155=VERTEX_POINT ( 'NONE', #216722 ) ;
#204162=CIRCLE ( 'NONE', #216651, 0.3999999999999926392 ) ;
#204202=CARTESIAN_POINT ( 'NONE',  ( -18.50000000000000000, 52.81534179157634412, -244.1198638051726277 ) ) ;
#204210=CARTESIAN_POINT ( 'NONE',  ( -23.25000000000000000, 80.78317333349157536, -192.9003134612049166 ) ) ;
#204212=CYLINDRICAL_SURFACE ( 'NONE', #138393, 0.09999999999999789613 ) ;
#204227=VERTEX_POINT ( 'NONE', #165767 ) ;
#204240=CIRCLE ( 'NONE', #200156, 12.87500000000000178 ) ;
#204252=CIRCLE ( 'NONE', #45867, 0.09999999999999961697 ) ;
#204296=AXIS2_PLACEMENT_3D ( 'NONE', #254864, #76278, #155852 ) ;
#204305=DIRECTION ( 'NONE',  ( -0.000000000000000000, -0.3896596508880123544, -0.9209589331071349472 ) ) ;
#204343=CIRCLE ( 'NONE', #12661, 0.1999999999999987899 ) ;
#204365=CARTESIAN_POINT ( 'NONE',  ( -21.07928932188134041, 65.47931918658504458, -241.9371126717015841 ) ) ;
#204366=VERTEX_POINT ( 'NONE', #208741 ) ;
#204382=DIRECTION ( 'NONE',  ( -1.000000000000000000, 0.000000000000000000, 0.000000000000000000 ) ) ;
#204386=DIRECTION ( 'NONE',  ( 1.000000000000000000, -0.000000000000000000, -0.000000000000000000 ) ) ;
#204393=CARTESIAN_POINT ( 'NONE',  ( -22.00356870066586623, 65.33245486361551002, -242.8564489551603458 ) ) ;
#204398=CARTESIAN_POINT ( 'NONE',  ( -23.15000000000000213, 76.00000000001126921, -203.5231074845248997 ) ) ;
#204404=ORIENTED_EDGE ( 'NONE', *, *, #194905, .F. ) ;
#204431=VECTOR ( 'NONE', #74207, 1000.000000000000000 ) ;
#204435=VERTEX_POINT ( 'NONE', #9231 ) ;
#204443=EDGE_LOOP ( 'NONE', ( #125694, #203788, #238090, #99937 ) ) ;
#204447=CARTESIAN_POINT ( 'NONE',  ( -23.25000000000000000, 82.09643798151613225, -215.4278993322501208 ) ) ;
#204456=CYLINDRICAL_SURFACE ( 'NONE', #153814, 11.79999999999999361 ) ;
#204474=CARTESIAN_POINT ( 'NONE',  ( -20.94999999999999929, 86.43238724539048690, -209.5644480942280836 ) ) ;
#204507=AXIS2_PLACEMENT_3D ( 'NONE', #230666, #72897, #14202 ) ;
#204520=EDGE_CURVE ( 'NONE', #148919, #95393, #216401, .T. ) ;
#204602=ORIENTED_EDGE ( 'NONE', *, *, #99735, .T. ) ;
#204604=LINE ( 'NONE', #238611, #68144 ) ;
#204611=ORIENTED_EDGE ( 'NONE', *, *, #231957, .F. ) ;
#204625=VERTEX_POINT ( 'NONE', #222830 ) ;
#204652=CARTESIAN_POINT ( 'NONE',  ( -20.54999999999999716, 76.00000000001126921, -203.5231074845248997 ) ) ;
#204676=DIRECTION ( 'NONE',  ( 1.000000000000000000, 0.000000000000000000, 0.000000000000000000 ) ) ;
#204691=DIRECTION ( 'NONE',  ( -1.000000000000000000, 2.849773892568378313E-16, -7.728835255496647986E-17 ) ) ;
#204693=DIRECTION ( 'NONE',  ( 0.000000000000000000, 0.2617529984165031243, 0.9651348961777157509 ) ) ;
#204719=VERTEX_POINT ( 'NONE', #208441 ) ;
#204724=TOROIDAL_SURFACE ( 'NONE', #21592, 0.6000000000000013101, 0.1000000000000000056 ) ;
#204726=CARTESIAN_POINT ( 'NONE',  ( -18.59999994787167310, 86.99309687513043343, -199.3734559884612452 ) ) ;
#204729=CARTESIAN_POINT ( 'NONE',  ( 18.58143601961857883, 63.63777463829045900, -209.2364543610155465 ) ) ;
#204732=PLANE ( 'NONE',  #52472 ) ;
#204738=ADVANCED_FACE ( 'NONE', ( #29819 ), #169336, .T. ) ;
#204793=ADVANCED_FACE ( 'NONE', ( #227983 ), #141562, .T. ) ;
#204823=DIRECTION ( 'NONE',  ( 0.000000000000000000, 0.2617529984165152257, 0.9651348961777124202 ) ) ;
#204828=CARTESIAN_POINT ( 'NONE',  ( -20.12071067811865888, 61.46818095087364497, -221.4959865713132956 ) ) ;
#204829=AXIS2_PLACEMENT_3D ( 'NONE', #22758, #43584, #42298 ) ;
#204834=VERTEX_POINT ( 'NONE', #8937 ) ;
#204841=CARTESIAN_POINT ( 'NONE',  ( 22.24259225415828922, 65.17462541034674928, -243.0599263933218595 ) ) ;
#204869=CIRCLE ( 'NONE', #238189, 0.1000000000000124678 ) ;
#204891=ORIENTED_EDGE ( 'NONE', *, *, #121865, .F. ) ;
#204893=DIRECTION ( 'NONE',  ( 0.000000000000000000, 0.2617529984164506107, 0.9651348961777299618 ) ) ;
#204921=CARTESIAN_POINT ( 'NONE',  ( 23.14999999999998437, 66.17117490947157421, -239.7639228359981303 ) ) ;
#204960=EDGE_CURVE ( 'NONE', #35199, #53814, #187374, .T. ) ;
#204976=CARTESIAN_POINT ( 'NONE',  ( -21.05000000000000071, 74.95298800634525094, -207.3836470692357636 ) ) ;
#205011=DIRECTION ( 'NONE',  ( 0.000000000000000000, -0.2768012769485524438, -0.9609271840673728748 ) ) ;
#205084=AXIS2_PLACEMENT_3D ( 'NONE', #46455, #67316, #148140 ) ;
#205098=CARTESIAN_POINT ( 'NONE',  ( 21.04999999999999716, 65.63508186416100898, -242.0676793166472294 ) ) ;
#205120=ADVANCED_FACE ( 'NONE', ( #242086 ), #4742, .T. ) ;
#205139=EDGE_CURVE ( 'NONE', #231216, #191603, #129291, .T. ) ;
#205160=DIRECTION ( 'NONE',  ( -1.000000000000000000, -0.000000000000000000, 0.000000000000000000 ) ) ;
#205161=DIRECTION ( 'NONE',  ( 0.000000000000000000, -0.7092521942343974484, -0.7049548389604062271 ) ) ;
#205164=EDGE_CURVE ( 'NONE', #134353, #88487, #200024, .T. ) ;
#205192=CARTESIAN_POINT ( 'NONE',  ( 21.05000000000000071, 58.88775506787933978, -225.6504858384382999 ) ) ;
#205209=DIRECTION ( 'NONE',  ( 0.000000000000000000, -0.2617529984165030132, -0.9651348961777157509 ) ) ;
#205222=AXIS2_PLACEMENT_3D ( 'NONE', #147469, #225687, #250418 ) ;
#205234=ORIENTED_EDGE ( 'NONE', *, *, #10938, .T. ) ;
#205237=CARTESIAN_POINT ( 'NONE',  ( -23.25000000000000000, 67.55989888862310977, -211.9120700681549465 ) ) ;
#205248=AXIS2_PLACEMENT_3D ( 'NONE', #7662, #127602, #202003 ) ;
#205294=AXIS2_PLACEMENT_3D ( 'NONE', #1481, #203547, #74960 ) ;
#205311=VERTEX_POINT ( 'NONE', #33342 ) ;
#205337=EDGE_CURVE ( 'NONE', #132493, #130829, #116808, .T. ) ;
#205443=AXIS2_PLACEMENT_3D ( 'NONE', #180204, #1536, #61532 ) ;
#205469=CARTESIAN_POINT ( 'NONE',  ( 21.05000000000000071, 60.85896401437205583, -225.4389122456526025 ) ) ;
#205487=AXIS2_PLACEMENT_3D ( 'NONE', #208815, #109695, #107134 ) ;
#205495=ORIENTED_EDGE ( 'NONE', *, *, #200362, .T. ) ;
#205509=CARTESIAN_POINT ( 'NONE',  ( 18.39999999999999858, 78.24390740893980478, -231.6169762517609456 ) ) ;
#205537=ORIENTED_EDGE ( 'NONE', *, *, #1754, .F. ) ;
#205542=CIRCLE ( 'NONE', #247240, 0.09999999999999939493 ) ;
#205587=AXIS2_PLACEMENT_3D ( 'NONE', #151828, #23879, #43413 ) ;
#205597=CONICAL_SURFACE ( 'NONE', #93172, 4.299999999999945643, 0.7853981633974466137 ) ;
#205607=DIRECTION ( 'NONE',  ( 0.000000000000000000, 0.1290532225515392817, 0.9916376685811522096 ) ) ;
#205608=AXIS2_PLACEMENT_3D ( 'NONE', #251692, #131745, #112210 ) ;
#205613=EDGE_LOOP ( 'NONE', ( #150442, #92788, #89894, #134513 ) ) ;
#205616=CARTESIAN_POINT ( 'NONE',  ( 20.94999999999999929, 80.78317333349157536, -192.9003134612048882 ) ) ;
#205621=AXIS2_PLACEMENT_3D ( 'NONE', #63139, #123140, #202663 ) ;
#205622=DIRECTION ( 'NONE',  ( 0.000000000000000000, -0.9651348961777157509, 0.2617529984165031243 ) ) ;
#205628=DIRECTION ( 'NONE',  ( -0.7071067811865475727, 0.6824534298470373850, -0.1850873201762210096 ) ) ;
#205642=EDGE_CURVE ( 'NONE', #65394, #19933, #192035, .T. ) ;
#205688=EDGE_CURVE ( 'NONE', #52103, #181022, #171280, .T. ) ;
#205692=ORIENTED_EDGE ( 'NONE', *, *, #86654, .T. ) ;
#205693=FACE_OUTER_BOUND ( 'NONE', #158547, .T. ) ;
#205762=DIRECTION ( 'NONE',  ( -0.000000000000000000, 0.2617529984165031243, 0.9651348961777157509 ) ) ;
#205786=CARTESIAN_POINT ( 'NONE',  ( -21.04999999999999716, 61.00622636567305079, -234.0632267055443378 ) ) ;
#205787=VERTEX_POINT ( 'NONE', #137231 ) ;
#205807=CARTESIAN_POINT ( 'NONE',  ( -18.59999999999999787, 70.47363787294415260, -228.3418745167492432 ) ) ;
#205884=CARTESIAN_POINT ( 'NONE',  ( 18.59999999999999076, 66.47189219944506533, -213.6315278230738102 ) ) ;
#205891=EDGE_CURVE ( 'NONE', #153125, #250378, #230077, .T. ) ;
#205908=DIRECTION ( 'NONE',  ( -0.000000000000000000, 0.9651348961777155289, -0.2617529984165036794 ) ) ;
#205931=AXIS2_PLACEMENT_3D ( 'NONE', #114585, #235800, #191587 ) ;
#205933=CIRCLE ( 'NONE', #210048, 11.74999999999999822 ) ;
#205945=ORIENTED_EDGE ( 'NONE', *, *, #114301, .F. ) ;
#205954=AXIS2_PLACEMENT_3D ( 'NONE', #67696, #72866, #33754 ) ;
#205983=ORIENTED_EDGE ( 'NONE', *, *, #114124, .F. ) ;
#206001=AXIS2_PLACEMENT_3D ( 'NONE', #160860, #44757, #124296 ) ;
#206029=CARTESIAN_POINT ( 'NONE',  ( -18.40904629823846506, 86.89640092179662645, -199.6396877013420692 ) ) ;
#206042=VERTEX_POINT ( 'NONE', #246595 ) ;
#206043=VERTEX_POINT ( 'NONE', #67967 ) ;
#206050=CARTESIAN_POINT ( 'NONE',  ( -22.50000000000094147, 64.05844819680045532, -247.1686437718134357 ) ) ;
#206055=ORIENTED_EDGE ( 'NONE', *, *, #881, .F. ) ;
#206068=EDGE_CURVE ( 'NONE', #7826, #158463, #246813, .T. ) ;
#206070=AXIS2_PLACEMENT_3D ( 'NONE', #240776, #122110, #201634 ) ;
#206095=ORIENTED_EDGE ( 'NONE', *, *, #75312, .T. ) ;
#206108=CARTESIAN_POINT ( 'NONE',  ( 21.05000000000000071, 60.85896401437205583, -225.4389122456526025 ) ) ;
#206112=EDGE_CURVE ( 'NONE', #115416, #257696, #221853, .T. ) ;
#206149=CARTESIAN_POINT ( 'NONE',  ( 21.00023020733502577, 65.55844536562159419, -242.0231774319958049 ) ) ;
#206187=SPHERICAL_SURFACE ( 'NONE', #165103, 0.1000000000000000056 ) ;
#206253=ADVANCED_FACE ( 'NONE', ( #178660 ), #78227, .F. ) ;
#206275=DIRECTION ( 'NONE',  ( 1.000000000000000000, 0.000000000000000000, 0.000000000000000000 ) ) ;
#206303=VERTEX_POINT ( 'NONE', #143340 ) ;
#206307=VECTOR ( 'NONE', #70577, 1000.000000000000000 ) ;
#206316=( BOUNDED_CURVE ( )  B_SPLINE_CURVE ( 3, ( #33513, #89574, #169161, #111721 ),
 .UNSPECIFIED., .F., .F. ) 
 B_SPLINE_CURVE_WITH_KNOTS ( ( 4, 4 ),
 ( 3.141592653589778461, 4.712388980384684345 ),
 .UNSPECIFIED. ) 
 CURVE ( )  GEOMETRIC_REPRESENTATION_ITEM ( )  RATIONAL_B_SPLINE_CURVE ( ( 1.000000000000000000, 0.8047378541243628280, 0.8047378541243628280, 1.000000000000000000 ) ) 
 REPRESENTATION_ITEM ( '' )  );
#206319=DIRECTION ( 'NONE',  ( 0.000000000000000000, -0.9651348961777157509, 0.2617529984165031243 ) ) ;
#206369=EDGE_LOOP ( 'NONE', ( #253829, #13485, #182650, #31228 ) ) ;
#206378=AXIS2_PLACEMENT_3D ( 'NONE', #198542, #44614, #201113 ) ;
#206392=FACE_OUTER_BOUND ( 'NONE', #57167, .T. ) ;
#206395=ORIENTED_EDGE ( 'NONE', *, *, #174018, .T. ) ;
#206406=CARTESIAN_POINT ( 'NONE',  ( 21.04999999999999716, 65.61001066310818430, -241.9764486272661372 ) ) ;
#206423=DIRECTION ( 'NONE',  ( 0.7071359030027966064, 0.6824253222083512815, -0.1850796971394955137 ) ) ;
#206432=AXIS2_PLACEMENT_3D ( 'NONE', #41445, #63542, #101338 ) ;
#206452=CARTESIAN_POINT ( 'NONE',  ( -20.94999999999999929, 79.23417978893665747, -236.1056577391152587 ) ) ;
#206462=CARTESIAN_POINT ( 'NONE',  ( 22.60000000000000142, 64.05844819680034163, -247.1686437718134073 ) ) ;
#206475=VERTEX_POINT ( 'NONE', #248874 ) ;
#206478=CARTESIAN_POINT ( 'NONE',  ( -21.05000000000000071, 86.52890073500824997, -209.5906233940697234 ) ) ;
#206482=VERTEX_POINT ( 'NONE', #208480 ) ;
#206506=CARTESIAN_POINT ( 'NONE',  ( -23.15000000000000213, 86.43238724539048690, -209.5644480942280836 ) ) ;
#206526=VERTEX_POINT ( 'NONE', #55433 ) ;
#206547=EDGE_CURVE ( 'NONE', #66884, #170116, #8987, .T. ) ;
#206550=DIRECTION ( 'NONE',  ( -0.000000000000000000, 0.9651348961777156399, -0.2617529984165037349 ) ) ;
#206597=EDGE_CURVE ( 'NONE', #231873, #252932, #1897, .T. ) ;
#206640=ADVANCED_FACE ( 'NONE', ( #146542 ), #194068, .T. ) ;
#206651=DIRECTION ( 'NONE',  ( 0.000000000000000000, 0.9651348961777157509, -0.2617529984165031243 ) ) ;
#206695=DIRECTION ( 'NONE',  ( 0.000000000000000000, 0.2617529984164506107, 0.9651348961777299618 ) ) ;
#206699=ORIENTED_EDGE ( 'NONE', *, *, #175474, .F. ) ;
#206711=VERTEX_POINT ( 'NONE', #250798 ) ;
#206713=DIRECTION ( 'NONE',  ( 4.504528286903032433E-15, 0.3848449534832963370, 0.9229812358755945523 ) ) ;
#206783=DIRECTION ( 'NONE',  ( 0.000000000000000000, 0.9667078373770138233, 0.2558827019434041783 ) ) ;
#206788=EDGE_LOOP ( 'NONE', ( #66842, #109183, #6571, #68845 ) ) ;
#206843=ORIENTED_EDGE ( 'NONE', *, *, #172178, .F. ) ;
#206853=DIRECTION ( 'NONE',  ( -1.000000000000000000, -0.000000000000000000, -0.000000000000000000 ) ) ;
#206859=ORIENTED_EDGE ( 'NONE', *, *, #216233, .T. ) ;
#206871=ORIENTED_EDGE ( 'NONE', *, *, #180210, .T. ) ;
#206900=ORIENTED_EDGE ( 'NONE', *, *, #178964, .F. ) ;
#206924=EDGE_CURVE ( 'NONE', #6279, #116117, #213167, .T. ) ;
#206939=DIRECTION ( 'NONE',  ( -2.940209281316620030E-16, -0.9651348961777150848, 0.2617529984165054002 ) ) ;
#206940=ORIENTED_EDGE ( 'NONE', *, *, #119763, .F. ) ;
#206956=EDGE_LOOP ( 'NONE', ( #230344, #123361, #235686, #200220 ) ) ;
#206960=FACE_OUTER_BOUND ( 'NONE', #192287, .T. ) ;
#206985=DIRECTION ( 'NONE',  ( 0.000000000000000000, -0.9651348961777157509, 0.2617529984165032353 ) ) ;
#206987=CARTESIAN_POINT ( 'NONE',  ( -22.59999999999999787, 64.05844819680034163, -247.1686437718134073 ) ) ;
#207020=DIRECTION ( 'NONE',  ( 0.000000000000000000, 0.9651348961777118651, -0.2617529984165174461 ) ) ;
#207040=LINE ( 'NONE', #105324, #11920 ) ;
#207046=VERTEX_POINT ( 'NONE', #165848 ) ;
#207082=CARTESIAN_POINT ( 'NONE',  ( -20.00857864376270001, 61.63293978347611812, -221.5406706031726003 ) ) ;
#207084=CARTESIAN_POINT ( 'NONE',  ( -21.05000000000000426, 61.12960278649826762, -234.1614078874438860 ) ) ;
#207090=VECTOR ( 'NONE', #67842, 1000.000000000000000 ) ;
#207114=DIRECTION ( 'NONE',  ( 0.000000000000000000, -0.2617529984165030132, -0.9651348961777157509 ) ) ;
#207115=DIRECTION ( 'NONE',  ( 0.000000000000000000, -0.9916376685811618685, 0.1290532225514649800 ) ) ;
#207116=DIRECTION ( 'NONE',  ( 1.000000000000000000, 0.000000000000000000, 0.000000000000000000 ) ) ;
#207126=( BOUNDED_SURFACE ( )  B_SPLINE_SURFACE ( 3, 2, ( 
 ( #141142, #79846, #144965 ),
 ( #223221, #26329, #326 ),
 ( #60297, #42051, #159427 ),
 ( #201102, #238960, #139833 ),
 ( #22492, #219372, #101972 ),
 ( #181563, #2885, #82408 ) ),
 .UNSPECIFIED., .F., .F., .T. ) 
 B_SPLINE_SURFACE_WITH_KNOTS ( ( 4, 2, 4 ),
 ( 3, 3 ),
 ( 0.0001342700090130087912, 0.0002909192928057473108, 0.0004475685765984858304 ),
 ( 0.000000000000000000, 1.000000000000000000 ),
 .UNSPECIFIED. ) 
 GEOMETRIC_REPRESENTATION_ITEM ( )  RATIONAL_B_SPLINE_SURFACE ( (
 ( 1.000000000000000000, 0.7250110520819882387, 1.000000000000000000),
 ( 1.000000000000000000, 0.7257599279127958658, 1.000000000000000000),
 ( 1.000000000000000000, 0.7137594617292875032, 1.000000000000000000),
 ( 1.000000000000000000, 0.6959270178801479911, 1.000000000000000000),
 ( 1.000000000000000000, 0.6919879549344875036, 1.000000000000000000),
 ( 1.000000000000000000, 0.7071067811866664776, 1.000000000000000000) ) ) 
 REPRESENTATION_ITEM ( '' )  SURFACE ( )  );
#207136=VECTOR ( 'NONE', #48469, 1000.000000000000114 ) ;
#207145=CARTESIAN_POINT ( 'NONE',  ( -20.85000000000000142, 76.00000000001126921, -203.5231074845248997 ) ) ;
#207199=ORIENTED_EDGE ( 'NONE', *, *, #81130, .T. ) ;
#207230=VECTOR ( 'NONE', #138759, 1000.000000000000000 ) ;
#207251=DIRECTION ( 'NONE',  ( 1.000000000000000000, 0.000000000000000000, 0.000000000000000000 ) ) ;
#207256=LINE ( 'NONE', #92411, #247592 ) ;
#207269=CARTESIAN_POINT ( 'NONE',  ( 21.08134388332232234, 61.09760743966705832, -234.2701803535934459 ) ) ;
#207274=ORIENTED_EDGE ( 'NONE', *, *, #79863, .T. ) ;
#207288=VECTOR ( 'NONE', #191158, 1000.000000000000000 ) ;
#207302=CARTESIAN_POINT ( 'NONE',  ( 23.14999999999999858, 65.71172719659838890, -223.0701118083454446 ) ) ;
#207333=CARTESIAN_POINT ( 'NONE',  ( 18.49999999999999289, 63.82873662800449210, -209.2836886274109247 ) ) ;
#207346=ORIENTED_EDGE ( 'NONE', *, *, #75773, .T. ) ;
#207349=ORIENTED_EDGE ( 'NONE', *, *, #79922, .F. ) ;
#207353=EDGE_LOOP ( 'NONE', ( #157176, #155695, #235309, #80913 ) ) ;
#207362=AXIS2_PLACEMENT_3D ( 'NONE', #199524, #119998, #255570 ) ;
#207383=CARTESIAN_POINT ( 'NONE',  ( 23.14999999999998437, 71.14007088257814360, -236.9152261500652514 ) ) ;
#207389=DIRECTION ( 'NONE',  ( 0.000000000000000000, 0.2617529984166090395, 0.9651348961776869961 ) ) ;
#207394=VERTEX_POINT ( 'NONE', #22179 ) ;
#207397=VECTOR ( 'NONE', #194820, 1000.000000000000000 ) ;
#207427=CARTESIAN_POINT ( 'NONE',  ( 18.39999999999999858, 86.99291436658650412, -199.6658631664729739 ) ) ;
#207440=CIRCLE ( 'NONE', #169872, 0.09999999999999935330 ) ;
#207480=DIRECTION ( 'NONE',  ( -1.000000000000000000, -0.000000000000000000, -0.000000000000000000 ) ) ;
#207494=ADVANCED_FACE ( 'NONE', ( #168136 ), #49425, .F. ) ;
#207505=DIRECTION ( 'NONE',  ( 0.000000000000000000, 0.2617529984165031243, 0.9651348961777157509 ) ) ;
#207520=CARTESIAN_POINT ( 'NONE',  ( -20.96077737575326339, 62.98594959644117353, -207.1005776826179954 ) ) ;
#207521=ORIENTED_EDGE ( 'NONE', *, *, #81122, .F. ) ;
#207582=CARTESIAN_POINT ( 'NONE',  ( 20.95378194480896639, 59.04383896832029421, -225.7962839547865883 ) ) ;
#207586=AXIS2_PLACEMENT_3D ( 'NONE', #60265, #220638, #201067 ) ;
#207615=CARTESIAN_POINT ( 'NONE',  ( -22.59999999999999787, 64.08545097430041437, -247.0723585184913986 ) ) ;
#207641=DIRECTION ( 'NONE',  ( -1.000000000000000000, 3.151514657663852580E-16, -8.547182517843351137E-17 ) ) ;
#207668=AXIS2_PLACEMENT_3D ( 'NONE', #193551, #57857, #94428 ) ;
#207671=EDGE_CURVE ( 'NONE', #50639, #124804, #51194, .T. ) ;
#207684=DIRECTION ( 'NONE',  ( 0.000000000000000000, -0.9651348961777158619, 0.2617529984165031243 ) ) ;
#207713=DIRECTION ( 'NONE',  ( 1.000000000000000000, 0.000000000000000000, 0.000000000000000000 ) ) ;
#207737=TOROIDAL_SURFACE ( 'NONE', #111869, 0.9750000000000019762, 0.1000000000000000056 ) ;
#207764=( BOUNDED_CURVE ( )  B_SPLINE_CURVE ( 3, ( #188525, #108976, #189818, #93269 ),
 .UNSPECIFIED., .F., .F. ) 
 B_SPLINE_CURVE_WITH_KNOTS ( ( 4, 4 ),
 ( 0.000000000000000000, 1.570796326794908992 ),
 .UNSPECIFIED. ) 
 CURVE ( )  GEOMETRIC_REPRESENTATION_ITEM ( )  RATIONAL_B_SPLINE_CURVE ( ( 1.000000000000000000, 0.8047378541243619399, 0.8047378541243619399, 1.000000000000000000 ) ) 
 REPRESENTATION_ITEM ( '' )  );
#207769=LINE ( 'NONE', #6970, #13010 ) ;
#207794=VERTEX_POINT ( 'NONE', #68682 ) ;
#207816=DIRECTION ( 'NONE',  ( 0.000000000000000000, 0.2617529984165046231, 0.9651348961777154178 ) ) ;
#207822=DIRECTION ( 'NONE',  ( 1.000000000000000000, 0.000000000000000000, 0.000000000000000000 ) ) ;
#207827=CARTESIAN_POINT ( 'NONE',  ( -23.25000000000000000, 68.78821595027156377, -214.2597350192734211 ) ) ;
#207828=ADVANCED_FACE ( 'NONE', ( #109074 ), #170399, .F. ) ;
#207854=VERTEX_POINT ( 'NONE', #93365 ) ;
#207856=LINE ( 'NONE', #205237, #19660 ) ;
#207885=AXIS2_PLACEMENT_3D ( 'NONE', #122322, #184849, #201853 ) ;
#207888=VECTOR ( 'NONE', #214128, 1000.000000000000114 ) ;
#207894=DIRECTION ( 'NONE',  ( 0.000000000000000000, 0.9651348961777157509, -0.2617529984165031243 ) ) ;
#207899=DIRECTION ( 'NONE',  ( 0.000000000000000000, 0.2617529984165044565, 0.9651348961777151958 ) ) ;
#207916=EDGE_CURVE ( 'NONE', #82519, #66786, #122155, .T. ) ;
#207917=AXIS2_PLACEMENT_3D ( 'NONE', #131087, #50251, #192354 ) ;
#207929=VECTOR ( 'NONE', #107742, 1000.000000000000000 ) ;
#207952=DIRECTION ( 'NONE',  ( 7.304098846218134667E-16, 0.9651348961777158619, -0.2617529984165031243 ) ) ;
#207978=CARTESIAN_POINT ( 'NONE',  ( 21.05000000000000071, 76.00000000001126921, -203.5231074845248997 ) ) ;
#208005=CARTESIAN_POINT ( 'NONE',  ( 20.85000000000000142, 70.37092869010230345, -198.1237041667535550 ) ) ;
#208006=ADVANCED_FACE ( 'NONE', ( #157228 ), #84691, .F. ) ;
#208010=TOROIDAL_SURFACE ( 'NONE', #124609, 0.2000000000000000111, 0.1000000000000000056 ) ;
#208014=VERTEX_POINT ( 'NONE', #137611 ) ;
#208049=DIRECTION ( 'NONE',  ( 1.000000000000000000, 0.000000000000000000, 0.000000000000000000 ) ) ;
#208061=ORIENTED_EDGE ( 'NONE', *, *, #31813, .T. ) ;
#208063=FILL_AREA_STYLE ('',( #242028 ) ) ;
#208066=CARTESIAN_POINT ( 'NONE',  ( 21.05000000000000071, 79.07891399537199106, -236.0635483022085452 ) ) ;
#208106=EDGE_CURVE ( 'NONE', #227798, #217285, #122330, .T. ) ;
#208123=DIRECTION ( 'NONE',  ( -1.000000000000000000, 0.000000000000000000, 0.000000000000000000 ) ) ;
#208158=CIRCLE ( 'NONE', #170778, 0.09999999999999939493 ) ;
#208167=ORIENTED_EDGE ( 'NONE', *, *, #212210, .T. ) ;
#208190=CARTESIAN_POINT ( 'NONE',  ( -23.15000000000000213, 70.85002333954264486, -215.2140597723681879 ) ) ;
#208193=CARTESIAN_POINT ( 'NONE',  ( 18.54271179734040587, 87.05300735455581673, -199.5362999912227053 ) ) ;
#208229=ORIENTED_EDGE ( 'NONE', *, *, #55642, .F. ) ;
#208264=CARTESIAN_POINT ( 'NONE',  ( -23.15000000000000213, 76.52350599684427834, -201.5928376921694678 ) ) ;
#208267=ORIENTED_EDGE ( 'NONE', *, *, #224165, .F. ) ;
#208284=AXIS2_PLACEMENT_3D ( 'NONE', #105397, #125013, #207115 ) ;
#208310=ORIENTED_EDGE ( 'NONE', *, *, #79922, .T. ) ;
#208317=ADVANCED_FACE ( 'NONE', ( #157913 ), #156617, .T. ) ;
#208322=ORIENTED_EDGE ( 'NONE', *, *, #207916, .F. ) ;
#208337=DIRECTION ( 'NONE',  ( 0.000000000000000000, -0.9916376685811618685, 0.1290532225514649800 ) ) ;
#208344=ORIENTED_EDGE ( 'NONE', *, *, #82573, .F. ) ;
#208357=CARTESIAN_POINT ( 'NONE',  ( 20.94999999999999929, 67.23127455305841238, -235.8551265064783991 ) ) ;
#208387=VERTEX_POINT ( 'NONE', #213519 ) ;
#208441=CARTESIAN_POINT ( 'NONE',  ( 21.05000000000000071, 86.45856254523212669, -209.4679346046102921 ) ) ;
#208452=DIRECTION ( 'NONE',  ( -1.000000000000000000, 0.000000000000000000, 0.000000000000000000 ) ) ;
#208468=DIRECTION ( 'NONE',  ( 0.000000000000000000, 0.9651348961777157509, -0.2617529984165031243 ) ) ;
#208480=CARTESIAN_POINT ( 'NONE',  ( 23.14999999999999503, 59.19392724319016708, -220.9828015967491126 ) ) ;
#208489=ORIENTED_EDGE ( 'NONE', *, *, #39419, .T. ) ;
#208495=AXIS2_PLACEMENT_3D ( 'NONE', #73431, #134630, #214201 ) ;
#208522=CYLINDRICAL_SURFACE ( 'NONE', #77274, 0.09999999999999543976 ) ;
#208535=CYLINDRICAL_SURFACE ( 'NONE', #155168, 0.1000000000000106498 ) ;
#208548=DIRECTION ( 'NONE',  ( 0.000000000000000000, -0.7035695228903323661, -0.7106264324241465813 ) ) ;
#208552=CARTESIAN_POINT ( 'NONE',  ( 21.07933241753356768, 61.09883511494023622, -234.2887083548779685 ) ) ;
#208584=EDGE_CURVE ( 'NONE', #45271, #12116, #105917, .T. ) ;
#208586=CARTESIAN_POINT ( 'NONE',  ( 20.12481660106788439, 60.19028478040584673, -225.4222410168123929 ) ) ;
#208623=ORIENTED_EDGE ( 'NONE', *, *, #45849, .T. ) ;
#208630=DIRECTION ( 'NONE',  ( 1.000000000000000000, 0.000000000000000000, 0.000000000000000000 ) ) ;
#208637=ORIENTED_EDGE ( 'NONE', *, *, #138131, .F. ) ;
#208638=EDGE_CURVE ( 'NONE', #56738, #162791, #160135, .T. ) ;
#208653=VECTOR ( 'NONE', #96561, 1000.000000000000000 ) ;
#208676=CARTESIAN_POINT ( 'NONE',  ( 19.75857864376268935, 62.49201502323811752, -208.8221019049098857 ) ) ;
#208677=CARTESIAN_POINT ( 'NONE',  ( -20.64999999999999858, 82.57900542960499024, -215.5587758314583482 ) ) ;
#208689=DIRECTION ( 'NONE',  ( 1.000000000000000000, 0.000000000000000000, 0.000000000000000000 ) ) ;
#208699=DIRECTION ( 'NONE',  ( 0.000000000000000000, -0.4105728183244014562, -0.9118278131605539460 ) ) ;
#208710=CARTESIAN_POINT ( 'NONE',  ( -18.50000000000000000, 70.47363787294415260, -228.3418745167492432 ) ) ;
#208725=EDGE_CURVE ( 'NONE', #60383, #242024, #222429, .T. ) ;
#208741=CARTESIAN_POINT ( 'NONE',  ( 21.05000000000000071, 78.08573236070779444, -228.9307947190811774 ) ) ;
#208766=AXIS2_PLACEMENT_3D ( 'NONE', #2168, #41343, #102532 ) ;
#208778=ORIENTED_EDGE ( 'NONE', *, *, #124433, .T. ) ;
#208781=EDGE_CURVE ( 'NONE', #181475, #132493, #96362, .T. ) ;
#208815=CARTESIAN_POINT ( 'NONE',  ( 21.05000000000000071, 82.48249193998721296, -215.5326005316167084 ) ) ;
#208840=DIRECTION ( 'NONE',  ( 0.000000000000000000, 0.9916376685811618685, -0.1290532225514649800 ) ) ;
#208848=CARTESIAN_POINT ( 'NONE',  ( 18.59999999999999432, 68.22930980752001062, -227.7331931781284879 ) ) ;
#208850=CARTESIAN_POINT ( 'NONE',  ( 20.95556889135987788, 58.98008573395630805, -225.6988595695161166 ) ) ;
#208856=EDGE_CURVE ( 'NONE', #247, #220817, #61104, .T. ) ;
#208879=CARTESIAN_POINT ( 'NONE',  ( -21.05000000000000071, 61.18226735070197009, -234.2477531894260494 ) ) ;
#208927=ORIENTED_EDGE ( 'NONE', *, *, #247502, .T. ) ;
#208983=CARTESIAN_POINT ( 'NONE',  ( -18.39999999999999858, 87.01908966642815813, -199.5693496768551825 ) ) ;
#209013=AXIS2_PLACEMENT_3D ( 'NONE', #126089, #45288, #88234 ) ;
#209023=DIRECTION ( 'NONE',  ( -1.836970198721029934E-16, -0.9651348961777157509, 0.2617529984165031243 ) ) ;
#209073=CARTESIAN_POINT ( 'NONE',  ( -20.00857864376270001, 63.76951449014745066, -212.8986194275075832 ) ) ;
#209083=ADVANCED_FACE ( 'NONE', ( #248737 ), #170535, .F. ) ;
#209110=DIRECTION ( 'NONE',  ( 0.000000000000000000, -0.2617529984165031243, -0.9651348961777157509 ) ) ;
#209112=ORIENTED_EDGE ( 'NONE', *, *, #154989, .T. ) ;
#209119=AXIS2_PLACEMENT_3D ( 'NONE', #147829, #95541, #132111 ) ;
#209130=ORIENTED_EDGE ( 'NONE', *, *, #41732, .T. ) ;
#209169=EDGE_CURVE ( 'NONE', #198528, #44180, #10286, .T. ) ;
#209191=ORIENTED_EDGE ( 'NONE', *, *, #17523, .T. ) ;
#209201=ORIENTED_EDGE ( 'NONE', *, *, #29941, .T. ) ;
#209254=DIRECTION ( 'NONE',  ( 1.000000000000000000, 0.000000000000000000, 0.000000000000000000 ) ) ;
#209264=FACE_BOUND ( 'NONE', #66296, .T. ) ;
#209298=ORIENTED_EDGE ( 'NONE', *, *, #140664, .F. ) ;
#209307=EDGE_CURVE ( 'NONE', #235134, #50332, #234746, .T. ) ;
#209316=CARTESIAN_POINT ( 'NONE',  ( 18.59999999999999076, 70.08587962373171365, -198.1273832143211848 ) ) ;
#209318=AXIS2_PLACEMENT_3D ( 'NONE', #228824, #90570, #167579 ) ;
#209325=DIRECTION ( 'NONE',  ( 0.000000000000000000, 0.9916376685811618685, -0.1290532225514649800 ) ) ;
#209338=PLANE ( 'NONE',  #144357 ) ;
#209411=CARTESIAN_POINT ( 'NONE',  ( 18.59999999999999432, 71.84303044094815505, -225.1053209871248271 ) ) ;
#209412=DIRECTION ( 'NONE',  ( 1.000000000000000000, 0.000000000000000000, 0.000000000000000000 ) ) ;
#209432=CIRCLE ( 'NONE', #230277, 0.09999999999998951394 ) ;
#209452=AXIS2_PLACEMENT_3D ( 'NONE', #133835, #255000, #95978 ) ;
#209458=DIRECTION ( 'NONE',  ( 1.000000000000000000, 0.000000000000000000, 0.000000000000000000 ) ) ;
#209491=EDGE_CURVE ( 'NONE', #252057, #122792, #18267, .T. ) ;
#209499=DIRECTION ( 'NONE',  ( 0.000000000000000000, -0.9121259477928120862, 0.4099100576505341209 ) ) ;
#209502=ORIENTED_EDGE ( 'NONE', *, *, #198687, .F. ) ;
#209510=DIRECTION ( 'NONE',  ( 0.000000000000000000, -0.2617529984165078982, -0.9651348961777145297 ) ) ;
#209541=EDGE_LOOP ( 'NONE', ( #114586, #126869, #231716, #147434 ) ) ;
#209561=FACE_OUTER_BOUND ( 'NONE', #205613, .T. ) ;
#209585=EDGE_CURVE ( 'NONE', #43859, #29044, #47271, .T. ) ;
#209588=CARTESIAN_POINT ( 'NONE',  ( -20.85000000000000142, 79.16909458115067366, -196.2854372848902926 ) ) ;
#209644=DIRECTION ( 'NONE',  ( 1.000000000000000000, 0.000000000000000000, 0.000000000000000000 ) ) ;
#209648=DIRECTION ( 'NONE',  ( 0.000000000000000000, 0.2617529984165152257, 0.9651348961777124202 ) ) ;
#209657=VECTOR ( 'NONE', #19917, 1000.000000000000000 ) ;
#209660=EDGE_LOOP ( 'NONE', ( #188026, #64591 ) ) ;
#209703=ORIENTED_EDGE ( 'NONE', *, *, #163982, .T. ) ;
#209710=EDGE_CURVE ( 'NONE', #157096, #148469, #43384, .T. ) ;
#209733=DIRECTION ( 'NONE',  ( 0.000000000000000000, 0.2617529984165152257, 0.9651348961777124202 ) ) ;
#209741=ORIENTED_EDGE ( 'NONE', *, *, #247748, .F. ) ;
#209749=CARTESIAN_POINT ( 'NONE',  ( -20.94999999999999929, 79.10508929521364507, -235.9670348125907537 ) ) ;
#209754=ORIENTED_EDGE ( 'NONE', *, *, #230150, .T. ) ;
#209769=DIRECTION ( 'NONE',  ( -0.000000000000000000, -0.2617529984165031243, -0.9651348961777157509 ) ) ;
#209770=EDGE_CURVE ( 'NONE', #207394, #222651, #184840, .T. ) ;
#209781=B_SPLINE_CURVE_WITH_KNOTS ( 'NONE', 3,
 ( #160732, #240248, #61596, #201103, #101973, #2886, #70615, #148850, #108429, #110994 ),
 .UNSPECIFIED., .F., .F.,
 ( 4, 3, 3, 4 ),
 ( 0.000000000000000000, 0.0002000000000008546862, 0.001000000000082975097, 0.001967863649483340624 ),
 .UNSPECIFIED. ) ;
#209782=ORIENTED_EDGE ( 'NONE', *, *, #210388, .T. ) ;
#209789=AXIS2_PLACEMENT_3D ( 'NONE', #68015, #230967, #251785 ) ;
#209790=CARTESIAN_POINT ( 'NONE',  ( 20.99780126800947144, 62.98982820228305002, -207.1569994557046073 ) ) ;
#209798=CARTESIAN_POINT ( 'NONE',  ( 20.85000000000000142, 76.00000000001126921, -203.5231074845248997 ) ) ;
#209808=EDGE_CURVE ( 'NONE', #133447, #29429, #189143, .T. ) ;
#209816=DIRECTION ( 'NONE',  ( 0.000000000000000000, -0.2617529984165152257, -0.9651348961777124202 ) ) ;
#209826=VERTEX_POINT ( 'NONE', #206108 ) ;
#209848=ADVANCED_FACE ( 'NONE', ( #69194 ), #110858, .F. ) ;
#209861=AXIS2_PLACEMENT_3D ( 'NONE', #122615, #104292, #182587 ) ;
#209863=AXIS2_PLACEMENT_3D ( 'NONE', #38210, #198543, #135986 ) ;
#209868=ADVANCED_FACE ( 'NONE', ( #245245 ), #114104, .F. ) ;
#209902=VERTEX_POINT ( 'NONE', #194280 ) ;
#209924=VECTOR ( 'NONE', #126296, 1000.000000000000000 ) ;
#209933=CARTESIAN_POINT ( 'NONE',  ( -18.59999999999999787, 70.22659352830977753, -197.9852579278363578 ) ) ;
#209951=CARTESIAN_POINT ( 'NONE',  ( 21.14999999999999858, 59.07123845373075000, -221.0531397865252075 ) ) ;
#209993=ADVANCED_FACE ( 'NONE', ( #16908 ), #36488, .F. ) ;
#209998=DIRECTION ( 'NONE',  ( -1.000000000000000000, -0.000000000000000000, 0.000000000000000000 ) ) ;
#210003=ADVANCED_FACE ( 'NONE', ( #52154 ), #37766, .T. ) ;
#210048=AXIS2_PLACEMENT_3D ( 'NONE', #209798, #211076, #69018 ) ;
#210050=DIRECTION ( 'NONE',  ( 0.000000000000000000, 0.2617529984165031243, 0.9651348961777157509 ) ) ;
#210075=CARTESIAN_POINT ( 'NONE',  ( 20.12500000000000000, 59.94448977088796937, -225.4740812377367263 ) ) ;
#210076=CIRCLE ( 'NONE', #172516, 0.09999999999999918676 ) ;
#210080=VECTOR ( 'NONE', #243802, 1000.000000000000000 ) ;
#210155=EDGE_CURVE ( 'NONE', #110447, #79096, #118610, .T. ) ;
#210181=EDGE_CURVE ( 'NONE', #197069, #163468, #45444, .T. ) ;
#210196=ADVANCED_FACE ( 'NONE', ( #107987, #147093, #126252 ), #188799, .F. ) ;
#210200=DIRECTION ( 'NONE',  ( 1.000000000000000000, -2.849773892568378313E-16, 7.728835255496647986E-17 ) ) ;
#210217=ORIENTED_EDGE ( 'NONE', *, *, #234766, .T. ) ;
#210223=CIRCLE ( 'NONE', #164428, 0.09999999999999395484 ) ;
#210256=AXIS2_PLACEMENT_3D ( 'NONE', #212407, #254069, #155011 ) ;
#210265=ORIENTED_EDGE ( 'NONE', *, *, #54254, .F. ) ;
#210304=ORIENTED_EDGE ( 'NONE', *, *, #122609, .F. ) ;
#210332=CARTESIAN_POINT ( 'NONE',  ( 21.05000000000000071, 65.65271564877468791, -222.5736063831752176 ) ) ;
#210337=CARTESIAN_POINT ( 'NONE',  ( -20.94999999999999929, 71.93512633425886804, -225.1442869522136334 ) ) ;
#210353=SPHERICAL_SURFACE ( 'NONE', #208495, 0.1000000000000000056 ) ;
#210388=EDGE_CURVE ( 'NONE', #55134, #197715, #101795, .T. ) ;
#210424=DIRECTION ( 'NONE',  ( -1.000000000000000000, -0.000000000000000000, -0.000000000000000000 ) ) ;
#210429=EDGE_CURVE ( 'NONE', #197715, #213407, #72828, .T. ) ;
#210434=DIRECTION ( 'NONE',  ( -1.000000000000000000, 0.000000000000000000, 0.000000000000000000 ) ) ;
#210451=CARTESIAN_POINT ( 'NONE',  ( 21.97500000000000497, 63.35728523183471594, -212.8904317177587870 ) ) ;
#210479=ADVANCED_FACE ( 'NONE', ( #146770 ), #107667, .T. ) ;
#210526=EDGE_CURVE ( 'NONE', #179646, #88490, #243667, .T. ) ;
#210539=EDGE_LOOP ( 'NONE', ( #184021, #147466, #125282, #35665, #117171 ) ) ;
#210566=ORIENTED_EDGE ( 'NONE', *, *, #37378, .F. ) ;
#210629=PLANE ( 'NONE',  #73513 ) ;
#210631=VERTEX_POINT ( 'NONE', #151962 ) ;
#210633=CARTESIAN_POINT ( 'NONE',  ( 22.40000000000010516, 64.18196446391901588, -247.0985338183336353 ) ) ;
#210636=CARTESIAN_POINT ( 'NONE',  ( -21.05000000000000071, 67.63082410804655353, -211.8415745842588649 ) ) ;
#210654=CARTESIAN_POINT ( 'NONE',  ( 23.25000000000000000, 86.52890073500824997, -209.5906233940697234 ) ) ;
#210678=FACE_OUTER_BOUND ( 'NONE', #149823, .T. ) ;
#210721=ORIENTED_EDGE ( 'NONE', *, *, #249562, .F. ) ;
#210733=DIRECTION ( 'NONE',  ( -4.336808689941751890E-15, -0.9667078373770149335, -0.2558827019434000150 ) ) ;
#210745=ORIENTED_EDGE ( 'NONE', *, *, #51760, .F. ) ;
#210752=DIRECTION ( 'NONE',  ( -0.000000000000000000, 0.2617529984165037349, 0.9651348961777156399 ) ) ;
#210755=CARTESIAN_POINT ( 'NONE',  ( 18.59999999999999076, 52.91185528119410009, -244.1460391050142675 ) ) ;
#210756=CARTESIAN_POINT ( 'NONE',  ( -18.50000324121759121, 67.49461024981998492, -195.5605382655040216 ) ) ;
#210769=CARTESIAN_POINT ( 'NONE',  ( -21.14999999999999858, 65.69183180257304855, -241.9133949074307566 ) ) ;
#210779=LINE ( 'NONE', #146935, #156483 ) ;
#210786=VERTEX_POINT ( 'NONE', #18834 ) ;
#210787=DIRECTION ( 'NONE',  ( 0.000000000000000000, 0.7216758089626587047, -0.6922311945860948335 ) ) ;
#210789=ORIENTED_EDGE ( 'NONE', *, *, #1803, .T. ) ;
#210798=DIRECTION ( 'NONE',  ( 0.000000000000000000, 0.2617529984165032908, 0.9651348961777156399 ) ) ;
#210805=ORIENTED_EDGE ( 'NONE', *, *, #121668, .T. ) ;
#210840=ADVANCED_FACE ( 'NONE', ( #103491 ), #125643, .F. ) ;
#210851=DIRECTION ( 'NONE',  ( 1.000000000000000000, 0.000000000000000000, 0.000000000000000000 ) ) ;
#210854=CARTESIAN_POINT ( 'NONE',  ( -23.15000000000000213, 68.63171270270233038, -223.0506438513196770 ) ) ;
#210875=CARTESIAN_POINT ( 'NONE',  ( -21.05000000000000071, 64.21185867012613357, -224.4479740254296303 ) ) ;
#210886=DIRECTION ( 'NONE',  ( 0.000000000000000000, 0.2617529984165152257, 0.9651348961777124202 ) ) ;
#210901=DIRECTION ( 'NONE',  ( -3.265361837132813093E-16, -0.9651348961777157509, 0.2617529984165031243 ) ) ;
#210904=CARTESIAN_POINT ( 'NONE',  ( -22.59999999999999787, 55.87393739788256397, -232.8427108587849261 ) ) ;
#210910=EDGE_CURVE ( 'NONE', #66847, #163406, #247937, .T. ) ;
#210931=ORIENTED_EDGE ( 'NONE', *, *, #63703, .F. ) ;
#210937=ORIENTED_EDGE ( 'NONE', *, *, #173127, .F. ) ;
#210940=CARTESIAN_POINT ( 'NONE',  ( -23.15000000000000213, 70.60814576644823148, -215.7631455941064189 ) ) ;
#210943=CARTESIAN_POINT ( 'NONE',  ( 22.57320508075687115, 55.89093952297024970, -232.7795287750844579 ) ) ;
#210993=EDGE_CURVE ( 'NONE', #75171, #229678, #127136, .T. ) ;
#211003=ORIENTED_EDGE ( 'NONE', *, *, #94958, .F. ) ;
#211005=EDGE_CURVE ( 'NONE', #174802, #248032, #98063, .T. ) ;
#211006=EDGE_CURVE ( 'NONE', #241107, #42365, #113777, .T. ) ;
#211033=CARTESIAN_POINT ( 'NONE',  ( 18.59999999999999432, 65.87552587769046397, -245.8195358697090001 ) ) ;
#211076=DIRECTION ( 'NONE',  ( -1.000000000000000000, -0.000000000000000000, -0.000000000000000000 ) ) ;
#211107=VERTEX_POINT ( 'NONE', #235026 ) ;
#211122=ORIENTED_EDGE ( 'NONE', *, *, #104602, .F. ) ;
#211125=CARTESIAN_POINT ( 'NONE',  ( -23.15000000000000213, 82.22731448072437388, -214.9453318841612486 ) ) ;
#211132=CARTESIAN_POINT ( 'NONE',  ( 20.77526135991770317, 60.82735416649695281, -225.3438353432380552 ) ) ;
#211135=TOROIDAL_SURFACE ( 'NONE', #73793, 0.2000000000000000111, 0.1000000000000000056 ) ;
#211141=EDGE_CURVE ( 'NONE', #62395, #9358, #159864, .T. ) ;
#211142=CARTESIAN_POINT ( 'NONE',  ( -20.85000000000000142, 87.24382154048164750, -206.5725299160771726 ) ) ;
#211159=CARTESIAN_POINT ( 'NONE',  ( -23.15000000000000213, 59.09741375357241111, -220.9566262969074444 ) ) ;
#211168=ORIENTED_EDGE ( 'NONE', *, *, #116727, .T. ) ;
#211175=AXIS2_PLACEMENT_3D ( 'NONE', #50822, #70457, #126541 ) ;
#211245=DIRECTION ( 'NONE',  ( -1.000000000000000000, 0.000000000000000000, 0.000000000000000000 ) ) ;
#211251=VERTEX_POINT ( 'NONE', #7647 ) ;
#211273=VECTOR ( 'NONE', #153723, 1000.000000000000000 ) ;
#211285=DIRECTION ( 'NONE',  ( -0.7071067811865431318, -0.6824534298469886462, 0.1850873201764167419 ) ) ;
#211290=DIRECTION ( 'NONE',  ( -0.7071067811865460184, -0.6824534298470606997, 0.1850873201761399356 ) ) ;
#211291=DIRECTION ( 'NONE',  ( 1.000000000000000000, 0.000000000000000000, 0.000000000000000000 ) ) ;
#211356=AXIS2_PLACEMENT_3D ( 'NONE', #85744, #87039, #207020 ) ;
#211365=LINE ( 'NONE', #229639, #16358 ) ;
#211369=CARTESIAN_POINT ( 'NONE',  ( -21.05000000000000071, 66.10573665986746050, -240.0052065600425237 ) ) ;
#211419=CARTESIAN_POINT ( 'NONE',  ( 20.95496329884391784, 59.01487433854230602, -225.7788383491038360 ) ) ;
#211458=ORIENTED_EDGE ( 'NONE', *, *, #172631, .T. ) ;
#211474=DIRECTION ( 'NONE',  ( 1.000000000000000000, 0.000000000000000000, 0.000000000000000000 ) ) ;
#211510=VERTEX_POINT ( 'NONE', #3465 ) ;
#211523=CARTESIAN_POINT ( 'NONE',  ( 20.94999999999999574, 68.09270462032664284, -227.9033695786537805 ) ) ;
#211553=DIRECTION ( 'NONE',  ( 1.000000000000000000, 0.000000000000000000, 0.000000000000000000 ) ) ;
#211679=DIRECTION ( 'NONE',  ( 0.000000000000000000, 0.9651348961776677893, -0.2617529984166795387 ) ) ;
#211694=CIRCLE ( 'NONE', #20146, 0.1000000000000132172 ) ;
#211704=ORIENTED_EDGE ( 'NONE', *, *, #221494, .F. ) ;
#211706=FACE_OUTER_BOUND ( 'NONE', #126511, .T. ) ;
#211725=AXIS2_PLACEMENT_3D ( 'NONE', #207978, #188388, #108848 ) ;
#211733=VERTEX_POINT ( 'NONE', #35902 ) ;
#211751=VERTEX_POINT ( 'NONE', #15050 ) ;
#211760=EDGE_LOOP ( 'NONE', ( #194969, #177407, #124588, #139259 ) ) ;
#211772=CIRCLE ( 'NONE', #141043, 0.1000000000000088318 ) ;
#211783=VECTOR ( 'NONE', #19088, 1000.000000000000000 ) ;
#211784=ADVANCED_FACE ( 'NONE', ( #90707 ), #194977, .T. ) ;
#211845=VECTOR ( 'NONE', #81081, 1000.000000000000000 ) ;
#211903=VECTOR ( 'NONE', #96449, 1000.000000000000000 ) ;
#211904=VERTEX_POINT ( 'NONE', #166140 ) ;
#211928=DIRECTION ( 'NONE',  ( -1.000000000000000000, 2.849773892568378313E-16, -7.728835255496647986E-17 ) ) ;
#211948=CARTESIAN_POINT ( 'NONE',  ( 20.94999999999999574, 60.83337574417771521, -225.3422414619149095 ) ) ;
#211956=DIRECTION ( 'NONE',  ( 0.7071067811865460184, 0.6824534298470606997, -0.1850873201761399356 ) ) ;
#211970=AXIS2_PLACEMENT_3D ( 'NONE', #226762, #187667, #212360 ) ;
#211983=FACE_OUTER_BOUND ( 'NONE', #227148, .T. ) ;
#211993=CARTESIAN_POINT ( 'NONE',  ( 18.59999999999999076, 63.85700577439690306, -209.2959117565043243 ) ) ;
#211996=CARTESIAN_POINT ( 'NONE',  ( 20.95512820512820440, 64.22684239030566289, -213.0226507412649255 ) ) ;
#212018=LINE ( 'NONE', #32104, #1573 ) ;
#212020=CIRCLE ( 'NONE', #253682, 2.000000000000000000 ) ;
#212060=CIRCLE ( 'NONE', #49557, 0.1999999999999987899 ) ;
#212078=ORIENTED_EDGE ( 'NONE', *, *, #172631, .F. ) ;
#212082=DIRECTION ( 'NONE',  ( -1.000000000000000000, -0.000000000000000000, 0.000000000000000000 ) ) ;
#212099=CARTESIAN_POINT ( 'NONE',  ( 22.49436431346199683, 64.11729402989250559, -247.0813885053079275 ) ) ;
#212100=CARTESIAN_POINT ( 'NONE',  ( 21.00000000000000000, 61.05385884576949707, -221.3836188041226762 ) ) ;
#212103=CARTESIAN_POINT ( 'NONE',  ( -20.99142135623731065, 62.99095723518624368, -207.1734234082435364 ) ) ;
#212157=ORIENTED_EDGE ( 'NONE', *, *, #122609, .T. ) ;
#212199=CIRCLE ( 'NONE', #116507, 0.1999999999999945155 ) ;
#212202=EDGE_CURVE ( 'NONE', #142261, #148565, #256810, .T. ) ;
#212210=EDGE_CURVE ( 'NONE', #41069, #87179, #107017, .T. ) ;
#212217=ORIENTED_EDGE ( 'NONE', *, *, #197516, .T. ) ;
#212226=CARTESIAN_POINT ( 'NONE',  ( 20.94999999999999929, 82.20113918088273408, -215.0418453737790401 ) ) ;
#212273=DIRECTION ( 'NONE',  ( 0.000000000000000000, 0.2617529984165030688, 0.9651348961777157509 ) ) ;
#212280=PLANE ( 'NONE',  #75730 ) ;
#212282=FACE_OUTER_BOUND ( 'NONE', #90323, .T. ) ;
#212286=ORIENTED_EDGE ( 'NONE', *, *, #124284, .F. ) ;
#212296=PLANE ( 'NONE',  #129652 ) ;
#212339=EDGE_CURVE ( 'NONE', #22805, #72701, #197913, .T. ) ;
#212358=CYLINDRICAL_SURFACE ( 'NONE', #187166, 0.1000000000000124678 ) ;
#212360=DIRECTION ( 'NONE',  ( 0.000000000000000000, 0.2617529984165180013, 0.9651348961777117541 ) ) ;
#212380=EDGE_LOOP ( 'NONE', ( #36470, #169756, #226629, #212552 ) ) ;
#212407=CARTESIAN_POINT ( 'NONE',  ( 23.14999999999999503, 66.34920340998563404, -213.7018660128499334 ) ) ;
#212415=CIRCLE ( 'NONE', #186906, 0.1000000000000018374 ) ;
#212477=CARTESIAN_POINT ( 'NONE',  ( 20.94999999999999929, 82.22731448072437388, -214.9453318841612486 ) ) ;
#212506=CARTESIAN_POINT ( 'NONE',  ( 20.94999999999999574, 71.93512633425886804, -225.1442869522136334 ) ) ;
#212529=DIRECTION ( 'NONE',  ( 0.000000000000000000, 0.9651348961777160840, -0.2617529984165015700 ) ) ;
#212552=ORIENTED_EDGE ( 'NONE', *, *, #5630, .T. ) ;
#212583=FACE_OUTER_BOUND ( 'NONE', #155765, .T. ) ;
#212605=CARTESIAN_POINT ( 'NONE',  ( -21.05000000000000071, 86.30329675166747450, -209.4258251677035787 ) ) ;
#212612=DIRECTION ( 'NONE',  ( 0.000000000000000000, -0.9651348961777157509, 0.2617529984165031243 ) ) ;
#212614=CIRCLE ( 'NONE', #170962, 0.8750000000000007772 ) ;
#212626=CYLINDRICAL_SURFACE ( 'NONE', #243586, 0.09999999999999961697 ) ;
#212629=DIRECTION ( 'NONE',  ( -1.000000000000000000, -0.000000000000000000, -0.000000000000000000 ) ) ;
#212644=CARTESIAN_POINT ( 'NONE',  ( -21.55000000000000426, 62.98412863812492901, -221.9071248009556712 ) ) ;
#212648=CARTESIAN_POINT ( 'NONE',  ( -21.07928932188134041, 65.47931918658504458, -241.9371126717015841 ) ) ;
#212671=DIRECTION ( 'NONE',  ( 0.000000000000000000, 0.2617529984164915779, 0.9651348961777189706 ) ) ;
#212695=ADVANCED_FACE ( 'NONE', ( #69990 ), #34714, .F. ) ;
#212712=CARTESIAN_POINT ( 'NONE',  ( 20.95568717954149562, 58.98889948345964740, -225.7425766489790533 ) ) ;
#212717=AXIS2_PLACEMENT_3D ( 'NONE', #107711, #187273, #86845 ) ;
#212727=CARTESIAN_POINT ( 'NONE',  ( -21.14999999999999858, 65.51923798433686841, -242.1677427744926092 ) ) ;
#212745=AXIS2_PLACEMENT_3D ( 'NONE', #123760, #62503, #23401 ) ;
#212792=ORIENTED_EDGE ( 'NONE', *, *, #24001, .F. ) ;
#212838=VERTEX_POINT ( 'NONE', #120671 ) ;
#212862=CIRCLE ( 'NONE', #100396, 0.1000000000000124678 ) ;
#212877=EDGE_CURVE ( 'NONE', #201773, #230992, #138879, .T. ) ;
#212893=DIRECTION ( 'NONE',  ( 0.000000000000000000, 0.2617529984165031243, 0.9651348961777157509 ) ) ;
#212917=CARTESIAN_POINT ( 'NONE',  ( 23.14999999999999858, 79.86053958472213310, -204.5701194781909180 ) ) ;
#212964=DIRECTION ( 'NONE',  ( 0.000000000000000000, 0.2617529984165031243, 0.9651348961777157509 ) ) ;
#212974=DIRECTION ( 'NONE',  ( -0.000000000000000000, -0.2617529984165030132, -0.9651348961777158619 ) ) ;
#212984=CARTESIAN_POINT ( 'NONE',  ( 23.24999999999999289, 59.07123845373075000, -221.0531397865252075 ) ) ;
#213020=TOROIDAL_SURFACE ( 'NONE', #34004, 0.4000000000000012990, 0.1000000000000000056 ) ;
#213034=EDGE_LOOP ( 'NONE', ( #15941, #74302, #170134, #170341 ) ) ;
#213036=CARTESIAN_POINT ( 'NONE',  ( 23.24999999999999289, 52.81534179157632991, -244.1198638051726277 ) ) ;
#213039=ORIENTED_EDGE ( 'NONE', *, *, #15550, .F. ) ;
#213108=EDGE_CURVE ( 'NONE', #171727, #94242, #144974, .T. ) ;
#213110=CIRCLE ( 'NONE', #17323, 0.1999999999999945155 ) ;
#213114=EDGE_CURVE ( 'NONE', #74489, #116965, #74294, .T. ) ;
#213167=CIRCLE ( 'NONE', #100710, 11.70000000000000817 ) ;
#213194=FACE_OUTER_BOUND ( 'NONE', #65558, .T. ) ;
#213221=EDGE_CURVE ( 'NONE', #19150, #178237, #240856, .T. ) ;
#213224=ORIENTED_EDGE ( 'NONE', *, *, #100915, .F. ) ;
#213246=VERTEX_POINT ( 'NONE', #10674 ) ;
#213337=ORIENTED_EDGE ( 'NONE', *, *, #28139, .F. ) ;
#213341=DIRECTION ( 'NONE',  ( 0.000000000000000000, -0.9651348961777157509, 0.2617529984165031243 ) ) ;
#213349=CARTESIAN_POINT ( 'NONE',  ( 22.42196299218230493, 64.17959721473168599, -247.0979341721383378 ) ) ;
#213369=LINE ( 'NONE', #59402, #202710 ) ;
#213385=CARTESIAN_POINT ( 'NONE',  ( 18.59999999999999432, 80.78317333349157536, -192.9003134612048882 ) ) ;
#213390=EDGE_CURVE ( 'NONE', #165864, #211107, #20101, .T. ) ;
#213407=VERTEX_POINT ( 'NONE', #36686 ) ;
#213416=EDGE_CURVE ( 'NONE', #111271, #151453, #78338, .T. ) ;
#213512=DIRECTION ( 'NONE',  ( -2.940209281316622002E-16, -0.9651348961777163060, 0.2617529984165007928 ) ) ;
#213519=CARTESIAN_POINT ( 'NONE',  ( 18.59999999999999432, 71.93512633425886804, -225.1442869522136334 ) ) ;
#213551=CIRCLE ( 'NONE', #30418, 0.6000000000000005329 ) ;
#213562=CARTESIAN_POINT ( 'NONE',  ( 20.94999999999999929, 86.27712145182582049, -209.5223386573213702 ) ) ;
#213588=ORIENTED_EDGE ( 'NONE', *, *, #218961, .F. ) ;
#213608=ADVANCED_FACE ( 'NONE', ( #32189 ), #182600, .T. ) ;
#213621=ADVANCED_FACE ( 'NONE', ( #86012 ), #195272, .F. ) ;
#213638=AXIS2_PLACEMENT_3D ( 'NONE', #93415, #118126, #115549 ) ;
#213653=DIRECTION ( 'NONE',  ( 0.000000000000000000, 0.2617529984165031243, 0.9651348961777157509 ) ) ;
#213662=CARTESIAN_POINT ( 'NONE',  ( -23.15000000000000213, 72.91131461869652242, -214.9116992594219369 ) ) ;
#213663=DIRECTION ( 'NONE',  ( 0.000000000000000000, -0.2617529984165031243, -0.9651348961777157509 ) ) ;
#213683=DIRECTION ( 'NONE',  ( 0.000000000000000000, 0.2617529984165152257, 0.9651348961777124202 ) ) ;
#213704=ORIENTED_EDGE ( 'NONE', *, *, #179070, .T. ) ;
#213717=FACE_OUTER_BOUND ( 'NONE', #82961, .T. ) ;
#213720=ADVANCED_FACE ( 'NONE', ( #97220 ), #207737, .F. ) ;
#213764=EDGE_CURVE ( 'NONE', #236044, #52, #70195, .T. ) ;
#213810=AXIS2_PLACEMENT_3D ( 'NONE', #158266, #100767, #98203 ) ;
#213818=CARTESIAN_POINT ( 'NONE',  ( 21.14999999999999503, 55.98745301258800566, -232.8057040749260977 ) ) ;
#213823=DIRECTION ( 'NONE',  ( 1.000000000000000000, 0.000000000000000000, 0.000000000000000000 ) ) ;
#213864=DIRECTION ( 'NONE',  ( -1.000000000000000000, -0.000000000000000000, -0.000000000000000000 ) ) ;
#213879=DIRECTION ( 'NONE',  ( 0.000000000000000000, 0.2617529984165044565, 0.9651348961777151958 ) ) ;
#213883=EDGE_CURVE ( 'NONE', #225653, #78723, #244726, .T. ) ;
#213893=ORIENTED_EDGE ( 'NONE', *, *, #218005, .F. ) ;
#213917=DIRECTION ( 'NONE',  ( -1.000000000000000000, -0.000000000000000000, 0.000000000000000000 ) ) ;
#213970=ADVANCED_FACE ( 'NONE', ( #163667 ), #224454, .F. ) ;
#213991=CIRCLE ( 'NONE', #255626, 0.09999999999999939493 ) ;
#214005=AXIS2_PLACEMENT_3D ( 'NONE', #157614, #237111, #123581 ) ;
#214063=ORIENTED_EDGE ( 'NONE', *, *, #164578, .T. ) ;
#214120=CARTESIAN_POINT ( 'NONE',  ( -21.05000000000000071, 57.76315019072730905, -226.2583585926041110 ) ) ;
#214126=AXIS2_PLACEMENT_3D ( 'NONE', #45643, #251185, #210798 ) ;
#214128=DIRECTION ( 'NONE',  ( 0.000000000000000000, 0.9651348961777157509, -0.2617529984165028467 ) ) ;
#214135=LINE ( 'NONE', #18505, #94567 ) ;
#214150=DIRECTION ( 'NONE',  ( 4.377807931758638789E-15, -0.5041370733442360752, -0.8636236514129915776 ) ) ;
#214154=EDGE_CURVE ( 'NONE', #232695, #66196, #76112, .T. ) ;
#214158=CARTESIAN_POINT ( 'NONE',  ( 21.53752568622107333, 65.35928353583771866, -242.3794047578606410 ) ) ;
#214201=DIRECTION ( 'NONE',  ( 1.000000000000000000, 0.000000000000000000, 0.000000000000000000 ) ) ;
#214212=DIRECTION ( 'NONE',  ( 0.000000000000000000, 0.2617529984164955192, 0.9651348961777178603 ) ) ;
#214214=DIRECTION ( 'NONE',  ( 0.000000000000000000, -0.2617529984165031243, -0.9651348961777157509 ) ) ;
#214223=DIRECTION ( 'NONE',  ( -1.000000000000000000, 0.000000000000000000, 0.000000000000000000 ) ) ;
#214258=ORIENTED_EDGE ( 'NONE', *, *, #27098, .F. ) ;
#214280=ADVANCED_FACE ( 'NONE', ( #220768 ), #219785, .F. ) ;
#214282=ADVANCED_FACE ( 'NONE', ( #44708 ), #111650, .F. ) ;
#214319=DIRECTION ( 'NONE',  ( 1.000000000000000000, 0.000000000000000000, 0.000000000000000000 ) ) ;
#214332=ORIENTED_EDGE ( 'NONE', *, *, #140664, .T. ) ;
#214334=ORIENTED_EDGE ( 'NONE', *, *, #238731, .T. ) ;
#214337=EDGE_LOOP ( 'NONE', ( #73057, #216297, #121417, #243540 ) ) ;
#214339=CIRCLE ( 'NONE', #10348, 0.1000000000000124678 ) ;
#214406=CARTESIAN_POINT ( 'NONE',  ( 21.10642757222115407, 60.08602150078414894, -221.2343838615410618 ) ) ;
#214413=DIRECTION ( 'NONE',  ( 1.000000000000000000, 0.000000000000000000, 0.000000000000000000 ) ) ;
#214415=CARTESIAN_POINT ( 'NONE',  ( 21.00000000000000000, 63.35728523183471594, -212.8904317177587870 ) ) ;
#214487=LINE ( 'NONE', #95807, #235842 ) ;
#214493=FACE_OUTER_BOUND ( 'NONE', #37450, .T. ) ;
#214516=CYLINDRICAL_SURFACE ( 'NONE', #43342, 0.1000000000000124678 ) ;
#214539=CIRCLE ( 'NONE', #10556, 0.1999999999999981515 ) ;
#214541=DIRECTION ( 'NONE',  ( 1.000000000000000000, 0.000000000000000000, 0.000000000000000000 ) ) ;
#214546=CARTESIAN_POINT ( 'NONE',  ( 23.24999999999999645, 67.92720994251783395, -214.1870976236629929 ) ) ;
#214563=CARTESIAN_POINT ( 'NONE',  ( 21.05000000000000426, 61.06350993105852609, -234.0935366736971162 ) ) ;
#214605=AXIS2_PLACEMENT_3D ( 'NONE', #28052, #128409, #150546 ) ;
#214619=DIRECTION ( 'NONE',  ( -3.265361837132813093E-16, -0.9651348961777146407, 0.2617529984165072321 ) ) ;
#214621=ORIENTED_EDGE ( 'NONE', *, *, #128913, .F. ) ;
#214691=CARTESIAN_POINT ( 'NONE',  ( 23.15000000000000213, 86.27712145182582049, -209.5223386573213702 ) ) ;
#214710=DIRECTION ( 'NONE',  ( 0.000000000000000000, -0.2617529984163859957, -0.9651348961777475033 ) ) ;
#214726=ORIENTED_EDGE ( 'NONE', *, *, #236653, .F. ) ;
#214730=EDGE_CURVE ( 'NONE', #142564, #158004, #186863, .T. ) ;
#214757=EDGE_CURVE ( 'NONE', #252099, #60383, #103429, .T. ) ;
#214780=ADVANCED_FACE ( 'NONE', ( #181354 ), #60086, .T. ) ;
#214804=ORIENTED_EDGE ( 'NONE', *, *, #110469, .T. ) ;
#214805=CARTESIAN_POINT ( 'NONE',  ( 20.85000000000000142, 79.19526988099229925, -196.1889237952725296 ) ) ;
#214835=AXIS2_PLACEMENT_3D ( 'NONE', #49551, #11727, #251599 ) ;
#214839=CARTESIAN_POINT ( 'NONE',  ( 20.94999999999999929, 67.44464249442897597, -214.0562211244547655 ) ) ;
#214853=CARTESIAN_POINT ( 'NONE',  ( -23.25000000000000000, 67.23127455305841238, -235.8551265064783991 ) ) ;
#214855=ADVANCED_FACE ( 'NONE', ( #143482 ), #88939, .T. ) ;
#214869=EDGE_CURVE ( 'NONE', #122630, #128703, #24858, .T. ) ;
#214891=DIRECTION ( 'NONE',  ( 0.000000000000000000, 0.2617529984165152257, 0.9651348961777124202 ) ) ;
#214899=DIRECTION ( 'NONE',  ( 0.000000000000000000, -0.2617529984165031243, -0.9651348961777157509 ) ) ;
#214902=ORIENTED_EDGE ( 'NONE', *, *, #9229, .F. ) ;
#214903=ORIENTED_EDGE ( 'NONE', *, *, #113890, .F. ) ;
#214911=CARTESIAN_POINT ( 'NONE',  ( 20.94999999999999574, 62.98323157773585734, -207.0610388790105958 ) ) ;
#214912=DIRECTION ( 'NONE',  ( 0.000000000000000000, 0.2617529984165152257, 0.9651348961777124202 ) ) ;
#214938=CARTESIAN_POINT ( 'NONE',  ( -22.50000000000000000, 55.96169194136206215, -232.9023299069559130 ) ) ;
#214958=CARTESIAN_POINT ( 'NONE',  ( -21.05000000000000071, 68.13014604066189861, -227.7202878558733516 ) ) ;
#214991=EDGE_CURVE ( 'NONE', #193988, #165270, #31288, .T. ) ;
#215025=CIRCLE ( 'NONE', #102563, 0.09999999999999657774 ) ;
#215062=ORIENTED_EDGE ( 'NONE', *, *, #55888, .F. ) ;
#215077=ORIENTED_EDGE ( 'NONE', *, *, #136189, .T. ) ;
#215131=ORIENTED_EDGE ( 'NONE', *, *, #234164, .F. ) ;
#215135=DIRECTION ( 'NONE',  ( 0.000000000000000000, 0.2617529984165152257, 0.9651348961777124202 ) ) ;
#215162=CARTESIAN_POINT ( 'NONE',  ( 22.50000000000000000, 67.23127455305841238, -235.8551265064783991 ) ) ;
#215206=DIRECTION ( 'NONE',  ( 0.000000000000000000, -0.9667078373770112698, -0.2558827019434132821 ) ) ;
#215236=CYLINDRICAL_SURFACE ( 'NONE', #239890, 0.09999999999999939493 ) ;
#215260=EDGE_LOOP ( 'NONE', ( #19612, #216706, #57366, #220223 ) ) ;
#215292=AXIS2_PLACEMENT_3D ( 'NONE', #373, #79885, #232607 ) ;
#215300=DIRECTION ( 'NONE',  ( 0.000000000000000000, 0.2617529984165031243, 0.9651348961777157509 ) ) ;
#215303=EDGE_CURVE ( 'NONE', #228033, #189967, #87041, .T. ) ;
#215313=DIRECTION ( 'NONE',  ( -0.000000000000000000, -0.9651348961777157509, 0.2617529984165031243 ) ) ;
#215318=EDGE_CURVE ( 'NONE', #77283, #79198, #143161, .T. ) ;
#215342=DIRECTION ( 'NONE',  ( -1.000000000000000000, -0.000000000000000000, -0.000000000000000000 ) ) ;
#215348=ORIENTED_EDGE ( 'NONE', *, *, #17558, .T. ) ;
#215414=DIRECTION ( 'NONE',  ( 1.000000000000000000, 0.000000000000000000, 0.000000000000000000 ) ) ;
#215434=FACE_OUTER_BOUND ( 'NONE', #252997, .T. ) ;
#215441=DIRECTION ( 'NONE',  ( -3.265361837132813093E-16, -0.9651348961777157509, 0.2617529984165031243 ) ) ;
#215455=ORIENTED_EDGE ( 'NONE', *, *, #156511, .F. ) ;
#215514=AXIS2_PLACEMENT_3D ( 'NONE', #116005, #134247, #57271 ) ;
#215519=ORIENTED_EDGE ( 'NONE', *, *, #193954, .F. ) ;
#215527=ORIENTED_EDGE ( 'NONE', *, *, #97299, .T. ) ;
#215536=CARTESIAN_POINT ( 'NONE',  ( 18.59999999999999076, 66.37537870982728805, -213.6053525232321704 ) ) ;
#215540=AXIS2_PLACEMENT_3D ( 'NONE', #184910, #181080, #6255 ) ;
#215562=ORIENTED_EDGE ( 'NONE', *, *, #48003, .T. ) ;
#215577=CARTESIAN_POINT ( 'NONE',  ( 18.59999999999999432, 70.44746257310249860, -228.4383880063670347 ) ) ;
#215601=EDGE_CURVE ( 'NONE', #88487, #255725, #235541, .T. ) ;
#215618=CARTESIAN_POINT ( 'NONE',  ( -20.64999999999999858, 66.23941198528750363, -222.8935984851895853 ) ) ;
#215621=VECTOR ( 'NONE', #80133, 1000.000000000000000 ) ;
#215638=ADVANCED_FACE ( 'NONE', ( #229787 ), #49862, .T. ) ;
#215641=DIRECTION ( 'NONE',  ( 0.000000000000000000, -0.2617529984172316526, -0.9651348961775180202 ) ) ;
#215655=CIRCLE ( 'NONE', #232271, 0.4000000000000085154 ) ;
#215685=AXIS2_PLACEMENT_3D ( 'NONE', #167112, #44567, #245337 ) ;
#215687=CARTESIAN_POINT ( 'NONE',  ( -23.15000000000000213, 73.42097182497056451, -249.7082903213649558 ) ) ;
#215689=DIRECTION ( 'NONE',  ( 0.000000000000000000, -0.2617529984165031243, -0.9651348961777157509 ) ) ;
#215700=AXIS2_PLACEMENT_3D ( 'NONE', #67216, #227570, #9809 ) ;
#215712=PLANE ( 'NONE',  #56970 ) ;
#215727=DIRECTION ( 'NONE',  ( 0.000000000000000000, 0.7049548389605067023, -0.7092521942342977503 ) ) ;
#215748=AXIS2_PLACEMENT_3D ( 'NONE', #53077, #33569, #192599 ) ;
#215754=CARTESIAN_POINT ( 'NONE',  ( -18.59999999999999787, 80.78317333349157536, -192.9003134612049166 ) ) ;
#215781=VECTOR ( 'NONE', #20466, 1000.000000000000114 ) ;
#215793=CARTESIAN_POINT ( 'NONE',  ( -21.05000000000000071, 68.20313450767837082, -227.8297066677462794 ) ) ;
#215797=AXIS2_PLACEMENT_3D ( 'NONE', #97794, #1275, #41727 ) ;
#215820=AXIS2_PLACEMENT_3D ( 'NONE', #60231, #5372, #62808 ) ;
#215824=CARTESIAN_POINT ( 'NONE',  ( 18.49999999999999289, 63.61019970229975229, -209.1253633388161006 ) ) ;
#215840=ORIENTED_EDGE ( 'NONE', *, *, #57206, .T. ) ;
#215869=CARTESIAN_POINT ( 'NONE',  ( -18.52643265882458579, 67.49293571122092317, -195.4648732548341741 ) ) ;
#215881=AXIS2_PLACEMENT_3D ( 'NONE', #232188, #53527, #133073 ) ;
#215885=VERTEX_POINT ( 'NONE', #248929 ) ;
#215920=DIRECTION ( 'NONE',  ( 0.000000000000000000, 0.9651348961777163060, -0.2617529984165013479 ) ) ;
#215927=FACE_OUTER_BOUND ( 'NONE', #206369, .T. ) ;
#215929=EDGE_CURVE ( 'NONE', #251815, #251232, #233674, .T. ) ;
#215963=CARTESIAN_POINT ( 'NONE',  ( -20.94999999999999929, 68.17695920783671681, -227.9262201573640141 ) ) ;
#215981=ORIENTED_EDGE ( 'NONE', *, *, #60834, .F. ) ;
#215987=DIRECTION ( 'NONE',  ( -1.000000000000000000, -0.000000000000000000, 0.000000000000000000 ) ) ;
#215995=ORIENTED_EDGE ( 'NONE', *, *, #199277, .F. ) ;
#216022=VERTEX_POINT ( 'NONE', #237105 ) ;
#216027=AXIS2_PLACEMENT_3D ( 'NONE', #71740, #173451, #152579 ) ;
#216037=VERTEX_POINT ( 'NONE', #201820 ) ;
#216094=CARTESIAN_POINT ( 'NONE',  ( -20.64999999999999858, 66.26558728512915764, -222.7970849955717938 ) ) ;
#216119=DIRECTION ( 'NONE',  ( 0.000000000000000000, -0.2617529984165701262, -0.9651348961776977653 ) ) ;
#216159=ORIENTED_EDGE ( 'NONE', *, *, #123051, .F. ) ;
#216162=ADVANCED_FACE ( 'NONE', ( #206960 ), #71321, .T. ) ;
#216173=ORIENTED_EDGE ( 'NONE', *, *, #238707, .F. ) ;
#216179=ORIENTED_EDGE ( 'NONE', *, *, #109401, .F. ) ;
#216192=CIRCLE ( 'NONE', #107870, 4.000000000000000000 ) ;
#216233=EDGE_CURVE ( 'NONE', #256658, #166855, #238585, .T. ) ;
#216262=ORIENTED_EDGE ( 'NONE', *, *, #91200, .F. ) ;
#216268=VECTOR ( 'NONE', #64152, 1000.000000000000000 ) ;
#216275=EDGE_CURVE ( 'NONE', #101319, #137094, #76079, .T. ) ;
#216292=CIRCLE ( 'NONE', #112273, 11.80000000000000071 ) ;
#216297=ORIENTED_EDGE ( 'NONE', *, *, #233944, .F. ) ;
#216326=ORIENTED_EDGE ( 'NONE', *, *, #90242, .F. ) ;
#216338=ORIENTED_EDGE ( 'NONE', *, *, #37698, .F. ) ;
#216344=CARTESIAN_POINT ( 'NONE',  ( -21.05000000000000071, 68.03098227380377239, -227.7073825336181869 ) ) ;
#216348=CIRCLE ( 'NONE', #195539, 11.75000000000000178 ) ;
#216356=ADVANCED_FACE ( 'NONE', ( #12328 ), #255093, .F. ) ;
#216381=EDGE_CURVE ( 'NONE', #185866, #55604, #50132, .T. ) ;
#216401=CIRCLE ( 'NONE', #137283, 0.1000000000000124678 ) ;
#216423=CARTESIAN_POINT ( 'NONE',  ( -18.59999999999999787, 65.82247307196232100, -213.3517872345644832 ) ) ;
#216449=DIRECTION ( 'NONE',  ( 0.000000000000000000, -0.2617529984165031243, -0.9651348961777157509 ) ) ;
#216474=CARTESIAN_POINT ( 'NONE',  ( -23.25000000000000000, 79.15532900748003442, -196.2806010913881778 ) ) ;
#216484=ADVANCED_FACE ( 'NONE', ( #72292 ), #146649, .T. ) ;
#216510=EDGE_LOOP ( 'NONE', ( #242590, #121452, #115147, #172721 ) ) ;
#216536=DIRECTION ( 'NONE',  ( 0.000000000000000000, 0.2617529984165152257, 0.9651348961777124202 ) ) ;
#216540=( BOUNDED_SURFACE ( )  B_SPLINE_SURFACE ( 3, 2, ( 
 ( #235323, #56655, #17551 ),
 ( #12455, #132385, #77510 ),
 ( #236601, #33323, #192359 ),
 ( #210633, #54117, #172844 ) ),
 .UNSPECIFIED., .F., .F., .T. ) 
 B_SPLINE_SURFACE_WITH_KNOTS ( ( 4, 4 ),
 ( 3, 3 ),
 ( -1.330858166725956693E-17, 0.0003124336600439406547 ),
 ( 0.000000000000000000, 1.000000000000000000 ),
 .UNSPECIFIED. ) 
 GEOMETRIC_REPRESENTATION_ITEM ( )  RATIONAL_B_SPLINE_SURFACE ( (
 ( 1.000000000000000000, 0.7071067811865475727, 1.000000000000000000),
 ( 1.000000000000000000, 0.7089187706049858706, 1.000000000000000000),
 ( 1.000000000000000000, 0.7039288185051936209, 1.000000000000000000),
 ( 1.000000000000000000, 0.7040654476016059427, 1.000000000000000000) ) ) 
 REPRESENTATION_ITEM ( '' )  SURFACE ( )  );
#216554=CARTESIAN_POINT ( 'NONE',  ( 21.05000000000000071, 55.98745301258800566, -232.8057040749261262 ) ) ;
#216555=ORIENTED_EDGE ( 'NONE', *, *, #256277, .T. ) ;
#216557=ADVANCED_FACE ( 'NONE', ( #255679 ), #118798, .F. ) ;
#216591=TOROIDAL_SURFACE ( 'NONE', #25090, 7.800000000000000711, 0.1000000000000000056 ) ;
#216603=CARTESIAN_POINT ( 'NONE',  ( -23.15000000000000213, 86.27712145182582049, -209.5223386573213702 ) ) ;
#216618=ORIENTED_EDGE ( 'NONE', *, *, #121257, .F. ) ;
#216629=ORIENTED_EDGE ( 'NONE', *, *, #41182, .F. ) ;
#216635=VERTEX_POINT ( 'NONE', #238733 ) ;
#216643=DIRECTION ( 'NONE',  ( -0.000000000000000000, 0.9651348961777157509, -0.2617529984165031243 ) ) ;
#216651=AXIS2_PLACEMENT_3D ( 'NONE', #123820, #202070, #162959 ) ;
#216652=CARTESIAN_POINT ( 'NONE',  ( -20.94999999999999929, 64.75617845954087670, -200.4736850529726269 ) ) ;
#216665=ADVANCED_FACE ( 'NONE', ( #7835 ), #146039, .T. ) ;
#216678=AXIS2_PLACEMENT_3D ( 'NONE', #230752, #170818, #55919 ) ;
#216706=ORIENTED_EDGE ( 'NONE', *, *, #32998, .T. ) ;
#216720=VECTOR ( 'NONE', #138981, 1000.000000000000000 ) ;
#216722=CARTESIAN_POINT ( 'NONE',  ( 21.05000000000000071, 78.47509609352879068, -238.9045489380306435 ) ) ;
#216734=VECTOR ( 'NONE', #140300, 1000.000000000000000 ) ;
#216739=DIRECTION ( 'NONE',  ( 1.000000000000000000, 0.000000000000000000, 0.000000000000000000 ) ) ;
#216756=FACE_OUTER_BOUND ( 'NONE', #256464, .T. ) ;
#216789=ADVANCED_FACE ( 'NONE', ( #12985 ), #51302, .T. ) ;
#216793=DIRECTION ( 'NONE',  ( 1.000000000000000000, 0.000000000000000000, 0.000000000000000000 ) ) ;
#216820=CIRCLE ( 'NONE', #175189, 0.09999999999999095723 ) ;
#216839=ORIENTED_EDGE ( 'NONE', *, *, #29765, .T. ) ;
#216847=EDGE_CURVE ( 'NONE', #18097, #225728, #250285, .T. ) ;
#216903=DIRECTION ( 'NONE',  ( -1.000000000000000000, -0.000000000000000000, -0.000000000000000000 ) ) ;
#216912=SPHERICAL_SURFACE ( 'NONE', #251333, 0.1000000000000000056 ) ;
#216932=CARTESIAN_POINT ( 'NONE',  ( -20.64999999999999858, 65.89281126173843006, -213.4744760240239145 ) ) ;
#216950=DIRECTION ( 'NONE',  ( -3.265361837132813093E-16, -0.9651348961777158619, 0.2617529984165024026 ) ) ;
#216959=CIRCLE ( 'NONE', #254378, 0.09999999999999939493 ) ;
#216964=FACE_OUTER_BOUND ( 'NONE', #3037, .T. ) ;
#216982=CARTESIAN_POINT ( 'NONE',  ( 20.94999999999999929, 67.92720994251783395, -214.1870976236629929 ) ) ;
#217037=AXIS2_PLACEMENT_3D ( 'NONE', #141849, #204386, #146974 ) ;
#217094=CARTESIAN_POINT ( 'NONE',  ( 18.50000000000000000, 78.24072131640578220, -231.5548844243369047 ) ) ;
#217130=CARTESIAN_POINT ( 'NONE',  ( -18.59999999999999787, 70.47363787294415260, -228.3418745167492432 ) ) ;
#217139=FACE_OUTER_BOUND ( 'NONE', #118892, .T. ) ;
#217140=EDGE_LOOP ( 'NONE', ( #156951, #227605, #53356, #76443 ) ) ;
#217174=CIRCLE ( 'NONE', #29973, 0.1999999999999945155 ) ;
#217186=AXIS2_PLACEMENT_3D ( 'NONE', #2554, #96508, #256830 ) ;
#217254=ORIENTED_EDGE ( 'NONE', *, *, #155090, .T. ) ;
#217260=ORIENTED_EDGE ( 'NONE', *, *, #160764, .F. ) ;
#217281=VECTOR ( 'NONE', #65629, 1000.000000000000000 ) ;
#217285=VERTEX_POINT ( 'NONE', #210854 ) ;
#217294=EDGE_CURVE ( 'NONE', #193988, #129974, #64175, .T. ) ;
#217368=ORIENTED_EDGE ( 'NONE', *, *, #253350, .F. ) ;
#217417=VERTEX_POINT ( 'NONE', #45048 ) ;
#217474=CARTESIAN_POINT ( 'NONE',  ( 20.94999999999999574, 79.00474222147506964, -236.0434322704576573 ) ) ;
#217493=VERTEX_POINT ( 'NONE', #24223 ) ;
#217586=EDGE_LOOP ( 'NONE', ( #84922, #120132, #70230, #232643, #120179, #97336, #123374, #31032 ) ) ;
#217591=EDGE_CURVE ( 'NONE', #16549, #184365, #9769, .T. ) ;
#217595=DIRECTION ( 'NONE',  ( -0.000000000000000000, 0.2617529984165031243, 0.9651348961777157509 ) ) ;
#217608=CARTESIAN_POINT ( 'NONE',  ( -22.49533356619863866, 55.97040697583999247, -232.8685561480747310 ) ) ;
#217611=AXIS2_PLACEMENT_3D ( 'NONE', #15360, #94866, #196536 ) ;
#217628=ORIENTED_EDGE ( 'NONE', *, *, #218422, .T. ) ;
#217636=AXIS2_PLACEMENT_3D ( 'NONE', #112039, #173335, #54606 ) ;
#217638=DIRECTION ( 'NONE',  ( 0.000000000000000000, -0.2617529984165031243, -0.9651348961777157509 ) ) ;
#217657=DIRECTION ( 'NONE',  ( 1.000000000000000000, 0.000000000000000000, 0.000000000000000000 ) ) ;
#217668=CARTESIAN_POINT ( 'NONE',  ( 22.50497660315938120, 64.23170377028679923, -247.2158688254707215 ) ) ;
#217675=LINE ( 'NONE', #39094, #132209 ) ;
#217684=DIRECTION ( 'NONE',  ( 0.000000000000000000, 0.9651348961777157509, -0.2617529984165031243 ) ) ;
#217685=DIRECTION ( 'NONE',  ( 0.000000000000000000, 0.2617529984165152257, 0.9651348961777124202 ) ) ;
#217690=EDGE_CURVE ( 'NONE', #140929, #32310, #247692, .T. ) ;
#217692=EDGE_CURVE ( 'NONE', #41172, #128036, #51858, .T. ) ;
#217696=VECTOR ( 'NONE', #157649, 1000.000000000000000 ) ;
#217706=EDGE_CURVE ( 'NONE', #17556, #188870, #85152, .T. ) ;
#217737=ORIENTED_EDGE ( 'NONE', *, *, #182945, .F. ) ;
#217760=ORIENTED_EDGE ( 'NONE', *, *, #8710, .F. ) ;
#217791=CARTESIAN_POINT ( 'NONE',  ( 20.95443524775735256, 60.89599939867935063, -225.2949451438352355 ) ) ;
#217797=LINE ( 'NONE', #163007, #241376 ) ;
#217809=FACE_BOUND ( 'NONE', #144160, .T. ) ;
#217827=ORIENTED_EDGE ( 'NONE', *, *, #228776, .T. ) ;
#217841=ORIENTED_EDGE ( 'NONE', *, *, #211005, .F. ) ;
#217869=AXIS2_PLACEMENT_3D ( 'NONE', #31415, #88757, #246558 ) ;
#217884=ORIENTED_EDGE ( 'NONE', *, *, #114051, .T. ) ;
#217901=CIRCLE ( 'NONE', #155426, 7.799999999999997158 ) ;
#217914=ADVANCED_FACE ( 'NONE', ( #103409 ), #139337, .T. ) ;
#217922=EDGE_CURVE ( 'NONE', #94361, #206526, #143453, .T. ) ;
#217938=ORIENTED_EDGE ( 'NONE', *, *, #43825, .F. ) ;
#217949=CARTESIAN_POINT ( 'NONE',  ( -20.64999999999999858, 63.44052078637213299, -222.1345147897817185 ) ) ;
#217962=FACE_OUTER_BOUND ( 'NONE', #255620, .T. ) ;
#217966=ORIENTED_EDGE ( 'NONE', *, *, #220718, .F. ) ;
#217985=VERTEX_POINT ( 'NONE', #227228 ) ;
#218005=EDGE_CURVE ( 'NONE', #53814, #122630, #180497, .T. ) ;
#218006=TOROIDAL_SURFACE ( 'NONE', #251340, 0.2000000000000000111, 0.1000000000000000056 ) ;
#218036=ADVANCED_FACE ( 'NONE', ( #206392 ), #114013, .F. ) ;
#218037=CARTESIAN_POINT ( 'NONE',  ( 21.05000000000000071, 70.50554186077093277, -228.5577520746950597 ) ) ;
#218061=DIRECTION ( 'NONE',  ( 0.000000000000000000, 0.9651348961777157509, -0.2617529984165031243 ) ) ;
#218157=VECTOR ( 'NONE', #26668, 1000.000000000000000 ) ;
#218158=CARTESIAN_POINT ( 'NONE',  ( 20.94999999999999574, 68.11887992016828264, -227.8068560890360175 ) ) ;
#218165=ORIENTED_EDGE ( 'NONE', *, *, #87150, .T. ) ;
#218180=DIRECTION ( 'NONE',  ( 1.000000000000000000, 0.000000000000000000, 0.000000000000000000 ) ) ;
#218220=CIRCLE ( 'NONE', #22640, 0.1000000000000124678 ) ;
#218234=AXIS2_PLACEMENT_3D ( 'NONE', #130041, #88333, #208337 ) ;
#218257=DIRECTION ( 'NONE',  ( -0.000000000000000000, -0.9651348961777157509, 0.2617529984165031243 ) ) ;
#218278=B_SPLINE_CURVE_WITH_KNOTS ( 'NONE', 3,
 ( #212648, #174842, #194381, #234762, #32755, #130518, #112268, #34037, #254305, #249205, #232222, #230935, #53563, #150117, #91410, #170991, #172272, #250467, #56097 ),
 .UNSPECIFIED., .F., .F.,
 ( 4, 3, 3, 3, 3, 3, 4 ),
 ( 0.000000000000000000, 1.655171619024644586E-05, 2.773500582848746404E-05, 5.941817267377038920E-05, 0.0001114174635873305049, 0.0001914169455916114393, 0.0002627181070750297790 ),
 .UNSPECIFIED. ) ;
#218282=ADVANCED_FACE ( 'NONE', ( #181413 ), #205597, .F. ) ;
#218308=ORIENTED_EDGE ( 'NONE', *, *, #170709, .F. ) ;
#218313=CARTESIAN_POINT ( 'NONE',  ( 23.14999999999999858, 76.00000000001126921, -203.5231074845248997 ) ) ;
#218340=CARTESIAN_POINT ( 'NONE',  ( 20.94999999999999929, 67.49463558145296815, -195.5618716440587548 ) ) ;
#218347=CARTESIAN_POINT ( 'NONE',  ( -18.42609945526421455, 78.23215990615727833, -231.5864509253183314 ) ) ;
#218357=FACE_OUTER_BOUND ( 'NONE', #229395, .T. ) ;
#218375=DIRECTION ( 'NONE',  ( -0.000000000000000000, -0.2617529984165031243, -0.9651348961777157509 ) ) ;
#218378=VERTEX_POINT ( 'NONE', #62730 ) ;
#218392=EDGE_LOOP ( 'NONE', ( #256190, #156381, #70094, #60286 ) ) ;
#218422=EDGE_CURVE ( 'NONE', #70430, #185866, #133916, .T. ) ;
#218459=ORIENTED_EDGE ( 'NONE', *, *, #128120, .T. ) ;
#218460=DIRECTION ( 'NONE',  ( 0.000000000000000000, -0.9651348961777157509, 0.2617529984165031243 ) ) ;
#218467=DIRECTION ( 'NONE',  ( 0.000000000000000000, 0.2617529984165152257, 0.9651348961777124202 ) ) ;
#218488=DIRECTION ( 'NONE',  ( -1.000000000000000000, -0.000000000000000000, 0.000000000000000000 ) ) ;
#218502=AXIS2_PLACEMENT_3D ( 'NONE', #54294, #175561, #77700 ) ;
#218527=VECTOR ( 'NONE', #104206, 1000.000000000000000 ) ;
#218557=FACE_OUTER_BOUND ( 'NONE', #54696, .T. ) ;
#218558=ORIENTED_EDGE ( 'NONE', *, *, #79863, .F. ) ;
#218560=ORIENTED_EDGE ( 'NONE', *, *, #112314, .T. ) ;
#218563=CIRCLE ( 'NONE', #122925, 0.1000000000000124678 ) ;
#218603=CARTESIAN_POINT ( 'NONE',  ( -23.15000000000000213, 68.69170246065380070, -214.2335597194317813 ) ) ;
#218614=DIRECTION ( 'NONE',  ( -1.000000000000000000, 5.945622153099073960E-16, -5.981866248895714834E-16 ) ) ;
#218615=CIRCLE ( 'NONE', #143614, 3.999999999999996447 ) ;
#218627=CARTESIAN_POINT ( 'NONE',  ( -18.50000000000000000, 63.24832102809784118, -245.4188802514362635 ) ) ;
#218670=CARTESIAN_POINT ( 'NONE',  ( 21.05000000000000071, 58.88775506787933978, -225.6504858384382999 ) ) ;
#218672=EDGE_CURVE ( 'NONE', #79058, #193922, #31058, .T. ) ;
#218701=AXIS2_PLACEMENT_3D ( 'NONE', #117502, #78359, #35433 ) ;
#218703=CARTESIAN_POINT ( 'NONE',  ( -20.00857864376270001, 63.83985267992358104, -213.0213082169670145 ) ) ;
#218707=EDGE_CURVE ( 'NONE', #79203, #211510, #26946, .T. ) ;
#218709=DIRECTION ( 'NONE',  ( 1.000000000000000000, 0.000000000000000000, 0.000000000000000000 ) ) ;
#218713=ORIENTED_EDGE ( 'NONE', *, *, #179627, .T. ) ;
#218744=CIRCLE ( 'NONE', #256284, 0.1000000000000051958 ) ;
#218757=DIRECTION ( 'NONE',  ( -1.000000000000000000, -0.000000000000000000, -0.000000000000000000 ) ) ;
#218815=DIRECTION ( 'NONE',  ( -1.000000000000000000, -0.000000000000000000, -0.000000000000000000 ) ) ;
#218823=AXIS2_PLACEMENT_3D ( 'NONE', #52607, #228705, #31807 ) ;
#218832=ORIENTED_EDGE ( 'NONE', *, *, #22295, .F. ) ;
#218894=LINE ( 'NONE', #160252, #142527 ) ;
#218897=CARTESIAN_POINT ( 'NONE',  ( -21.05000000000000071, 66.10573665986746050, -240.0052065600425237 ) ) ;
#218915=DIRECTION ( 'NONE',  ( 0.000000000000000000, -0.9673461469267405910, 0.2534589355812664757 ) ) ;
#218932=EDGE_LOOP ( 'NONE', ( #112545, #81433, #27091, #116624 ) ) ;
#218961=EDGE_CURVE ( 'NONE', #245391, #48041, #139317, .T. ) ;
#219024=DIRECTION ( 'NONE',  ( 0.000000000000000000, 0.2617529984165033463, 0.9651348961777157509 ) ) ;
#219080=ADVANCED_FACE ( 'NONE', ( #42229 ), #85332, .F. ) ;
#219082=LINE ( 'NONE', #23503, #242917 ) ;
#219083=ADVANCED_FACE ( 'NONE', ( #200019 ), #10370, .F. ) ;
#219095=ORIENTED_EDGE ( 'NONE', *, *, #233998, .F. ) ;
#219139=VECTOR ( 'NONE', #76707, 999.9999999999998863 ) ;
#219146=AXIS2_PLACEMENT_3D ( 'NONE', #191371, #92226, #171815 ) ;
#219150=CYLINDRICAL_SURFACE ( 'NONE', #218701, 0.09999999999999939493 ) ;
#219154=ORIENTED_EDGE ( 'NONE', *, *, #182613, .T. ) ;
#219177=CARTESIAN_POINT ( 'NONE',  ( 21.05000000000000071, 61.94127660284455317, -221.8315191551248517 ) ) ;
#219196=TOROIDAL_SURFACE ( 'NONE', #223284, 4.149999999999999467, 0.1000000000000000056 ) ;
#219227=ORIENTED_EDGE ( 'NONE', *, *, #109352, .F. ) ;
#219234=EDGE_CURVE ( 'NONE', #252932, #207854, #23540, .T. ) ;
#219290=ORIENTED_EDGE ( 'NONE', *, *, #253350, .T. ) ;
#219309=CYLINDRICAL_SURFACE ( 'NONE', #215820, 0.09999999999999939493 ) ;
#219330=DIRECTION ( 'NONE',  ( 0.000000000000000000, 0.2617529984165036239, 0.9651348961777156399 ) ) ;
#219334=LINE ( 'NONE', #195952, #45590 ) ;
#219340=VECTOR ( 'NONE', #126096, 1000.000000000000114 ) ;
#219361=DIRECTION ( 'NONE',  ( 0.000000000000000000, 0.2617529984165039569, 0.9651348961777155289 ) ) ;
#219372=CARTESIAN_POINT ( 'NONE',  ( 21.11344571971201134, 60.18902167132765157, -221.2568027326728384 ) ) ;
#219391=ADVANCED_FACE ( 'NONE', ( #149889 ), #33815, .T. ) ;
#219444=ORIENTED_EDGE ( 'NONE', *, *, #30815, .F. ) ;
#219467=CIRCLE ( 'NONE', #19584, 0.1000000000000124678 ) ;
#219485=EDGE_CURVE ( 'NONE', #125182, #4469, #187731, .T. ) ;
#219527=CARTESIAN_POINT ( 'NONE',  ( -22.43310005002225438, 64.17650015117389728, -247.0971464675484413 ) ) ;
#219558=CARTESIAN_POINT ( 'NONE',  ( -21.14999999999999858, 79.23417978893665747, -236.1056577391152587 ) ) ;
#219566=ORIENTED_EDGE ( 'NONE', *, *, #99096, .T. ) ;
#219576=EDGE_CURVE ( 'NONE', #159934, #161458, #101563, .T. ) ;
#219591=DIRECTION ( 'NONE',  ( 0.000000000000000000, 0.2617529984165033463, 0.9651348961777157509 ) ) ;
#219610=ORIENTED_EDGE ( 'NONE', *, *, #181564, .F. ) ;
#219642=DIRECTION ( 'NONE',  ( 0.000000000000000000, 0.9684149032218615227, -0.2493442905257554076 ) ) ;
#219648=TOROIDAL_SURFACE ( 'NONE', #169643, 0.2000000000000000111, 0.1000000000000000056 ) ;
#219655=VERTEX_POINT ( 'NONE', #32370 ) ;
#219679=AXIS2_PLACEMENT_3D ( 'NONE', #87105, #47985, #188784 ) ;
#219712=EDGE_CURVE ( 'NONE', #142261, #47754, #27324, .T. ) ;
#219715=DIRECTION ( 'NONE',  ( 1.000000000000000000, -3.151514657663852580E-16, 8.547182517843351137E-17 ) ) ;
#219732=ADVANCED_FACE ( 'NONE', ( #148440 ), #102251, .T. ) ;
#219739=DIRECTION ( 'NONE',  ( 1.000000000000000000, 0.000000000000000000, 0.000000000000000000 ) ) ;
#219757=FACE_OUTER_BOUND ( 'NONE', #6658, .T. ) ;
#219785=TOROIDAL_SURFACE ( 'NONE', #249041, 7.791421356237316687, 0.1000000000000000056 ) ;
#219792=ORIENTED_EDGE ( 'NONE', *, *, #124774, .F. ) ;
#219860=EDGE_LOOP ( 'NONE', ( #147948, #45611, #36381, #168229 ) ) ;
#219862=DIRECTION ( 'NONE',  ( 1.000000000000000000, 0.000000000000000000, 0.000000000000000000 ) ) ;
#219905=CARTESIAN_POINT ( 'NONE',  ( -21.07946286933444568, 61.10282755137055233, -234.2724922642379681 ) ) ;
#219930=DIRECTION ( 'NONE',  ( 0.000000000000000000, 0.2617529984164506107, 0.9651348961777299618 ) ) ;
#219950=EDGE_CURVE ( 'NONE', #4559, #39036, #160777, .T. ) ;
#219962=AXIS2_PLACEMENT_3D ( 'NONE', #204447, #62390, #124934 ) ;
#219976=VECTOR ( 'NONE', #104335, 1000.000000000000000 ) ;
#220017=EDGE_LOOP ( 'NONE', ( #230208, #209201, #138222 ) ) ;
#220024=DIRECTION ( 'NONE',  ( 0.000000000000000000, 0.2617529984165152257, 0.9651348961777124202 ) ) ;
#220041=CARTESIAN_POINT ( 'NONE',  ( -21.14999999999999858, 56.01362831242966678, -232.7091905853083347 ) ) ;
#220071=DIRECTION ( 'NONE',  ( 0.000000000000000000, 0.9651348961777149738, -0.2617529984165058998 ) ) ;
#220097=EDGE_CURVE ( 'NONE', #47300, #166855, #226012, .T. ) ;
#220107=CARTESIAN_POINT ( 'NONE',  ( 21.00023020733438983, 61.06322362754158917, -234.1822973190417088 ) ) ;
#220109=EDGE_CURVE ( 'NONE', #115416, #137749, #175113, .T. ) ;
#220147=CIRCLE ( 'NONE', #216027, 0.1000000000000124678 ) ;
#220158=ORIENTED_EDGE ( 'NONE', *, *, #69972, .T. ) ;
#220166=VERTEX_POINT ( 'NONE', #130792 ) ;
#220183=CARTESIAN_POINT ( 'NONE',  ( -22.39999999999999858, 64.27847795353595473, -247.1247091181747066 ) ) ;
#220223=ORIENTED_EDGE ( 'NONE', *, *, #20517, .T. ) ;
#220226=AXIS2_PLACEMENT_3D ( 'NONE', #124095, #82348, #185340 ) ;
#220237=CARTESIAN_POINT ( 'NONE',  ( 20.95595012432476523, 58.98502654666104661, -225.7485087577998399 ) ) ;
#220253=CARTESIAN_POINT ( 'NONE',  ( 21.87500000000000355, 63.38346053167636995, -212.7939182281409956 ) ) ;
#220291=FACE_OUTER_BOUND ( 'NONE', #34908, .T. ) ;
#220310=ORIENTED_EDGE ( 'NONE', *, *, #140288, .F. ) ;
#220325=VECTOR ( 'NONE', #253533, 1000.000000000000000 ) ;
#220326=CARTESIAN_POINT ( 'NONE',  ( -18.59999999999999787, 63.93636616954134411, -213.0474835168086827 ) ) ;
#220333=CARTESIAN_POINT ( 'NONE',  ( -21.14999999999999858, 65.49889199258218753, -241.8691648588935266 ) ) ;
#220337=EDGE_LOOP ( 'NONE', ( #40895, #199526, #158658, #205495, #252152, #176050, #84134, #203175, #234504 ) ) ;
#220353=ORIENTED_EDGE ( 'NONE', *, *, #45841, .F. ) ;
#220367=CARTESIAN_POINT ( 'NONE',  ( -22.39999999999999858, 55.96127771274636586, -232.9022175645438892 ) ) ;
#220400=DIRECTION ( 'NONE',  ( 0.000000000000000000, 0.2617529984164856383, 0.9651348961777204138 ) ) ;
#220414=CIRCLE ( 'NONE', #53802, 0.09999999999999935330 ) ;
#220440=DIRECTION ( 'NONE',  ( -0.7071067811865460184, -0.6824534298470606997, 0.1850873201761399356 ) ) ;
#220446=ADVANCED_FACE ( 'NONE', ( #168393 ), #155231, .F. ) ;
#220453=DIRECTION ( 'NONE',  ( -1.000000000000000000, -0.000000000000000000, -0.000000000000000000 ) ) ;
#220535=DIRECTION ( 'NONE',  ( -1.000000000000000000, 0.000000000000000000, 0.000000000000000000 ) ) ;
#220542=DIRECTION ( 'NONE',  ( 1.000000000000000000, 0.000000000000000000, 0.000000000000000000 ) ) ;
#220616=TOROIDAL_SURFACE ( 'NONE', #158117, 0.2000000000000000111, 0.1000000000000000056 ) ;
#220624=AXIS2_PLACEMENT_3D ( 'NONE', #238527, #97701, #114737 ) ;
#220636=CARTESIAN_POINT ( 'NONE',  ( 23.14999999999999147, 67.23127455305841238, -235.8551265064783991 ) ) ;
#220638=DIRECTION ( 'NONE',  ( 0.000000000000000000, -0.2617529984165031243, -0.9651348961777157509 ) ) ;
#220658=CARTESIAN_POINT ( 'NONE',  ( -21.07928932188134397, 65.47931918658504458, -241.9371126717015841 ) ) ;
#220691=ORIENTED_EDGE ( 'NONE', *, *, #78201, .T. ) ;
#220696=DIRECTION ( 'NONE',  ( 0.000000000000000000, 0.2617529984165035684, 0.9651348961777156399 ) ) ;
#220718=EDGE_CURVE ( 'NONE', #82125, #256377, #202788, .T. ) ;
#220738=VERTEX_POINT ( 'NONE', #48078 ) ;
#220768=FACE_OUTER_BOUND ( 'NONE', #244177, .T. ) ;
#220797=ADVANCED_FACE ( 'NONE', ( #67642 ), #83323, .T. ) ;
#220804=AXIS2_PLACEMENT_3D ( 'NONE', #55594, #13952, #229144 ) ;
#220813=ORIENTED_EDGE ( 'NONE', *, *, #209491, .T. ) ;
#220817=VERTEX_POINT ( 'NONE', #24699 ) ;
#220847=AXIS2_PLACEMENT_3D ( 'NONE', #186928, #87775, #167366 ) ;
#220871=SPHERICAL_SURFACE ( 'NONE', #125098, 0.1000000000000000056 ) ;
#220908=CARTESIAN_POINT ( 'NONE',  ( -18.50000000000000000, 61.57587952878036930, -212.2000740415318774 ) ) ;
#220932=DIRECTION ( 'NONE',  ( 0.000000000000000000, 0.2617529984165030688, 0.9651348961777157509 ) ) ;
#220934=EDGE_LOOP ( 'NONE', ( #240279, #233675, #46923, #186755, #158849 ) ) ;
#220936=EDGE_CURVE ( 'NONE', #232566, #185866, #194458, .T. ) ;
#220957=EDGE_CURVE ( 'NONE', #255695, #52077, #114473, .T. ) ;
#220960=VECTOR ( 'NONE', #174939, 1000.000000000000000 ) ;
#221018=ORIENTED_EDGE ( 'NONE', *, *, #223502, .F. ) ;
#221020=EDGE_CURVE ( 'NONE', #47754, #78772, #236297, .T. ) ;
#221053=DIRECTION ( 'NONE',  ( 1.000000000000000000, 0.000000000000000000, -0.000000000000000000 ) ) ;
#221088=ORIENTED_EDGE ( 'NONE', *, *, #206597, .F. ) ;
#221106=AXIS2_PLACEMENT_3D ( 'NONE', #26917, #142954, #106397 ) ;
#221123=DIRECTION ( 'NONE',  ( 0.000000000000000000, -0.2617529984164506107, -0.9651348961777299618 ) ) ;
#221164=ADVANCED_FACE ( 'NONE', ( #105130 ), #7357, .F. ) ;
#221167=VERTEX_POINT ( 'NONE', #23098 ) ;
#221203=EDGE_CURVE ( 'NONE', #209826, #38549, #232042, .T. ) ;
#221222=CARTESIAN_POINT ( 'NONE',  ( 21.03675099975491136, 61.89177620496869991, -221.6362106908973431 ) ) ;
#221228=ADVANCED_FACE ( 'NONE', ( #182158 ), #198697, .T. ) ;
#221236=ADVANCED_FACE ( 'NONE', ( #184704 ), #127978, .T. ) ;
#221257=DIRECTION ( 'NONE',  ( 0.000000000000000000, -0.2617529984165031243, -0.9651348961777157509 ) ) ;
#221262=LINE ( 'NONE', #66051, #52168 ) ;
#221275=ORIENTED_EDGE ( 'NONE', *, *, #138912, .F. ) ;
#221281=VECTOR ( 'NONE', #62550, 1000.000000000000000 ) ;
#221309=FACE_OUTER_BOUND ( 'NONE', #180687, .T. ) ;
#221321=DIRECTION ( 'NONE',  ( 1.000000000000000000, 0.000000000000000000, 0.000000000000000000 ) ) ;
#221332=ORIENTED_EDGE ( 'NONE', *, *, #30763, .F. ) ;
#221341=LINE ( 'NONE', #177136, #124188 ) ;
#221345=EDGE_CURVE ( 'NONE', #176003, #204625, #131154, .T. ) ;
#221362=DIRECTION ( 'NONE',  ( 0.000000000000000000, -0.2617529984165031243, -0.9651348961777157509 ) ) ;
#221381=DIRECTION ( 'NONE',  ( 1.000000000000000000, 0.000000000000000000, -0.000000000000000000 ) ) ;
#221389=ADVANCED_FACE ( 'NONE', ( #158459 ), #179304, .F. ) ;
#221477=EDGE_CURVE ( 'NONE', #225728, #20618, #256173, .T. ) ;
#221483=ORIENTED_EDGE ( 'NONE', *, *, #148958, .F. ) ;
#221494=EDGE_CURVE ( 'NONE', #146108, #151096, #197545, .T. ) ;
#221557=CIRCLE ( 'NONE', #96843, 0.1999999999999945155 ) ;
#221565=EDGE_CURVE ( 'NONE', #241107, #17556, #5750, .T. ) ;
#221574=FACE_OUTER_BOUND ( 'NONE', #75389, .T. ) ;
#221584=ORIENTED_EDGE ( 'NONE', *, *, #56297, .T. ) ;
#221590=VERTEX_POINT ( 'NONE', #163575 ) ;
#221602=VECTOR ( 'NONE', #22229, 1000.000000000000000 ) ;
#221654=CARTESIAN_POINT ( 'NONE',  ( -23.25000000000000000, 64.25313205997782973, -247.2214437328673853 ) ) ;
#221676=ADVANCED_FACE ( 'NONE', ( #188265 ), #150447, .T. ) ;
#221678=DIRECTION ( 'NONE',  ( -0.000000000000000000, -0.9651348961777157509, 0.2617529984165028467 ) ) ;
#221705=EDGE_CURVE ( 'NONE', #68619, #90505, #15942, .T. ) ;
#221712=CIRCLE ( 'NONE', #246675, 0.1000000000000124678 ) ;
#221718=EDGE_LOOP ( 'NONE', ( #257543, #78365, #215519, #109801 ) ) ;
#221732=VERTEX_POINT ( 'NONE', #174851 ) ;
#221764=CARTESIAN_POINT ( 'NONE',  ( -21.14999999999999858, 61.16604239671104892, -234.3115055913011417 ) ) ;
#221786=CARTESIAN_POINT ( 'NONE',  ( -21.05000000000000071, 77.07318729351892728, -199.5660544101962728 ) ) ;
#221787=CIRCLE ( 'NONE', #47008, 0.1000000000000000333 ) ;
#221803=TOROIDAL_SURFACE ( 'NONE', #176069, 0.2000000000000000111, 0.1000000000000000056 ) ;
#221812=DIRECTION ( 'NONE',  ( -1.000000000000000000, -0.000000000000000000, 0.000000000000000000 ) ) ;
#221835=DIRECTION ( 'NONE',  ( -1.000000000000000000, 1.772924042024179204E-16, -4.808324575169891715E-17 ) ) ;
#221847=CYLINDRICAL_SURFACE ( 'NONE', #37744, 0.1000000000000124678 ) ;
#221853=CIRCLE ( 'NONE', #26088, 0.09999999999999939493 ) ;
#221862=EDGE_CURVE ( 'NONE', #20618, #78065, #49216, .T. ) ;
#221875=ORIENTED_EDGE ( 'NONE', *, *, #121322, .T. ) ;
#221885=DIRECTION ( 'NONE',  ( 1.000000000000000000, 0.000000000000000000, 0.000000000000000000 ) ) ;
#221895=CARTESIAN_POINT ( 'NONE',  ( -20.85000000000000142, 76.00000000001126921, -203.5231074845248997 ) ) ;
#221904=CARTESIAN_POINT ( 'NONE',  ( -21.11833042828139284, 65.53725477864057325, -242.0741845493446078 ) ) ;
#221942=DIRECTION ( 'NONE',  ( 0.000000000000000000, -0.9651348961777379554, 0.2617529984164210233 ) ) ;
#221944=AXIS2_PLACEMENT_3D ( 'NONE', #141164, #257196, #220696 ) ;
#221960=LINE ( 'NONE', #124195, #189490 ) ;
#221966=ORIENTED_EDGE ( 'NONE', *, *, #101163, .T. ) ;
#221987=CONICAL_SURFACE ( 'NONE', #38879, 6.249999999999995559, 0.7853981633974431720 ) ;
#221994=CARTESIAN_POINT ( 'NONE',  ( -23.15000000000000213, 66.17117490947157421, -239.7639228359981303 ) ) ;
#222009=EDGE_CURVE ( 'NONE', #16173, #232481, #257449, .T. ) ;
#222010=LINE ( 'NONE', #160813, #77317 ) ;
#222041=DIRECTION ( 'NONE',  ( 0.000000000000000000, 0.2617529984165028467, 0.9651348961777159730 ) ) ;
#222045=VERTEX_POINT ( 'NONE', #194074 ) ;
#222082=DIRECTION ( 'NONE',  ( -1.000000000000000000, 0.000000000000000000, 0.000000000000000000 ) ) ;
#222090=EDGE_CURVE ( 'NONE', #66196, #63643, #115800, .T. ) ;
#222148=CIRCLE ( 'NONE', #176414, 11.64999999999999680 ) ;
#222177=CARTESIAN_POINT ( 'NONE',  ( 23.14999999999999858, 64.04577702392042227, -222.1950530992138226 ) ) ;
#222192=DIRECTION ( 'NONE',  ( 1.000000000000000000, 0.000000000000000000, 0.000000000000000000 ) ) ;
#222208=ADVANCED_FACE ( 'NONE', ( #239601 ), #81764, .T. ) ;
#222224=CARTESIAN_POINT ( 'NONE',  ( 21.09096482362066993, 61.07927011738019019, -234.2275225987165754 ) ) ;
#222234=LINE ( 'NONE', #4486, #227416 ) ;
#222241=FACE_OUTER_BOUND ( 'NONE', #222699, .T. ) ;
#222261=CARTESIAN_POINT ( 'NONE',  ( -20.54999999999999716, 70.76939748184450707, -215.3970883796142743 ) ) ;
#222274=VECTOR ( 'NONE', #181740, 1000.000000000000000 ) ;
#222278=CIRCLE ( 'NONE', #255587, 0.1999999999999945155 ) ;
#222285=EDGE_CURVE ( 'NONE', #138829, #101113, #161357, .T. ) ;
#222306=CIRCLE ( 'NONE', #197390, 12.97499999999998366 ) ;
#222319=DIRECTION ( 'NONE',  ( 1.000000000000000000, 0.000000000000000000, 0.000000000000000000 ) ) ;
#222372=B_SPLINE_CURVE_WITH_KNOTS ( 'NONE', 3,
 ( #219177, #82210, #3990, #122684, #78386, #18423, #21020, #19724, #40597, #41865, #199654, #161814, #157982, #177540, #100493, #180078 ),
 .UNSPECIFIED., .F., .F.,
 ( 4, 3, 3, 3, 3, 4 ),
 ( 0.000000000000000000, 2.372700795692865946E-05, 5.739057815865495515E-05, 9.073899019180231584E-05, 0.0001243544287365729863, 0.0001585386695601217349 ),
 .UNSPECIFIED. ) ;
#222388=FACE_OUTER_BOUND ( 'NONE', #36707, .T. ) ;
#222414=VERTEX_POINT ( 'NONE', #6099 ) ;
#222429=CIRCLE ( 'NONE', #118430, 0.1000000000000124678 ) ;
#222452=CYLINDRICAL_SURFACE ( 'NONE', #246317, 0.09999999999999939493 ) ;
#222468=DIRECTION ( 'NONE',  ( 0.000000000000000000, 0.3896596508880098009, 0.9209589331071360574 ) ) ;
#222473=DIRECTION ( 'NONE',  ( -1.000000000000000000, 2.849773892568378313E-16, -7.728835255496647986E-17 ) ) ;
#222476=AXIS2_PLACEMENT_3D ( 'NONE', #237098, #178433, #200531 ) ;
#222490=EDGE_CURVE ( 'NONE', #143687, #250542, #186415, .T. ) ;
#222500=SPHERICAL_SURFACE ( 'NONE', #29952, 0.1000000000000000056 ) ;
#222508=DIRECTION ( 'NONE',  ( 0.000000000000000000, 0.2617529984165152257, 0.9651348961777124202 ) ) ;
#222518=TOROIDAL_SURFACE ( 'NONE', #255814, 0.2000000000000000111, 0.1000000000000000056 ) ;
#222523=AXIS2_PLACEMENT_3D ( 'NONE', #28246, #149466, #26959 ) ;
#222526=CARTESIAN_POINT ( 'NONE',  ( 18.52928932188133970, 63.76258513157054608, -209.3739165141045078 ) ) ;
#222536=DIRECTION ( 'NONE',  ( 1.000000000000000000, 0.000000000000000000, 0.000000000000000000 ) ) ;
#222537=LINE ( 'NONE', #226381, #14602 ) ;
#222578=CARTESIAN_POINT ( 'NONE',  ( 18.41832399655374886, 87.08727404907521930, -199.6327534953675240 ) ) ;
#222583=ORIENTED_EDGE ( 'NONE', *, *, #156479, .T. ) ;
#222589=CARTESIAN_POINT ( 'NONE',  ( 18.49999999999999645, 65.87552587769046397, -245.8195358697090001 ) ) ;
#222597=VECTOR ( 'NONE', #55873, 1000.000000000000000 ) ;
#222631=EDGE_CURVE ( 'NONE', #125182, #34168, #153123, .T. ) ;
#222638=DIRECTION ( 'NONE',  ( 0.000000000000000000, 0.2617529984164506107, 0.9651348961777299618 ) ) ;
#222651=VERTEX_POINT ( 'NONE', #76337 ) ;
#222699=EDGE_LOOP ( 'NONE', ( #192578, #123232, #122557, #128621, #47073, #158799, #216338, #161977, #195821, #92963, #171500, #252082, #128722, #94626, #245210, #202402 ) ) ;
#222712=ORIENTED_EDGE ( 'NONE', *, *, #249005, .F. ) ;
#222742=ORIENTED_EDGE ( 'NONE', *, *, #229735, .F. ) ;
#222751=DIRECTION ( 'NONE',  ( 0.000000000000000000, 0.2617529984165029022, 0.9651348961777158619 ) ) ;
#222759=AXIS2_PLACEMENT_3D ( 'NONE', #239442, #120795, #17801 ) ;
#222816=CARTESIAN_POINT ( 'NONE',  ( 20.95512820512820440, 61.84489010471549619, -221.8053782964821323 ) ) ;
#222825=AXIS2_PLACEMENT_3D ( 'NONE', #81838, #117167, #196684 ) ;
#222830=CARTESIAN_POINT ( 'NONE',  ( -18.39999999999999858, 86.89640087696872683, -199.6396878666313341 ) ) ;
#222837=ORIENTED_EDGE ( 'NONE', *, *, #94315, .F. ) ;
#222858=CIRCLE ( 'NONE', #193835, 4.050000000000000711 ) ;
#222932=DIRECTION ( 'NONE',  ( 0.000000000000000000, 0.2617529984164506107, 0.9651348961777299618 ) ) ;
#222945=CIRCLE ( 'NONE', #27181, 0.09999999999999939493 ) ;
#222946=DIRECTION ( 'NONE',  ( 0.000000000000000000, -0.2617529984165031243, -0.9651348961777157509 ) ) ;
#222979=DIRECTION ( 'NONE',  ( 0.000000000000000000, 0.2617529984165033463, 0.9651348961777157509 ) ) ;
#222981=ORIENTED_EDGE ( 'NONE', *, *, #98678, .F. ) ;
#222991=ORIENTED_EDGE ( 'NONE', *, *, #225396, .F. ) ;
#223005=CARTESIAN_POINT ( 'NONE',  ( -18.46154800491017056, 86.89228561700184628, -199.5792417787053807 ) ) ;
#223031=AXIS2_PLACEMENT_3D ( 'NONE', #170488, #190000, #12667 ) ;
#223038=ORIENTED_EDGE ( 'NONE', *, *, #168728, .T. ) ;
#223044=AXIS2_PLACEMENT_3D ( 'NONE', #123925, #163066, #104323 ) ;
#223058=DIRECTION ( 'NONE',  ( -0.7071067811865389130, 0.1850873201762231746, 0.6824534298470456006 ) ) ;
#223060=EDGE_CURVE ( 'NONE', #252099, #206043, #32503, .T. ) ;
#223071=DIRECTION ( 'NONE',  ( -1.000000000000000000, -0.000000000000000000, 0.000000000000000000 ) ) ;
#223094=LINE ( 'NONE', #66604, #53940 ) ;
#223150=CIRCLE ( 'NONE', #252361, 0.2000000000000048406 ) ;
#223198=CARTESIAN_POINT ( 'NONE',  ( -21.04386569057571421, 62.86478208612209073, -207.0655967136950721 ) ) ;
#223221=CARTESIAN_POINT ( 'NONE',  ( 20.95512840106819752, 60.17186297114481874, -221.2972637402838245 ) ) ;
#223247=AXIS2_PLACEMENT_3D ( 'NONE', #95652, #175246, #196056 ) ;
#223284=AXIS2_PLACEMENT_3D ( 'NONE', #46085, #228602, #248149 ) ;
#223327=FACE_OUTER_BOUND ( 'NONE', #11677, .T. ) ;
#223347=EDGE_CURVE ( 'NONE', #200249, #177586, #119913, .T. ) ;
#223355=CARTESIAN_POINT ( 'NONE',  ( -21.05000000000000071, 76.00000000001126921, -203.5231074845248997 ) ) ;
#223363=DIRECTION ( 'NONE',  ( 0.000000000000000000, -0.2617529984165045120, -0.9651348961777153068 ) ) ;
#223374=VERTEX_POINT ( 'NONE', #24167 ) ;
#223375=DIRECTION ( 'NONE',  ( 0.000000000000000000, -0.9651348961777157509, 0.2617529984165031243 ) ) ;
#223439=ORIENTED_EDGE ( 'NONE', *, *, #87234, .T. ) ;
#223479=CARTESIAN_POINT ( 'NONE',  ( 20.94999999999999929, 62.96536896499190306, -207.0767526245058150 ) ) ;
#223501=DIRECTION ( 'NONE',  ( 1.000000000000000000, 0.000000000000000000, 0.000000000000000000 ) ) ;
#223502=EDGE_CURVE ( 'NONE', #14172, #248822, #82674, .T. ) ;
#223517=CARTESIAN_POINT ( 'NONE',  ( 21.11833042828126139, 61.00849935111920530, -234.1748126302079243 ) ) ;
#223532=ORIENTED_EDGE ( 'NONE', *, *, #48499, .T. ) ;
#223555=CARTESIAN_POINT ( 'NONE',  ( 18.59999999999997655, 64.65966496992309942, -200.4475097531309586 ) ) ;
#223579=CARTESIAN_POINT ( 'NONE',  ( 18.50000000000000000, 78.21362219944488459, -231.2727646510690533 ) ) ;
#223586=VERTEX_POINT ( 'NONE', #127098 ) ;
#223616=EDGE_LOOP ( 'NONE', ( #30737, #67585, #69610, #151894 ) ) ;
#223639=DIRECTION ( 'NONE',  ( 0.000000000000000000, 0.2617529984165055668, 0.9651348961777149738 ) ) ;
#223686=ORIENTED_EDGE ( 'NONE', *, *, #256647, .F. ) ;
#223738=DIRECTION ( 'NONE',  ( 0.000000000000000000, 0.2617529984165030132, 0.9651348961777157509 ) ) ;
#223749=LINE ( 'NONE', #184635, #248879 ) ;
#223756=TOROIDAL_SURFACE ( 'NONE', #15515, 0.6000000000000017542, 0.1000000000000000056 ) ;
#223766=FACE_OUTER_BOUND ( 'NONE', #189364, .T. ) ;
#223772=CIRCLE ( 'NONE', #103533, 4.100000000000008527 ) ;
#223784=CARTESIAN_POINT ( 'NONE',  ( 18.39999999999999858, 78.24072131640578220, -231.5548844243369331 ) ) ;
#223797=DIRECTION ( 'NONE',  ( 1.000000000000000000, 0.000000000000000000, 0.000000000000000000 ) ) ;
#223893=CARTESIAN_POINT ( 'NONE',  ( -21.05000000000000071, 79.13126459505528487, -235.8705213229730191 ) ) ;
#223936=VERTEX_POINT ( 'NONE', #42144 ) ;
#224023=AXIS2_PLACEMENT_3D ( 'NONE', #21449, #203905, #181784 ) ;
#224063=ORIENTED_EDGE ( 'NONE', *, *, #14971, .T. ) ;
#224083=ORIENTED_EDGE ( 'NONE', *, *, #228535, .F. ) ;
#224094=VECTOR ( 'NONE', #66450, 1000.000000000000114 ) ;
#224159=EDGE_CURVE ( 'NONE', #161458, #211904, #33066, .T. ) ;
#224165=EDGE_CURVE ( 'NONE', #128905, #247, #216348, .T. ) ;
#224187=CARTESIAN_POINT ( 'NONE',  ( -21.14999999999999858, 57.65152438469984730, -226.2879053819737010 ) ) ;
#224213=CIRCLE ( 'NONE', #249179, 0.1000000000000124678 ) ;
#224257=AXIS2_PLACEMENT_3D ( 'NONE', #79642, #103056, #21004 ) ;
#224263=DIRECTION ( 'NONE',  ( 1.000000000000000000, 0.000000000000000000, -0.000000000000000000 ) ) ;
#224282=VERTEX_POINT ( 'NONE', #157965 ) ;
#224298=CARTESIAN_POINT ( 'NONE',  ( -18.43634282235120025, 87.08574601666215642, -199.6283932421960685 ) ) ;
#224300=VECTOR ( 'NONE', #9172, 1000.000000000000000 ) ;
#224305=CARTESIAN_POINT ( 'NONE',  ( 18.50000000000002132, 63.58402440245807696, -209.2218768284338637 ) ) ;
#224308=FACE_OUTER_BOUND ( 'NONE', #245881, .T. ) ;
#224319=AXIS2_PLACEMENT_3D ( 'NONE', #56830, #191273, #13898 ) ;
#224324=CARTESIAN_POINT ( 'NONE',  ( -22.50047199488095728, 64.11232401186653362, -247.1837530084900436 ) ) ;
#224340=AXIS2_PLACEMENT_3D ( 'NONE', #37853, #54807, #20860 ) ;
#224341=ORIENTED_EDGE ( 'NONE', *, *, #177141, .T. ) ;
#224342=AXIS2_PLACEMENT_3D ( 'NONE', #200316, #24265, #179489 ) ;
#224364=ADVANCED_FACE ( 'NONE', ( #24857 ), #74753, .T. ) ;
#224377=CARTESIAN_POINT ( 'NONE',  ( 20.85000000000000142, 80.78317333349157536, -192.9003134612048882 ) ) ;
#224404=EDGE_LOOP ( 'NONE', ( #38736, #109997, #118792, #34331 ) ) ;
#224440=CIRCLE ( 'NONE', #82941, 0.1999999999999987899 ) ;
#224454=TOROIDAL_SURFACE ( 'NONE', #136371, 11.70000000000000462, 0.1000000000000000056 ) ;
#224462=DIRECTION ( 'NONE',  ( 0.7071067811865486830, 0.1850873201762206766, 0.6824534298470361637 ) ) ;
#224469=CARTESIAN_POINT ( 'NONE',  ( 20.99999999999997868, 67.23127455305841238, -235.8551265064783991 ) ) ;
#224485=DIRECTION ( 'NONE',  ( 1.000000000000000000, 0.000000000000000000, 0.000000000000000000 ) ) ;
#224531=DIRECTION ( 'NONE',  ( 1.000000000000000000, 0.000000000000000000, 0.000000000000000000 ) ) ;
#224541=DIRECTION ( 'NONE',  ( 0.000000000000000000, 0.2617529984165031243, 0.9651348961777157509 ) ) ;
#224545=DIRECTION ( 'NONE',  ( 0.000000000000000000, 0.2617529984164915779, 0.9651348961777189706 ) ) ;
#224549=DIRECTION ( 'NONE',  ( -2.952720810173289112E-16, -0.9651348961777157509, 0.2617529984165031243 ) ) ;
#224567=ADVANCED_FACE ( 'NONE', ( #229450 ), #72972, .F. ) ;
#224581=CARTESIAN_POINT ( 'NONE',  ( -21.09107601085561257, 61.07898507579771064, -234.2272990812096225 ) ) ;
#224610=DIRECTION ( 'NONE',  ( 0.000000000000000000, -0.2617529984165152257, -0.9651348961777124202 ) ) ;
#224654=CARTESIAN_POINT ( 'NONE',  ( 21.14999999999999503, 67.23127455305841238, -235.8551265064783991 ) ) ;
#224655=CARTESIAN_POINT ( 'NONE',  ( -23.15000000000000213, 70.60814576644823148, -215.7631455941064189 ) ) ;
#224728=FACE_OUTER_BOUND ( 'NONE', #2608, .T. ) ;
#224764=LINE ( 'NONE', #223479, #163072 ) ;
#224805=CARTESIAN_POINT ( 'NONE',  ( 21.05000000000001492, 61.10422374072478391, -234.2088091958333678 ) ) ;
#224811=VECTOR ( 'NONE', #106493, 1000.000000000000000 ) ;
#224817=FACE_OUTER_BOUND ( 'NONE', #199279, .T. ) ;
#224832=CARTESIAN_POINT ( 'NONE',  ( -20.85000000000000142, 79.24821784679178904, -196.3217825494968736 ) ) ;
#224836=ORIENTED_EDGE ( 'NONE', *, *, #177769, .T. ) ;
#224856=PLANE ( 'NONE',  #56854 ) ;
#224861=DIRECTION ( 'NONE',  ( 0.000000000000000000, 0.9651348961777163060, -0.2617529984165013479 ) ) ;
#224866=DIRECTION ( 'NONE',  ( 0.000000000000000000, 0.9651348961777156399, -0.2617529984165037349 ) ) ;
#224870=EDGE_CURVE ( 'NONE', #84512, #164185, #79143, .T. ) ;
#224873=CARTESIAN_POINT ( 'NONE',  ( -18.44448725179913495, 86.89435926455711012, -199.6093239235941894 ) ) ;
#224881=AXIS2_PLACEMENT_3D ( 'NONE', #175153, #76002, #172589 ) ;
#224886=DIRECTION ( 'NONE',  ( 2.952720810173289112E-16, 0.9651348961777191926, -0.2617529984164898571 ) ) ;
#224918=ORIENTED_EDGE ( 'NONE', *, *, #220109, .T. ) ;
#224944=CARTESIAN_POINT ( 'NONE',  ( 18.59999999999999432, 68.22930980752001062, -227.7331931781284879 ) ) ;
#224954=CARTESIAN_POINT ( 'NONE',  ( 20.94999999999999929, 76.00000000001126921, -203.5231074845248997 ) ) ;
#225008=AXIS2_PLACEMENT_3D ( 'NONE', #126594, #7942, #226978 ) ;
#225011=CIRCLE ( 'NONE', #173, 0.1000000000000124678 ) ;
#225041=ADVANCED_FACE ( 'NONE', ( #242924 ), #141695, .T. ) ;
#225050=ADVANCED_FACE ( 'NONE', ( #182976 ), #199977, .F. ) ;
#225064=DIRECTION ( 'NONE',  ( 0.000000000000000000, -0.2617529984165031243, -0.9651348961777157509 ) ) ;
#225073=VECTOR ( 'NONE', #60802, 1000.000000000000000 ) ;
#225092=ORIENTED_EDGE ( 'NONE', *, *, #9843, .F. ) ;
#225096=EDGE_CURVE ( 'NONE', #250042, #126428, #241655, .T. ) ;
#225129=ADVANCED_FACE ( 'NONE', ( #150269 ), #96076, .T. ) ;
#225135=AXIS2_PLACEMENT_3D ( 'NONE', #244649, #208123, #30775 ) ;
#225159=CARTESIAN_POINT ( 'NONE',  ( -18.53317502108577131, 67.49276774653023381, -195.4544018784149841 ) ) ;
#225189=CARTESIAN_POINT ( 'NONE',  ( -20.94999999999999929, 62.93978069479755533, -206.9800818407681220 ) ) ;
#225221=AXIS2_PLACEMENT_3D ( 'NONE', #114600, #35104, #113311 ) ;
#225224=EDGE_CURVE ( 'NONE', #132493, #135164, #41954, .T. ) ;
#225238=EDGE_CURVE ( 'NONE', #177774, #63643, #46016, .T. ) ;
#225244=DIRECTION ( 'NONE',  ( 0.000000000000000000, 0.2617529984165152257, 0.9651348961777124202 ) ) ;
#225252=CIRCLE ( 'NONE', #112858, 11.70000000000000817 ) ;
#225303=CARTESIAN_POINT ( 'NONE',  ( -20.94999999999999929, 79.07891399537199106, -236.0635483022085452 ) ) ;
#225316=ORIENTED_EDGE ( 'NONE', *, *, #67095, .F. ) ;
#225331=DIRECTION ( 'NONE',  ( 0.000000000000000000, 0.2617529984165152257, 0.9651348961777124202 ) ) ;
#225350=EDGE_CURVE ( 'NONE', #53100, #221732, #129414, .T. ) ;
#225355=DIRECTION ( 'NONE',  ( 0.000000000000000000, 0.2617529984163859957, 0.9651348961777475033 ) ) ;
#225357=EDGE_CURVE ( 'NONE', #156950, #29429, #173724, .T. ) ;
#225379=CARTESIAN_POINT ( 'NONE',  ( 20.95512828230154767, 61.85861388774331715, -221.7547760186666892 ) ) ;
#225396=EDGE_CURVE ( 'NONE', #4584, #54157, #142240, .T. ) ;
#225416=CARTESIAN_POINT ( 'NONE',  ( 22.59999999999999787, 55.96169194136206215, -232.9023299069559130 ) ) ;
#225417=CARTESIAN_POINT ( 'NONE',  ( -18.39999999999999858, 87.08727414655710675, -199.6327537731849873 ) ) ;
#225457=AXIS2_PLACEMENT_3D ( 'NONE', #240317, #61668, #158240 ) ;
#225499=DIRECTION ( 'NONE',  ( 0.000000000000000000, 0.9651348961777157509, -0.2617529984165031243 ) ) ;
#225524=EDGE_LOOP ( 'NONE', ( #186095, #87082, #82461 ) ) ;
#225542=LINE ( 'NONE', #149907, #58280 ) ;
#225547=EDGE_CURVE ( 'NONE', #88879, #163406, #138423, .T. ) ;
#225555=DIRECTION ( 'NONE',  ( -4.801466763864313332E-15, 0.5041370733442360752, 0.8636236514129915776 ) ) ;
#225561=VECTOR ( 'NONE', #217638, 1000.000000000000000 ) ;
#225562=CARTESIAN_POINT ( 'NONE',  ( -18.47130263965444286, 86.89034400014838866, -199.5518236931774823 ) ) ;
#225567=ORIENTED_EDGE ( 'NONE', *, *, #223060, .F. ) ;
#225578=CIRCLE ( 'NONE', #34116, 4.049999999999987388 ) ;
#225609=EDGE_LOOP ( 'NONE', ( #82442, #243077, #135648, #238452 ) ) ;
#225630=DIRECTION ( 'NONE',  ( 1.000000000000000000, 0.000000000000000000, 0.000000000000000000 ) ) ;
#225653=VERTEX_POINT ( 'NONE', #151251 ) ;
#225668=EDGE_CURVE ( 'NONE', #100977, #128703, #96725, .T. ) ;
#225678=ORIENTED_EDGE ( 'NONE', *, *, #110243, .T. ) ;
#225687=DIRECTION ( 'NONE',  ( 0.000000000000000000, -0.9651348961777066471, 0.2617529984165365975 ) ) ;
#225701=FACE_OUTER_BOUND ( 'NONE', #40599, .T. ) ;
#225709=EDGE_CURVE ( 'NONE', #220166, #133447, #80144, .T. ) ;
#225728=VERTEX_POINT ( 'NONE', #13036 ) ;
#225731=DIRECTION ( 'NONE',  ( 0.000000000000000000, -0.2617529984165030132, -0.9651348961777157509 ) ) ;
#225735=ORIENTED_EDGE ( 'NONE', *, *, #241252, .F. ) ;
#225736=DIRECTION ( 'NONE',  ( 0.000000000000000000, -0.9691069652679039637, 0.2466408114429434750 ) ) ;
#225753=VECTOR ( 'NONE', #243102, 1000.000000000000000 ) ;
#225833=CIRCLE ( 'NONE', #234228, 4.050000000000000711 ) ;
#225859=EDGE_CURVE ( 'NONE', #107947, #198131, #218894, .T. ) ;
#225892=VECTOR ( 'NONE', #215441, 1000.000000000000000 ) ;
#225900=DIRECTION ( 'NONE',  ( 0.000000000000000000, 0.2617529984165031243, 0.9651348961777157509 ) ) ;
#225915=VECTOR ( 'NONE', #183426, 1000.000000000000000 ) ;
#225930=SURFACE_STYLE_USAGE ( .BOTH. , #87719 ) ;
#225960=CIRCLE ( 'NONE', #51181, 0.09999999999999939493 ) ;
#226006=VERTEX_POINT ( 'NONE', #106638 ) ;
#226012=LINE ( 'NONE', #227328, #39958 ) ;
#226021=CARTESIAN_POINT ( 'NONE',  ( -20.54999999999999716, 70.60814576644823148, -215.7631455941064189 ) ) ;
#226025=ADVANCED_FACE ( 'NONE', ( #144483 ), #147058, .T. ) ;
#226038=CARTESIAN_POINT ( 'NONE',  ( -18.52328366898030865, 87.06376465862938119, -199.5663074770583592 ) ) ;
#226045=ORIENTED_EDGE ( 'NONE', *, *, #190900, .F. ) ;
#226089=AXIS2_PLACEMENT_3D ( 'NONE', #107851, #187407, #88262 ) ;
#226090=CIRCLE ( 'NONE', #251042, 0.1000000000000124678 ) ;
#226106=AXIS2_PLACEMENT_3D ( 'NONE', #116662, #119248, #138753 ) ;
#226133=DIRECTION ( 'NONE',  ( 0.000000000000000000, 0.9651348961777118651, -0.2617529984165174461 ) ) ;
#226155=EDGE_CURVE ( 'NONE', #160843, #211107, #51802, .T. ) ;
#226225=DIRECTION ( 'NONE',  ( -0.000000000000000000, 0.6922311945860614157, 0.7216758089626911232 ) ) ;
#226235=AXIS2_PLACEMENT_3D ( 'NONE', #170184, #209254, #206695 ) ;
#226271=EDGE_LOOP ( 'NONE', ( #5880, #130845, #217966, #121807 ) ) ;
#226280=ORIENTED_EDGE ( 'NONE', *, *, #134268, .F. ) ;
#226318=TOROIDAL_SURFACE ( 'NONE', #209789, 12.77500000000000036, 0.1000000000000000056 ) ;
#226344=DIRECTION ( 'NONE',  ( 1.000000000000000000, 0.000000000000000000, -0.000000000000000000 ) ) ;
#226346=CARTESIAN_POINT ( 'NONE',  ( -18.50000000000000355, 79.28756800457986742, -196.2274082906208434 ) ) ;
#226381=CARTESIAN_POINT ( 'NONE',  ( 21.14999999999999503, 55.89093952297024970, -232.7795287750844579 ) ) ;
#226386=ADVANCED_FACE ( 'NONE', ( #243285 ), #218006, .F. ) ;
#226397=DIRECTION ( 'NONE',  ( 0.000000000000000000, 0.9651348961777157509, -0.2617529984165028467 ) ) ;
#226403=CARTESIAN_POINT ( 'NONE',  ( 20.12500000000000000, 59.94448977088796937, -225.4740812377367263 ) ) ;
#226410=AXIS2_PLACEMENT_3D ( 'NONE', #49412, #165521, #190214 ) ;
#226444=DIRECTION ( 'NONE',  ( 1.000000000000000000, -2.849773892568378313E-16, 7.728835255496647986E-17 ) ) ;
#226497=TOROIDAL_SURFACE ( 'NONE', #159904, 0.2000000000000000111, 0.1000000000000000056 ) ;
#226512=VECTOR ( 'NONE', #256930, 1000.000000000000114 ) ;
#226547=EDGE_CURVE ( 'NONE', #68121, #146093, #170237, .T. ) ;
#226557=ORIENTED_EDGE ( 'NONE', *, *, #124433, .F. ) ;
#226569=ORIENTED_EDGE ( 'NONE', *, *, #256427, .F. ) ;
#226577=TOROIDAL_SURFACE ( 'NONE', #14239, 0.2000000000000000111, 0.1000000000000000056 ) ;
#226578=CARTESIAN_POINT ( 'NONE',  ( -21.14999999999999858, 57.76315019072730905, -226.2583585926041110 ) ) ;
#226596=ORIENTED_EDGE ( 'NONE', *, *, #55339, .F. ) ;
#226607=ORIENTED_EDGE ( 'NONE', *, *, #217692, .T. ) ;
#226624=EDGE_LOOP ( 'NONE', ( #222991, #217368, #201176, #124874 ) ) ;
#226628=CARTESIAN_POINT ( 'NONE',  ( -23.25000000000000000, 61.47936603916258491, -212.1738987416902376 ) ) ;
#226629=ORIENTED_EDGE ( 'NONE', *, *, #72590, .F. ) ;
#226644=DIRECTION ( 'NONE',  ( 0.000000000000000000, 0.2617529984165152257, 0.9651348961777124202 ) ) ;
#226671=CYLINDRICAL_SURFACE ( 'NONE', #256224, 3.999999999999996447 ) ;
#226680=DIRECTION ( 'NONE',  ( 0.000000000000000000, 0.3848449534832868446, 0.9229812358755982160 ) ) ;
#226731=EDGE_CURVE ( 'NONE', #194529, #34168, #201294, .T. ) ;
#226762=CARTESIAN_POINT ( 'NONE',  ( 20.94999999999999929, 67.92720994251783395, -214.1870976236629929 ) ) ;
#226766=CARTESIAN_POINT ( 'NONE',  ( -18.59999999999999787, 80.69087520990402140, -192.8618289658565743 ) ) ;
#226774=DIRECTION ( 'NONE',  ( 1.000000000000000000, 7.049440681616510987E-16, -1.911869773728121864E-16 ) ) ;
#226782=ORIENTED_EDGE ( 'NONE', *, *, #154379, .F. ) ;
#226798=EDGE_CURVE ( 'NONE', #38549, #29044, #58753, .T. ) ;
#226801=CARTESIAN_POINT ( 'NONE',  ( -23.25000000000000000, 70.22889768795992893, -198.1282601183952750 ) ) ;
#226805=CARTESIAN_POINT ( 'NONE',  ( 21.08078803292165659, 61.09833557356314060, -234.2738665335206463 ) ) ;
#226857=ORIENTED_EDGE ( 'NONE', *, *, #76556, .F. ) ;
#226883=CARTESIAN_POINT ( 'NONE',  ( 18.49999999999999645, 68.50594083727658301, -224.0235912779512830 ) ) ;
#226919=CARTESIAN_POINT ( 'NONE',  ( -20.54999999999999716, 68.56901367119438362, -214.3038979092079046 ) ) ;
#226933=DIRECTION ( 'NONE',  ( -1.000000000000000000, -0.000000000000000000, -0.000000000000000000 ) ) ;
#226944=EDGE_CURVE ( 'NONE', #9432, #30065, #172476, .T. ) ;
#226949=ORIENTED_EDGE ( 'NONE', *, *, #67365, .F. ) ;
#226978=DIRECTION ( 'NONE',  ( 0.000000000000000000, 0.2617529984164915779, 0.9651348961777189706 ) ) ;
#226979=ADVANCED_FACE ( 'NONE', ( #202148 ), #143447, .F. ) ;
#226989=VECTOR ( 'NONE', #182243, 1000.000000000000114 ) ;
#226993=FACE_OUTER_BOUND ( 'NONE', #106981, .T. ) ;
#226996=ORIENTED_EDGE ( 'NONE', *, *, #37178, .F. ) ;
#227014=VECTOR ( 'NONE', #91835, 1000.000000000000000 ) ;
#227017=EDGE_CURVE ( 'NONE', #164049, #187774, #22422, .T. ) ;
#227023=DIRECTION ( 'NONE',  ( 0.000000000000000000, 0.2617529984165042345, 0.9651348961777153068 ) ) ;
#227040=DIRECTION ( 'NONE',  ( 0.000000000000000000, 0.9651348961777157509, -0.2617529984165031243 ) ) ;
#227046=ORIENTED_EDGE ( 'NONE', *, *, #251062, .F. ) ;
#227048=EDGE_CURVE ( 'NONE', #166855, #81393, #170442, .T. ) ;
#227051=AXIS2_PLACEMENT_3D ( 'NONE', #215687, #179181, #157036 ) ;
#227062=CARTESIAN_POINT ( 'NONE',  ( 23.24999999999999645, 65.72352950616313194, -223.1694128933794730 ) ) ;
#227084=ORIENTED_EDGE ( 'NONE', *, *, #140428, .F. ) ;
#227117=FACE_OUTER_BOUND ( 'NONE', #106126, .T. ) ;
#227139=CIRCLE ( 'NONE', #223044, 0.2000000000000031197 ) ;
#227148=EDGE_LOOP ( 'NONE', ( #39629, #33857, #131631, #36220 ) ) ;
#227160=DIRECTION ( 'NONE',  ( 0.000000000000000000, -0.9609271840673806464, 0.2768012769485257429 ) ) ;
#227170=ORIENTED_EDGE ( 'NONE', *, *, #197750, .T. ) ;
#227195=ORIENTED_EDGE ( 'NONE', *, *, #55953, .F. ) ;
#227228=CARTESIAN_POINT ( 'NONE',  ( 18.59999999999999432, 68.13014604066189861, -227.7202878558733516 ) ) ;
#227254=CARTESIAN_POINT ( 'NONE',  ( -18.60000000000001208, 78.14848145811066615, -231.3763360729035412 ) ) ;
#227271=DIRECTION ( 'NONE',  ( 1.000000000000000000, 0.000000000000000000, 0.000000000000000000 ) ) ;
#227328=CARTESIAN_POINT ( 'NONE',  ( -21.44999999999999929, 65.79629777212066699, -213.4483007241822747 ) ) ;
#227345=DIRECTION ( 'NONE',  ( 0.000000000000000000, 0.2617529984165152257, 0.9651348961777124202 ) ) ;
#227361=CARTESIAN_POINT ( 'NONE',  ( -20.85000000000000142, 80.78317333349157536, -192.9003134612049166 ) ) ;
#227388=DIRECTION ( 'NONE',  ( 0.000000000000000000, -0.2617529984165031243, -0.9651348961777157509 ) ) ;
#227398=VECTOR ( 'NONE', #29738, 1000.000000000000000 ) ;
#227401=CARTESIAN_POINT ( 'NONE',  ( -23.25000000000000000, 75.49601185175265528, -250.2710592679604531 ) ) ;
#227416=VECTOR ( 'NONE', #87863, 1000.000000000000000 ) ;
#227432=CARTESIAN_POINT ( 'NONE',  ( 20.94999999999999574, 59.10678033798691189, -225.7992625810339575 ) ) ;
#227449=CARTESIAN_POINT ( 'NONE',  ( -18.45140287520616695, 86.89352149375004331, -199.5971161776188580 ) ) ;
#227453=ORIENTED_EDGE ( 'NONE', *, *, #24882, .F. ) ;
#227463=EDGE_LOOP ( 'NONE', ( #45640, #164019, #193573, #195925, #88100, #252173, #256653 ) ) ;
#227491=AXIS2_PLACEMENT_3D ( 'NONE', #93621, #158757, #253961 ) ;
#227509=CARTESIAN_POINT ( 'NONE',  ( 20.94999999999999929, 68.03098227380377239, -227.7073825336181869 ) ) ;
#227529=FACE_OUTER_BOUND ( 'NONE', #13867, .T. ) ;
#227530=CARTESIAN_POINT ( 'NONE',  ( 20.85000000000000142, 64.75617845954087670, -200.4736850529726269 ) ) ;
#227570=DIRECTION ( 'NONE',  ( 0.000000000000000000, 0.1290532225515392817, 0.9916376685811520986 ) ) ;
#227605=ORIENTED_EDGE ( 'NONE', *, *, #218422, .F. ) ;
#227608=LINE ( 'NONE', #202917, #11564 ) ;
#227647=EDGE_CURVE ( 'NONE', #206303, #148934, #210223, .T. ) ;
#227677=FACE_OUTER_BOUND ( 'NONE', #66924, .T. ) ;
#227680=DIRECTION ( 'NONE',  ( -0.000000000000000000, 0.2617529984165031243, 0.9651348961777157509 ) ) ;
#227721=DIRECTION ( 'NONE',  ( 0.000000000000000000, -0.2558827019433787542, 0.9667078373770204847 ) ) ;
#227730=CARTESIAN_POINT ( 'NONE',  ( 18.52326479938715309, 87.06379029406096492, -199.5663785907607348 ) ) ;
#227750=ORIENTED_EDGE ( 'NONE', *, *, #45535, .F. ) ;
#227786=DIRECTION ( 'NONE',  ( 1.000000000000000000, 0.000000000000000000, 0.000000000000000000 ) ) ;
#227798=VERTEX_POINT ( 'NONE', #29331 ) ;
#227810=ORIENTED_EDGE ( 'NONE', *, *, #58933, .T. ) ;
#227820=DIRECTION ( 'NONE',  ( 1.000000000000000000, 0.000000000000000000, 0.000000000000000000 ) ) ;
#227829=ORIENTED_EDGE ( 'NONE', *, *, #90933, .F. ) ;
#227837=AXIS2_PLACEMENT_3D ( 'NONE', #245313, #207480, #107067 ) ;
#227851=DIRECTION ( 'NONE',  ( -1.000000000000000000, -0.000000000000000000, -0.000000000000000000 ) ) ;
#227864=ORIENTED_EDGE ( 'NONE', *, *, #157850, .T. ) ;
#227868=ORIENTED_EDGE ( 'NONE', *, *, #119837, .F. ) ;
#227890=DIRECTION ( 'NONE',  ( 1.000000000000000000, 0.000000000000000000, 0.000000000000000000 ) ) ;
#227983=FACE_OUTER_BOUND ( 'NONE', #154168, .T. ) ;
#227989=EDGE_CURVE ( 'NONE', #53100, #207854, #10490, .T. ) ;
#227996=DIRECTION ( 'NONE',  ( 0.000000000000000000, -0.2617529984165152257, -0.9651348961777124202 ) ) ;
#228000=EDGE_LOOP ( 'NONE', ( #208322, #120450, #143387, #114340, #53650, #128533, #134693 ) ) ;
#228033=VERTEX_POINT ( 'NONE', #184196 ) ;
#228055=DIRECTION ( 'NONE',  ( 0.000000000000000000, -0.2558827019433787542, 0.9667078373770204847 ) ) ;
#228076=CARTESIAN_POINT ( 'NONE',  ( -21.05000000000000071, 86.19075908668452257, -209.4719249499869136 ) ) ;
#228091=ORIENTED_EDGE ( 'NONE', *, *, #56608, .F. ) ;
#228110=CARTESIAN_POINT ( 'NONE',  ( 21.07971444708685738, 61.09918328174379099, -234.2830459128522307 ) ) ;
#228121=DIRECTION ( 'NONE',  ( 0.000000000000000000, -0.2617529984165031243, -0.9651348961777157509 ) ) ;
#228126=ORIENTED_EDGE ( 'NONE', *, *, #184232, .T. ) ;
#228172=CARTESIAN_POINT ( 'NONE',  ( 18.52928932188133970, 63.76258513157055319, -209.3739165141044793 ) ) ;
#228175=CARTESIAN_POINT ( 'NONE',  ( 18.47654891039378455, 78.23178726748734846, -231.4551625896290545 ) ) ;
#228187=ORIENTED_EDGE ( 'NONE', *, *, #151936, .T. ) ;
#228227=LINE ( 'NONE', #112143, #203505 ) ;
#228285=VECTOR ( 'NONE', #222468, 1000.000000000000114 ) ;
#228309=CARTESIAN_POINT ( 'NONE',  ( 21.05000000000000071, 67.70174932746996888, -211.7710791003628401 ) ) ;
#228339=CARTESIAN_POINT ( 'NONE',  ( 21.14999999999999858, 61.16604239671103471, -234.3115055913011417 ) ) ;
#228352=ORIENTED_EDGE ( 'NONE', *, *, #163865, .T. ) ;
#228354=CARTESIAN_POINT ( 'NONE',  ( -1.820710678118658388, 83.26658958281765877, -214.6635725678450797 ) ) ;
#228436=PLANE ( 'NONE',  #113297 ) ;
#228448=CARTESIAN_POINT ( 'NONE',  ( 21.07928932188134397, 67.23127455305841238, -235.8551265064783991 ) ) ;
#228454=ADVANCED_FACE ( 'NONE', ( #209561 ), #54320, .T. ) ;
#228509=VERTEX_POINT ( 'NONE', #154743 ) ;
#228535=EDGE_CURVE ( 'NONE', #155707, #193211, #248172, .T. ) ;
#228547=FACE_OUTER_BOUND ( 'NONE', #174666, .T. ) ;
#228572=CARTESIAN_POINT ( 'NONE',  ( -21.05000000000000071, 68.22930980752001062, -227.7331931781284879 ) ) ;
#228600=CIRCLE ( 'NONE', #241081, 0.4999999999999892308 ) ;
#228602=DIRECTION ( 'NONE',  ( -1.000000000000000000, 2.849773892568378313E-16, -7.728835255496647986E-17 ) ) ;
#228611=CIRCLE ( 'NONE', #24618, 0.1000000000000106498 ) ;
#228631=ADVANCED_FACE ( 'NONE', ( #58159 ), #235863, .T. ) ;
#228640=CARTESIAN_POINT ( 'NONE',  ( -21.05000000000000071, 65.61575147395463148, -242.1939180743342774 ) ) ;
#228646=DIRECTION ( 'NONE',  ( 1.000000000000000000, 0.000000000000000000, 0.000000000000000000 ) ) ;
#228698=CARTESIAN_POINT ( 'NONE',  ( -23.15000000000000213, 76.33602373114293016, -220.7416935524190365 ) ) ;
#228699=DIRECTION ( 'NONE',  ( -1.000000000000000000, -0.000000000000000000, -0.000000000000000000 ) ) ;
#228705=DIRECTION ( 'NONE',  ( 1.000000000000000000, 0.000000000000000000, 0.000000000000000000 ) ) ;
#228747=CARTESIAN_POINT ( 'NONE',  ( -20.85000000000000142, 62.98048128140160173, -207.0210305352945852 ) ) ;
#228776=EDGE_CURVE ( 'NONE', #133438, #200563, #248351, .T. ) ;
#228819=VECTOR ( 'NONE', #22378, 1000.000000000000000 ) ;
#228823=EDGE_CURVE ( 'NONE', #217985, #165864, #215025, .T. ) ;
#228824=CARTESIAN_POINT ( 'NONE',  ( -21.14999999999999858, 64.27847795353595473, -247.1247091181747066 ) ) ;
#228845=EDGE_LOOP ( 'NONE', ( #256980, #197375, #196874, #1947 ) ) ;
#228860=EDGE_CURVE ( 'NONE', #163993, #47050, #169287, .T. ) ;
#228894=DIRECTION ( 'NONE',  ( -0.7071067811865475727, 0.6824534298470373850, -0.1850873201762210096 ) ) ;
#228915=DIRECTION ( 'NONE',  ( 0.000000000000000000, 0.2617529984165031243, 0.9651348961777157509 ) ) ;
#228954=CARTESIAN_POINT ( 'NONE',  ( 23.14999999999999858, 73.97321671803807419, -202.9734261878502366 ) ) ;
#228969=CARTESIAN_POINT ( 'NONE',  ( -18.59999999999999787, 55.11435547888748232, -226.8560373590520101 ) ) ;
#228980=EDGE_LOOP ( 'NONE', ( #62829, #132885, #240311 ) ) ;
#228981=CARTESIAN_POINT ( 'NONE',  ( 21.00000000000000000, 63.38346053167636995, -212.7939182281409956 ) ) ;
#228997=CARTESIAN_POINT ( 'NONE',  ( -20.00857864376270001, 61.63293978347611812, -221.5406706031726003 ) ) ;
#229001=EDGE_CURVE ( 'NONE', #28102, #248002, #52705, .T. ) ;
#229023=DIRECTION ( 'NONE',  ( 1.040834085586131715E-13, -0.9651348961777379554, 0.2617529984164210233 ) ) ;
#229034=CARTESIAN_POINT ( 'NONE',  ( -18.59999999999999787, 79.37986612816742138, -196.2658927859692142 ) ) ;
#229042=ORIENTED_EDGE ( 'NONE', *, *, #21696, .T. ) ;
#229140=TOROIDAL_SURFACE ( 'NONE', #70953, 0.9750000000000019762, 0.1000000000000000056 ) ;
#229144=DIRECTION ( 'NONE',  ( 0.000000000000000000, 0.2617529984165152257, 0.9651348961777124202 ) ) ;
#229148=ORIENTED_EDGE ( 'NONE', *, *, #123894, .F. ) ;
#229158=CARTESIAN_POINT ( 'NONE',  ( -23.25000000000000000, 80.69087520990402140, -192.8618289658565743 ) ) ;
#229179=CARTESIAN_POINT ( 'NONE',  ( -20.54999999999999716, 82.09643798151613225, -215.4278993322501208 ) ) ;
#229181=TOROIDAL_SURFACE ( 'NONE', #33586, 2.100000000000002309, 0.1000000000000000056 ) ;
#229210=ORIENTED_EDGE ( 'NONE', *, *, #102169, .T. ) ;
#229212=CARTESIAN_POINT ( 'NONE',  ( -21.05000000000000071, 79.23417978893665747, -236.1056577391152587 ) ) ;
#229223=DIRECTION ( 'NONE',  ( 0.000000000000000000, 0.9651348961777158619, -0.2617529984165028467 ) ) ;
#229246=ORIENTED_EDGE ( 'NONE', *, *, #186171, .T. ) ;
#229276=DIRECTION ( 'NONE',  ( 0.000000000000000000, 0.2617529984165152257, 0.9651348961777124202 ) ) ;
#229284=CARTESIAN_POINT ( 'NONE',  ( -20.85000000000000142, 86.48473784507379492, -209.3714211149925575 ) ) ;
#229290=ORIENTED_EDGE ( 'NONE', *, *, #91168, .T. ) ;
#229348=DIRECTION ( 'NONE',  ( 0.000000000000000000, -0.9651348961777156399, 0.2617529984165037349 ) ) ;
#229350=ADVANCED_FACE ( 'NONE', ( #246779 ), #223756, .T. ) ;
#229351=ORIENTED_EDGE ( 'NONE', *, *, #60861, .T. ) ;
#229366=AXIS2_PLACEMENT_3D ( 'NONE', #247691, #69075, #164319 ) ;
#229371=EDGE_LOOP ( 'NONE', ( #238752, #221332, #3962, #254140 ) ) ;
#229393=CARTESIAN_POINT ( 'NONE',  ( 21.14250536705908345, 60.94035912585616188, -234.1489753949848023 ) ) ;
#229395=EDGE_LOOP ( 'NONE', ( #190289, #51510, #202589, #17848 ) ) ;
#229403=CARTESIAN_POINT ( 'NONE',  ( -21.44999999999999929, 63.53703427598990316, -222.1606900896233583 ) ) ;
#229450=FACE_OUTER_BOUND ( 'NONE', #131606, .T. ) ;
#229455=CARTESIAN_POINT ( 'NONE',  ( 18.45068634130097962, 78.23730655674349066, -231.5159231784034546 ) ) ;
#229492=AXIS2_PLACEMENT_3D ( 'NONE', #242809, #162020, #19939 ) ;
#229500=VERTEX_POINT ( 'NONE', #216652 ) ;
#229506=CIRCLE ( 'NONE', #29606, 0.09999999999999975575 ) ;
#229507=DIRECTION ( 'NONE',  ( -0.000000000000000000, -0.2617529984165031243, -0.9651348961777157509 ) ) ;
#229537=EDGE_CURVE ( 'NONE', #14440, #133775, #105669, .T. ) ;
#229601=EDGE_CURVE ( 'NONE', #25862, #62, #182089, .T. ) ;
#229637=FACE_OUTER_BOUND ( 'NONE', #217140, .T. ) ;
#229639=CARTESIAN_POINT ( 'NONE',  ( -21.05000000000000071, 86.55507603484990398, -209.4941099044519603 ) ) ;
#229655=CARTESIAN_POINT ( 'NONE',  ( -23.15000000000000213, 75.49601185175265528, -250.2710592679604531 ) ) ;
#229678=VERTEX_POINT ( 'NONE', #209951 ) ;
#229684=TOROIDAL_SURFACE ( 'NONE', #13211, 12.97499999999999787, 0.1000000000000000056 ) ;
#229693=ORIENTED_EDGE ( 'NONE', *, *, #157634, .F. ) ;
#229735=EDGE_CURVE ( 'NONE', #99142, #223586, #119561, .T. ) ;
#229743=VECTOR ( 'NONE', #47047, 1000.000000000000114 ) ;
#229745=AXIS2_PLACEMENT_3D ( 'NONE', #198079, #234644, #155146 ) ;
#229770=ORIENTED_EDGE ( 'NONE', *, *, #235169, .F. ) ;
#229782=CARTESIAN_POINT ( 'NONE',  ( -20.64999999999999858, 76.00000000001126921, -203.5231074845248997 ) ) ;
#229783=VERTEX_POINT ( 'NONE', #49577 ) ;
#229784=CARTESIAN_POINT ( 'NONE',  ( -18.50000000000000000, 86.88220057837979482, -199.3100076076936205 ) ) ;
#229787=FACE_OUTER_BOUND ( 'NONE', #17881, .T. ) ;
#229818=FACE_OUTER_BOUND ( 'NONE', #165881, .T. ) ;
#229929=VERTEX_POINT ( 'NONE', #216344 ) ;
#230006=VECTOR ( 'NONE', #79592, 999.9999999999998863 ) ;
#230008=AXIS2_PLACEMENT_3D ( 'NONE', #65253, #82213, #101777 ) ;
#230014=DIRECTION ( 'NONE',  ( 2.952720810173289112E-16, 0.9651348961777159730, -0.2617529984165024026 ) ) ;
#230038=VERTEX_POINT ( 'NONE', #128476 ) ;
#230040=DIRECTION ( 'NONE',  ( 0.000000000000000000, -0.2617529984165152257, -0.9651348961777124202 ) ) ;
#230043=ORIENTED_EDGE ( 'NONE', *, *, #210181, .T. ) ;
#230046=CARTESIAN_POINT ( 'NONE',  ( 23.14999999999999858, 76.52350599684427834, -201.5928376921694678 ) ) ;
#230061=CARTESIAN_POINT ( 'NONE',  ( 22.39999999999999503, 55.96127771274635876, -232.9022175645438892 ) ) ;
#230063=DIRECTION ( 'NONE',  ( 0.000000000000000000, -0.2617529984165152257, -0.9651348961777124202 ) ) ;
#230066=ORIENTED_EDGE ( 'NONE', *, *, #237201, .T. ) ;
#230077=CIRCLE ( 'NONE', #238450, 0.09999999999999939493 ) ;
#230078=EDGE_LOOP ( 'NONE', ( #255627, #67763, #198527, #236064 ) ) ;
#230141=CARTESIAN_POINT ( 'NONE',  ( -22.48660254037843487, 55.97436536266719997, -232.8539608197349651 ) ) ;
#230150=EDGE_CURVE ( 'NONE', #171424, #159934, #148575, .T. ) ;
#230179=ADVANCED_FACE ( 'NONE', ( #111479 ), #53277, .T. ) ;
#230190=DIRECTION ( 'NONE',  ( 0.000000000000000000, 0.2617529984165031243, 0.9651348961777157509 ) ) ;
#230206=DIRECTION ( 'NONE',  ( 1.000000000000000000, 0.000000000000000000, 0.000000000000000000 ) ) ;
#230208=ORIENTED_EDGE ( 'NONE', *, *, #53240, .F. ) ;
#230220=ORIENTED_EDGE ( 'NONE', *, *, #155311, .T. ) ;
#230222=DIRECTION ( 'NONE',  ( -1.000000000000000000, -0.000000000000000000, 0.000000000000000000 ) ) ;
#230238=CARTESIAN_POINT ( 'NONE',  ( 18.59999999999998366, 76.00000000001126921, -203.5231074845248997 ) ) ;
#230259=EDGE_CURVE ( 'NONE', #146449, #237933, #73578, .T. ) ;
#230272=DIRECTION ( 'NONE',  ( -1.000000000000000000, 0.000000000000000000, 0.000000000000000000 ) ) ;
#230277=AXIS2_PLACEMENT_3D ( 'NONE', #180536, #61869, #239213 ) ;
#230312=CARTESIAN_POINT ( 'NONE',  ( -18.59117750673697245, 67.49222854868494892, -195.4187676019683693 ) ) ;
#230344=ORIENTED_EDGE ( 'NONE', *, *, #149896, .T. ) ;
#230355=CARTESIAN_POINT ( 'NONE',  ( -20.54999999999999716, 65.77012247227901298, -213.5448142138000378 ) ) ;
#230357=CARTESIAN_POINT ( 'NONE',  ( 18.51697539158856642, 67.49317130920637453, -195.4795610751097286 ) ) ;
#230366=CARTESIAN_POINT ( 'NONE',  ( 18.46905048506370051, 86.89090060965958173, -199.5596611130660847 ) ) ;
#230369=DIRECTION ( 'NONE',  ( -0.7071067811865475727, 0.6824534298470373850, -0.1850873201762210096 ) ) ;
#230394=VECTOR ( 'NONE', #144923, 999.9999999999998863 ) ;
#230400=EDGE_CURVE ( 'NONE', #242024, #231796, #27822, .T. ) ;
#230406=DIRECTION ( 'NONE',  ( -0.000000000000000000, -0.2617529984165031243, -0.9651348961777157509 ) ) ;
#230437=DIRECTION ( 'NONE',  ( 0.000000000000000000, -0.2617529984165152257, -0.9651348961777124202 ) ) ;
#230459=DIRECTION ( 'NONE',  ( -2.827886303505248273E-16, -0.9667078373770112698, -0.2558827019434133376 ) ) ;
#230500=ORIENTED_EDGE ( 'NONE', *, *, #152117, .T. ) ;
#230515=VECTOR ( 'NONE', #131050, 999.9999999999998863 ) ;
#230520=CARTESIAN_POINT ( 'NONE',  ( 20.85000000000000142, 86.48473784507378070, -209.3714211149925575 ) ) ;
#230649=CARTESIAN_POINT ( 'NONE',  ( -18.59999999999999787, 63.86602797976523505, -212.9247947273492514 ) ) ;
#230666=CARTESIAN_POINT ( 'NONE',  ( 20.85000000000000142, 76.00000000001126921, -203.5231074845248997 ) ) ;
#230677=CARTESIAN_POINT ( 'NONE',  ( -20.94999999999999929, 70.56573376625485139, -228.3808404818380779 ) ) ;
#230687=ORIENTED_EDGE ( 'NONE', *, *, #225859, .F. ) ;
#230696=EDGE_CURVE ( 'NONE', #185637, #42744, #214135, .T. ) ;
#230722=ORIENTED_EDGE ( 'NONE', *, *, #252911, .F. ) ;
#230752=CARTESIAN_POINT ( 'NONE',  ( 18.49999999999998934, 63.81702857804527440, -209.2850695923107480 ) ) ;
#230769=DIRECTION ( 'NONE',  ( 0.000000000000000000, -0.2617529984165033463, -0.9651348961777157509 ) ) ;
#230797=DIRECTION ( 'NONE',  ( 0.000000000000000000, 0.9651348961777148627, -0.2617529984165062329 ) ) ;
#230828=ORIENTED_EDGE ( 'NONE', *, *, #169692, .T. ) ;
#230831=CARTESIAN_POINT ( 'NONE',  ( 18.59999999999999076, 58.01113881014391893, -224.9619361160449387 ) ) ;
#230836=CIRCLE ( 'NONE', #180927, 11.90000000000000213 ) ;
#230920=DIRECTION ( 'NONE',  ( 0.000000000000000000, 0.2617529984164506107, 0.9651348961777299618 ) ) ;
#230935=CARTESIAN_POINT ( 'NONE',  ( -21.09813707148783735, 65.52970697556288826, -242.0093664099801174 ) ) ;
#230936=AXIS2_PLACEMENT_3D ( 'NONE', #20287, #99779, #196334 ) ;
#230967=DIRECTION ( 'NONE',  ( -1.000000000000000000, 2.849773892568378313E-16, -7.728835255496647986E-17 ) ) ;
#230979=AXIS2_PLACEMENT_3D ( 'NONE', #184080, #101946, #244044 ) ;
#230992=VERTEX_POINT ( 'NONE', #39304 ) ;
#231023=ORIENTED_EDGE ( 'NONE', *, *, #232517, .T. ) ;
#231049=ORIENTED_EDGE ( 'NONE', *, *, #33173, .T. ) ;
#231095=ADVANCED_FACE ( 'NONE', ( #82218 ), #219648, .T. ) ;
#231147=DIRECTION ( 'NONE',  ( 0.000000000000000000, 0.2617529984165039569, 0.9651348961777155289 ) ) ;
#231149=EDGE_LOOP ( 'NONE', ( #14012, #225735, #254697, #226996 ) ) ;
#231178=ORIENTED_EDGE ( 'NONE', *, *, #96188, .T. ) ;
#231205=CARTESIAN_POINT ( 'NONE',  ( -21.52071067811865746, 65.28546217739872759, -213.3097576571499872 ) ) ;
#231216=VERTEX_POINT ( 'NONE', #69137 ) ;
#231228=EDGE_LOOP ( 'NONE', ( #208489, #131770, #159728 ) ) ;
#231272=DIRECTION ( 'NONE',  ( 0.000000000000000000, -0.4031292884907143326, -0.9151430362303863975 ) ) ;
#231284=CARTESIAN_POINT ( 'NONE',  ( -20.54999999999999716, 82.57900542960499024, -215.5587758314583482 ) ) ;
#231296=EDGE_CURVE ( 'NONE', #29044, #38549, #189470, .T. ) ;
#231308=CARTESIAN_POINT ( 'NONE',  ( -20.64999999999999858, 82.20113918088273408, -215.0418453737790401 ) ) ;
#231331=LINE ( 'NONE', #76081, #130951 ) ;
#231334=EDGE_CURVE ( 'NONE', #240058, #138829, #86539, .T. ) ;
#231368=CARTESIAN_POINT ( 'NONE',  ( 18.49999999999999289, 62.96704557978079464, -212.5773704035085814 ) ) ;
#231395=FACE_OUTER_BOUND ( 'NONE', #100404, .T. ) ;
#231418=DIRECTION ( 'NONE',  ( 0.000000000000000000, 0.2617529984165031243, 0.9651348961777157509 ) ) ;
#231428=CARTESIAN_POINT ( 'NONE',  ( 21.05000000000000071, 60.06173988932783203, -221.3217724115915814 ) ) ;
#231445=CARTESIAN_POINT ( 'NONE',  ( -22.49231231312462853, 55.97148680618423100, -232.8646322987703456 ) ) ;
#231446=CARTESIAN_POINT ( 'NONE',  ( -23.15000000000000213, 61.54970422893871529, -212.2965875311496688 ) ) ;
#231482=CARTESIAN_POINT ( 'NONE',  ( -22.32929514600008503, 65.15191943456896695, -243.1436103818390677 ) ) ;
#231498=CARTESIAN_POINT ( 'NONE',  ( -23.15000000000000213, 82.25348978056602789, -214.8488183945435139 ) ) ;
#231518=ADVANCED_FACE ( 'NONE', ( #246158 ), #122365, .T. ) ;
#231550=EDGE_CURVE ( 'NONE', #226006, #84528, #72681, .T. ) ;
#231566=LINE ( 'NONE', #153353, #237190 ) ;
#231596=CYLINDRICAL_SURFACE ( 'NONE', #351, 0.09999999999999543976 ) ;
#231654=VERTEX_POINT ( 'NONE', #59460 ) ;
#231656=EDGE_LOOP ( 'NONE', ( #200887, #140232, #238057, #81628, #152416, #238163 ) ) ;
#231688=VERTEX_POINT ( 'NONE', #116911 ) ;
#231697=VECTOR ( 'NONE', #32307, 1000.000000000000000 ) ;
#231710=DIRECTION ( 'NONE',  ( 0.000000000000000000, -0.9651348961777157509, 0.2617529984165031243 ) ) ;
#231715=DIRECTION ( 'NONE',  ( 0.000000000000000000, 0.2617529984165031243, 0.9651348961777157509 ) ) ;
#231716=ORIENTED_EDGE ( 'NONE', *, *, #140541, .F. ) ;
#231760=ORIENTED_EDGE ( 'NONE', *, *, #30319, .F. ) ;
#231772=DIRECTION ( 'NONE',  ( 0.000000000000000000, -0.2617529984165031243, -0.9651348961777157509 ) ) ;
#231778=AXIS2_PLACEMENT_3D ( 'NONE', #69989, #89510, #205607 ) ;
#231793=AXIS2_PLACEMENT_3D ( 'NONE', #210755, #249883, #12582 ) ;
#231795=CIRCLE ( 'NONE', #44354, 0.1000000000000105804 ) ;
#231796=VERTEX_POINT ( 'NONE', #22975 ) ;
#231824=CARTESIAN_POINT ( 'NONE',  ( -20.94999999999999929, 57.84918772656043018, -226.1321410194968280 ) ) ;
#231826=ORIENTED_EDGE ( 'NONE', *, *, #185670, .F. ) ;
#231844=CIRCLE ( 'NONE', #173614, 11.79999999999999361 ) ;
#231873=VERTEX_POINT ( 'NONE', #133290 ) ;
#231920=FACE_OUTER_BOUND ( 'NONE', #149714, .T. ) ;
#231937=CIRCLE ( 'NONE', #202689, 12.87499999999999822 ) ;
#231957=EDGE_CURVE ( 'NONE', #4469, #71652, #12079, .T. ) ;
#231982=FACE_OUTER_BOUND ( 'NONE', #174278, .T. ) ;
#232030=ORIENTED_EDGE ( 'NONE', *, *, #158165, .F. ) ;
#232033=CARTESIAN_POINT ( 'NONE',  ( -18.39999999999999858, 73.22794484573502416, -249.6559397216816478 ) ) ;
#232037=CYLINDRICAL_SURFACE ( 'NONE', #19172, 11.79999999999999361 ) ;
#232042=CIRCLE ( 'NONE', #132069, 0.1000000000000048767 ) ;
#232063=EDGE_LOOP ( 'NONE', ( #98887, #134614, #249527, #237563 ) ) ;
#232097=CIRCLE ( 'NONE', #119653, 0.09999999999999829858 ) ;
#232108=ORIENTED_EDGE ( 'NONE', *, *, #113890, .T. ) ;
#232179=ORIENTED_EDGE ( 'NONE', *, *, #188260, .F. ) ;
#232180=ADVANCED_FACE ( 'NONE', ( #4040 ), #69185, .F. ) ;
#232188=CARTESIAN_POINT ( 'NONE',  ( -20.85000000000000142, 75.77017861926654518, -203.7552340087416951 ) ) ;
#232222=CARTESIAN_POINT ( 'NONE',  ( -21.09316766718153247, 65.52597334342877389, -241.9929064490658845 ) ) ;
#232227=VECTOR ( 'NONE', #174186, 1000.000000000000000 ) ;
#232240=ORIENTED_EDGE ( 'NONE', *, *, #5265, .T. ) ;
#232258=CARTESIAN_POINT ( 'NONE',  ( -21.64999999999999858, 65.77012247227901298, -213.5448142138000378 ) ) ;
#232271=AXIS2_PLACEMENT_3D ( 'NONE', #196654, #80533, #96263 ) ;
#232289=CARTESIAN_POINT ( 'NONE',  ( 20.95132126680579887, 59.08861302114610936, -225.8029662872950212 ) ) ;
#232306=DIRECTION ( 'NONE',  ( 0.000000000000000000, -0.2617529984165152257, -0.9651348961777124202 ) ) ;
#232315=VECTOR ( 'NONE', #141487, 1000.000000000000000 ) ;
#232331=ORIENTED_EDGE ( 'NONE', *, *, #91700, .T. ) ;
#232360=EDGE_LOOP ( 'NONE', ( #197765, #175800, #142479, #66546 ) ) ;
#232378=VECTOR ( 'NONE', #107278, 1000.000000000000000 ) ;
#232383=DIRECTION ( 'NONE',  ( 0.000000000000000000, -0.2617529984165152257, -0.9651348961777124202 ) ) ;
#232481=VERTEX_POINT ( 'NONE', #8877 ) ;
#232486=CARTESIAN_POINT ( 'NONE',  ( -18.59999999999999787, 67.23127455305841238, -235.8551265064783991 ) ) ;
#232491=DIRECTION ( 'NONE',  ( -1.000000000000000000, 2.849773892568378313E-16, -7.728835255496647986E-17 ) ) ;
#232517=EDGE_CURVE ( 'NONE', #22805, #224282, #195474, .T. ) ;
#232566=VERTEX_POINT ( 'NONE', #66288 ) ;
#232572=CARTESIAN_POINT ( 'NONE',  ( 20.95512820512820440, 60.90483797576754910, -225.2715357783924333 ) ) ;
#232607=DIRECTION ( 'NONE',  ( 0.000000000000000000, 0.2617529984165033463, 0.9651348961777157509 ) ) ;
#232608=ORIENTED_EDGE ( 'NONE', *, *, #255549, .T. ) ;
#232624=CARTESIAN_POINT ( 'NONE',  ( -21.53752568617661467, 60.65518257771915245, -234.1741829020439241 ) ) ;
#232643=ORIENTED_EDGE ( 'NONE', *, *, #198071, .T. ) ;
#232650=FACE_OUTER_BOUND ( 'NONE', #17743, .T. ) ;
#232652=LINE ( 'NONE', #171412, #227014 ) ;
#232660=ORIENTED_EDGE ( 'NONE', *, *, #28576, .F. ) ;
#232672=EDGE_LOOP ( 'NONE', ( #172842, #173302, #206055, #209703 ) ) ;
#232695=VERTEX_POINT ( 'NONE', #60818 ) ;
#232702=ORIENTED_EDGE ( 'NONE', *, *, #84595, .F. ) ;
#232704=CIRCLE ( 'NONE', #153640, 0.9750000000000036415 ) ;
#232726=FACE_OUTER_BOUND ( 'NONE', #177090, .T. ) ;
#232755=DIRECTION ( 'NONE',  ( 1.000000000000000000, 0.000000000000000000, 0.000000000000000000 ) ) ;
#232789=DIRECTION ( 'NONE',  ( -1.000000000000000000, 2.849773892568378313E-16, -7.728835255496647986E-17 ) ) ;
#232819=DIRECTION ( 'NONE',  ( 0.000000000000000000, 0.2617529984165152257, 0.9651348961777124202 ) ) ;
#232825=AXIS2_PLACEMENT_3D ( 'NONE', #220041, #37570, #117098 ) ;
#232838=AXIS2_PLACEMENT_3D ( 'NONE', #243561, #148318, #182325 ) ;
#232845=DIRECTION ( 'NONE',  ( 0.000000000000000000, -0.2617529984165031243, -0.9651348961777157509 ) ) ;
#232856=EDGE_CURVE ( 'NONE', #184365, #133447, #83156, .T. ) ;
#232876=AXIS2_PLACEMENT_3D ( 'NONE', #225416, #70249, #147180 ) ;
#232885=AXIS2_PLACEMENT_3D ( 'NONE', #179790, #234612, #18134 ) ;
#232890=DIRECTION ( 'NONE',  ( 0.000000000000000000, -0.2558827019434435912, 0.9667078373770033872 ) ) ;
#232897=DIRECTION ( 'NONE',  ( 0.000000000000000000, 0.3589373870825496859, -0.9333616406058007353 ) ) ;
#232912=CARTESIAN_POINT ( 'NONE',  ( 21.14999999999999858, 64.08993991385487732, -222.4142553782910454 ) ) ;
#232915=CARTESIAN_POINT ( 'NONE',  ( -18.50596464788227635, 67.49374512151688066, -195.5131169347613991 ) ) ;
#232970=CARTESIAN_POINT ( 'NONE',  ( -23.25000000000000000, 66.17117490947157421, -239.7639228359981303 ) ) ;
#232992=ORIENTED_EDGE ( 'NONE', *, *, #67095, .T. ) ;
#233004=CARTESIAN_POINT ( 'NONE',  ( -20.64999999999999858, 70.22209180797715078, -215.6584443947398313 ) ) ;
#233047=FACE_OUTER_BOUND ( 'NONE', #67669, .T. ) ;
#233059=DIRECTION ( 'NONE',  ( 0.000000000000000000, -0.2617529984165152257, -0.9651348961777124202 ) ) ;
#233061=DIRECTION ( 'NONE',  ( 0.000000000000000000, 0.2617529984165030132, 0.9651348961777158619 ) ) ;
#233083=SPHERICAL_SURFACE ( 'NONE', #128400, 0.1000000000000000056 ) ;
#233106=ORIENTED_EDGE ( 'NONE', *, *, #50493, .T. ) ;
#233118=CARTESIAN_POINT ( 'NONE',  ( -21.00448002041601470, 57.68351327785831018, -226.1699560279491834 ) ) ;
#233125=ORIENTED_EDGE ( 'NONE', *, *, #159583, .F. ) ;
#233129=EDGE_CURVE ( 'NONE', #149408, #164185, #8383, .T. ) ;
#233140=EDGE_CURVE ( 'NONE', #99142, #178237, #117473, .T. ) ;
#233184=AXIS2_PLACEMENT_3D ( 'NONE', #207145, #130152, #170632 ) ;
#233188=ADVANCED_FACE ( 'NONE', ( #201317 ), #220871, .F. ) ;
#233195=ORIENTED_EDGE ( 'NONE', *, *, #7946, .F. ) ;
#233218=AXIS2_PLACEMENT_3D ( 'NONE', #150762, #33421, #13817 ) ;
#233239=ORIENTED_EDGE ( 'NONE', *, *, #211006, .F. ) ;
#233249=AXIS2_PLACEMENT_3D ( 'NONE', #239178, #60523, #32352 ) ;
#233253=DIRECTION ( 'NONE',  ( 1.000000000000000000, 0.000000000000000000, 0.000000000000000000 ) ) ;
#233272=DIRECTION ( 'NONE',  ( 1.000000000000000000, 0.000000000000000000, 0.000000000000000000 ) ) ;
#233279=FACE_OUTER_BOUND ( 'NONE', #123621, .T. ) ;
#233283=EDGE_LOOP ( 'NONE', ( #127822, #193401, #182971, #22135 ) ) ;
#233287=ORIENTED_EDGE ( 'NONE', *, *, #201611, .T. ) ;
#233288=CARTESIAN_POINT ( 'NONE',  ( 20.97565083910961548, 59.10540512327582263, -225.7996265934505686 ) ) ;
#233301=ORIENTED_EDGE ( 'NONE', *, *, #99306, .F. ) ;
#233303=AXIS2_PLACEMENT_3D ( 'NONE', #55118, #52571, #211679 ) ;
#233306=EDGE_LOOP ( 'NONE', ( #91014, #170107, #225092 ) ) ;
#233323=ORIENTED_EDGE ( 'NONE', *, *, #25441, .F. ) ;
#233336=CARTESIAN_POINT ( 'NONE',  ( 18.49999999999999645, 68.58368164137472434, -224.2353459317783120 ) ) ;
#233338=EDGE_LOOP ( 'NONE', ( #215562, #222583 ) ) ;
#233351=CARTESIAN_POINT ( 'NONE',  ( 20.94999999999999574, 62.98661795304985844, -207.1103002134590554 ) ) ;
#233357=DIRECTION ( 'NONE',  ( -0.7071067811865474617, 0.6824534298470372740, -0.1850873201762209819 ) ) ;
#233358=TOROIDAL_SURFACE ( 'NONE', #71035, 0.2000000000000000111, 0.1000000000000000056 ) ;
#233360=AXIS2_PLACEMENT_3D ( 'NONE', #148731, #45759, #129161 ) ;
#233365=CARTESIAN_POINT ( 'NONE',  ( -23.25000000000000000, 79.28653038861995128, -235.9126307598797325 ) ) ;
#233440=CARTESIAN_POINT ( 'NONE',  ( -20.64999999999999858, 66.26558728512915764, -222.7970849955717938 ) ) ;
#233477=DIRECTION ( 'NONE',  ( 0.000000000000000000, 0.2617529984164506107, 0.9651348961777299618 ) ) ;
#233521=ORIENTED_EDGE ( 'NONE', *, *, #213221, .F. ) ;
#233526=VERTEX_POINT ( 'NONE', #61187 ) ;
#233562=DIRECTION ( 'NONE',  ( -1.000000000000000000, -0.000000000000000000, -0.000000000000000000 ) ) ;
#233567=CARTESIAN_POINT ( 'NONE',  ( -18.59999999999999787, 68.13014604066189861, -227.7202878558733516 ) ) ;
#233578=ORIENTED_EDGE ( 'NONE', *, *, #2175, .T. ) ;
#233579=VECTOR ( 'NONE', #45782, 1000.000000000000000 ) ;
#233583=CARTESIAN_POINT ( 'NONE',  ( 21.05000000000000071, 56.88144095856731752, -233.0481614001508319 ) ) ;
#233595=DIRECTION ( 'NONE',  ( 1.000000000000000000, 0.000000000000000000, -0.000000000000000000 ) ) ;
#233649=AXIS2_PLACEMENT_3D ( 'NONE', #188367, #73590, #230063 ) ;
#233674=CIRCLE ( 'NONE', #67067, 0.09999999999999642508 ) ;
#233675=ORIENTED_EDGE ( 'NONE', *, *, #23373, .F. ) ;
#233707=DIRECTION ( 'NONE',  ( 0.000000000000000000, -0.2617529984165031243, -0.9651348961777157509 ) ) ;
#233711=AXIS2_PLACEMENT_3D ( 'NONE', #171344, #190885, #189582 ) ;
#233714=CARTESIAN_POINT ( 'NONE',  ( -23.25000000000000000, 78.06784868750165174, -195.8985418047209350 ) ) ;
#233716=DIRECTION ( 'NONE',  ( 0.000000000000000000, 0.2617529984165022361, 0.9651348961777160840 ) ) ;
#233782=AXIS2_PLACEMENT_3D ( 'NONE', #15051, #134947, #234072 ) ;
#233801=AXIS2_PLACEMENT_3D ( 'NONE', #188977, #88567, #129009 ) ;
#233802=CIRCLE ( 'NONE', #121395, 0.1000000000000124678 ) ;
#233805=DIRECTION ( 'NONE',  ( -1.000000000000000000, 2.849773892568378313E-16, -7.728835255496647986E-17 ) ) ;
#233814=EDGE_LOOP ( 'NONE', ( #182589, #219095, #48873, #208229 ) ) ;
#233817=ORIENTED_EDGE ( 'NONE', *, *, #27098, .T. ) ;
#233944=EDGE_CURVE ( 'NONE', #123814, #160843, #7319, .T. ) ;
#233949=DIRECTION ( 'NONE',  ( 0.000000000000000000, 0.2617529984165152257, 0.9651348961777124202 ) ) ;
#233978=CARTESIAN_POINT ( 'NONE',  ( 20.84999999999999432, 79.19526988099229925, -196.1889237952725296 ) ) ;
#233998=EDGE_CURVE ( 'NONE', #122095, #185020, #43885, .T. ) ;
#234016=CARTESIAN_POINT ( 'NONE',  ( 21.00000000000000000, 61.05385884576949707, -221.3836188041226762 ) ) ;
#234020=DIRECTION ( 'NONE',  ( -1.000000000000000000, -0.000000000000000000, -0.000000000000000000 ) ) ;
#234032=EDGE_CURVE ( 'NONE', #88879, #62193, #4622, .T. ) ;
#234034=CARTESIAN_POINT ( 'NONE',  ( 20.02499999999999858, 63.35728523183471594, -212.8904317177587870 ) ) ;
#234038=ORIENTED_EDGE ( 'NONE', *, *, #190363, .F. ) ;
#234042=CARTESIAN_POINT ( 'NONE',  ( 23.14999999999999858, 76.00000000001126921, -203.5231074845248997 ) ) ;
#234049=CARTESIAN_POINT ( 'NONE',  ( 20.85000000000000142, 76.00000000001126921, -203.5231074845248997 ) ) ;
#234051=FACE_OUTER_BOUND ( 'NONE', #5641, .T. ) ;
#234072=DIRECTION ( 'NONE',  ( 0.000000000000000000, -0.2617529984165152257, -0.9651348961777124202 ) ) ;
#234085=CIRCLE ( 'NONE', #121693, 0.1000000000000022676 ) ;
#234093=VERTEX_POINT ( 'NONE', #15042 ) ;
#234123=CARTESIAN_POINT ( 'NONE',  ( 22.48660254037843842, 55.87785187304942980, -232.8277855198933253 ) ) ;
#234130=AXIS2_PLACEMENT_3D ( 'NONE', #157473, #75363, #55726 ) ;
#234161=FACE_OUTER_BOUND ( 'NONE', #82256, .T. ) ;
#234162=CARTESIAN_POINT ( 'NONE',  ( -18.51697539158856998, 67.49317130920637453, -195.4795610751097286 ) ) ;
#234164=EDGE_CURVE ( 'NONE', #16173, #125683, #207764, .T. ) ;
#234166=ORIENTED_EDGE ( 'NONE', *, *, #73056, .F. ) ;
#234171=CIRCLE ( 'NONE', #22002, 0.09999999999999939493 ) ;
#234196=CARTESIAN_POINT ( 'NONE',  ( 22.49066049874202022, 64.12747008008147986, -247.0842118427744651 ) ) ;
#234199=CARTESIAN_POINT ( 'NONE',  ( 18.50000972452444969, 67.49459761544854075, -195.5598716110968951 ) ) ;
#234201=AXIS2_PLACEMENT_3D ( 'NONE', #100820, #240388, #79990 ) ;
#234228=AXIS2_PLACEMENT_3D ( 'NONE', #202348, #181523, #118975 ) ;
#234246=FACE_OUTER_BOUND ( 'NONE', #725, .T. ) ;
#234288=AXIS2_PLACEMENT_3D ( 'NONE', #243692, #105424, #144575 ) ;
#234312=TOROIDAL_SURFACE ( 'NONE', #92667, 0.4000000000000009104, 0.1000000000000000056 ) ;
#234317=VECTOR ( 'NONE', #165523, 1000.000000000000000 ) ;
#234346=ORIENTED_EDGE ( 'NONE', *, *, #159485, .T. ) ;
#234362=CARTESIAN_POINT ( 'NONE',  ( -21.14999999999999858, 57.66663670110953888, -226.2321832927624712 ) ) ;
#234366=ORIENTED_EDGE ( 'NONE', *, *, #48003, .F. ) ;
#234379=CARTESIAN_POINT ( 'NONE',  ( 18.50000000000000000, 73.32445833535280144, -249.6821150215233160 ) ) ;
#234421=ORIENTED_EDGE ( 'NONE', *, *, #30031, .F. ) ;
#234430=EDGE_CURVE ( 'NONE', #188870, #200249, #224764, .T. ) ;
#234458=ORIENTED_EDGE ( 'NONE', *, *, #24457, .T. ) ;
#234504=ORIENTED_EDGE ( 'NONE', *, *, #61150, .T. ) ;
#234518=EDGE_CURVE ( 'NONE', #4833, #25796, #96390, .T. ) ;
#234538=EDGE_CURVE ( 'NONE', #140485, #213407, #178680, .T. ) ;
#234539=ORIENTED_EDGE ( 'NONE', *, *, #121777, .T. ) ;
#234541=DIRECTION ( 'NONE',  ( 0.000000000000000000, 0.2617529984165035128, 0.9651348961777155289 ) ) ;
#234554=FACE_OUTER_BOUND ( 'NONE', #711, .T. ) ;
#234560=ORIENTED_EDGE ( 'NONE', *, *, #173253, .T. ) ;
#234612=DIRECTION ( 'NONE',  ( 1.000000000000000000, 0.000000000000000000, 0.000000000000000000 ) ) ;
#234644=DIRECTION ( 'NONE',  ( 1.000000000000000000, 0.000000000000000000, 0.000000000000000000 ) ) ;
#234655=VERTEX_POINT ( 'NONE', #108098 ) ;
#234730=DIRECTION ( 'NONE',  ( 1.000000000000000000, 0.000000000000000000, 0.000000000000000000 ) ) ;
#234746=CIRCLE ( 'NONE', #55635, 0.09999999999999939493 ) ;
#234762=CARTESIAN_POINT ( 'NONE',  ( -21.08035267497491816, 65.49412562536262783, -241.9444337344500298 ) ) ;
#234766=EDGE_CURVE ( 'NONE', #207854, #74489, #10288, .T. ) ;
#234788=DIRECTION ( 'NONE',  ( 1.000000000000000000, 0.000000000000000000, -0.000000000000000000 ) ) ;
#234800=CARTESIAN_POINT ( 'NONE',  ( -21.14999999999999858, 78.47509609352879068, -238.9045489380306435 ) ) ;
#234841=DIRECTION ( 'NONE',  ( -1.000000000000000000, -0.000000000000000000, 0.000000000000000000 ) ) ;
#234844=DIRECTION ( 'NONE',  ( 0.000000000000000000, -0.2617529984165033463, -0.9651348961777157509 ) ) ;
#234849=ORIENTED_EDGE ( 'NONE', *, *, #14740, .F. ) ;
#234880=( BOUNDED_SURFACE ( )  B_SPLINE_SURFACE ( 3, 2, ( 
 ( #70306, #74161, #153719 ),
 ( #148534, #50678, #248924 ),
 ( #209790, #31193, #110681 ),
 ( #190228, #11601, #257835 ),
 ( #214911, #174566, #235750 ),
 ( #196625, #177103, #79231 ) ),
 .UNSPECIFIED., .F., .F., .F. ) 
 B_SPLINE_SURFACE_WITH_KNOTS ( ( 4, 2, 4 ),
 ( 3, 3 ),
 ( -1.776356839400250465E-15, 0.7853981633974468357, 1.570796326794895448 ),
 ( 0.000000000000000000, 1.000000000000000000 ),
 .UNSPECIFIED. ) 
 GEOMETRIC_REPRESENTATION_ITEM ( )  RATIONAL_B_SPLINE_SURFACE ( (
 ( 1.000000000000000000, 0.4999999999999439337, 1.000000000000000000),
 ( 1.000000000000000000, 0.4993418825329671851, 1.000000000000000000),
 ( 1.000000000000000000, 0.5278258667062272202, 1.000000000000000000),
 ( 1.000000000000000000, 0.6092287576688484307, 1.000000000000000000),
 ( 1.000000000000000000, 0.6611148371785092737, 1.000000000000000000),
 ( 1.000000000000000000, 0.7071067811866070807, 1.000000000000000000) ) ) 
 REPRESENTATION_ITEM ( '' )  SURFACE ( )  );
#234883=LINE ( 'NONE', #14567, #68458 ) ;
#234887=ORIENTED_EDGE ( 'NONE', *, *, #195618, .T. ) ;
#234894=CIRCLE ( 'NONE', #72401, 0.09999999999999642508 ) ;
#234918=VERTEX_POINT ( 'NONE', #141446 ) ;
#234944=DIRECTION ( 'NONE',  ( 0.000000000000000000, 0.9651348961777158619, -0.2617529984165028467 ) ) ;
#234982=CARTESIAN_POINT ( 'NONE',  ( 21.05000000000000071, 63.99342642423710714, -222.3880800784493772 ) ) ;
#234995=CARTESIAN_POINT ( 'NONE',  ( 20.94999999999999929, 76.00000000001126921, -203.5231074845248997 ) ) ;
#235006=CIRCLE ( 'NONE', #176748, 0.09999999999999939493 ) ;
#235026=CARTESIAN_POINT ( 'NONE',  ( 18.49999999999999645, 68.22930980752001062, -227.7331931781284879 ) ) ;
#235077=EDGE_CURVE ( 'NONE', #5675, #8746, #168779, .T. ) ;
#235080=VERTEX_POINT ( 'NONE', #129603 ) ;
#235113=ORIENTED_EDGE ( 'NONE', *, *, #140851, .F. ) ;
#235134=VERTEX_POINT ( 'NONE', #14816 ) ;
#235153=AXIS2_PLACEMENT_3D ( 'NONE', #122917, #202444, #120374 ) ;
#235169=EDGE_CURVE ( 'NONE', #94125, #229678, #133448, .T. ) ;
#235192=ADVANCED_FACE ( 'NONE', ( #151757 ), #132168, .T. ) ;
#235203=DIRECTION ( 'NONE',  ( -3.469446951953772592E-14, -0.9651348961777379554, 0.2617529984164210233 ) ) ;
#235265=CARTESIAN_POINT ( 'NONE',  ( -22.49436431346200038, 55.96998815520995407, -232.8702878457373231 ) ) ;
#235292=AXIS2_PLACEMENT_3D ( 'NONE', #14543, #36683, #195748 ) ;
#235299=DIRECTION ( 'NONE',  ( 0.000000000000000000, -0.7092521942342977503, -0.7049548389605067023 ) ) ;
#235306=CARTESIAN_POINT ( 'NONE',  ( -22.37643362114956602, 65.13957426554411256, -243.1891076939221534 ) ) ;
#235309=ORIENTED_EDGE ( 'NONE', *, *, #3372, .F. ) ;
#235323=CARTESIAN_POINT ( 'NONE',  ( 22.49999999999999645, 64.08545097430041437, -247.0723585184914270 ) ) ;
#235331=DIRECTION ( 'NONE',  ( 1.000000000000000000, 0.000000000000000000, -0.000000000000000000 ) ) ;
#235346=ADVANCED_FACE ( 'NONE', ( #21235 ), #100700, .T. ) ;
#235363=AXIS2_PLACEMENT_3D ( 'NONE', #205807, #126263, #226644 ) ;
#235378=EDGE_CURVE ( 'NONE', #136295, #192701, #42068, .T. ) ;
#235426=ORIENTED_EDGE ( 'NONE', *, *, #112314, .F. ) ;
#235503=CARTESIAN_POINT ( 'NONE',  ( 21.05000000000000071, 86.19075908668452257, -209.4719249499869136 ) ) ;
#235504=ORIENTED_EDGE ( 'NONE', *, *, #148958, .T. ) ;
#235511=ORIENTED_EDGE ( 'NONE', *, *, #156272, .F. ) ;
#235524=VECTOR ( 'NONE', #224541, 1000.000000000000000 ) ;
#235528=DIRECTION ( 'NONE',  ( -1.000000000000000000, 0.000000000000000000, 0.000000000000000000 ) ) ;
#235529=CARTESIAN_POINT ( 'NONE',  ( 20.95512820512820440, 58.98414156600839675, -225.6766266970810477 ) ) ;
#235541=LINE ( 'NONE', #77742, #216720 ) ;
#235557=DIRECTION ( 'NONE',  ( 1.000000000000000000, 0.000000000000000000, 0.000000000000000000 ) ) ;
#235591=CARTESIAN_POINT ( 'NONE',  ( -21.14999999999999858, 78.57160958314655375, -238.9307242378722833 ) ) ;
#235599=ORIENTED_EDGE ( 'NONE', *, *, #62450, .T. ) ;
#235600=EDGE_LOOP ( 'NONE', ( #36704, #227810, #210721 ) ) ;
#235625=AXIS2_PLACEMENT_3D ( 'NONE', #12170, #228646, #91681 ) ;
#235647=ADVANCED_FACE ( 'NONE', ( #23499 ), #19623, .T. ) ;
#235649=ORIENTED_EDGE ( 'NONE', *, *, #86654, .F. ) ;
#235656=ORIENTED_EDGE ( 'NONE', *, *, #177505, .F. ) ;
#235672=AXIS2_PLACEMENT_3D ( 'NONE', #3873, #57409, #79537 ) ;
#235686=ORIENTED_EDGE ( 'NONE', *, *, #44126, .F. ) ;
#235690=ORIENTED_EDGE ( 'NONE', *, *, #106139, .F. ) ;
#235693=DIRECTION ( 'NONE',  ( -0.000000000000000000, 0.2617529984165031243, 0.9651348961777157509 ) ) ;
#235709=CARTESIAN_POINT ( 'NONE',  ( 18.59999999999999076, 80.82423061532404063, -192.8091306798888525 ) ) ;
#235732=DIRECTION ( 'NONE',  ( 5.603264701231746180E-32, -0.2617529984165030132, -0.9651348961777158619 ) ) ;
#235736=CARTESIAN_POINT ( 'NONE',  ( 21.05000000000000071, 63.38977744132975545, -224.6138528564904107 ) ) ;
#235750=CARTESIAN_POINT ( 'NONE',  ( 20.85000000106584750, 62.86809779110724605, -207.0533710558942744 ) ) ;
#235770=ADVANCED_FACE ( 'NONE', ( #128990 ), #208535, .F. ) ;
#235792=DIRECTION ( 'NONE',  ( 0.000000000000000000, -0.9651348961777379554, 0.2617529984164210233 ) ) ;
#235800=DIRECTION ( 'NONE',  ( -1.000000000000000000, 0.000000000000000000, 0.000000000000000000 ) ) ;
#235804=VERTEX_POINT ( 'NONE', #48152 ) ;
#235828=ORIENTED_EDGE ( 'NONE', *, *, #57024, .T. ) ;
#235835=EDGE_LOOP ( 'NONE', ( #181709, #7951, #61721, #81010 ) ) ;
#235837=DIRECTION ( 'NONE',  ( -0.000000000000000000, 0.3896596508880124654, 0.9209589331071350582 ) ) ;
#235842=VECTOR ( 'NONE', #97067, 1000.000000000000000 ) ;
#235863=TOROIDAL_SURFACE ( 'NONE', #11026, 4.149999999999999467, 0.1000000000000000056 ) ;
#235901=CARTESIAN_POINT ( 'NONE',  ( -22.59999999999999787, 55.86495732666938352, -232.8769840133977880 ) ) ;
#235936=ORIENTED_EDGE ( 'NONE', *, *, #98678, .T. ) ;
#235950=DIRECTION ( 'NONE',  ( 0.000000000000000000, -0.2617529984165031243, -0.9651348961777157509 ) ) ;
#235975=ADVANCED_FACE ( 'NONE', ( #132844 ), #143155, .F. ) ;
#236044=VERTEX_POINT ( 'NONE', #120995 ) ;
#236060=EDGE_LOOP ( 'NONE', ( #57028, #246421, #238572, #156493, #132384, #202159, #58974, #85363, #28747, #79624, #109088, #168331, #143898, #64099, #156979, #48636, #227170, #217628, #108195, #41072, #249146, #190207, #229693 ) ) ;
#236064=ORIENTED_EDGE ( 'NONE', *, *, #178113, .T. ) ;
#236100=CARTESIAN_POINT ( 'NONE',  ( 20.94999999999999574, 68.22930980752001062, -227.7331931781284879 ) ) ;
#236103=CARTESIAN_POINT ( 'NONE',  ( -20.54999999999999716, 72.62993014539878800, -215.9492192728129965 ) ) ;
#236107=ORIENTED_EDGE ( 'NONE', *, *, #176667, .F. ) ;
#236116=DIRECTION ( 'NONE',  ( 1.000000000000000000, -0.000000000000000000, -0.000000000000000000 ) ) ;
#236120=DIRECTION ( 'NONE',  ( 0.000000000000000000, -0.2617529984164955192, -0.9651348961777178603 ) ) ;
#236134=CARTESIAN_POINT ( 'NONE',  ( 22.39999999999999503, 55.89093952297024970, -232.7795287750844579 ) ) ;
#236150=CARTESIAN_POINT ( 'NONE',  ( -20.54999999999999716, 82.95597230662299637, -222.7647147268955337 ) ) ;
#236152=EDGE_CURVE ( 'NONE', #216022, #60484, #109843, .T. ) ;
#236166=CARTESIAN_POINT ( 'NONE',  ( 21.14999999999999503, 67.23127455305841238, -235.8551265064783991 ) ) ;
#236201=EDGE_LOOP ( 'NONE', ( #105020, #74574, #246994, #195146 ) ) ;
#236207=DIRECTION ( 'NONE',  ( 0.000000000000000000, 0.2617529984165030132, 0.9651348961777157509 ) ) ;
#236217=ADVANCED_FACE ( 'NONE', ( #249900 ), #192493, .T. ) ;
#236243=AXIS2_PLACEMENT_3D ( 'NONE', #108276, #229507, #13045 ) ;
#236254=FACE_OUTER_BOUND ( 'NONE', #147644, .T. ) ;
#236293=CARTESIAN_POINT ( 'NONE',  ( 18.47149038651512143, 87.08088263100174231, -199.6145014482960960 ) ) ;
#236297=CIRCLE ( 'NONE', #123891, 4.149999999999999467 ) ;
#236355=( BOUNDED_CURVE ( )  B_SPLINE_CURVE ( 3, ( #135552, #33952, #19483, #58576 ),
 .UNSPECIFIED., .F., .T. ) 
 B_SPLINE_CURVE_WITH_KNOTS ( ( 4, 4 ),
 ( -4.796163466380676255E-14, 1.570796326794913211 ),
 .UNSPECIFIED. ) 
 CURVE ( )  GEOMETRIC_REPRESENTATION_ITEM ( )  RATIONAL_B_SPLINE_CURVE ( ( 1.000000000000000000, 0.8047378541243498384, 0.8047378541243498384, 1.000000000000000000 ) ) 
 REPRESENTATION_ITEM ( '' )  );
#236366=AXIS2_PLACEMENT_3D ( 'NONE', #77157, #78439, #185 ) ;
#236391=AXIS2_PLACEMENT_3D ( 'NONE', #120802, #101156, #185875 ) ;
#236458=EDGE_LOOP ( 'NONE', ( #77245, #235504, #203087, #41083 ) ) ;
#236497=AXIS2_PLACEMENT_3D ( 'NONE', #252657, #111894, #92306 ) ;
#236543=DIRECTION ( 'NONE',  ( 0.000000000000000000, 0.2617529984165152257, 0.9651348961777124202 ) ) ;
#236552=DIRECTION ( 'NONE',  ( 1.000000000000000000, 0.000000000000000000, 0.000000000000000000 ) ) ;
#236561=ORIENTED_EDGE ( 'NONE', *, *, #205337, .T. ) ;
#236601=CARTESIAN_POINT ( 'NONE',  ( 22.45463910399150009, 64.18196446322802728, -247.0985338208812436 ) ) ;
#236617=CIRCLE ( 'NONE', #124217, 0.1000000000000124678 ) ;
#236648=DIRECTION ( 'NONE',  ( 0.000000000000000000, 0.2617529984165152257, 0.9651348961777124202 ) ) ;
#236653=EDGE_CURVE ( 'NONE', #4288, #22691, #185245, .T. ) ;
#236664=CARTESIAN_POINT ( 'NONE',  ( -21.05000000000000071, 86.48473784507379492, -209.3714211149925575 ) ) ;
#236695=DIRECTION ( 'NONE',  ( -1.000000000000000000, -0.000000000000000000, -0.000000000000000000 ) ) ;
#236712=FACE_OUTER_BOUND ( 'NONE', #72555, .T. ) ;
#236718=CARTESIAN_POINT ( 'NONE',  ( -22.39999999999999858, 67.23127455305841238, -235.8551265064783991 ) ) ;
#236726=ORIENTED_EDGE ( 'NONE', *, *, #150804, .F. ) ;
#236775=CARTESIAN_POINT ( 'NONE',  ( -22.39999999999999858, 55.98745301258801987, -232.8057040749261262 ) ) ;
#236780=ORIENTED_EDGE ( 'NONE', *, *, #242099, .T. ) ;
#236801=CIRCLE ( 'NONE', #165925, 0.09999999999999577283 ) ;
#236804=DIRECTION ( 'NONE',  ( 0.000000000000000000, 0.2617529984165152257, 0.9651348961777124202 ) ) ;
#236808=ORIENTED_EDGE ( 'NONE', *, *, #254490, .F. ) ;
#236822=ORIENTED_EDGE ( 'NONE', *, *, #182922, .F. ) ;
#236862=AXIS2_PLACEMENT_3D ( 'NONE', #239895, #157824, #219024 ) ;
#236878=ORIENTED_EDGE ( 'NONE', *, *, #225096, .F. ) ;
#236915=VECTOR ( 'NONE', #242267, 999.9999999999998863 ) ;
#236919=ORIENTED_EDGE ( 'NONE', *, *, #255207, .T. ) ;
#236975=ORIENTED_EDGE ( 'NONE', *, *, #222490, .T. ) ;
#237025=AXIS2_PLACEMENT_3D ( 'NONE', #245835, #125871, #237187 ) ;
#237070=ORIENTED_EDGE ( 'NONE', *, *, #165643, .T. ) ;
#237098=CARTESIAN_POINT ( 'NONE',  ( -20.94999999999999929, 70.42128727326085880, -228.5349014959848262 ) ) ;
#237101=EDGE_CURVE ( 'NONE', #66847, #62193, #139603, .T. ) ;
#237105=CARTESIAN_POINT ( 'NONE',  ( -23.25000000000000000, 82.67551891922275331, -215.5849511313000164 ) ) ;
#237111=DIRECTION ( 'NONE',  ( 0.000000000000000000, 0.2617529984165027912, 0.9651348961777157509 ) ) ;
#237112=CARTESIAN_POINT ( 'NONE',  ( -20.54999999999999716, 68.70534379447684614, -223.0647885566232560 ) ) ;
#237130=ORIENTED_EDGE ( 'NONE', *, *, #221705, .F. ) ;
#237136=DIRECTION ( 'NONE',  ( 0.000000000000000000, 0.9209589331071864615, -0.3896596508878908960 ) ) ;
#237142=EDGE_CURVE ( 'NONE', #42744, #99142, #115485, .T. ) ;
#237187=DIRECTION ( 'NONE',  ( 0.000000000000000000, -0.2700277750006208621, -0.9628525332200221776 ) ) ;
#237188=CARTESIAN_POINT ( 'NONE',  ( 21.14999999999999503, 75.49601185175264106, -250.2710592679604531 ) ) ;
#237190=VECTOR ( 'NONE', #52910, 1000.000000000000114 ) ;
#237201=EDGE_CURVE ( 'NONE', #252329, #180736, #52135, .T. ) ;
#237268=CARTESIAN_POINT ( 'NONE',  ( 22.60000000000000142, 64.10951975586338847, -247.1829665668249447 ) ) ;
#237279=CYLINDRICAL_SURFACE ( 'NONE', #69748, 0.5000000000000014433 ) ;
#237287=CARTESIAN_POINT ( 'NONE',  ( -21.44999999999999929, 63.56320957583155717, -222.0641766000055668 ) ) ;
#237348=CARTESIAN_POINT ( 'NONE',  ( 21.09107601085559835, 65.52757369511267882, -241.9868384472909213 ) ) ;
#237364=LINE ( 'NONE', #140830, #179424 ) ;
#237368=VECTOR ( 'NONE', #32845, 1000.000000000000000 ) ;
#237374=ORIENTED_EDGE ( 'NONE', *, *, #142097, .F. ) ;
#237383=CARTESIAN_POINT ( 'NONE',  ( 20.95224633520496127, 60.86421059253439125, -225.3282306591363522 ) ) ;
#237395=ORIENTED_EDGE ( 'NONE', *, *, #194952, .T. ) ;
#237403=DIRECTION ( 'NONE',  ( 1.836970198721029934E-16, 0.9651348961777157509, -0.2617529984165031243 ) ) ;
#237470=VECTOR ( 'NONE', #158210, 1000.000000000000000 ) ;
#237477=CARTESIAN_POINT ( 'NONE',  ( -22.39999999999999858, 64.15556351076547514, -247.1958793361846745 ) ) ;
#237488=ADVANCED_FACE ( 'NONE', ( #135104 ), #85601, .T. ) ;
#237538=DIRECTION ( 'NONE',  ( 0.000000000000000000, -0.2617529984165152257, -0.9651348961777124202 ) ) ;
#237548=ORIENTED_EDGE ( 'NONE', *, *, #76817, .T. ) ;
#237563=ORIENTED_EDGE ( 'NONE', *, *, #107874, .F. ) ;
#237626=DIRECTION ( 'NONE',  ( 1.000000000000000000, 0.000000000000000000, 0.000000000000000000 ) ) ;
#237642=EDGE_LOOP ( 'NONE', ( #149891, #171441, #89945, #189464 ) ) ;
#237652=CARTESIAN_POINT ( 'NONE',  ( -23.15000000000000213, 67.63082410804655353, -211.8415745842588649 ) ) ;
#237658=CARTESIAN_POINT ( 'NONE',  ( 19.86930884467592406, 62.42739552316976415, -208.9193556810753591 ) ) ;
#237693=CARTESIAN_POINT ( 'NONE',  ( -23.15000000000000213, 68.59518897103603763, -214.2073844195901131 ) ) ;
#237732=CARTESIAN_POINT ( 'NONE',  ( 22.39999999999999503, 55.91711482281188950, -232.6830152854666949 ) ) ;
#237750=VECTOR ( 'NONE', #256408, 1000.000000000000000 ) ;
#237770=FACE_OUTER_BOUND ( 'NONE', #97807, .T. ) ;
#237861=DIRECTION ( 'NONE',  ( 0.000000000000000000, -0.9651348961777379554, 0.2617529984164210233 ) ) ;
#237878=CARTESIAN_POINT ( 'NONE',  ( 21.10257677756355577, 65.53239810784317854, -242.0238970717508380 ) ) ;
#237900=ADVANCED_FACE ( 'NONE', ( #165830 ), #6727, .T. ) ;
#237909=AXIS2_PLACEMENT_3D ( 'NONE', #202601, #20122, #59190 ) ;
#237933=VERTEX_POINT ( 'NONE', #5414 ) ;
#237990=EDGE_CURVE ( 'NONE', #84395, #151423, #218278, .T. ) ;
#238048=EDGE_CURVE ( 'NONE', #250042, #171580, #214487, .T. ) ;
#238057=ORIENTED_EDGE ( 'NONE', *, *, #248299, .T. ) ;
#238068=ADVANCED_FACE ( 'NONE', ( #116672, #234051 ), #239191, .T. ) ;
#238070=DIRECTION ( 'NONE',  ( 0.000000000000000000, -0.9930108503404238007, -0.1180230956473711790 ) ) ;
#238090=ORIENTED_EDGE ( 'NONE', *, *, #232517, .F. ) ;
#238096=LINE ( 'NONE', #75212, #13658 ) ;
#238111=CARTESIAN_POINT ( 'NONE',  ( 18.59999999999999076, 76.00000000001126921, -203.5231074845248997 ) ) ;
#238123=DIRECTION ( 'NONE',  ( 0.000000000000000000, 0.2617529984165180013, 0.9651348961777117541 ) ) ;
#238163=ORIENTED_EDGE ( 'NONE', *, *, #205164, .T. ) ;
#238165=ORIENTED_EDGE ( 'NONE', *, *, #182945, .T. ) ;
#238189=AXIS2_PLACEMENT_3D ( 'NONE', #185514, #181672, #241633 ) ;
#238199=CARTESIAN_POINT ( 'NONE',  ( -20.94999999999999929, 76.00000000001126921, -203.5231074845248997 ) ) ;
#238324=EDGE_CURVE ( 'NONE', #152104, #159875, #2788, .T. ) ;
#238330=FACE_OUTER_BOUND ( 'NONE', #255996, .T. ) ;
#238334=FACE_OUTER_BOUND ( 'NONE', #115577, .T. ) ;
#238359=CARTESIAN_POINT ( 'NONE',  ( -20.54999999999999716, 68.76258920191057200, -222.5680764032308048 ) ) ;
#238376=FACE_OUTER_BOUND ( 'NONE', #127515, .T. ) ;
#238383=VECTOR ( 'NONE', #213653, 1000.000000000000000 ) ;
#238404=AXIS2_PLACEMENT_3D ( 'NONE', #240320, #45956, #203752 ) ;
#238425=CIRCLE ( 'NONE', #167909, 0.09999999999999543976 ) ;
#238426=CARTESIAN_POINT ( 'NONE',  ( 20.94999999999999929, 78.93126476241668854, -235.8702625865613243 ) ) ;
#238439=EDGE_CURVE ( 'NONE', #157096, #22805, #19855, .T. ) ;
#238443=ORIENTED_EDGE ( 'NONE', *, *, #231334, .F. ) ;
#238450=AXIS2_PLACEMENT_3D ( 'NONE', #55096, #214214, #17303 ) ;
#238452=ORIENTED_EDGE ( 'NONE', *, *, #105037, .T. ) ;
#238480=CARTESIAN_POINT ( 'NONE',  ( -22.50000000000000000, 55.96169194136206215, -232.9023299069559130 ) ) ;
#238488=ORIENTED_EDGE ( 'NONE', *, *, #26948, .T. ) ;
#238492=CARTESIAN_POINT ( 'NONE',  ( 21.14999999999999858, 65.51923798433685420, -242.1677427744926092 ) ) ;
#238506=AXIS2_PLACEMENT_3D ( 'NONE', #241960, #43766, #88001 ) ;
#238511=ORIENTED_EDGE ( 'NONE', *, *, #230696, .F. ) ;
#238527=CARTESIAN_POINT ( 'NONE',  ( -18.59999999999999787, 55.32469252163839712, -244.8004216010555183 ) ) ;
#238552=FACE_OUTER_BOUND ( 'NONE', #64075, .T. ) ;
#238572=ORIENTED_EDGE ( 'NONE', *, *, #184297, .T. ) ;
#238577=EDGE_CURVE ( 'NONE', #249034, #94242, #242724, .T. ) ;
#238585=CIRCLE ( 'NONE', #213638, 0.09999999999999939493 ) ;
#238589=DIRECTION ( 'NONE',  ( 1.000000000000000000, 0.000000000000000000, 0.000000000000000000 ) ) ;
#238604=ORIENTED_EDGE ( 'NONE', *, *, #70239, .T. ) ;
#238611=CARTESIAN_POINT ( 'NONE',  ( -23.25000000000000000, 78.06784868750165174, -195.8985418047209350 ) ) ;
#238653=EDGE_LOOP ( 'NONE', ( #225678, #18471, #208310, #110118 ) ) ;
#238664=CARTESIAN_POINT ( 'NONE',  ( 20.95159278453404283, 60.85485389494746755, -225.3345583954844358 ) ) ;
#238674=ORIENTED_EDGE ( 'NONE', *, *, #128933, .F. ) ;
#238690=CIRCLE ( 'NONE', #167793, 0.09999999999999939493 ) ;
#238707=EDGE_CURVE ( 'NONE', #255725, #17623, #40451, .T. ) ;
#238731=EDGE_CURVE ( 'NONE', #121380, #7048, #169637, .T. ) ;
#238733=CARTESIAN_POINT ( 'NONE',  ( -21.05000000000000071, 65.61575147395463148, -242.1939180743342774 ) ) ;
#238743=ORIENTED_EDGE ( 'NONE', *, *, #185618, .F. ) ;
#238748=ADVANCED_FACE ( 'NONE', ( #50927 ), #151363, .F. ) ;
#238752=ORIENTED_EDGE ( 'NONE', *, *, #209169, .T. ) ;
#238815=CARTESIAN_POINT ( 'NONE',  ( -20.54999999999999716, 84.10768549965561647, -218.5181211837136175 ) ) ;
#238835=CARTESIAN_POINT ( 'NONE',  ( -20.64999999999999858, 68.76258920191057200, -222.5680764032308048 ) ) ;
#238842=AXIS2_PLACEMENT_3D ( 'NONE', #170092, #50087, #230014 ) ;
#238858=AXIS2_PLACEMENT_3D ( 'NONE', #120215, #41945, #201001 ) ;
#238868=DIRECTION ( 'NONE',  ( 1.000000000000000000, 0.000000000000000000, 0.000000000000000000 ) ) ;
#238881=CARTESIAN_POINT ( 'NONE',  ( -22.50000000000000000, 64.18196446391819165, -247.0985338183330668 ) ) ;
#238895=CARTESIAN_POINT ( 'NONE',  ( -21.05000000000000071, 70.44746257310249860, -228.4383880063670347 ) ) ;
#238904=ORIENTED_EDGE ( 'NONE', *, *, #224159, .F. ) ;
#238914=CYLINDRICAL_SURFACE ( 'NONE', #59223, 0.5000000000000014433 ) ;
#238926=DIRECTION ( 'NONE',  ( 0.000000000000000000, 0.9651348961777157509, -0.2617529984165031243 ) ) ;
#238931=AXIS2_PLACEMENT_3D ( 'NONE', #114818, #53566, #194385 ) ;
#238952=EDGE_LOOP ( 'NONE', ( #63894, #58958, #77469, #233106 ) ) ;
#238960=CARTESIAN_POINT ( 'NONE',  ( 21.09551895715285852, 60.18325881433904101, -221.2644573946620596 ) ) ;
#239002=DIRECTION ( 'NONE',  ( 0.000000000000000000, -0.2617529984165031243, -0.9651348961777157509 ) ) ;
#239018=DIRECTION ( 'NONE',  ( 0.000000000000000000, 0.9616958981405249185, -0.2741185865637160157 ) ) ;
#239026=DIRECTION ( 'NONE',  ( 1.000000000000000000, 0.000000000000000000, 0.000000000000000000 ) ) ;
#239048=DIRECTION ( 'NONE',  ( -1.000000000000000000, -0.000000000000000000, -0.000000000000000000 ) ) ;
#239063=DIRECTION ( 'NONE',  ( 0.000000000000000000, 0.2617529984164915779, 0.9651348961777189706 ) ) ;
#239095=AXIS2_PLACEMENT_3D ( 'NONE', #100376, #118705, #177406 ) ;
#239127=ORIENTED_EDGE ( 'NONE', *, *, #156789, .F. ) ;
#239151=DIRECTION ( 'NONE',  ( 0.000000000000000000, -0.2617529984165031243, -0.9651348961777157509 ) ) ;
#239178=CARTESIAN_POINT ( 'NONE',  ( 23.15000000000000213, 82.09643798151613225, -215.4278993322501208 ) ) ;
#239186=DIRECTION ( 'NONE',  ( 0.000000000000000000, 0.9651348961777148627, -0.2617529984165062329 ) ) ;
#239191=PLANE ( 'NONE',  #123434 ) ;
#239213=DIRECTION ( 'NONE',  ( 0.000000000000000000, 0.1180230956474139226, -0.9930108503404186937 ) ) ;
#239225=FACE_OUTER_BOUND ( 'NONE', #137558, .T. ) ;
#239226=CARTESIAN_POINT ( 'NONE',  ( -20.54999999999999716, 66.26558728512915764, -222.7970849955717938 ) ) ;
#239235=VECTOR ( 'NONE', #42994, 1000.000000000000000 ) ;
#239239=CARTESIAN_POINT ( 'NONE',  ( 22.50000000000000000, 67.23127455305841238, -235.8551265064783991 ) ) ;
#239271=CARTESIAN_POINT ( 'NONE',  ( 23.14999999999999503, 62.92003201576280702, -207.2439188921395612 ) ) ;
#239364=ORIENTED_EDGE ( 'NONE', *, *, #24328, .T. ) ;
#239374=EDGE_CURVE ( 'NONE', #210631, #84318, #111683, .T. ) ;
#239376=DIRECTION ( 'NONE',  ( 0.000000000000000000, 0.3896596508880098009, 0.9209589331071361684 ) ) ;
#239380=PLANE ( 'NONE',  #193261 ) ;
#239397=DIRECTION ( 'NONE',  ( -1.000000000000000000, 0.000000000000000000, 0.000000000000000000 ) ) ;
#239414=FACE_OUTER_BOUND ( 'NONE', #175900, .T. ) ;
#239442=CARTESIAN_POINT ( 'NONE',  ( -23.15000000000000213, 67.23127455305841238, -235.8551265064783991 ) ) ;
#239505=DIRECTION ( 'NONE',  ( 1.000000000000000000, 0.000000000000000000, 0.000000000000000000 ) ) ;
#239537=CARTESIAN_POINT ( 'NONE',  ( -23.24999999999999645, 86.99291436658650412, -199.6658631664729739 ) ) ;
#239547=LINE ( 'NONE', #64748, #225915 ) ;
#239577=VECTOR ( 'NONE', #130870, 1000.000000000000000 ) ;
#239592=ORIENTED_EDGE ( 'NONE', *, *, #63698, .F. ) ;
#239601=FACE_OUTER_BOUND ( 'NONE', #129404, .T. ) ;
#239682=VERTEX_POINT ( 'NONE', #237652 ) ;
#239758=AXIS2_PLACEMENT_3D ( 'NONE', #203462, #225555, #182626 ) ;
#239762=ORIENTED_EDGE ( 'NONE', *, *, #128126, .T. ) ;
#239790=TOROIDAL_SURFACE ( 'NONE', #169076, 11.65000000000000036, 0.1000000000000000056 ) ;
#239819=CARTESIAN_POINT ( 'NONE',  ( -18.39999999999999858, 86.99291436658650412, -199.6658631664729739 ) ) ;
#239822=AXIS2_PLACEMENT_3D ( 'NONE', #79768, #81059, #182765 ) ;
#239839=VECTOR ( 'NONE', #47233, 1000.000000000000000 ) ;
#239858=AXIS2_PLACEMENT_3D ( 'NONE', #199688, #234944, #178853 ) ;
#239873=AXIS2_PLACEMENT_3D ( 'NONE', #246126, #88294, #164023 ) ;
#239890=AXIS2_PLACEMENT_3D ( 'NONE', #234800, #52284, #131842 ) ;
#239892=ADVANCED_FACE ( 'NONE', ( #32761 ), #172277, .T. ) ;
#239895=CARTESIAN_POINT ( 'NONE',  ( 21.05000000000000071, 76.00000000001126921, -203.5231074845248997 ) ) ;
#239962=DIRECTION ( 'NONE',  ( -1.000000000000000000, -0.000000000000000000, -0.000000000000000000 ) ) ;
#239992=ORIENTED_EDGE ( 'NONE', *, *, #173006, .F. ) ;
#240009=EDGE_CURVE ( 'NONE', #242569, #5530, #66073, .T. ) ;
#240020=EDGE_LOOP ( 'NONE', ( #90389, #232331, #89861, #26158 ) ) ;
#240049=CARTESIAN_POINT ( 'NONE',  ( -22.39999999999999858, 64.25313205997782973, -247.2214437328673853 ) ) ;
#240058=VERTEX_POINT ( 'NONE', #79523 ) ;
#240074=FACE_OUTER_BOUND ( 'NONE', #196917, .T. ) ;
#240076=EDGE_LOOP ( 'NONE', ( #235113, #242586, #37380, #192710 ) ) ;
#240096=DIRECTION ( 'NONE',  ( 0.000000000000000000, 0.2617529984165031243, 0.9651348961777157509 ) ) ;
#240098=FACE_OUTER_BOUND ( 'NONE', #117425, .T. ) ;
#240100=DIRECTION ( 'NONE',  ( 0.000000000000000000, 0.2558827019434435912, -0.9667078373770033872 ) ) ;
#240101=CARTESIAN_POINT ( 'NONE',  ( -23.15000000000000213, 67.23127455305841238, -235.8551265064783991 ) ) ;
#240133=CARTESIAN_POINT ( 'NONE',  ( 23.14999999999999858, 65.07363471106805264, -222.4165545841253220 ) ) ;
#240144=CARTESIAN_POINT ( 'NONE',  ( 22.01447462590973103, 65.23436900571785202, -242.8397503278283125 ) ) ;
#240159=CARTESIAN_POINT ( 'NONE',  ( 23.14999999999999858, 67.23127455305841238, -235.8551265064783991 ) ) ;
#240173=AXIS2_PLACEMENT_3D ( 'NONE', #157005, #39638, #233949 ) ;
#240248=CARTESIAN_POINT ( 'NONE',  ( -21.12642695952773764, 61.05201444521252796, -234.2817334149543456 ) ) ;
#240258=AXIS2_PLACEMENT_3D ( 'NONE', #107031, #184012, #24972 ) ;
#240263=AXIS2_PLACEMENT_3D ( 'NONE', #67905, #28837, #6641 ) ;
#240265=EDGE_LOOP ( 'NONE', ( #66781, #251516, #247459, #218459, #147085, #91453, #69420, #252159, #27873, #132804, #166022 ) ) ;
#240279=ORIENTED_EDGE ( 'NONE', *, *, #68486, .T. ) ;
#240311=ORIENTED_EDGE ( 'NONE', *, *, #132678, .F. ) ;
#240313=CIRCLE ( 'NONE', #107021, 11.79999999999999361 ) ;
#240317=CARTESIAN_POINT ( 'NONE',  ( -20.94999999999999929, 70.47363787294415260, -228.3418745167492432 ) ) ;
#240320=CARTESIAN_POINT ( 'NONE',  ( -23.15000000000000213, 76.00000000001126921, -203.5231074845248997 ) ) ;
#240331=AXIS2_PLACEMENT_3D ( 'NONE', #249170, #49671, #47081 ) ;
#240332=ORIENTED_EDGE ( 'NONE', *, *, #13488, .F. ) ;
#240344=DIRECTION ( 'NONE',  ( 0.000000000000000000, 0.2617529984162567103, 0.9651348961777825863 ) ) ;
#240355=ORIENTED_EDGE ( 'NONE', *, *, #36179, .F. ) ;
#240367=ADVANCED_FACE ( 'NONE', ( #174544 ), #154951, .T. ) ;
#240388=DIRECTION ( 'NONE',  ( 0.000000000000000000, 0.2617529984165031243, 0.9651348961777157509 ) ) ;
#240397=CIRCLE ( 'NONE', #211175, 0.09999999999999875655 ) ;
#240398=CARTESIAN_POINT ( 'NONE',  ( -22.49510344025093644, 64.11707268185745079, -247.0813483233072532 ) ) ;
#240399=ORIENTED_EDGE ( 'NONE', *, *, #161934, .T. ) ;
#240400=AXIS2_PLACEMENT_3D ( 'NONE', #62207, #45201, #86870 ) ;
#240404=CARTESIAN_POINT ( 'NONE',  ( 21.05000000000000426, 65.55640845144084494, -241.8974783712178862 ) ) ;
#240411=CARTESIAN_POINT ( 'NONE',  ( -20.93302460841143287, 67.49317130920637453, -195.4795610751097286 ) ) ;
#240441=ORIENTED_EDGE ( 'NONE', *, *, #75082, .T. ) ;
#240445=DIRECTION ( 'NONE',  ( 1.000000000000000000, 0.000000000000000000, 0.000000000000000000 ) ) ;
#240459=EDGE_LOOP ( 'NONE', ( #165706, #251137, #248845, #121389 ) ) ;
#240490=CARTESIAN_POINT ( 'NONE',  ( 22.57320508075688537, 55.98745301258801987, -232.8057040749261262 ) ) ;
#240498=EDGE_LOOP ( 'NONE', ( #253734, #105590, #96591, #108395 ) ) ;
#240499=CARTESIAN_POINT ( 'NONE',  ( -23.25000000000000000, 78.50726470275243685, -228.6618886302502176 ) ) ;
#240550=CIRCLE ( 'NONE', #203121, 2.000000000000013323 ) ;
#240594=ORIENTED_EDGE ( 'NONE', *, *, #256061, .T. ) ;
#240608=DIRECTION ( 'NONE',  ( 2.694716079187273439E-16, 0.9651348961777159730, -0.2617529984165023471 ) ) ;
#240615=AXIS2_PLACEMENT_3D ( 'NONE', #2292, #139229, #60996 ) ;
#240619=ORIENTED_EDGE ( 'NONE', *, *, #205139, .F. ) ;
#240626=ORIENTED_EDGE ( 'NONE', *, *, #187650, .F. ) ;
#240630=CARTESIAN_POINT ( 'NONE',  ( 18.55121869061587958, 67.49249915771264341, -195.4369143829851510 ) ) ;
#240706=ORIENTED_EDGE ( 'NONE', *, *, #174223, .T. ) ;
#240721=STYLED_ITEM ( 'NONE', ( #124663 ), #18376 ) ;
#240726=DIRECTION ( 'NONE',  ( 0.000000000000000000, 0.9229812358756199764, -0.3848449534832346086 ) ) ;
#240740=ORIENTED_EDGE ( 'NONE', *, *, #48499, .F. ) ;
#240776=CARTESIAN_POINT ( 'NONE',  ( -20.85000000000000142, 79.11538813396778380, -196.3722783875038544 ) ) ;
#240783=DIRECTION ( 'NONE',  ( 0.000000000000000000, -0.9651348961777379554, 0.2617529984164210233 ) ) ;
#240805=CARTESIAN_POINT ( 'NONE',  ( 18.43473516226063325, 78.23945979424732400, -231.5402134245487105 ) ) ;
#240807=CYLINDRICAL_SURFACE ( 'NONE', #208766, 0.09999999999999939493 ) ;
#240813=AXIS2_PLACEMENT_3D ( 'NONE', #169980, #30439, #171270 ) ;
#240821=EDGE_CURVE ( 'NONE', #185020, #113811, #136597, .T. ) ;
#240823=ORIENTED_EDGE ( 'NONE', *, *, #87605, .T. ) ;
#240856=CIRCLE ( 'NONE', #3312, 6.329289321881358177 ) ;
#240936=DIRECTION ( 'NONE',  ( 1.000000000000000000, 0.000000000000000000, 0.000000000000000000 ) ) ;
#240942=ORIENTED_EDGE ( 'NONE', *, *, #122702, .F. ) ;
#240954=CARTESIAN_POINT ( 'NONE',  ( 18.59999999999999076, 66.47189219944506533, -213.6315278230738102 ) ) ;
#240977=CARTESIAN_POINT ( 'NONE',  ( -22.47071067811865319, 65.11488425470511743, -243.2801022963548689 ) ) ;
#241002=ORIENTED_EDGE ( 'NONE', *, *, #212339, .F. ) ;
#241031=EDGE_LOOP ( 'NONE', ( #218713, #2808, #88539, #12096 ) ) ;
#241052=DIRECTION ( 'NONE',  ( 0.7071359030027296599, 0.1850796971394779999, 0.6824253222084255555 ) ) ;
#241075=LINE ( 'NONE', #156422, #164872 ) ;
#241081=AXIS2_PLACEMENT_3D ( 'NONE', #30047, #226933, #207389 ) ;
#241086=CARTESIAN_POINT ( 'NONE',  ( 21.05000000000000071, 76.52350599684427834, -201.5928376921694678 ) ) ;
#241107=VERTEX_POINT ( 'NONE', #223555 ) ;
#241146=FACE_OUTER_BOUND ( 'NONE', #141189, .T. ) ;
#241198=CARTESIAN_POINT ( 'NONE',  ( -20.85000000000000142, 80.80934863333322937, -192.8037999715871535 ) ) ;
#241234=ORIENTED_EDGE ( 'NONE', *, *, #144619, .T. ) ;
#241239=ORIENTED_EDGE ( 'NONE', *, *, #214991, .T. ) ;
#241252=EDGE_CURVE ( 'NONE', #257242, #234655, #93051, .T. ) ;
#241262=VERTEX_POINT ( 'NONE', #145972 ) ;
#241314=AXIS2_PLACEMENT_3D ( 'NONE', #130585, #224549, #9352 ) ;
#241323=DIRECTION ( 'NONE',  ( -0.000000000000000000, 0.9651348961777157509, -0.2617529984165031243 ) ) ;
#241369=DIRECTION ( 'NONE',  ( 1.000000000000000000, -1.772924042024179943E-16, 4.808324575169860901E-17 ) ) ;
#241376=VECTOR ( 'NONE', #222946, 1000.000000000000000 ) ;
#241396=CARTESIAN_POINT ( 'NONE',  ( -20.00857864376270001, 63.93636616954134411, -213.0474835168086827 ) ) ;
#241451=PLANE ( 'NONE',  #239822 ) ;
#241465=EDGE_CURVE ( 'NONE', #194645, #193988, #12923, .T. ) ;
#241489=ORIENTED_EDGE ( 'NONE', *, *, #83812, .F. ) ;
#241501=CARTESIAN_POINT ( 'NONE',  ( -21.05000000000000071, 65.63520407022599557, -242.0679395242962357 ) ) ;
#241531=AXIS2_PLACEMENT_3D ( 'NONE', #110595, #151020, #229276 ) ;
#241590=DIRECTION ( 'NONE',  ( 0.000000000000000000, 0.2617529984164856383, 0.9651348961777204138 ) ) ;
#241619=VERTEX_POINT ( 'NONE', #183391 ) ;
#241633=DIRECTION ( 'NONE',  ( 0.000000000000000000, -0.2617529984165152257, -0.9651348961777124202 ) ) ;
#241639=EDGE_LOOP ( 'NONE', ( #150634, #83933, #16027, #93418, #181149, #147782, #56696, #40608, #111828, #128779, #206095, #128067 ) ) ;
#241652=CIRCLE ( 'NONE', #233303, 0.1000000000000027117 ) ;
#241655=CIRCLE ( 'NONE', #129244, 0.09999999999999939493 ) ;
#241660=DIRECTION ( 'NONE',  ( 1.000000000000000000, 0.000000000000000000, 0.000000000000000000 ) ) ;
#241671=DIRECTION ( 'NONE',  ( 0.000000000000000000, 0.2617529984165031243, 0.9651348961777157509 ) ) ;
#241688=CARTESIAN_POINT ( 'NONE',  ( -20.94983749550516450, 67.49429988484537546, -195.5441618131978601 ) ) ;
#241703=DIRECTION ( 'NONE',  ( 1.000000000000000000, 0.000000000000000000, 0.000000000000000000 ) ) ;
#241706=CARTESIAN_POINT ( 'NONE',  ( -21.44999999999999929, 63.37018259659601682, -222.0118260003222872 ) ) ;
#241710=AXIS2_PLACEMENT_3D ( 'NONE', #11177, #90696, #211956 ) ;
#241717=SHAPE_REPRESENTATION ( 'Injection Molded Chain Links 10', ( #2425 ), #89914 ) ;
#241719=EDGE_LOOP ( 'NONE', ( #249961, #112080, #70606, #60413 ) ) ;
#241726=CARTESIAN_POINT ( 'NONE',  ( -18.59999999999999787, 76.00000000001126921, -203.5231074845248997 ) ) ;
#241737=ORIENTED_EDGE ( 'NONE', *, *, #112146, .F. ) ;
#241773=CARTESIAN_POINT ( 'NONE',  ( 20.92356734117541706, 67.49293571122092317, -195.4648732548341741 ) ) ;
#241784=DIRECTION ( 'NONE',  ( 0.000000000000000000, 0.2617529984165031243, 0.9651348961777157509 ) ) ;
#241789=AXIS2_PLACEMENT_3D ( 'NONE', #149725, #68896, #207114 ) ;
#241793=ADVANCED_FACE ( 'NONE', ( #9581 ), #244336, .F. ) ;
#241805=CARTESIAN_POINT ( 'NONE',  ( 20.04142135623730070, 61.47936603916258491, -212.1738987416902376 ) ) ;
#241810=CARTESIAN_POINT ( 'NONE',  ( 21.05000000000000071, 61.06337788713324244, -234.0934405812916168 ) ) ;
#241851=CARTESIAN_POINT ( 'NONE',  ( -22.39999999999999858, 59.68594599439717285, -233.9123800762197902 ) ) ;
#241960=CARTESIAN_POINT ( 'NONE',  ( 20.94999999999999929, 66.37537870982728805, -213.6053525232321704 ) ) ;
#241977=EDGE_CURVE ( 'NONE', #137749, #224282, #219334, .T. ) ;
#242024=VERTEX_POINT ( 'NONE', #1565 ) ;
#242027=DIRECTION ( 'NONE',  ( 0.000000000000000000, -0.9209589331071864615, 0.3896596508878908960 ) ) ;
#242028=FILL_AREA_STYLE_COLOUR ( '', #153275 ) ;
#242049=VERTEX_POINT ( 'NONE', #137236 ) ;
#242086=FACE_OUTER_BOUND ( 'NONE', #114558, .T. ) ;
#242099=EDGE_CURVE ( 'NONE', #195218, #30065, #195638, .T. ) ;
#242102=CIRCLE ( 'NONE', #200420, 4.049999999999999822 ) ;
#242146=ORIENTED_EDGE ( 'NONE', *, *, #168383, .F. ) ;
#242188=FACE_OUTER_BOUND ( 'NONE', #39286, .T. ) ;
#242232=ADVANCED_FACE ( 'NONE', ( #64126 ), #28900, .F. ) ;
#242242=CARTESIAN_POINT ( 'NONE',  ( -21.00023020733502932, 65.55844536562159419, -242.0231774319958049 ) ) ;
#242267=DIRECTION ( 'NONE',  ( 0.000000000000000000, -0.3848449534832867891, -0.9229812358755983270 ) ) ;
#242268=ORIENTED_EDGE ( 'NONE', *, *, #44073, .F. ) ;
#242278=TOROIDAL_SURFACE ( 'NONE', #100606, 1.900000000000002576, 0.1000000000000000056 ) ;
#242290=CIRCLE ( 'NONE', #225135, 0.1000000000000124678 ) ;
#242325=FACE_OUTER_BOUND ( 'NONE', #41469, .T. ) ;
#242353=SPHERICAL_SURFACE ( 'NONE', #50292, 0.1000000000000000056 ) ;
#242398=ORIENTED_EDGE ( 'NONE', *, *, #168060, .F. ) ;
#242407=VECTOR ( 'NONE', #231715, 1000.000000000000000 ) ;
#242487=CIRCLE ( 'NONE', #59284, 0.09999999999999543976 ) ;
#242510=CARTESIAN_POINT ( 'NONE',  ( 23.14999999999999503, 66.44571689960341132, -213.7280413126916017 ) ) ;
#242528=CARTESIAN_POINT ( 'NONE',  ( 20.94999999999999929, 72.02722222756959525, -225.1832529173024398 ) ) ;
#242550=FACE_OUTER_BOUND ( 'NONE', #190428, .T. ) ;
#242554=VECTOR ( 'NONE', #101588, 1000.000000000000000 ) ;
#242569=VERTEX_POINT ( 'NONE', #104207 ) ;
#242581=VERTEX_POINT ( 'NONE', #164214 ) ;
#242586=ORIENTED_EDGE ( 'NONE', *, *, #178084, .F. ) ;
#242590=ORIENTED_EDGE ( 'NONE', *, *, #217706, .T. ) ;
#242593=FACE_OUTER_BOUND ( 'NONE', #100632, .T. ) ;
#242598=CARTESIAN_POINT ( 'NONE',  ( -22.57320508075687115, 55.89093952297024970, -232.7795287750844579 ) ) ;
#242606=CIRCLE ( 'NONE', #113623, 0.1999999999999945155 ) ;
#242667=CARTESIAN_POINT ( 'NONE',  ( 18.59999999999999076, 62.49201502323811752, -208.8221019049098857 ) ) ;
#242719=ADVANCED_FACE ( 'NONE', ( #153682 ), #70267, .T. ) ;
#242724=LINE ( 'NONE', #238895, #23688 ) ;
#242736=VERTEX_POINT ( 'NONE', #51927 ) ;
#242752=VECTOR ( 'NONE', #29209, 1000.000000000000000 ) ;
#242762=CARTESIAN_POINT ( 'NONE',  ( -20.96428641294356510, 62.87317279473557363, -207.0346585172401603 ) ) ;
#242763=ORIENTED_EDGE ( 'NONE', *, *, #119112, .T. ) ;
#242809=CARTESIAN_POINT ( 'NONE',  ( -21.14999999999999858, 56.01362831242966678, -232.7091905853083347 ) ) ;
#242849=ORIENTED_EDGE ( 'NONE', *, *, #183941, .T. ) ;
#242904=ORIENTED_EDGE ( 'NONE', *, *, #16380, .T. ) ;
#242905=ORIENTED_EDGE ( 'NONE', *, *, #241252, .T. ) ;
#242914=ORIENTED_EDGE ( 'NONE', *, *, #164177, .T. ) ;
#242917=VECTOR ( 'NONE', #45599, 1000.000000000000000 ) ;
#242924=FACE_OUTER_BOUND ( 'NONE', #99603, .T. ) ;
#242932=DIRECTION ( 'NONE',  ( -1.000000000000000000, -0.000000000000000000, 0.000000000000000000 ) ) ;
#242944=EDGE_LOOP ( 'NONE', ( #162988, #186073, #186126, #162805 ) ) ;
#242957=DIRECTION ( 'NONE',  ( 0.000000000000000000, -0.9651348961777157509, 0.2617529984165031243 ) ) ;
#242965=VERTEX_POINT ( 'NONE', #141745 ) ;
#242973=CIRCLE ( 'NONE', #172310, 0.1000000000000124678 ) ;
#242990=VERTEX_POINT ( 'NONE', #101285 ) ;
#243001=DIRECTION ( 'NONE',  ( 1.000000000000000000, 0.000000000000000000, 0.000000000000000000 ) ) ;
#243003=FACE_OUTER_BOUND ( 'NONE', #224404, .T. ) ;
#243004=CARTESIAN_POINT ( 'NONE',  ( 21.07928932188134397, 65.47931918658503037, -241.9371126717015841 ) ) ;
#243014=DIRECTION ( 'NONE',  ( 0.000000000000000000, -0.2617529984165152257, -0.9651348961777124202 ) ) ;
#243064=CARTESIAN_POINT ( 'NONE',  ( -18.58693740092205005, 78.17469254045161620, -231.4408793351767315 ) ) ;
#243065=AXIS2_PLACEMENT_3D ( 'NONE', #104610, #160803, #19995 ) ;
#243068=DIRECTION ( 'NONE',  ( -0.000000000000000000, 0.2617529984165031243, 0.9651348961777157509 ) ) ;
#243077=ORIENTED_EDGE ( 'NONE', *, *, #238577, .T. ) ;
#243102=DIRECTION ( 'NONE',  ( 1.000000000000000000, 0.000000000000000000, 0.000000000000000000 ) ) ;
#243109=EDGE_CURVE ( 'NONE', #110910, #74710, #111617, .T. ) ;
#243113=DIRECTION ( 'NONE',  ( -1.000000000000000000, 0.000000000000000000, 0.000000000000000000 ) ) ;
#243214=VECTOR ( 'NONE', #132286, 1000.000000000000000 ) ;
#243233=CARTESIAN_POINT ( 'NONE',  ( -18.59999999999999787, 61.53642629385834795, -221.5144953033309321 ) ) ;
#243285=FACE_OUTER_BOUND ( 'NONE', #179331, .T. ) ;
#243312=CARTESIAN_POINT ( 'NONE',  ( 21.05000000000000071, 60.92723693130623985, -225.4208407479578113 ) ) ;
#243340=FACE_OUTER_BOUND ( 'NONE', #218392, .T. ) ;
#243344=CIRCLE ( 'NONE', #222476, 0.1000000000000124678 ) ;
#243355=DIRECTION ( 'NONE',  ( 0.000000000000000000, -0.9651348961777428404, 0.2617529984164035373 ) ) ;
#243371=DIRECTION ( 'NONE',  ( -1.000000000000000000, -0.000000000000000000, -0.000000000000000000 ) ) ;
#243415=EDGE_LOOP ( 'NONE', ( #26986, #216159, #1571, #33175 ) ) ;
#243428=EDGE_CURVE ( 'NONE', #7048, #23903, #50379, .T. ) ;
#243445=CARTESIAN_POINT ( 'NONE',  ( 18.39999999999999858, 86.89640087696871262, -199.6396878666313341 ) ) ;
#243452=ORIENTED_EDGE ( 'NONE', *, *, #52489, .F. ) ;
#243455=CIRCLE ( 'NONE', #131022, 0.5000000000000051070 ) ;
#243466=CARTESIAN_POINT ( 'NONE',  ( -18.59999999999999787, 76.00000000001126921, -203.5231074845248997 ) ) ;
#243502=CARTESIAN_POINT ( 'NONE',  ( 18.59999999999999076, 66.56840568906282840, -213.6577031229154500 ) ) ;
#243540=ORIENTED_EDGE ( 'NONE', *, *, #8141, .F. ) ;
#243541=ORIENTED_EDGE ( 'NONE', *, *, #249005, .T. ) ;
#243558=EDGE_CURVE ( 'NONE', #84528, #148169, #237364, .T. ) ;
#243560=AXIS2_PLACEMENT_3D ( 'NONE', #242667, #202272, #23663 ) ;
#243561=CARTESIAN_POINT ( 'NONE',  ( -20.94999999999999929, 64.23744694032048130, -224.5446448091673233 ) ) ;
#243586=AXIS2_PLACEMENT_3D ( 'NONE', #56079, #75689, #135631 ) ;
#243593=DIRECTION ( 'NONE',  ( -1.000000000000000000, 0.000000000000000000, 0.000000000000000000 ) ) ;
#243635=EDGE_LOOP ( 'NONE', ( #50512, #250938, #18214, #21332 ) ) ;
#243642=EDGE_CURVE ( 'NONE', #134983, #203694, #200803, .T. ) ;
#243653=DIRECTION ( 'NONE',  ( -1.000000000000000000, -0.000000000000000000, -0.000000000000000000 ) ) ;
#243666=CIRCLE ( 'NONE', #160488, 0.6000000000000139666 ) ;
#243667=CIRCLE ( 'NONE', #131229, 0.1000000000000124678 ) ;
#243668=TOROIDAL_SURFACE ( 'NONE', #18799, 3.899999999999999467, 0.1000000000000000056 ) ;
#243679=CARTESIAN_POINT ( 'NONE',  ( 21.06086055316007943, 61.95649253837676440, -221.7814335778687962 ) ) ;
#243692=CARTESIAN_POINT ( 'NONE',  ( 23.14999999999999858, 76.00000000001126921, -203.5231074845248997 ) ) ;
#243696=ORIENTED_EDGE ( 'NONE', *, *, #125291, .F. ) ;
#243781=CARTESIAN_POINT ( 'NONE',  ( 23.24999999999999289, 66.40155400966892785, -213.5088390336144073 ) ) ;
#243796=CARTESIAN_POINT ( 'NONE',  ( 21.05000000000000071, 67.92720994251783395, -214.1870976236629929 ) ) ;
#243802=DIRECTION ( 'NONE',  ( 1.000000000000000000, 0.000000000000000000, 0.000000000000000000 ) ) ;
#243815=CARTESIAN_POINT ( 'NONE',  ( 20.94999999999999929, 68.19849547655701372, -211.6586561550524834 ) ) ;
#243833=CYLINDRICAL_SURFACE ( 'NONE', #100135, 0.09999999999999939493 ) ;
#243849=ORIENTED_EDGE ( 'NONE', *, *, #224870, .T. ) ;
#243859=CARTESIAN_POINT ( 'NONE',  ( -18.54260524012582323, 87.05308753821724110, -199.5365204736072258 ) ) ;
#243904=DIRECTION ( 'NONE',  ( -1.000000000000000000, -0.000000000000000000, 0.000000000000000000 ) ) ;
#243920=ORIENTED_EDGE ( 'NONE', *, *, #129233, .T. ) ;
#243922=ADVANCED_FACE ( 'NONE', ( #14178 ), #234880, .T. ) ;
#243927=DIRECTION ( 'NONE',  ( 0.000000000000000000, -0.2617529984165031243, -0.9651348961777157509 ) ) ;
#243936=EDGE_LOOP ( 'NONE', ( #53395, #66434, #170971, #173768 ) ) ;
#243965=CYLINDRICAL_SURFACE ( 'NONE', #108198, 0.09999999999999789613 ) ;
#243987=FACE_OUTER_BOUND ( 'NONE', #204443, .T. ) ;
#243991=CARTESIAN_POINT ( 'NONE',  ( 20.94999999999999574, 79.10508929521364507, -235.9670348125907537 ) ) ;
#244011=CARTESIAN_POINT ( 'NONE',  ( 20.85000000000000142, 70.29876110920605470, -198.0544810472949564 ) ) ;
#244014=CARTESIAN_POINT ( 'NONE',  ( -18.59999999999999787, 57.82359945636609666, -226.0354702357591350 ) ) ;
#244040=DIRECTION ( 'NONE',  ( -1.000000000000000000, -0.000000000000000000, 0.000000000000000000 ) ) ;
#244044=DIRECTION ( 'NONE',  ( 0.000000000000000000, -0.2617529984165031243, -0.9651348961777157509 ) ) ;
#244045=EDGE_CURVE ( 'NONE', #242569, #141218, #59115, .T. ) ;
#244047=CARTESIAN_POINT ( 'NONE',  ( -21.05000000000000071, 62.82351852614505106, -207.2177435922979498 ) ) ;
#244063=FACE_OUTER_BOUND ( 'NONE', #160264, .T. ) ;
#244064=EDGE_LOOP ( 'NONE', ( #87528, #20691, #235690, #80789 ) ) ;
#244089=ORIENTED_EDGE ( 'NONE', *, *, #249628, .T. ) ;
#244155=CARTESIAN_POINT ( 'NONE',  ( -20.94999999999999929, 86.25530027761219287, -209.3091956463349277 ) ) ;
#244167=CARTESIAN_POINT ( 'NONE',  ( 20.85000000000000142, 75.77017861926654518, -203.7552340087416951 ) ) ;
#244177=EDGE_LOOP ( 'NONE', ( #63934, #146733, #195985, #104295 ) ) ;
#244207=CARTESIAN_POINT ( 'NONE',  ( 23.24999999999999645, 76.00000000001126921, -203.5231074845248997 ) ) ;
#244226=SURFACE_STYLE_FILL_AREA ( #141296 ) ;
#244310=ORIENTED_EDGE ( 'NONE', *, *, #241977, .F. ) ;
#244336=PLANE ( 'NONE',  #249601 ) ;
#244342=CARTESIAN_POINT ( 'NONE',  ( -18.54270223418605923, 87.05302002691458085, -199.5363343069655571 ) ) ;
#244344=CARTESIAN_POINT ( 'NONE',  ( -18.50000000000000711, 78.21981816082171690, -231.3313247107103052 ) ) ;
#244346=VERTEX_POINT ( 'NONE', #56780 ) ;
#244358=DIRECTION ( 'NONE',  ( 0.000000000000000000, 0.2617529984165021806, 0.9651348961777159730 ) ) ;
#244391=PLANE ( 'NONE',  #76885 ) ;
#244405=AXIS2_PLACEMENT_3D ( 'NONE', #207615, #6827, #88914 ) ;
#244413=EDGE_CURVE ( 'NONE', #236044, #225653, #197599, .T. ) ;
#244422=AXIS2_PLACEMENT_3D ( 'NONE', #151593, #72038, #154180 ) ;
#244446=CARTESIAN_POINT ( 'NONE',  ( -18.50000000000000000, 86.87843599112028414, -199.3967987332378584 ) ) ;
#244532=EDGE_CURVE ( 'NONE', #206526, #138829, #163399, .T. ) ;
#244538=ORIENTED_EDGE ( 'NONE', *, *, #186509, .F. ) ;
#244544=DIRECTION ( 'NONE',  ( 1.000000000000000000, 0.000000000000000000, 0.000000000000000000 ) ) ;
#244558=FACE_OUTER_BOUND ( 'NONE', #249787, .T. ) ;
#244594=AXIS2_PLACEMENT_3D ( 'NONE', #176158, #154056, #117452 ) ;
#244644=EDGE_LOOP ( 'NONE', ( #138413, #25103, #144236, #129488 ) ) ;
#244649=CARTESIAN_POINT ( 'NONE',  ( 20.94999999999999574, 68.48451787451661232, -224.2224406095231757 ) ) ;
#244653=DIRECTION ( 'NONE',  ( 0.000000000000000000, 0.2617529984165180013, 0.9651348961777117541 ) ) ;
#244706=DIRECTION ( 'NONE',  ( -1.000000000000000000, -0.000000000000000000, 0.000000000000000000 ) ) ;
#244726=CIRCLE ( 'NONE', #148899, 11.80000000000001137 ) ;
#244745=EDGE_CURVE ( 'NONE', #41329, #251252, #110058, .T. ) ;
#244749=DIRECTION ( 'NONE',  ( -1.000000000000000000, 2.849773892568378313E-16, -7.728835255496647986E-17 ) ) ;
#244752=ORIENTED_EDGE ( 'NONE', *, *, #217294, .T. ) ;
#244766=DIRECTION ( 'NONE',  ( 0.000000000000000000, -0.4099100576505548821, -0.9121259477928028714 ) ) ;
#244863=DIRECTION ( 'NONE',  ( 0.000000000000000000, 0.2617529984165031243, 0.9651348961777157509 ) ) ;
#244874=CIRCLE ( 'NONE', #132454, 0.6000000000000139666 ) ;
#244875=FACE_OUTER_BOUND ( 'NONE', #258001, .T. ) ;
#244950=ORIENTED_EDGE ( 'NONE', *, *, #218672, .T. ) ;
#244985=VECTOR ( 'NONE', #221362, 1000.000000000000000 ) ;
#244987=AXIS2_PLACEMENT_3D ( 'NONE', #59988, #182544, #101665 ) ;
#244996=( GEOMETRIC_REPRESENTATION_CONTEXT ( 3 ) GLOBAL_UNCERTAINTY_ASSIGNED_CONTEXT ( ( #203095 ) ) GLOBAL_UNIT_ASSIGNED_CONTEXT ( ( #48959, #24293, #128509 ) ) REPRESENTATION_CONTEXT ( 'NONE', 'WORKASPACE' ) );
#245017=EDGE_CURVE ( 'NONE', #204155, #247, #39175, .T. ) ;
#245028=LINE ( 'NONE', #27302, #247197 ) ;
#245059=CARTESIAN_POINT ( 'NONE',  ( -20.54999999999999716, 61.41373750439892376, -221.5848334931070553 ) ) ;
#245114=ORIENTED_EDGE ( 'NONE', *, *, #135245, .T. ) ;
#245130=DIRECTION ( 'NONE',  ( 1.000000000000000000, 0.000000000000000000, 0.000000000000000000 ) ) ;
#245164=CARTESIAN_POINT ( 'NONE',  ( 18.50000000000030553, 63.78126560769650411, -209.3017168652885971 ) ) ;
#245198=AXIS2_PLACEMENT_3D ( 'NONE', #152459, #134135, #213683 ) ;
#245210=ORIENTED_EDGE ( 'NONE', *, *, #26137, .T. ) ;
#245211=EDGE_LOOP ( 'NONE', ( #180027, #135400, #249390, #167215 ) ) ;
#245236=CARTESIAN_POINT ( 'NONE',  ( 21.00000000000000000, 63.38346053167636995, -212.7939182281409956 ) ) ;
#245245=FACE_OUTER_BOUND ( 'NONE', #105560, .T. ) ;
#245248=ORIENTED_EDGE ( 'NONE', *, *, #129086, .T. ) ;
#245258=CARTESIAN_POINT ( 'NONE',  ( -23.15000000000000213, 75.39949836213489220, -250.2448839681187849 ) ) ;
#245280=TOROIDAL_SURFACE ( 'NONE', #132855, 0.4000000000000010214, 0.1000000000000000056 ) ;
#245281=CARTESIAN_POINT ( 'NONE',  ( 21.59780538579341780, 65.34350030841025614, -242.4375845506680207 ) ) ;
#245283=CARTESIAN_POINT ( 'NONE',  ( 21.07094088545368038, 65.48150606888252412, -241.9290547188616074 ) ) ;
#245313=CARTESIAN_POINT ( 'NONE',  ( -23.15000000000000213, 78.50726470275243685, -228.6618886302502176 ) ) ;
#245334=DIRECTION ( 'NONE',  ( -1.000000000000000000, -0.000000000000000000, -0.000000000000000000 ) ) ;
#245335=CARTESIAN_POINT ( 'NONE',  ( -18.59999999999999787, 64.75617845954087670, -200.4736850529726269 ) ) ;
#245337=DIRECTION ( 'NONE',  ( 0.000000000000000000, 0.2617529984165033463, 0.9651348961777156399 ) ) ;
#245338=LINE ( 'NONE', #8018, #206307 ) ;
#245340=VECTOR ( 'NONE', #122763, 1000.000000000000000 ) ;
#245342=ORIENTED_EDGE ( 'NONE', *, *, #69755, .F. ) ;
#245391=VERTEX_POINT ( 'NONE', #54471 ) ;
#245394=ORIENTED_EDGE ( 'NONE', *, *, #125975, .T. ) ;
#245481=CARTESIAN_POINT ( 'NONE',  ( -20.94999999999999929, 67.46931694187804851, -235.9558427390807083 ) ) ;
#245483=CYLINDRICAL_SURFACE ( 'NONE', #103589, 0.09999999999999961697 ) ;
#245522=DIRECTION ( 'NONE',  ( 0.000000000000000000, 0.2617529984165152257, 0.9651348961777124202 ) ) ;
#245525=DIRECTION ( 'NONE',  ( -1.000000000000000000, 2.849773892568378313E-16, -7.728835255496647986E-17 ) ) ;
#245530=CIRCLE ( 'NONE', #170565, 0.09999999999999868716 ) ;
#245565=AXIS2_PLACEMENT_3D ( 'NONE', #172914, #39500, #73796 ) ;
#245599=DIRECTION ( 'NONE',  ( -1.000000000000000000, -0.000000000000000000, 0.000000000000000000 ) ) ;
#245610=DIRECTION ( 'NONE',  ( 0.000000000000000000, -0.2617529984165152257, -0.9651348961777124202 ) ) ;
#245619=AXIS2_PLACEMENT_3D ( 'NONE', #136140, #177885, #54062 ) ;
#245638=EDGE_LOOP ( 'NONE', ( #238165, #189814, #37706, #257008 ) ) ;
#245660=CIRCLE ( 'NONE', #62510, 0.1000000000000124678 ) ;
#245689=CARTESIAN_POINT ( 'NONE',  ( 18.49999999999999289, 63.77010848770628826, -209.1687319955904911 ) ) ;
#245701=ORIENTED_EDGE ( 'NONE', *, *, #120753, .F. ) ;
#245706=EDGE_CURVE ( 'NONE', #46773, #15410, #103159, .T. ) ;
#245715=ADVANCED_FACE ( 'NONE', ( #58889 ), #27068, .F. ) ;
#245791=ORIENTED_EDGE ( 'NONE', *, *, #53830, .T. ) ;
#245803=CONICAL_SURFACE ( 'NONE', #95751, 4.049999999999987388, 0.7853981633974604915 ) ;
#245817=CARTESIAN_POINT ( 'NONE',  ( -21.29999999999995808, 67.23127455305841238, -235.8551265064783991 ) ) ;
#245835=CARTESIAN_POINT ( 'NONE',  ( 22.59999999999999432, 64.08545097430041437, -247.0723585184913986 ) ) ;
#245868=ORIENTED_EDGE ( 'NONE', *, *, #173127, .T. ) ;
#245870=DIRECTION ( 'NONE',  ( -1.000000000000000000, -0.000000000000000000, 0.000000000000000000 ) ) ;
#245881=EDGE_LOOP ( 'NONE', ( #76126, #191809, #252364, #162253 ) ) ;
#245889=CIRCLE ( 'NONE', #133458, 0.09999999999999543976 ) ;
#245892=AXIS2_PLACEMENT_3D ( 'NONE', #81298, #203842, #160893 ) ;
#245910=DIRECTION ( 'NONE',  ( 0.000000000000000000, 0.2617529984165152257, 0.9651348961777124202 ) ) ;
#245916=CARTESIAN_POINT ( 'NONE',  ( -18.39999999999999858, 78.24072131640578220, -231.5548844243369047 ) ) ;
#245966=DIRECTION ( 'NONE',  ( 0.000000000000000000, 0.2617529984165055668, 0.9651348961777149738 ) ) ;
#246011=DIRECTION ( 'NONE',  ( 0.000000000000000000, 0.2617529984164955192, 0.9651348961777178603 ) ) ;
#246025=DIRECTION ( 'NONE',  ( -0.000000000000000000, 0.3848449534832920627, 0.9229812358755962176 ) ) ;
#246066=CARTESIAN_POINT ( 'NONE',  ( -21.59142135623730852, 65.19104153457237771, -213.3877624147501422 ) ) ;
#246070=CARTESIAN_POINT ( 'NONE',  ( -18.59999999999999787, 70.08587962373171365, -198.1273832143211848 ) ) ;
#246078=VECTOR ( 'NONE', #226344, 1000.000000000000000 ) ;
#246087=FACE_OUTER_BOUND ( 'NONE', #167114, .T. ) ;
#246096=CARTESIAN_POINT ( 'NONE',  ( -22.39999999999999858, 65.09550114356427741, -243.3481044654562879 ) ) ;
#246099=LINE ( 'NONE', #6178, #59390 ) ;
#246121=EDGE_LOOP ( 'NONE', ( #241239, #178869, #41830, #65646 ) ) ;
#246126=CARTESIAN_POINT ( 'NONE',  ( -21.14999999999999858, 64.27847795353595473, -247.1247091181747066 ) ) ;
#246129=ADVANCED_FACE ( 'NONE', ( #117306 ), #245280, .F. ) ;
#246143=EDGE_LOOP ( 'NONE', ( #75187, #88449, #17453, #158398, #161098 ) ) ;
#246149=ORIENTED_EDGE ( 'NONE', *, *, #8183, .T. ) ;
#246158=FACE_OUTER_BOUND ( 'NONE', #214337, .T. ) ;
#246213=ORIENTED_EDGE ( 'NONE', *, *, #92629, .F. ) ;
#246231=DIRECTION ( 'NONE',  ( 1.000000000000000000, 0.000000000000000000, 0.000000000000000000 ) ) ;
#246236=LINE ( 'NONE', #165421, #170921 ) ;
#246240=VECTOR ( 'NONE', #57418, 1000.000000000000114 ) ;
#246268=PLANE ( 'NONE',  #200994 ) ;
#246281=ORIENTED_EDGE ( 'NONE', *, *, #61535, .T. ) ;
#246317=AXIS2_PLACEMENT_3D ( 'NONE', #140369, #257698, #141660 ) ;
#246322=LINE ( 'NONE', #84630, #43607 ) ;
#246379=CARTESIAN_POINT ( 'NONE',  ( 21.08376601933332495, 61.09374636974325767, -234.2566552461101708 ) ) ;
#246421=ORIENTED_EDGE ( 'NONE', *, *, #161292, .T. ) ;
#246480=DIRECTION ( 'NONE',  ( 1.000000000000000000, 0.000000000000000000, 0.000000000000000000 ) ) ;
#246481=ORIENTED_EDGE ( 'NONE', *, *, #253871, .F. ) ;
#246484=ORIENTED_EDGE ( 'NONE', *, *, #173934, .T. ) ;
#246532=DIRECTION ( 'NONE',  ( -0.7071067811865460184, -0.6824534298470606997, 0.1850873201761399356 ) ) ;
#246558=DIRECTION ( 'NONE',  ( 0.000000000000000000, 0.2617529984165044565, 0.9651348961777151958 ) ) ;
#246565=DIRECTION ( 'NONE',  ( 0.000000000000000000, 0.7049548389605068133, -0.7092521942342977503 ) ) ;
#246595=CARTESIAN_POINT ( 'NONE',  ( 21.14999999999999858, 64.01960172407876826, -222.2915665888316141 ) ) ;
#246599=ORIENTED_EDGE ( 'NONE', *, *, #56297, .F. ) ;
#246615=CYLINDRICAL_SURFACE ( 'NONE', #189452, 0.09999999999999911737 ) ;
#246675=AXIS2_PLACEMENT_3D ( 'NONE', #102810, #83243, #66286 ) ;
#246682=ORIENTED_EDGE ( 'NONE', *, *, #182863, .T. ) ;
#246714=ADVANCED_FACE ( 'NONE', ( #213194 ), #216591, .T. ) ;
#246742=CARTESIAN_POINT ( 'NONE',  ( -22.39999999999999858, 59.68594599439717285, -233.9123800762197902 ) ) ;
#246760=AXIS2_PLACEMENT_3D ( 'NONE', #250410, #151342, #113468 ) ;
#246764=VECTOR ( 'NONE', #16430, 1000.000000000000000 ) ;
#246779=FACE_OUTER_BOUND ( 'NONE', #117529, .T. ) ;
#246804=EDGE_CURVE ( 'NONE', #125, #95393, #154556, .T. ) ;
#246813=CIRCLE ( 'NONE', #134382, 0.09999999999999939493 ) ;
#246814=CARTESIAN_POINT ( 'NONE',  ( -18.52139480978222963, 78.22076358160548182, -231.5572559401365424 ) ) ;
#246843=CIRCLE ( 'NONE', #26297, 0.6000000000000139666 ) ;
#246871=ADVANCED_FACE ( 'NONE', ( #22419 ), #221847, .F. ) ;
#246896=CARTESIAN_POINT ( 'NONE',  ( 23.14999999999999858, 76.00000000001126921, -203.5231074845248997 ) ) ;
#246901=DIRECTION ( 'NONE',  ( 0.000000000000000000, 0.2617529984165152257, 0.9651348961777124202 ) ) ;
#246912=CARTESIAN_POINT ( 'NONE',  ( -18.59999999999999787, 86.96699927712941758, -199.3055931863049466 ) ) ;
#246940=CARTESIAN_POINT ( 'NONE',  ( 21.13422380239049403, 60.96433854134358654, -234.1554788215306644 ) ) ;
#246942=DIRECTION ( 'NONE',  ( 1.000000000000000000, 0.000000000000000000, 0.000000000000000000 ) ) ;
#246952=DIRECTION ( 'NONE',  ( 2.840903330521633255E-16, 0.7106264324241464703, -0.7035695228903324772 ) ) ;
#246953=ORIENTED_EDGE ( 'NONE', *, *, #113796, .F. ) ;
#246959=ORIENTED_EDGE ( 'NONE', *, *, #89703, .T. ) ;
#246960=DIRECTION ( 'NONE',  ( -1.000000000000000000, 1.772924042024179204E-16, -4.808324575169891715E-17 ) ) ;
#246969=ORIENTED_EDGE ( 'NONE', *, *, #160011, .T. ) ;
#246978=ORIENTED_EDGE ( 'NONE', *, *, #65223, .T. ) ;
#246994=ORIENTED_EDGE ( 'NONE', *, *, #91168, .F. ) ;
#247041=LINE ( 'NONE', #127106, #252830 ) ;
#247042=DIRECTION ( 'NONE',  ( 1.000000000000000000, 0.000000000000000000, 0.000000000000000000 ) ) ;
#247044=DIRECTION ( 'NONE',  ( 0.000000000000000000, 0.2617529984165031243, 0.9651348961777157509 ) ) ;
#247083=CIRCLE ( 'NONE', #134656, 0.1000000000000124678 ) ;
#247091=ORIENTED_EDGE ( 'NONE', *, *, #243558, .T. ) ;
#247140=ORIENTED_EDGE ( 'NONE', *, *, #180461, .T. ) ;
#247154=SURFACE_STYLE_FILL_AREA ( #208063 ) ;
#247155=DIRECTION ( 'NONE',  ( -4.391705002472931063E-16, -0.9651348961777154178, 0.2617529984165040680 ) ) ;
#247164=CARTESIAN_POINT ( 'NONE',  ( 20.94999999999999574, 68.48451787451661232, -224.2224406095231757 ) ) ;
#247189=DIRECTION ( 'NONE',  ( 0.000000000000000000, 0.7035695228903320331, 0.7106264324241468033 ) ) ;
#247197=VECTOR ( 'NONE', #169388, 1000.000000000000114 ) ;
#247240=AXIS2_PLACEMENT_3D ( 'NONE', #199489, #216449, #238589 ) ;
#247248=DIRECTION ( 'NONE',  ( 0.000000000000000000, 0.2617529984165152257, 0.9651348961777124202 ) ) ;
#247249=DIRECTION ( 'NONE',  ( 0.000000000000000000, 0.2617529984165152257, 0.9651348961777124202 ) ) ;
#247253=VERTEX_POINT ( 'NONE', #74403 ) ;
#247280=AXIS2_PLACEMENT_3D ( 'NONE', #85553, #165139, #245966 ) ;
#247288=CARTESIAN_POINT ( 'NONE',  ( 18.50000000000000355, 86.87366311306884370, -199.3414869250131858 ) ) ;
#247312=ORIENTED_EDGE ( 'NONE', *, *, #1025, .T. ) ;
#247383=EDGE_LOOP ( 'NONE', ( #37099, #126118, #181850, #120053 ) ) ;
#247384=ADVANCED_FACE ( 'NONE', ( #200731 ), #22110, .T. ) ;
#247426=LINE ( 'NONE', #210875, #122986 ) ;
#247437=AXIS2_PLACEMENT_3D ( 'NONE', #253102, #75776, #234844 ) ;
#247459=ORIENTED_EDGE ( 'NONE', *, *, #147406, .T. ) ;
#247469=AXIS2_PLACEMENT_3D ( 'NONE', #137596, #159761, #123199 ) ;
#247502=EDGE_CURVE ( 'NONE', #92812, #7533, #150337, .T. ) ;
#247508=DIRECTION ( 'NONE',  ( -0.000000000000000000, 0.2617529984165031243, 0.9651348961777157509 ) ) ;
#247510=DIRECTION ( 'NONE',  ( 0.000000000000000000, -0.2617529984165031243, -0.9651348961777157509 ) ) ;
#247515=ORIENTED_EDGE ( 'NONE', *, *, #245706, .F. ) ;
#247527=AXIS2_PLACEMENT_3D ( 'NONE', #117690, #233805, #134662 ) ;
#247583=AXIS2_PLACEMENT_3D ( 'NONE', #56962, #116972, #180803 ) ;
#247592=VECTOR ( 'NONE', #248944, 1000.000000000000000 ) ;
#247599=CIRCLE ( 'NONE', #197696, 0.1000000000000057648 ) ;
#247631=CARTESIAN_POINT ( 'NONE',  ( -23.15000000000000213, 62.92003201576280702, -207.2439188921395612 ) ) ;
#247650=CARTESIAN_POINT ( 'NONE',  ( 20.94999999999999929, 86.30329675166747450, -209.4258251677035787 ) ) ;
#247673=LINE ( 'NONE', #250239, #177991 ) ;
#247681=ORIENTED_EDGE ( 'NONE', *, *, #219950, .T. ) ;
#247683=DIRECTION ( 'NONE',  ( 0.000000000000000000, -0.9651348961777157509, 0.2617529984165031243 ) ) ;
#247688=CARTESIAN_POINT ( 'NONE',  ( 18.49999999999999645, 71.84303044094815505, -225.1053209871248271 ) ) ;
#247691=CARTESIAN_POINT ( 'NONE',  ( -18.59999999999999787, 68.50594083727658301, -224.0235912779512830 ) ) ;
#247692=CIRCLE ( 'NONE', #47192, 0.09999999999999939493 ) ;
#247718=CARTESIAN_POINT ( 'NONE',  ( -18.37151313414731746, 87.02160168029750764, -199.4493498806463094 ) ) ;
#247722=CARTESIAN_POINT ( 'NONE',  ( 18.59999999999999432, 63.58402440245808407, -209.2218768284338921 ) ) ;
#247742=ADVANCED_FACE ( 'NONE', ( #132764 ), #212296, .F. ) ;
#247748=EDGE_CURVE ( 'NONE', #174802, #76073, #139120, .T. ) ;
#247779=PLANE ( 'NONE',  #182631 ) ;
#247789=CARTESIAN_POINT ( 'NONE',  ( 18.59999999999999432, 70.56573376625485139, -228.3808404818380779 ) ) ;
#247792=ORIENTED_EDGE ( 'NONE', *, *, #68489, .T. ) ;
#247800=EDGE_CURVE ( 'NONE', #9861, #189304, #200565, .T. ) ;
#247806=DIRECTION ( 'NONE',  ( 2.715809747126116015E-16, 0.9651348961777156399, -0.2617529984165029577 ) ) ;
#247808=ORIENTED_EDGE ( 'NONE', *, *, #221565, .T. ) ;
#247809=ORIENTED_EDGE ( 'NONE', *, *, #27846, .T. ) ;
#247811=CIRCLE ( 'NONE', #89569, 0.1000000000000106498 ) ;
#247819=EDGE_LOOP ( 'NONE', ( #105817, #203775, #51291, #3289 ) ) ;
#247846=AXIS2_PLACEMENT_3D ( 'NONE', #239819, #98973, #258035 ) ;
#247901=AXIS2_PLACEMENT_3D ( 'NONE', #233978, #214413, #236543 ) ;
#247914=CARTESIAN_POINT ( 'NONE',  ( 23.14999999999999858, 68.22899648672319017, -213.7884437866858889 ) ) ;
#247937=CIRCLE ( 'NONE', #143880, 0.09999999999999642508 ) ;
#247968=DIRECTION ( 'NONE',  ( 0.000000000000000000, -0.8430646840892555005, -0.5378121776619452232 ) ) ;
#247999=ORIENTED_EDGE ( 'NONE', *, *, #64241, .T. ) ;
#248002=VERTEX_POINT ( 'NONE', #89440 ) ;
#248006=AXIS2_PLACEMENT_3D ( 'NONE', #70647, #131867, #208840 ) ;
#248019=ORIENTED_EDGE ( 'NONE', *, *, #113571, .T. ) ;
#248032=VERTEX_POINT ( 'NONE', #123450 ) ;
#248036=AXIS2_PLACEMENT_3D ( 'NONE', #133992, #152311, #10218 ) ;
#248135=VERTEX_POINT ( 'NONE', #194995 ) ;
#248136=ADVANCED_FACE ( 'NONE', ( #211983 ), #114142, .T. ) ;
#248149=DIRECTION ( 'NONE',  ( 2.952720810173289605E-16, 0.9651348961777155289, -0.2617529984165038459 ) ) ;
#248169=DIRECTION ( 'NONE',  ( 0.000000000000000000, 0.2617529984165038459, 0.9651348961777155289 ) ) ;
#248172=CIRCLE ( 'NONE', #135731, 0.1000000000000124678 ) ;
#248187=CARTESIAN_POINT ( 'NONE',  ( -21.04999999999999716, 65.63518786100092939, -242.0677770231893078 ) ) ;
#248220=DIRECTION ( 'NONE',  ( 1.000000000000000000, -0.000000000000000000, -0.000000000000000000 ) ) ;
#248299=EDGE_CURVE ( 'NONE', #151453, #201773, #129993, .T. ) ;
#248327=CIRCLE ( 'NONE', #85794, 4.150000000000003020 ) ;
#248341=CARTESIAN_POINT ( 'NONE',  ( -21.93642651522410247, 60.15957072538983397, -233.9372187734386443 ) ) ;
#248351=CIRCLE ( 'NONE', #44178, 0.09999999999999543976 ) ;
#248411=EDGE_LOOP ( 'NONE', ( #130608, #14981, #226782, #42627 ) ) ;
#248419=DIRECTION ( 'NONE',  ( -2.602085213965226419E-14, -0.2617529984165031243, -0.9651348961777157509 ) ) ;
#248423=CARTESIAN_POINT ( 'NONE',  ( -20.54999999999999716, 63.44052078637213299, -222.1345147897817185 ) ) ;
#248424=DIRECTION ( 'NONE',  ( 1.000000000000000000, 0.000000000000000000, -0.000000000000000000 ) ) ;
#248435=AXIS2_PLACEMENT_3D ( 'NONE', #4978, #23321, #85789 ) ;
#248445=DIRECTION ( 'NONE',  ( 0.000000000000000000, 0.2617529984165033463, 0.9651348961777157509 ) ) ;
#248447=VERTEX_POINT ( 'NONE', #1589 ) ;
#248475=FACE_OUTER_BOUND ( 'NONE', #216510, .T. ) ;
#248487=DIRECTION ( 'NONE',  ( 0.000000000000000000, 0.7106264324241517993, -0.7035695228903270371 ) ) ;
#248512=AXIS2_PLACEMENT_3D ( 'NONE', #43694, #201468, #240608 ) ;
#248535=CARTESIAN_POINT ( 'NONE',  ( 23.14999999999999503, 66.47189219944506533, -213.6315278230738102 ) ) ;
#248546=LINE ( 'NONE', #49056, #147756 ) ;
#248567=VERTEX_POINT ( 'NONE', #204921 ) ;
#248570=FACE_OUTER_BOUND ( 'NONE', #89638, .T. ) ;
#248635=AXIS2_PLACEMENT_3D ( 'NONE', #229034, #246025, #129908 ) ;
#248637=ADVANCED_FACE ( 'NONE', ( #203656 ), #118360, .T. ) ;
#248689=CARTESIAN_POINT ( 'NONE',  ( -18.59999999999999787, 68.48451787451661232, -224.2224406095231757 ) ) ;
#248707=DIRECTION ( 'NONE',  ( 1.000000000000000000, -2.849773892568378313E-16, 7.728835255496647986E-17 ) ) ;
#248737=FACE_OUTER_BOUND ( 'NONE', #231656, .T. ) ;
#248740=AXIS2_PLACEMENT_3D ( 'NONE', #208676, #168292, #70469 ) ;
#248781=CARTESIAN_POINT ( 'NONE',  ( -21.05000000000000071, 70.47363787294415260, -228.3418745167492432 ) ) ;
#248785=CYLINDRICAL_SURFACE ( 'NONE', #53038, 0.1000000000000124678 ) ;
#248797=EDGE_LOOP ( 'NONE', ( #33738, #234458, #55639, #59332 ) ) ;
#248800=ORIENTED_EDGE ( 'NONE', *, *, #225668, .T. ) ;
#248817=CARTESIAN_POINT ( 'NONE',  ( -20.95613430942416144, 57.68582240677151418, -226.1614418145203445 ) ) ;
#248822=VERTEX_POINT ( 'NONE', #101293 ) ;
#248844=CARTESIAN_POINT ( 'NONE',  ( 23.15000000000000213, 82.57900542960499024, -215.5587758314583766 ) ) ;
#248845=ORIENTED_EDGE ( 'NONE', *, *, #196733, .T. ) ;
#248873=DIRECTION ( 'NONE',  ( 0.000000000000000000, 0.2617529984165038459, 0.9651348961777155289 ) ) ;
#248874=CARTESIAN_POINT ( 'NONE',  ( -18.50000000000000000, 86.87366311306884370, -199.3414869250131858 ) ) ;
#248879=VECTOR ( 'NONE', #128521, 1000.000000000000000 ) ;
#248896=ORIENTED_EDGE ( 'NONE', *, *, #34460, .T. ) ;
#248916=EDGE_LOOP ( 'NONE', ( #60117, #100734, #19131, #53397 ) ) ;
#248924=CARTESIAN_POINT ( 'NONE',  ( 20.99749315643148151, 62.82351852664101699, -207.2177435904691833 ) ) ;
#248929=CARTESIAN_POINT ( 'NONE',  ( -18.59999999999999787, 86.96699927712941758, -199.3055931863049466 ) ) ;
#248944=DIRECTION ( 'NONE',  ( 0.000000000000000000, 0.9651348961777157509, -0.2617529984165031243 ) ) ;
#248970=DIRECTION ( 'NONE',  ( -0.000000000000000000, 0.9651348961777157509, -0.2617529984165031243 ) ) ;
#248984=ORIENTED_EDGE ( 'NONE', *, *, #207671, .T. ) ;
#248992=CARTESIAN_POINT ( 'NONE',  ( 20.77766267348355811, 59.13395343506662272, -225.7920699989196294 ) ) ;
#249005=EDGE_CURVE ( 'NONE', #222414, #232695, #192198, .T. ) ;
#249028=CARTESIAN_POINT ( 'NONE',  ( 20.94999999999999929, 75.47649400317826007, -205.4533772768803317 ) ) ;
#249033=EDGE_CURVE ( 'NONE', #84512, #42158, #117175, .T. ) ;
#249034=VERTEX_POINT ( 'NONE', #90756 ) ;
#249041=AXIS2_PLACEMENT_3D ( 'NONE', #198626, #162097, #4268 ) ;
#249052=DIRECTION ( 'NONE',  ( 0.000000000000000000, -0.9651348961777158619, 0.2617529984165032353 ) ) ;
#249060=DIRECTION ( 'NONE',  ( -1.000000000000000000, -0.000000000000000000, -0.000000000000000000 ) ) ;
#249075=ORIENTED_EDGE ( 'NONE', *, *, #219576, .T. ) ;
#249090=AXIS2_PLACEMENT_3D ( 'NONE', #256680, #37714, #117229 ) ;
#249095=CIRCLE ( 'NONE', #32441, 0.1000000000000000333 ) ;
#249119=DIRECTION ( 'NONE',  ( 0.7070776581709139474, 0.6824815363281155900, -0.1850949428989116519 ) ) ;
#249136=EDGE_CURVE ( 'NONE', #242569, #195218, #46065, .T. ) ;
#249146=ORIENTED_EDGE ( 'NONE', *, *, #62009, .T. ) ;
#249170=CARTESIAN_POINT ( 'NONE',  ( 23.14999999999999503, 62.92003201576280702, -207.2439188921395612 ) ) ;
#249179=AXIS2_PLACEMENT_3D ( 'NONE', #114100, #230206, #193657 ) ;
#249182=EDGE_CURVE ( 'NONE', #18097, #140929, #54796, .T. ) ;
#249205=CARTESIAN_POINT ( 'NONE',  ( -21.08884785362073089, 65.51921272533262197, -241.9776447927261813 ) ) ;
#249257=CYLINDRICAL_SURFACE ( 'NONE', #248006, 0.1000000000000018374 ) ;
#249263=DIRECTION ( 'NONE',  ( -1.000000000000000000, -0.000000000000000000, 0.000000000000000000 ) ) ;
#249278=CARTESIAN_POINT ( 'NONE',  ( -20.94999999999999929, 87.19425987394825484, -209.6674621343692024 ) ) ;
#249301=VERTEX_POINT ( 'NONE', #46446 ) ;
#249314=AXIS2_PLACEMENT_3D ( 'NONE', #245236, #243927, #30057 ) ;
#249371=VERTEX_POINT ( 'NONE', #184675 ) ;
#249390=ORIENTED_EDGE ( 'NONE', *, *, #163691, .T. ) ;
#249393=DIRECTION ( 'NONE',  ( -0.000000000000000000, -0.2617529984165031243, -0.9651348961777157509 ) ) ;
#249409=AXIS2_PLACEMENT_3D ( 'NONE', #226578, #144469, #243593 ) ;
#249446=CARTESIAN_POINT ( 'NONE',  ( -23.15000000000000213, 76.54968129668591814, -201.4963242025517047 ) ) ;
#249475=AXIS2_PLACEMENT_3D ( 'NONE', #79445, #162880, #58598 ) ;
#249499=CYLINDRICAL_SURFACE ( 'NONE', #29900, 0.1000000000000124678 ) ;
#249527=ORIENTED_EDGE ( 'NONE', *, *, #89469, .F. ) ;
#249562=EDGE_CURVE ( 'NONE', #181858, #211733, #5071, .T. ) ;
#249570=ORIENTED_EDGE ( 'NONE', *, *, #37632, .T. ) ;
#249595=ADVANCED_FACE ( 'NONE', ( #180540 ), #56615, .T. ) ;
#249601=AXIS2_PLACEMENT_3D ( 'NONE', #47414, #146509, #29205 ) ;
#249608=ORIENTED_EDGE ( 'NONE', *, *, #80169, .T. ) ;
#249628=EDGE_CURVE ( 'NONE', #70163, #40334, #159250, .T. ) ;
#249629=EDGE_LOOP ( 'NONE', ( #73198, #93070, #99790, #103365 ) ) ;
#249639=EDGE_LOOP ( 'NONE', ( #103680, #86748, #33441, #76611 ) ) ;
#249645=DIRECTION ( 'NONE',  ( 0.000000000000000000, 0.7092521942343630315, 0.7049548389604409770 ) ) ;
#249650=DIRECTION ( 'NONE',  ( 0.000000000000000000, 0.2617529984165152257, 0.9651348961777124202 ) ) ;
#249656=CARTESIAN_POINT ( 'NONE',  ( -20.85000000000000142, 79.28756800457986742, -196.2274082906208434 ) ) ;
#249662=AXIS2_PLACEMENT_3D ( 'NONE', #199843, #40780, #159424 ) ;
#249682=B_SPLINE_CURVE_WITH_KNOTS ( 'NONE', 3,
 ( #154635, #199858, #214563, #150752, #112911, #133746 ),
 .UNSPECIFIED., .F., .F.,
 ( 4, 2, 4 ),
 ( 0.000000000000000000, 0.0001895189928937394052, 0.0003790379857874788105 ),
 .UNSPECIFIED. ) ;
#249714=CARTESIAN_POINT ( 'NONE',  ( -22.39999999999999858, 65.19201463318205469, -243.3742797652979561 ) ) ;
#249758=CARTESIAN_POINT ( 'NONE',  ( 18.49999999999999289, 52.91185528119410009, -244.1460391050142675 ) ) ;
#249759=AXIS2_PLACEMENT_3D ( 'NONE', #48114, #185058, #127666 ) ;
#249787=EDGE_LOOP ( 'NONE', ( #171127, #15987, #69156, #123438 ) ) ;
#249840=ORIENTED_EDGE ( 'NONE', *, *, #10747, .T. ) ;
#249843=ORIENTED_EDGE ( 'NONE', *, *, #148057, .F. ) ;
#249883=DIRECTION ( 'NONE',  ( 0.000000000000000000, 0.2617529984165031243, 0.9651348961777157509 ) ) ;
#249891=CIRCLE ( 'NONE', #99829, 0.09999999999999918676 ) ;
#249900=FACE_OUTER_BOUND ( 'NONE', #201220, .T. ) ;
#249901=EDGE_CURVE ( 'NONE', #116241, #90831, #105009, .T. ) ;
#249927=CARTESIAN_POINT ( 'NONE',  ( -20.64999999999999858, 76.00000000001126921, -203.5231074845248997 ) ) ;
#249931=CARTESIAN_POINT ( 'NONE',  ( 18.50596464788227280, 67.49374512151688066, -195.5131169347613707 ) ) ;
#249961=ORIENTED_EDGE ( 'NONE', *, *, #191362, .T. ) ;
#249975=CARTESIAN_POINT ( 'NONE',  ( -20.94999999999999929, 67.63082410804655353, -211.8415745842588649 ) ) ;
#249977=CYLINDRICAL_SURFACE ( 'NONE', #156820, 0.09999999999999939493 ) ;
#250018=ORIENTED_EDGE ( 'NONE', *, *, #62450, .F. ) ;
#250038=ORIENTED_EDGE ( 'NONE', *, *, #55190, .F. ) ;
#250042=VERTEX_POINT ( 'NONE', #26296 ) ;
#250065=DIRECTION ( 'NONE',  ( -1.000000000000000000, -0.000000000000000000, -0.000000000000000000 ) ) ;
#250154=CARTESIAN_POINT ( 'NONE',  ( -20.64999999999999858, 65.77012247227901298, -213.5448142138000378 ) ) ;
#250185=DIRECTION ( 'NONE',  ( 0.000000000000000000, 0.9667078373770113808, 0.2558827019434133376 ) ) ;
#250199=VECTOR ( 'NONE', #81, 1000.000000000000000 ) ;
#250209=DIRECTION ( 'NONE',  ( 0.000000000000000000, 0.1144908148674362580, 0.9934243067848653741 ) ) ;
#250222=DIRECTION ( 'NONE',  ( 0.000000000000000000, -0.9651348961777028723, 0.2617529984165503087 ) ) ;
#250238=CARTESIAN_POINT ( 'NONE',  ( 20.94999999999999929, 67.92720994251783395, -214.1870976236629929 ) ) ;
#250239=CARTESIAN_POINT ( 'NONE',  ( -18.50000000000000000, 63.89220327960687484, -212.8282812377314883 ) ) ;
#250257=CARTESIAN_POINT ( 'NONE',  ( 20.41140022480518823, 59.17705388698332314, -225.7806615260952015 ) ) ;
#250261=AXIS2_PLACEMENT_3D ( 'NONE', #138116, #81980, #1173 ) ;
#250274=ADVANCED_FACE ( 'NONE', ( #114810 ), #18275, .F. ) ;
#250282=VERTEX_POINT ( 'NONE', #78239 ) ;
#250285=LINE ( 'NONE', #211159, #80508 ) ;
#250313=DIRECTION ( 'NONE',  ( 0.000000000000000000, -0.2617529984165152257, -0.9651348961777124202 ) ) ;
#250327=AXIS2_PLACEMENT_3D ( 'NONE', #159158, #177443, #179992 ) ;
#250378=VERTEX_POINT ( 'NONE', #17011 ) ;
#250380=CARTESIAN_POINT ( 'NONE',  ( 20.94999999999999929, 86.48473784507378070, -209.3714211149925575 ) ) ;
#250399=LINE ( 'NONE', #186599, #167414 ) ;
#250400=DIRECTION ( 'NONE',  ( -0.7071067811865475727, 0.6824534298470373850, -0.1850873201762210096 ) ) ;
#250410=CARTESIAN_POINT ( 'NONE',  ( 21.14999999999999858, 70.41157348381892689, -224.1287375179191201 ) ) ;
#250418=DIRECTION ( 'NONE',  ( 0.000000000000000000, -0.2617529984165152257, -0.9651348961777124202 ) ) ;
#250460=ORIENTED_EDGE ( 'NONE', *, *, #133924, .F. ) ;
#250467=CARTESIAN_POINT ( 'NONE',  ( -21.14250536705909411, 65.52512344156484403, -242.1460419336806638 ) ) ;
#250473=DIRECTION ( 'NONE',  ( 0.000000000000000000, -0.9651348961777157509, 0.2617529984165031243 ) ) ;
#250522=FACE_OUTER_BOUND ( 'NONE', #153459, .T. ) ;
#250540=DIRECTION ( 'NONE',  ( 0.000000000000000000, 0.1071148137998806232, 0.9942466578594150173 ) ) ;
#250542=VERTEX_POINT ( 'NONE', #170677 ) ;
#250566=ORIENTED_EDGE ( 'NONE', *, *, #83812, .T. ) ;
#250590=EDGE_LOOP ( 'NONE', ( #244752, #101578, #83170, #188295 ) ) ;
#250625=ORIENTED_EDGE ( 'NONE', *, *, #253871, .T. ) ;
#250640=ORIENTED_EDGE ( 'NONE', *, *, #204088, .F. ) ;
#250657=CARTESIAN_POINT ( 'NONE',  ( -23.15000000000000213, 67.23127455305841238, -235.8551265064783991 ) ) ;
#250665=CARTESIAN_POINT ( 'NONE',  ( -18.54118089899633048, 78.20985128365940398, -231.5294076491229589 ) ) ;
#250683=AXIS2_PLACEMENT_3D ( 'NONE', #4822, #144329, #166523 ) ;
#250689=ORIENTED_EDGE ( 'NONE', *, *, #110469, .F. ) ;
#250754=DIRECTION ( 'NONE',  ( 0.000000000000000000, 0.2617529984165045120, 0.9651348961777153068 ) ) ;
#250786=AXIS2_PLACEMENT_3D ( 'NONE', #3332, #200278, #141578 ) ;
#250787=CARTESIAN_POINT ( 'NONE',  ( 18.39999999999999858, 86.89640087696871262, -199.6396878666313341 ) ) ;
#250798=CARTESIAN_POINT ( 'NONE',  ( -21.05000000000000071, 70.42128727326085880, -228.5349014959848262 ) ) ;
#250808=AXIS2_PLACEMENT_3D ( 'NONE', #19890, #194693, #156848 ) ;
#250827=CIRCLE ( 'NONE', #96864, 11.65000000000000391 ) ;
#250846=CARTESIAN_POINT ( 'NONE',  ( -18.59999999999999787, 70.47363787294415260, -228.3418745167492432 ) ) ;
#250859=AXIS2_PLACEMENT_3D ( 'NONE', #121666, #239026, #241590 ) ;
#250870=EDGE_CURVE ( 'NONE', #85926, #101417, #117858, .T. ) ;
#250884=AXIS2_PLACEMENT_3D ( 'NONE', #252729, #250185, #228055 ) ;
#250938=ORIENTED_EDGE ( 'NONE', *, *, #111242, .F. ) ;
#250951=ORIENTED_EDGE ( 'NONE', *, *, #170709, .T. ) ;
#250952=CARTESIAN_POINT ( 'NONE',  ( 21.08750232978087524, 60.08127493647409523, -221.2453635944128791 ) ) ;
#251009=TOROIDAL_SURFACE ( 'NONE', #217869, 1.900000000000002576, 0.1000000000000000056 ) ;
#251042=AXIS2_PLACEMENT_3D ( 'NONE', #181337, #5212, #99183 ) ;
#251048=CARTESIAN_POINT ( 'NONE',  ( 20.94999999999999929, 82.57900542960499024, -215.5587758314583766 ) ) ;
#251062=EDGE_CURVE ( 'NONE', #94361, #40333, #26517, .T. ) ;
#251066=AXIS2_PLACEMENT_3D ( 'NONE', #179643, #214899, #16717 ) ;
#251107=EDGE_LOOP ( 'NONE', ( #212157, #176083, #247999, #179792, #44204, #32662, #2880, #134797 ) ) ;
#251137=ORIENTED_EDGE ( 'NONE', *, *, #120153, .T. ) ;
#251151=CIRCLE ( 'NONE', #188825, 2.099999999999995204 ) ;
#251185=DIRECTION ( 'NONE',  ( 1.000000000000000000, 0.000000000000000000, 0.000000000000000000 ) ) ;
#251231=ORIENTED_EDGE ( 'NONE', *, *, #249033, .T. ) ;
#251232=VERTEX_POINT ( 'NONE', #104547 ) ;
#251233=CYLINDRICAL_SURFACE ( 'NONE', #99487, 11.75000000000000178 ) ;
#251240=DIRECTION ( 'NONE',  ( 0.000000000000000000, -0.2617529984165031243, -0.9651348961777157509 ) ) ;
#251246=VECTOR ( 'NONE', #109152, 1000.000000000000000 ) ;
#251252=VERTEX_POINT ( 'NONE', #61605 ) ;
#251303=CARTESIAN_POINT ( 'NONE',  ( -21.05000000000000071, 72.02722222756958104, -225.1832529173024398 ) ) ;
#251321=DIRECTION ( 'NONE',  ( 1.000000000000000000, -0.000000000000000000, 0.000000000000000000 ) ) ;
#251333=AXIS2_PLACEMENT_3D ( 'NONE', #194822, #18725, #53996 ) ;
#251340=AXIS2_PLACEMENT_3D ( 'NONE', #165047, #245870, #187199 ) ;
#251351=ORIENTED_EDGE ( 'NONE', *, *, #88917, .F. ) ;
#251355=VECTOR ( 'NONE', #48193, 1000.000000000000000 ) ;
#251360=CARTESIAN_POINT ( 'NONE',  ( 18.60000000000000497, 67.23127455305841238, -235.8551265064783991 ) ) ;
#251363=CARTESIAN_POINT ( 'NONE',  ( -21.05000000000000071, 57.76315019072730905, -226.2583585926041110 ) ) ;
#251448=AXIS2_PLACEMENT_3D ( 'NONE', #29371, #188397, #8491 ) ;
#251461=FACE_OUTER_BOUND ( 'NONE', #18625, .T. ) ;
#251475=ORIENTED_EDGE ( 'NONE', *, *, #65694, .T. ) ;
#251508=CARTESIAN_POINT ( 'NONE',  ( -23.25000000000000000, 67.23127455305841238, -235.8551265064783991 ) ) ;
#251516=ORIENTED_EDGE ( 'NONE', *, *, #80520, .T. ) ;
#251526=ORIENTED_EDGE ( 'NONE', *, *, #94314, .T. ) ;
#251532=CARTESIAN_POINT ( 'NONE',  ( 20.97438252431638972, 60.83470529572428376, -225.3418895363082868 ) ) ;
#251550=ORIENTED_EDGE ( 'NONE', *, *, #65280, .F. ) ;
#251557=CARTESIAN_POINT ( 'NONE',  ( 20.85000000000000142, 78.06784868750165174, -195.8985418047209350 ) ) ;
#251591=ORIENTED_EDGE ( 'NONE', *, *, #106139, .T. ) ;
#251599=DIRECTION ( 'NONE',  ( 0.000000000000000000, 0.2617529984164915779, 0.9651348961777189706 ) ) ;
#251635=EDGE_CURVE ( 'NONE', #29429, #2330, #205933, .T. ) ;
#251692=CARTESIAN_POINT ( 'NONE',  ( -20.64999999999999858, 68.76258920191057200, -222.5680764032308048 ) ) ;
#251693=EDGE_CURVE ( 'NONE', #72701, #146536, #149836, .T. ) ;
#251736=ORIENTED_EDGE ( 'NONE', *, *, #227989, .T. ) ;
#251764=DIRECTION ( 'NONE',  ( 1.000000000000000000, 0.000000000000000000, 0.000000000000000000 ) ) ;
#251785=DIRECTION ( 'NONE',  ( 2.952720810173289112E-16, 0.9651348961777159730, -0.2617529984165024026 ) ) ;
#251815=VERTEX_POINT ( 'NONE', #136653 ) ;
#251821=CARTESIAN_POINT ( 'NONE',  ( 20.95561247346651967, 58.99335862822155718, -225.7528268179844417 ) ) ;
#251874=ADVANCED_FACE ( 'NONE', ( #238330 ), #134089, .T. ) ;
#251875=EDGE_CURVE ( 'NONE', #255232, #160843, #68751, .T. ) ;
#251878=AXIS2_PLACEMENT_3D ( 'NONE', #66401, #68989, #25996 ) ;
#251887=CARTESIAN_POINT ( 'NONE',  ( -23.15000000000000213, 68.29137419664525055, -231.9463301769586394 ) ) ;
#251892=ORIENTED_EDGE ( 'NONE', *, *, #63372, .F. ) ;
#251909=EDGE_CURVE ( 'NONE', #54640, #167923, #25708, .T. ) ;
#251924=CARTESIAN_POINT ( 'NONE',  ( -23.25000000000000000, 74.97916330618691916, -207.2871335796180006 ) ) ;
#251928=DIRECTION ( 'NONE',  ( -1.000000000000000000, 7.049440681616512959E-16, -1.911869773728117674E-16 ) ) ;
#251986=DIRECTION ( 'NONE',  ( 1.000000000000000000, 0.000000000000000000, 0.000000000000000000 ) ) ;
#252001=ORIENTED_EDGE ( 'NONE', *, *, #152786, .F. ) ;
#252005=DIRECTION ( 'NONE',  ( 0.000000000000000000, 0.2617529984165031243, 0.9651348961777157509 ) ) ;
#252009=EDGE_CURVE ( 'NONE', #184365, #29429, #218563, .T. ) ;
#252012=ADVANCED_FACE ( 'NONE', ( #119686 ), #20590, .F. ) ;
#252057=VERTEX_POINT ( 'NONE', #12585 ) ;
#252082=ORIENTED_EDGE ( 'NONE', *, *, #60834, .T. ) ;
#252099=VERTEX_POINT ( 'NONE', #92093 ) ;
#252147=CARTESIAN_POINT ( 'NONE',  ( -22.00356870141068200, 60.22995210368382146, -233.9563068168642133 ) ) ;
#252152=ORIENTED_EDGE ( 'NONE', *, *, #151073, .T. ) ;
#252159=ORIENTED_EDGE ( 'NONE', *, *, #178084, .T. ) ;
#252173=ORIENTED_EDGE ( 'NONE', *, *, #107874, .T. ) ;
#252174=EDGE_CURVE ( 'NONE', #213246, #248567, #222858, .T. ) ;
#252191=ORIENTED_EDGE ( 'NONE', *, *, #111242, .T. ) ;
#252245=CARTESIAN_POINT ( 'NONE',  ( 21.07189867249812210, 60.07686761660588814, -221.2611677080064965 ) ) ;
#252254=VERTEX_POINT ( 'NONE', #75133 ) ;
#252258=CARTESIAN_POINT ( 'NONE',  ( -22.48970261584618058, 55.97295988302631997, -232.8591431001882484 ) ) ;
#252294=CARTESIAN_POINT ( 'NONE',  ( -21.95218792049439216, 65.25068255281803431, -242.7796317678790956 ) ) ;
#252318=DIRECTION ( 'NONE',  ( 1.000000000000000000, 0.000000000000000000, 0.000000000000000000 ) ) ;
#252324=CIRCLE ( 'NONE', #164871, 0.1000000000000124678 ) ;
#252329=VERTEX_POINT ( 'NONE', #223579 ) ;
#252330=FACE_OUTER_BOUND ( 'NONE', #76108, .T. ) ;
#252361=AXIS2_PLACEMENT_3D ( 'NONE', #3006, #222041, #82527 ) ;
#252364=ORIENTED_EDGE ( 'NONE', *, *, #212339, .T. ) ;
#252365=FACE_OUTER_BOUND ( 'NONE', #172174, .T. ) ;
#252387=ORIENTED_EDGE ( 'NONE', *, *, #12381, .F. ) ;
#252390=CARTESIAN_POINT ( 'NONE',  ( 22.49999999999999645, 55.96169194136206215, -232.9023299069559130 ) ) ;
#252393=ORIENTED_EDGE ( 'NONE', *, *, #126606, .F. ) ;
#252411=FACE_OUTER_BOUND ( 'NONE', #159122, .T. ) ;
#252439=ORIENTED_EDGE ( 'NONE', *, *, #243642, .F. ) ;
#252460=ORIENTED_EDGE ( 'NONE', *, *, #152368, .T. ) ;
#252463=CARTESIAN_POINT ( 'NONE',  ( 22.49436431346199683, 55.96998815520995407, -232.8702878457373231 ) ) ;
#252477=DIRECTION ( 'NONE',  ( -1.000000000000000000, -0.000000000000000000, 0.000000000000000000 ) ) ;
#252505=DIRECTION ( 'NONE',  ( -0.000000000000000000, 0.3848449534832604213, 0.9229812358756095403 ) ) ;
#252508=EDGE_CURVE ( 'NONE', #24254, #128036, #52342, .T. ) ;
#252530=CARTESIAN_POINT ( 'NONE',  ( 23.14999999999999503, 66.37537870982728805, -213.6053525232321704 ) ) ;
#252541=ADVANCED_FACE ( 'NONE', ( #103193 ), #241451, .F. ) ;
#252559=ORIENTED_EDGE ( 'NONE', *, *, #245017, .T. ) ;
#252574=AXIS2_PLACEMENT_3D ( 'NONE', #172873, #33356, #52862 ) ;
#252588=CARTESIAN_POINT ( 'NONE',  ( 20.95512820512820440, 60.17125644644785609, -221.2995001548250684 ) ) ;
#252595=EDGE_LOOP ( 'NONE', ( #144482, #99786, #28054, #130118 ) ) ;
#252597=VERTEX_POINT ( 'NONE', #203596 ) ;
#252606=DIRECTION ( 'NONE',  ( -0.000000000000000000, 0.9651348961777157509, -0.2617529984165031243 ) ) ;
#252637=CARTESIAN_POINT ( 'NONE',  ( -20.94999999999999929, 57.68174901751925177, -226.1764612035511846 ) ) ;
#252650=DIRECTION ( 'NONE',  ( -1.000000000000000000, 0.000000000000000000, 0.000000000000000000 ) ) ;
#252657=CARTESIAN_POINT ( 'NONE',  ( -20.64999999999999858, 67.23127455305841238, -235.8551265064783991 ) ) ;
#252668=AXIS2_PLACEMENT_3D ( 'NONE', #163450, #47327, #206423 ) ;
#252708=AXIS2_PLACEMENT_3D ( 'NONE', #195918, #1534, #39425 ) ;
#252729=CARTESIAN_POINT ( 'NONE',  ( 20.94999999999999574, 55.13994374908182294, -226.9527081427897315 ) ) ;
#252764=CARTESIAN_POINT ( 'NONE',  ( -18.39999999999999858, 78.24390740893980478, -231.6169762517609172 ) ) ;
#252771=LINE ( 'NONE', #194121, #77147 ) ;
#252812=CARTESIAN_POINT ( 'NONE',  ( 20.54374330479356914, 59.11474337034464099, -225.6490816854725949 ) ) ;
#252830=VECTOR ( 'NONE', #170136, 1000.000000000000000 ) ;
#252831=CARTESIAN_POINT ( 'NONE',  ( 21.70464131381650219, 60.38329692807814553, -233.9978952701749506 ) ) ;
#252891=AXIS2_PLACEMENT_3D ( 'NONE', #59868, #42907, #122447 ) ;
#252911=EDGE_CURVE ( 'NONE', #129114, #257242, #21777, .T. ) ;
#252920=CARTESIAN_POINT ( 'NONE',  ( -18.50000000000000000, 76.00000000001126921, -203.5231074845248997 ) ) ;
#252929=CARTESIAN_POINT ( 'NONE',  ( -23.25000000000000000, 66.14499960962993441, -239.8604363256158933 ) ) ;
#252932=VERTEX_POINT ( 'NONE', #116068 ) ;
#252969=DIRECTION ( 'NONE',  ( -0.000000000000000000, 0.9667078373770112698, 0.2558827019434132821 ) ) ;
#252997=EDGE_LOOP ( 'NONE', ( #11147, #110984, #2378, #198430 ) ) ;
#253012=ORIENTED_EDGE ( 'NONE', *, *, #143468, .F. ) ;
#253075=CARTESIAN_POINT ( 'NONE',  ( 21.05000000000000071, 60.83337574417770810, -225.3422414619149095 ) ) ;
#253102=CARTESIAN_POINT ( 'NONE',  ( -20.54999999999999716, 67.23127455305841238, -235.8551265064783991 ) ) ;
#253128=VERTEX_POINT ( 'NONE', #115567 ) ;
#253129=CIRCLE ( 'NONE', #28322, 0.3999999999999926392 ) ;
#253139=EDGE_LOOP ( 'NONE', ( #39566, #255668, #131829, #34766 ) ) ;
#253222=DIRECTION ( 'NONE',  ( 0.000000000000000000, -0.7106264324241465813, 0.7035695228903323661 ) ) ;
#253235=LINE ( 'NONE', #217949, #207888 ) ;
#253246=CARTESIAN_POINT ( 'NONE',  ( 20.85000000000000142, 86.58125133469154378, -209.3975964148341973 ) ) ;
#253251=CIRCLE ( 'NONE', #120022, 0.09999999999999939493 ) ;
#253259=ORIENTED_EDGE ( 'NONE', *, *, #225547, .F. ) ;
#253325=ORIENTED_EDGE ( 'NONE', *, *, #179024, .T. ) ;
#253330=CARTESIAN_POINT ( 'NONE',  ( -20.94999999999999929, 79.33069327855442054, -236.1318330389568985 ) ) ;
#253350=EDGE_CURVE ( 'NONE', #150591, #4584, #14780, .T. ) ;
#253368=DIRECTION ( 'NONE',  ( -1.000000000000000000, 0.000000000000000000, 0.000000000000000000 ) ) ;
#253403=ORIENTED_EDGE ( 'NONE', *, *, #55642, .T. ) ;
#253425=AXIS2_PLACEMENT_3D ( 'NONE', #17000, #96496, #176088 ) ;
#253431=CARTESIAN_POINT ( 'NONE',  ( -21.07094088545304800, 61.10557489434068401, -234.2962495489933872 ) ) ;
#253499=AXIS2_PLACEMENT_3D ( 'NONE', #82586, #26523, #64355 ) ;
#253520=CARTESIAN_POINT ( 'NONE',  ( -20.94999999999999929, 76.00000000001126921, -203.5231074845248997 ) ) ;
#253521=ORIENTED_EDGE ( 'NONE', *, *, #148583, .T. ) ;
#253525=AXIS2_PLACEMENT_3D ( 'NONE', #168852, #183239, #247042 ) ;
#253532=ORIENTED_EDGE ( 'NONE', *, *, #41732, .F. ) ;
#253533=DIRECTION ( 'NONE',  ( -0.000000000000000000, 0.9651348961777157509, -0.2617529984165031243 ) ) ;
#253583=FACE_OUTER_BOUND ( 'NONE', #82523, .T. ) ;
#253596=CARTESIAN_POINT ( 'NONE',  ( -21.05000000000000071, 86.45856254523214091, -209.4679346046102921 ) ) ;
#253606=VECTOR ( 'NONE', #41373, 1000.000000000000000 ) ;
#253611=DIRECTION ( 'NONE',  ( 0.000000000000000000, -0.7049548389605068133, 0.7092521942342977503 ) ) ;
#253614=CARTESIAN_POINT ( 'NONE',  ( -20.54999999999999716, 78.37638820354418101, -229.1444560783390898 ) ) ;
#253638=EDGE_CURVE ( 'NONE', #180985, #191649, #84810, .T. ) ;
#253660=CARTESIAN_POINT ( 'NONE',  ( -18.50000000000000000, 59.19392724319018129, -220.9828015967491126 ) ) ;
#253672=AXIS2_PLACEMENT_3D ( 'NONE', #42037, #17332, #219361 ) ;
#253677=ORIENTED_EDGE ( 'NONE', *, *, #205688, .T. ) ;
#253680=FACE_OUTER_BOUND ( 'NONE', #8065, .T. ) ;
#253682=AXIS2_PLACEMENT_3D ( 'NONE', #72069, #92888, #89037 ) ;
#253686=ADVANCED_FACE ( 'NONE', ( #23905 ), #103382, .F. ) ;
#253687=ORIENTED_EDGE ( 'NONE', *, *, #98462, .T. ) ;
#253702=DIRECTION ( 'NONE',  ( 0.000000000000000000, 0.2617529984165152257, 0.9651348961777124202 ) ) ;
#253717=CYLINDRICAL_SURFACE ( 'NONE', #231793, 0.09999999999999939493 ) ;
#253718=CARTESIAN_POINT ( 'NONE',  ( -23.15000000000000213, 86.45856254523214091, -209.4679346046102921 ) ) ;
#253728=ORIENTED_EDGE ( 'NONE', *, *, #221477, .F. ) ;
#253729=CARTESIAN_POINT ( 'NONE',  ( 21.05000000000000071, 61.16604239671103471, -234.3115055913011417 ) ) ;
#253734=ORIENTED_EDGE ( 'NONE', *, *, #120904, .T. ) ;
#253743=CARTESIAN_POINT ( 'NONE',  ( -23.15000000000000213, 67.55989888862310977, -211.9120700681549465 ) ) ;
#253759=DIRECTION ( 'NONE',  ( 1.441126678808781001E-14, -0.9942466578594195692, 0.1071148137998398919 ) ) ;
#253763=CARTESIAN_POINT ( 'NONE',  ( 18.42636655943170254, 86.89577902249435226, -199.6303068441001187 ) ) ;
#253798=ORIENTED_EDGE ( 'NONE', *, *, #175034, .F. ) ;
#253807=CARTESIAN_POINT ( 'NONE',  ( 20.46382478191415188, 59.01186707245664564, -225.6707791561468639 ) ) ;
#253829=ORIENTED_EDGE ( 'NONE', *, *, #24328, .F. ) ;
#253831=ORIENTED_EDGE ( 'NONE', *, *, #41153, .F. ) ;
#253863=VECTOR ( 'NONE', #33313, 1000.000000000000114 ) ;
#253871=EDGE_CURVE ( 'NONE', #240058, #151240, #194019, .T. ) ;
#253880=AXIS2_PLACEMENT_3D ( 'NONE', #178903, #98010, #233716 ) ;
#253891=FACE_OUTER_BOUND ( 'NONE', #80590, .T. ) ;
#253915=CARTESIAN_POINT ( 'NONE',  ( -23.25000000000000000, 81.82295291318693842, -214.8938525951558915 ) ) ;
#253924=DIRECTION ( 'NONE',  ( 0.000000000000000000, 0.2617529984164955192, 0.9651348961777178603 ) ) ;
#253961=DIRECTION ( 'NONE',  ( 0.000000000000000000, -0.7049548389605067023, 0.7092521942342977503 ) ) ;
#253992=CARTESIAN_POINT ( 'NONE',  ( -20.94999999999999929, 57.82359945636608956, -226.0354702357591350 ) ) ;
#254038=ORIENTED_EDGE ( 'NONE', *, *, #86400, .F. ) ;
#254069=DIRECTION ( 'NONE',  ( -1.000000000000000000, 2.849773892568378313E-16, -7.728835255496647986E-17 ) ) ;
#254090=CARTESIAN_POINT ( 'NONE',  ( 20.30531438145590784, 59.52703403250789904, -225.6880235420007352 ) ) ;
#254093=DIRECTION ( 'NONE',  ( 0.000000000000000000, 0.2617529984165503087, 0.9651348961777028723 ) ) ;
#254099=AXIS2_PLACEMENT_3D ( 'NONE', #48022, #188824, #207116 ) ;
#254106=VERTEX_POINT ( 'NONE', #106940 ) ;
#254109=CARTESIAN_POINT ( 'NONE',  ( 21.93642651522410603, 60.15957072538984107, -233.9372187734386728 ) ) ;
#254121=CARTESIAN_POINT ( 'NONE',  ( -18.39999999999999858, 86.98067499225015808, -199.3289525933214463 ) ) ;
#254140=ORIENTED_EDGE ( 'NONE', *, *, #125044, .T. ) ;
#254183=DIRECTION ( 'NONE',  ( 0.000000000000000000, -0.3896596508880098009, -0.9209589331071360574 ) ) ;
#254227=AXIS2_PLACEMENT_3D ( 'NONE', #72531, #152075, #186046 ) ;
#254236=ADVANCED_FACE ( 'NONE', ( #129091 ), #13017, .F. ) ;
#254241=CARTESIAN_POINT ( 'NONE',  ( -23.25000000000000000, 64.65966496992309942, -200.4475097531309586 ) ) ;
#254245=ORIENTED_EDGE ( 'NONE', *, *, #212210, .F. ) ;
#254246=DIRECTION ( 'NONE',  ( 1.000000000000000000, -0.000000000000000000, -0.000000000000000000 ) ) ;
#254264=EDGE_CURVE ( 'NONE', #148565, #78772, #48422, .T. ) ;
#254265=EDGE_CURVE ( 'NONE', #209902, #4726, #131634, .T. ) ;
#254270=TOROIDAL_SURFACE ( 'NONE', #141850, 0.2000000000000000111, 0.1000000000000000056 ) ;
#254282=AXIS2_PLACEMENT_3D ( 'NONE', #37026, #156974, #59089 ) ;
#254305=CARTESIAN_POINT ( 'NONE',  ( -21.08621493067320785, 65.51509213395192432, -241.9683428252619706 ) ) ;
#254371=CIRCLE ( 'NONE', #175311, 0.09999999999999939493 ) ;
#254378=AXIS2_PLACEMENT_3D ( 'NONE', #85013, #185434, #199879 ) ;
#254394=ORIENTED_EDGE ( 'NONE', *, *, #8809, .T. ) ;
#254413=CARTESIAN_POINT ( 'NONE',  ( -23.15000000000000213, 76.00000000001126921, -203.5231074845248997 ) ) ;
#254456=DIRECTION ( 'NONE',  ( 0.000000000000000000, 0.2617529984165031243, 0.9651348961777157509 ) ) ;
#254461=ORIENTED_EDGE ( 'NONE', *, *, #187128, .F. ) ;
#254465=DIRECTION ( 'NONE',  ( 0.000000000000000000, 0.2617529984165083423, 0.9651348961777143076 ) ) ;
#254490=EDGE_CURVE ( 'NONE', #151096, #103650, #231795, .T. ) ;
#254547=ORIENTED_EDGE ( 'NONE', *, *, #210910, .T. ) ;
#254560=DIRECTION ( 'NONE',  ( 0.000000000000000000, 0.7106264324241465813, -0.7035695228903323661 ) ) ;
#254616=ADVANCED_FACE ( 'NONE', ( #194866 ), #16233, .T. ) ;
#254648=FACE_OUTER_BOUND ( 'NONE', #91301, .T. ) ;
#254683=DIRECTION ( 'NONE',  ( 0.000000000000000000, -0.2617529984164915779, -0.9651348961777189706 ) ) ;
#254687=PLANE ( 'NONE',  #102416 ) ;
#254697=ORIENTED_EDGE ( 'NONE', *, *, #197697, .F. ) ;
#254765=DIRECTION ( 'NONE',  ( 1.000000000000000000, -7.049440681616510987E-16, 1.911869773728121864E-16 ) ) ;
#254784=CARTESIAN_POINT ( 'NONE',  ( -18.59999999999999787, 61.57587952878036930, -212.2000740415318774 ) ) ;
#254811=VECTOR ( 'NONE', #218375, 1000.000000000000000 ) ;
#254814=DIRECTION ( 'NONE',  ( 1.000000000000000000, 0.000000000000000000, 0.000000000000000000 ) ) ;
#254822=CARTESIAN_POINT ( 'NONE',  ( -21.05000000000000071, 68.48451787451661232, -224.2224406095231757 ) ) ;
#254845=EDGE_CURVE ( 'NONE', #146449, #155707, #148770, .T. ) ;
#254861=CARTESIAN_POINT ( 'NONE',  ( -18.59999999999999787, 63.79568978998910467, -212.8021059378898485 ) ) ;
#254864=CARTESIAN_POINT ( 'NONE',  ( 20.94999999999999929, 78.50726470275242264, -228.6618886302502176 ) ) ;
#254875=DIRECTION ( 'NONE',  ( 1.000000000000000000, 0.000000000000000000, 0.000000000000000000 ) ) ;
#254879=EDGE_CURVE ( 'NONE', #137789, #229678, #102938, .T. ) ;
#254933=DIRECTION ( 'NONE',  ( 1.000000000000000000, 7.049440681616511973E-16, -1.911869773728117427E-16 ) ) ;
#254990=LINE ( 'NONE', #154709, #176726 ) ;
#255000=DIRECTION ( 'NONE',  ( -1.000000000000000000, -0.000000000000000000, 0.000000000000000000 ) ) ;
#255043=ADVANCED_FACE ( 'NONE', ( #240098 ), #80993, .F. ) ;
#255062=B_SPLINE_CURVE_WITH_KNOTS ( 'NONE', 3,
 ( #245916, #162542, #4706, #33320, #112818, #111532, #51520, #73716, #93241, #52824 ),
 .UNSPECIFIED., .F., .F.,
 ( 4, 2, 2, 2, 4 ),
 ( 0.000000000000000000, 3.990160268014099847E-05, 7.980320536028199694E-05, 0.0001596064107204895363, 0.0003192128214409881257 ),
 .UNSPECIFIED. ) ;
#255074=CARTESIAN_POINT ( 'NONE',  ( -20.64999999999999858, 63.53703427598990316, -222.1606900896233583 ) ) ;
#255081=VERTEX_POINT ( 'NONE', #62742 ) ;
#255084=CIRCLE ( 'NONE', #117771, 0.09999999999999939493 ) ;
#255093=TOROIDAL_SURFACE ( 'NONE', #138588, 0.2000000000000000111, 0.1000000000000000056 ) ;
#255170=ORIENTED_EDGE ( 'NONE', *, *, #204520, .T. ) ;
#255191=B_SPLINE_CURVE_WITH_KNOTS ( 'NONE', 3,
 ( #153428, #171695, #75159, #252463, #73882, #33478, #112977 ),
 .UNSPECIFIED., .F., .F.,
 ( 4, 3, 4 ),
 ( 0.000000000000000000, 3.357501770812408679E-05, 5.199112466348557301E-05 ),
 .UNSPECIFIED. ) ;
#255193=CIRCLE ( 'NONE', #84518, 0.1000000000000124678 ) ;
#255200=ORIENTED_EDGE ( 'NONE', *, *, #190138, .T. ) ;
#255206=DIRECTION ( 'NONE',  ( 1.000000000000000000, 0.000000000000000000, 0.000000000000000000 ) ) ;
#255207=EDGE_CURVE ( 'NONE', #5675, #157096, #220147, .T. ) ;
#255232=VERTEX_POINT ( 'NONE', #247789 ) ;
#255248=CARTESIAN_POINT ( 'NONE',  ( -21.05000000000000071, 79.13126459505528487, -235.8705213229730191 ) ) ;
#255280=CARTESIAN_POINT ( 'NONE',  ( -23.25000000000000000, 68.29137419664525055, -231.9463301769586394 ) ) ;
#255285=CIRCLE ( 'NONE', #113883, 0.1000000000000124678 ) ;
#255288=LINE ( 'NONE', #114555, #135135 ) ;
#255301=LINE ( 'NONE', #55841, #219139 ) ;
#255309=CARTESIAN_POINT ( 'NONE',  ( 18.59999999999999076, 66.34920340998563404, -213.7018660128499334 ) ) ;
#255344=CYLINDRICAL_SURFACE ( 'NONE', #79124, 0.09999999999999939493 ) ;
#255351=ADVANCED_FACE ( 'NONE', ( #169590 ), #69182, .F. ) ;
#255355=AXIS2_PLACEMENT_3D ( 'NONE', #195028, #59308, #158481 ) ;
#255364=AXIS2_PLACEMENT_3D ( 'NONE', #160173, #218815, #121049 ) ;
#255397=DIRECTION ( 'NONE',  ( -1.000000000000000000, 0.000000000000000000, 0.000000000000000000 ) ) ;
#255407=EDGE_LOOP ( 'NONE', ( #177902, #2835, #200656, #180725 ) ) ;
#255500=DIRECTION ( 'NONE',  ( -0.000000000000000000, 0.9651348961777157509, -0.2617529984165031243 ) ) ;
#255521=DIRECTION ( 'NONE',  ( 0.000000000000000000, 0.2617529984165028467, 0.9651348961777158619 ) ) ;
#255549=EDGE_CURVE ( 'NONE', #60383, #138609, #221712, .T. ) ;
#255570=DIRECTION ( 'NONE',  ( 0.000000000000000000, 0.2617529984165065660, 0.9651348961777146407 ) ) ;
#255586=DIRECTION ( 'NONE',  ( 0.000000000000000000, 0.2617529984165032908, 0.9651348961777156399 ) ) ;
#255587=AXIS2_PLACEMENT_3D ( 'NONE', #10366, #50728, #66473 ) ;
#255604=CARTESIAN_POINT ( 'NONE',  ( 20.95512820512820440, 60.90483797576754910, -225.2715357783924333 ) ) ;
#255609=CARTESIAN_POINT ( 'NONE',  ( -23.25000000000000000, 66.26558728512915764, -222.7970849955717938 ) ) ;
#255620=EDGE_LOOP ( 'NONE', ( #256303, #61400, #148100, #94813 ) ) ;
#255624=PLANE ( 'NONE',  #156904 ) ;
#255625=DIRECTION ( 'NONE',  ( 0.000000000000000000, 0.2617529984165055668, 0.9651348961777149738 ) ) ;
#255626=AXIS2_PLACEMENT_3D ( 'NONE', #83220, #141935, #24589 ) ;
#255627=ORIENTED_EDGE ( 'NONE', *, *, #106783, .F. ) ;
#255631=CIRCLE ( 'NONE', #109920, 0.5000000000000014433 ) ;
#255659=CIRCLE ( 'NONE', #130805, 0.1000000000000057648 ) ;
#255668=ORIENTED_EDGE ( 'NONE', *, *, #216381, .F. ) ;
#255678=TOROIDAL_SURFACE ( 'NONE', #251448, 0.2000000000000000111, 0.1000000000000000056 ) ;
#255679=FACE_OUTER_BOUND ( 'NONE', #135626, .T. ) ;
#255695=VERTEX_POINT ( 'NONE', #68865 ) ;
#255721=AXIS2_PLACEMENT_3D ( 'NONE', #224377, #87428, #208699 ) ;
#255725=VERTEX_POINT ( 'NONE', #150955 ) ;
#255732=ORIENTED_EDGE ( 'NONE', *, *, #133247, .T. ) ;
#255762=DIRECTION ( 'NONE',  ( 0.000000000000000000, 0.2617529984165033463, 0.9651348961777157509 ) ) ;
#255772=DIRECTION ( 'NONE',  ( 0.000000000000000000, 0.2617529984165034018, 0.9651348961777157509 ) ) ;
#255774=LINE ( 'NONE', #77172, #157011 ) ;
#255807=LINE ( 'NONE', #138445, #149602 ) ;
#255814=AXIS2_PLACEMENT_3D ( 'NONE', #111285, #92992, #55120 ) ;
#255815=DIRECTION ( 'NONE',  ( -1.000000000000000000, 0.000000000000000000, 0.000000000000000000 ) ) ;
#255820=VECTOR ( 'NONE', #218061, 1000.000000000000000 ) ;
#255825=DIRECTION ( 'NONE',  ( 1.000000000000000000, 0.000000000000000000, -0.000000000000000000 ) ) ;
#255901=ORIENTED_EDGE ( 'NONE', *, *, #210526, .F. ) ;
#255906=ORIENTED_EDGE ( 'NONE', *, *, #147158, .T. ) ;
#255968=AXIS2_PLACEMENT_3D ( 'NONE', #191572, #151147, #12937 ) ;
#255976=ORIENTED_EDGE ( 'NONE', *, *, #83849, .T. ) ;
#255990=ORIENTED_EDGE ( 'NONE', *, *, #208584, .F. ) ;
#255996=EDGE_LOOP ( 'NONE', ( #247808, #249570, #106921, #167118 ) ) ;
#256027=CARTESIAN_POINT ( 'NONE',  ( -20.94999999999999929, 70.22659352830977753, -197.9852579278363578 ) ) ;
#256043=EDGE_CURVE ( 'NONE', #125, #57260, #63697, .T. ) ;
#256047=EDGE_LOOP ( 'NONE', ( #202357, #150136, #20293, #168266 ) ) ;
#256061=EDGE_CURVE ( 'NONE', #8721, #66884, #105358, .T. ) ;
#256063=CARTESIAN_POINT ( 'NONE',  ( -20.94999999999999929, 72.91131461869652242, -214.9116992594219369 ) ) ;
#256066=FACE_OUTER_BOUND ( 'NONE', #176365, .T. ) ;
#256080=ORIENTED_EDGE ( 'NONE', *, *, #249901, .F. ) ;
#256090=DIRECTION ( 'NONE',  ( 0.000000000000000000, 0.2617529984165033463, 0.9651348961777156399 ) ) ;
#256104=CARTESIAN_POINT ( 'NONE',  ( -21.37071067811865532, 62.64842427125413593, -221.9196913089517125 ) ) ;
#256120=DIRECTION ( 'NONE',  ( 0.000000000000000000, 0.2617529984165031243, 0.9651348961777157509 ) ) ;
#256173=LINE ( 'NONE', #253660, #232227 ) ;
#256182=CYLINDRICAL_SURFACE ( 'NONE', #39811, 0.09999999999999939493 ) ;
#256190=ORIENTED_EDGE ( 'NONE', *, *, #201565, .T. ) ;
#256224=AXIS2_PLACEMENT_3D ( 'NONE', #5036, #162886, #48038 ) ;
#256240=CARTESIAN_POINT ( 'NONE',  ( -18.59999999999999787, 79.15532900748003442, -196.2806010913881778 ) ) ;
#256247=DIRECTION ( 'NONE',  ( -0.7071067811865474617, 0.6824534298470372740, -0.1850873201762209819 ) ) ;
#256248=ORIENTED_EDGE ( 'NONE', *, *, #217692, .F. ) ;
#256254=ADVANCED_FACE ( 'NONE', ( #153781 ), #5595, .T. ) ;
#256266=CARTESIAN_POINT ( 'NONE',  ( 22.47809213839789066, 64.14563076733692526, -247.0890968714184055 ) ) ;
#256269=AXIS2_PLACEMENT_3D ( 'NONE', #28636, #37582, #93687 ) ;
#256277=EDGE_CURVE ( 'NONE', #85165, #150222, #201245, .T. ) ;
#256284=AXIS2_PLACEMENT_3D ( 'NONE', #137360, #239048, #240344 ) ;
#256303=ORIENTED_EDGE ( 'NONE', *, *, #256353, .F. ) ;
#256353=EDGE_CURVE ( 'NONE', #42158, #84512, #167977, .T. ) ;
#256356=EDGE_LOOP ( 'NONE', ( #1211, #238904, #156231, #222981 ) ) ;
#256364=FACE_OUTER_BOUND ( 'NONE', #203038, .T. ) ;
#256377=VERTEX_POINT ( 'NONE', #54615 ) ;
#256378=ORIENTED_EDGE ( 'NONE', *, *, #24993, .F. ) ;
#256404=ORIENTED_EDGE ( 'NONE', *, *, #113141, .T. ) ;
#256408=DIRECTION ( 'NONE',  ( -0.000000000000000000, -0.9651348961777157509, 0.2617529984165031243 ) ) ;
#256427=EDGE_CURVE ( 'NONE', #186212, #223374, #88810, .T. ) ;
#256450=AXIS2_PLACEMENT_3D ( 'NONE', #143666, #127969, #224485 ) ;
#256464=EDGE_LOOP ( 'NONE', ( #106368, #141960, #79915, #205983 ) ) ;
#256512=CARTESIAN_POINT ( 'NONE',  ( -20.94999999999999929, 70.65782965956557859, -228.4198064469268559 ) ) ;
#256609=DIRECTION ( 'NONE',  ( 2.659396599871503240E-15, -0.3850724248243104775, 0.9228863568391969530 ) ) ;
#256644=DIRECTION ( 'NONE',  ( -1.000000000000000000, -0.000000000000000000, -0.000000000000000000 ) ) ;
#256647=EDGE_CURVE ( 'NONE', #204435, #143126, #97349, .T. ) ;
#256653=ORIENTED_EDGE ( 'NONE', *, *, #11399, .T. ) ;
#256658=VERTEX_POINT ( 'NONE', #131594 ) ;
#256674=CIRCLE ( 'NONE', #85824, 11.75000000000000533 ) ;
#256680=CARTESIAN_POINT ( 'NONE',  ( 23.15000000000000213, 82.67551891922275331, -215.5849511313000164 ) ) ;
#256688=EDGE_LOOP ( 'NONE', ( #77923, #77754, #213893, #78060 ) ) ;
#256692=CIRCLE ( 'NONE', #6939, 0.1999999999999981515 ) ;
#256770=DIRECTION ( 'NONE',  ( -1.000000000000000000, 0.000000000000000000, 0.000000000000000000 ) ) ;
#256782=DIRECTION ( 'NONE',  ( 1.000000000000000000, 0.000000000000000000, -0.000000000000000000 ) ) ;
#256789=DIRECTION ( 'NONE',  ( 0.000000000000000000, -0.9651348961777157509, 0.2617529984165031243 ) ) ;
#256793=EDGE_CURVE ( 'NONE', #51386, #160519, #30782, .T. ) ;
#256810=CIRCLE ( 'NONE', #15280, 4.049999999999990941 ) ;
#256830=DIRECTION ( 'NONE',  ( 0.000000000000000000, 0.2617529984164564949, 0.9651348961777284075 ) ) ;
#256837=ORIENTED_EDGE ( 'NONE', *, *, #938, .T. ) ;
#256846=CARTESIAN_POINT ( 'NONE',  ( 21.05000000000000071, 65.60157203287515415, -241.9458622313809144 ) ) ;
#256918=LINE ( 'NONE', #216554, #84906 ) ;
#256930=DIRECTION ( 'NONE',  ( 0.000000000000000000, -0.9651348961777155289, 0.2617529984165036794 ) ) ;
#256934=AXIS2_PLACEMENT_3D ( 'NONE', #93901, #13104, #211291 ) ;
#256944=CARTESIAN_POINT ( 'NONE',  ( -23.15000000000000213, 70.60814576644823148, -215.7631455941064189 ) ) ;
#256957=FACE_OUTER_BOUND ( 'NONE', #159399, .T. ) ;
#256980=ORIENTED_EDGE ( 'NONE', *, *, #33969, .T. ) ;
#257008=ORIENTED_EDGE ( 'NONE', *, *, #205688, .F. ) ;
#257025=VECTOR ( 'NONE', #201515, 1000.000000000000000 ) ;
#257057=VECTOR ( 'NONE', #199704, 1000.000000000000000 ) ;
#257068=ORIENTED_EDGE ( 'NONE', *, *, #3372, .T. ) ;
#257069=CARTESIAN_POINT ( 'NONE',  ( 18.50000000000000000, 78.13562659007693867, -231.5603498355943373 ) ) ;
#257082=CIRCLE ( 'NONE', #211356, 0.5000000000000051070 ) ;
#257100=ORIENTED_EDGE ( 'NONE', *, *, #216233, .F. ) ;
#257105=DIRECTION ( 'NONE',  ( 0.000000000000000000, -0.2617529984165024026, -0.9651348961777158619 ) ) ;
#257147=VECTOR ( 'NONE', #239002, 1000.000000000000000 ) ;
#257167=CARTESIAN_POINT ( 'NONE',  ( -18.59999999999999787, 76.00000000001126921, -203.5231074845248997 ) ) ;
#257174=CIRCLE ( 'NONE', #186503, 0.1000000000000124678 ) ;
#257196=DIRECTION ( 'NONE',  ( 1.000000000000000000, 0.000000000000000000, 0.000000000000000000 ) ) ;
#257198=ADVANCED_FACE ( 'NONE', ( #4598, #123287 ), #239380, .F. ) ;
#257208=CARTESIAN_POINT ( 'NONE',  ( -23.25000000000000000, 76.00000000001126921, -203.5231074845248997 ) ) ;
#257225=AXIS2_PLACEMENT_3D ( 'NONE', #140062, #95801, #115378 ) ;
#257242=VERTEX_POINT ( 'NONE', #140251 ) ;
#257253=AXIS2_PLACEMENT_3D ( 'NONE', #90345, #168667, #13403 ) ;
#257271=DIRECTION ( 'NONE',  ( 0.000000000000000000, 0.2617529984163859957, 0.9651348961777475033 ) ) ;
#257272=DIRECTION ( 'NONE',  ( 0.000000000000000000, 0.2617529984165152257, 0.9651348961777124202 ) ) ;
#257276=CARTESIAN_POINT ( 'NONE',  ( -20.00857864376270001, 61.43991280424057777, -221.4883200034892923 ) ) ;
#257298=EDGE_LOOP ( 'NONE', ( #81961, #54625, #226857, #20004 ) ) ;
#257317=ORIENTED_EDGE ( 'NONE', *, *, #8142, .T. ) ;
#257349=CIRCLE ( 'NONE', #32609, 0.5000000000000014433 ) ;
#257358=CARTESIAN_POINT ( 'NONE',  ( 23.14999999999999147, 71.23658437219593509, -236.9414014499068912 ) ) ;
#257363=EDGE_CURVE ( 'NONE', #155936, #78065, #85395, .T. ) ;
#257428=CARTESIAN_POINT ( 'NONE',  ( 20.89192007715128341, 67.49241595948059569, -195.4314365843280541 ) ) ;
#257435=CARTESIAN_POINT ( 'NONE',  ( -18.39999999999999858, 87.08727414655710675, -199.6327537731849873 ) ) ;
#257438=CARTESIAN_POINT ( 'NONE',  ( -18.51991288638553002, 78.16601445863898334, -231.4194093194572588 ) ) ;
#257444=FACE_OUTER_BOUND ( 'NONE', #14900, .T. ) ;
#257445=LINE ( 'NONE', #215793, #66479 ) ;
#257449=CIRCLE ( 'NONE', #186616, 0.09999999999999939493 ) ;
#257512=DIRECTION ( 'NONE',  ( 0.000000000000000000, -0.2617529984165035128, -0.9651348961777155289 ) ) ;
#257543=ORIENTED_EDGE ( 'NONE', *, *, #151196, .F. ) ;
#257558=AXIS2_PLACEMENT_3D ( 'NONE', #172136, #74312, #16886 ) ;
#257579=DIRECTION ( 'NONE',  ( 0.000000000000000000, 0.1180230956474139226, -0.9930108503404186937 ) ) ;
#257587=DIRECTION ( 'NONE',  ( 0.000000000000000000, -0.9209589331071864615, 0.3896596508878908960 ) ) ;
#257589=ORIENTED_EDGE ( 'NONE', *, *, #148901, .F. ) ;
#257611=DIRECTION ( 'NONE',  ( 0.000000000000000000, 0.2617529984165152257, 0.9651348961777124202 ) ) ;
#257617=ORIENTED_EDGE ( 'NONE', *, *, #45849, .F. ) ;
#257627=ORIENTED_EDGE ( 'NONE', *, *, #67365, .T. ) ;
#257639=ORIENTED_EDGE ( 'NONE', *, *, #221203, .T. ) ;
#257668=CARTESIAN_POINT ( 'NONE',  ( 21.04999999999998650, 64.01960172407876826, -222.2915665888316141 ) ) ;
#257696=VERTEX_POINT ( 'NONE', #172093 ) ;
#257698=DIRECTION ( 'NONE',  ( 0.000000000000000000, 0.2617529984165031243, 0.9651348961777157509 ) ) ;
#257707=ORIENTED_EDGE ( 'NONE', *, *, #109709, .T. ) ;
#257710=FACE_OUTER_BOUND ( 'NONE', #40705, .T. ) ;
#257754=AXIS2_PLACEMENT_3D ( 'NONE', #110808, #190373, #10440 ) ;
#257780=LINE ( 'NONE', #59604, #58042 ) ;
#257811=DIRECTION ( 'NONE',  ( -0.000000000000000000, 0.9651348961777158619, -0.2617529984165031243 ) ) ;
#257835=CARTESIAN_POINT ( 'NONE',  ( 20.87155475150661132, 62.85241404162280077, -207.1112001314805582 ) ) ;
#257851=CIRCLE ( 'NONE', #66376, 11.75000000000000178 ) ;
#257854=ORIENTED_EDGE ( 'NONE', *, *, #96490, .T. ) ;
#257932=DIRECTION ( 'NONE',  ( 0.000000000000000000, 0.2617529984165432588, 0.9651348961777048707 ) ) ;
#257975=CARTESIAN_POINT ( 'NONE',  ( -20.85000000000000142, 79.37986612816742138, -196.2658927859692142 ) ) ;
#257980=CARTESIAN_POINT ( 'NONE',  ( -23.15000000000000213, 70.02906482874161043, -215.6060937950565233 ) ) ;
#258001=EDGE_LOOP ( 'NONE', ( #201164, #175389, #206900, #127808 ) ) ;
#258034=VERTEX_POINT ( 'NONE', #88316 ) ;
#258035=DIRECTION ( 'NONE',  ( 0.000000000000000000, -0.2617529984165152257, -0.9651348961777124202 ) ) ;
ENDSEC;
END-ISO-10303-21;
